ISO-10303-21;
HEADER;
FILE_DESCRIPTION (('STEP AP214'),
    '1' );
FILE_NAME ('Number Dial Wheels.step',
    '2026-10-06T10:59:17',
    ( '' ),
    ( '' ),
    'SwSTEP 2.0',
    'SolidWorks 2026',
    '' );
FILE_SCHEMA (( 'AUTOMOTIVE_DESIGN' ));
ENDSEC;

DATA;
#1=CARTESIAN_POINT ( 'NONE',  ( -5.668520211720758262, 50.55432463793220421, 79.06611278947218580 ) ) ;
#2=EDGE_CURVE ( 'NONE', #13018, #165, #5489, .T. ) ;
#3=DIRECTION ( 'NONE',  ( -0.007885122365275663500, -0.9999689119394085113, -1.805443505845543142E-16 ) ) ;
#5=CIRCLE ( 'NONE', #15294, 8.199999999999995737 ) ;
#7=EDGE_CURVE ( 'NONE', #18543, #18148, #5615, .T. ) ;
#9=CARTESIAN_POINT ( 'NONE',  ( 9.261243355884198891, 42.55025836209524215, 77.91040118276930571 ) ) ;
#10=ORIENTED_EDGE ( 'NONE', *, *, #4967, .T. ) ;
#11=CARTESIAN_POINT ( 'NONE',  ( 0.5922110576113025493, 52.20739479508054615, 75.36022115247205022 ) ) ;
#12=CARTESIAN_POINT ( 'NONE',  ( 4.579592178280777581, 52.10552964593085790, 78.58658920843723195 ) ) ;
#13=CARTESIAN_POINT ( 'NONE',  ( -4.517072128342570991, 36.94403992325788977, 76.53375056423675460 ) ) ;
#16=ORIENTED_EDGE ( 'NONE', *, *, #17837, .F. ) ;
#17=CARTESIAN_POINT ( 'NONE',  ( -4.383821200644077543, 51.47232351541473605, 78.52322435057745054 ) ) ;
#18=ORIENTED_EDGE ( 'NONE', *, *, #1917, .T. ) ;
#20=VECTOR ( 'NONE', #2644, 1000.000000000000000 ) ;
#21=DIRECTION ( 'NONE',  ( -0.9534635866061492715, -0.3015081906286096181, -2.009271279954799034E-16 ) ) ;
#26=VERTEX_POINT ( 'NONE', #13599 ) ;
#27=CARTESIAN_POINT ( 'NONE',  ( 4.987972048783305468, 51.80387588613526617, 77.70137231118654597 ) ) ;
#28=ORIENTED_EDGE ( 'NONE', *, *, #6498, .T. ) ;
#36=DIRECTION ( 'NONE',  ( -0.5941461771851783702, -0.8043570849667693867, -2.357623395011398763E-16 ) ) ;
#38=CARTESIAN_POINT ( 'NONE',  ( 5.756838674491786101, 51.23594508156129734, 75.97260389846793771 ) ) ;
#40=PLANE ( 'NONE',  #3794 ) ;
#42=CARTESIAN_POINT ( 'NONE',  ( -4.383767596367525776, 51.47236181906818331, 76.38961819735682468 ) ) ;
#45=CARTESIAN_POINT ( 'NONE',  ( 4.947340820402381212, 51.83388853781453776, 77.72408214165703555 ) ) ;
#46=CARTESIAN_POINT ( 'NONE',  ( -7.770838052284047670, 41.18381739692070198, 76.59276269229415846 ) ) ;
#49=VECTOR ( 'NONE', #11838, 1000.000000000000000 ) ;
#50=CARTESIAN_POINT ( 'NONE',  ( -4.705149740856862550, 37.08296527939383935, 78.93669174070734584 ) ) ;
#51=AXIS2_PLACEMENT_3D ( 'NONE', #3757, #13451, #252 ) ;
#53=CARTESIAN_POINT ( 'NONE',  ( -3.095340769291234473, 36.81869718614577636, 77.24173421363296654 ) ) ;
#54=VERTEX_POINT ( 'NONE', #8619 ) ;
#56=CARTESIAN_POINT ( 'NONE',  ( -3.319090015466918064, 36.97315379936787849, 77.82155188814751057 ) ) ;
#58=CARTESIAN_POINT ( 'NONE',  ( -8.080917653967048864, 42.28401339625642663, 76.87634113524943302 ) ) ;
#59=DIRECTION ( 'NONE',  ( -0.5813877811927011807, 0.8136266022444372803, 5.636455622144619183E-17 ) ) ;
#60=CARTESIAN_POINT ( 'NONE',  ( 9.342575031381675998, 42.79401455314646086, 78.75800315165874110 ) ) ;
#63=CARTESIAN_POINT ( 'NONE',  ( -5.888951387225215939, 37.95739186912707197, 75.98496980016291502 ) ) ;
#64=EDGE_LOOP ( 'NONE', ( #4003, #6865, #2890, #187 ) ) ;
#71=CARTESIAN_POINT ( 'NONE',  ( 4.142779209164833887, 51.51417078508897163, 78.58658920843723195 ) ) ;
#72=CARTESIAN_POINT ( 'NONE',  ( -4.555118767358855791, 36.97214344288707366, 78.05402056118774112 ) ) ;
#74=CARTESIAN_POINT ( 'NONE',  ( -7.805021908755670701, 41.31633897062200589, 78.88165831555673435 ) ) ;
#79=CARTESIAN_POINT ( 'NONE',  ( 0.3449000470298889676, 52.34510639596846460, 77.07502437766733294 ) ) ;
#83=CARTESIAN_POINT ( 'NONE',  ( -5.510184220575293779, 38.60782276366593635, 76.52855510524061344 ) ) ;
#84=CARTESIAN_POINT ( 'NONE',  ( 9.340212240349364592, 42.78693311852996572, 76.09591779779900378 ) ) ;
#85=CARTESIAN_POINT ( 'NONE',  ( 8.299662904660788598, 41.56403757284476796, 75.97198585835440099 ) ) ;
#86=CARTESIAN_POINT ( 'NONE',  ( 1.695410614910025870, 52.88397731476800345, 79.31282343688214098 ) ) ;
#87=ORIENTED_EDGE ( 'NONE', *, *, #18743, .F. ) ;
#88=CARTESIAN_POINT ( 'NONE',  ( 5.873814141894775354, 51.14954001584995069, 78.86250487280319987 ) ) ;
#94=CARTESIAN_POINT ( 'NONE',  ( 5.077155773762835445, 37.34368029226138219, 77.47144026546204998 ) ) ;
#96=LINE ( 'NONE', #16272, #3476 ) ;
#99=CARTESIAN_POINT ( 'NONE',  ( 6.470280134917119064, 49.78412166693355800, 77.24227907682649175 ) ) ;
#100=CARTESIAN_POINT ( 'NONE',  ( 4.485821066275814673, 51.34094918448491995, 77.76180969966527812 ) ) ;
#101=CARTESIAN_POINT ( 'NONE',  ( 5.384092268968043271, 50.76532863195453160, 75.97198585835440099 ) ) ;
#103=ORIENTED_EDGE ( 'NONE', *, *, #5988, .T. ) ;
#104=CARTESIAN_POINT ( 'NONE',  ( -5.234090592717892676, 38.40967907571953077, 79.34222993022952153 ) ) ;
#106=EDGE_CURVE ( 'NONE', #5849, #17982, #8716, .T. ) ;
#107=CARTESIAN_POINT ( 'NONE',  ( 8.951227662965957066, 41.62112166339042574, 78.59502675972919405 ) ) ;
#108=CARTESIAN_POINT ( 'NONE',  ( -4.895593109503404428, 37.22363812428621088, 78.53742703482498655 ) ) ;
#110=CARTESIAN_POINT ( 'NONE',  ( 8.529329397667178014, 40.35666579756309602, 75.60774188071792423 ) ) ;
#111=EDGE_LOOP ( 'NONE', ( #358, #7162, #18029, #16335 ) ) ;
#112=CARTESIAN_POINT ( 'NONE',  ( 0.5218139128070994337, 52.20794990243870615, 75.36134551364482093 ) ) ;
#113=CARTESIAN_POINT ( 'NONE',  ( 4.611645699796032893, 52.08185300078213942, 78.81874598975664981 ) ) ;
#114=CARTESIAN_POINT ( 'NONE',  ( 7.692705115657170190, 40.18434116893706687, 78.65627992829327297 ) ) ;
#119=CARTESIAN_POINT ( 'NONE',  ( -4.541431855014749885, 51.35970071229581180, 78.93463757479271692 ) ) ;
#121=VECTOR ( 'NONE', #9015, 1000.000000000000000 ) ;
#125=CARTESIAN_POINT ( 'NONE',  ( -7.372207198384979066, 41.95818682111052311, 78.62287654527649750 ) ) ;
#127=CARTESIAN_POINT ( 'NONE',  ( 8.647256388514012571, 43.05630782556218605, 78.60052408832618198 ) ) ;
#128=ORIENTED_EDGE ( 'NONE', *, *, #19583, .F. ) ;
#136=CARTESIAN_POINT ( 'NONE',  ( -5.850799091716242017, 37.92921030530281001, 79.12851299606570876 ) ) ;
#141=CARTESIAN_POINT ( 'NONE',  ( -4.572866156349838285, 51.33723891144499163, 75.97260225988416948 ) ) ;
#144=CARTESIAN_POINT ( 'NONE',  ( 4.577379499810326990, 52.10716406238486087, 78.43496551412393103 ) ) ;
#146=CARTESIAN_POINT ( 'NONE',  ( -7.419359026272076996, 40.07233033562560109, 78.47931198110067896 ) ) ;
#147=CARTESIAN_POINT ( 'NONE',  ( -5.170918566808907713, 50.90989255502720567, 75.43678921887351407 ) ) ;
#150=LINE ( 'NONE', #6632, #10274 ) ;
#153=ADVANCED_FACE ( 'NONE', ( #834 ), #13296, .T. ) ;
#154=CARTESIAN_POINT ( 'NONE',  ( -3.501255140781828423, 36.19369683415101946, 76.91456057462045237 ) ) ;
#155=ORIENTED_EDGE ( 'NONE', *, *, #1332, .F. ) ;
#156=CARTESIAN_POINT ( 'NONE',  ( 0.6393167648259392433, 52.21315491623544602, 79.54845644658969661 ) ) ;
#158=VERTEX_POINT ( 'NONE', #10219 ) ;
#159=DIRECTION ( 'NONE',  ( 0.9485903129789495791, -0.3165065846431930341, 8.934458285744763183E-17 ) ) ;
#162=ORIENTED_EDGE ( 'NONE', *, *, #19825, .F. ) ;
#164=CARTESIAN_POINT ( 'NONE',  ( -5.460139946343538497, 38.57665262741940637, 76.06004113464240390 ) ) ;
#165=VERTEX_POINT ( 'NONE', #16122 ) ;
#167=CARTESIAN_POINT ( 'NONE',  ( 0.7308905865242323330, 52.95996087887004933, 76.81167861208460579 ) ) ;
#168=PLANE ( 'NONE',  #8612 ) ;
#169=EDGE_LOOP ( 'NONE', ( #1521, #15928, #6222, #1148 ) ) ;
#171=CARTESIAN_POINT ( 'NONE',  ( -4.853788242550869825, 37.19275855307108003, 77.90854597583356167 ) ) ;
#173=DIRECTION ( 'NONE',  ( 1.540237394707284220E-16, 1.793354297423764243E-16, -1.000000000000000000 ) ) ;
#174=CARTESIAN_POINT ( 'NONE',  ( 5.506586839745581941, 50.67343267475700941, 78.88820493356335817 ) ) ;
#175=CARTESIAN_POINT ( 'NONE',  ( 1.314047178454490705, 52.92828027204963348, 75.43137060453751985 ) ) ;
#179=CARTESIAN_POINT ( 'NONE',  ( -4.518988042728760313, 37.69480848959909025, 76.08971211654539957 ) ) ;
#180=CARTESIAN_POINT ( 'NONE',  ( 0.8326822781444389587, 52.96411479610753759, 76.79008513575435302 ) ) ;
#181=CARTESIAN_POINT ( 'NONE',  ( 4.121594020068452657, 36.83821297622463220, 75.83703142516586126 ) ) ;
#182=ORIENTED_EDGE ( 'NONE', *, *, #1186, .F. ) ;
#184=DIRECTION ( 'NONE',  ( 0.3165065846431826535, 0.9485903129789529098, 2.188653791613874008E-16 ) ) ;
#186=CARTESIAN_POINT ( 'NONE',  ( 6.712139372526147341, 50.53030293778272863, 77.80505143490314879 ) ) ;
#187=ORIENTED_EDGE ( 'NONE', *, *, #7159, .F. ) ;
#188=VERTEX_POINT ( 'NONE', #4227 ) ;
#191=EDGE_CURVE ( 'NONE', #225, #12203, #12716, .T. ) ;
#192=CARTESIAN_POINT ( 'NONE',  ( 7.680545890134844456, 40.16247990082648300, 76.65742129588737441 ) ) ;
#193=PLANE ( 'NONE',  #3154 ) ;
#197=CARTESIAN_POINT ( 'NONE',  ( 4.102313797646099047, 51.53324301277321240, 76.36737811492949390 ) ) ;
#198=B_SPLINE_CURVE_WITH_KNOTS ( 'NONE', 3,
 ( #12240, #12351, #18723, #2450, #1065, #10868, #10667, #18831, #17129, #9158, #17339, #4238, #15432 ),
 .UNSPECIFIED., .F., .F.,
 ( 4, 1, 1, 1, 1, 1, 1, 1, 1, 1, 4 ),
 ( 0.000000000000000000, 0.08953921432355217702, 0.1742669454086417657, 0.2528767480256390865, 0.3294736160795620483, 0.4632125218299475988, 0.5712501803543521550, 0.6337422670347153675, 0.7254863994935087934, 0.8484041168876338412, 0.9999999999999998890 ),
 .UNSPECIFIED. ) ;
#200=LINE ( 'NONE', #5090, #121 ) ;
#202=ORIENTED_EDGE ( 'NONE', *, *, #9221, .T. ) ;
#203=LINE ( 'NONE', #6687, #3751 ) ;
#204=FACE_OUTER_BOUND ( 'NONE', #1503, .T. ) ;
#205=CARTESIAN_POINT ( 'NONE',  ( 5.347971804495873727, 50.79179859581513057, 78.93139168979107012 ) ) ;
#206=EDGE_CURVE ( 'NONE', #17910, #5649, #11129, .T. ) ;
#207=FACE_OUTER_BOUND ( 'NONE', #16478, .T. ) ;
#208=DIRECTION ( 'NONE',  ( -0.5813877811927012917, 0.8136266022444372803, 5.636455622144620416E-17 ) ) ;
#211=CARTESIAN_POINT ( 'NONE',  ( 6.223727862608700256, 38.34032085607169904, 75.70392102816973079 ) ) ;
#213=CARTESIAN_POINT ( 'NONE',  ( -3.510185363184279428, 36.20029322970840724, 76.30596599901106458 ) ) ;
#214=CARTESIAN_POINT ( 'NONE',  ( -4.348661956197086731, 37.56557963644259956, 78.93669174070734584 ) ) ;
#216=CARTESIAN_POINT ( 'NONE',  ( -4.405821937837398394, 51.45660259411479132, 78.79092181577959764 ) ) ;
#222=CARTESIAN_POINT ( 'NONE',  ( 2.099220375572687036, 52.20172610552850756, 77.53128952716078004 ) ) ;
#225=VERTEX_POINT ( 'NONE', #1542 ) ;
#226=DIRECTION ( 'NONE',  ( 1.540237394707284220E-16, 1.793354297423764243E-16, -1.000000000000000000 ) ) ;
#227=ORIENTED_EDGE ( 'NONE', *, *, #2629, .T. ) ;
#229=CARTESIAN_POINT ( 'NONE',  ( 0.3201111382462868971, 51.36399839264385037, 76.44919174070734869 ) ) ;
#236=CARTESIAN_POINT ( 'NONE',  ( -4.385374315297738690, 51.47121371654639432, 78.59092584394873882 ) ) ;
#238=ORIENTED_EDGE ( 'NONE', *, *, #14421, .F. ) ;
#239=CARTESIAN_POINT ( 'NONE',  ( 4.432284427945813121, 36.14044538431356557, 77.43080938776617472 ) ) ;
#240=ORIENTED_EDGE ( 'NONE', *, *, #5848, .T. ) ;
#244=FACE_OUTER_BOUND ( 'NONE', #17677, .T. ) ;
#247=CARTESIAN_POINT ( 'NONE',  ( 5.786794573647632944, 37.10832874265046399, 76.01697444493925104 ) ) ;
#249=CARTESIAN_POINT ( 'NONE',  ( -3.906146384357795043, 51.81365245034167799, 75.48713596493043099 ) ) ;
#252=DIRECTION ( 'NONE',  ( 0.3165065846431827645, 0.9485903129789529098, 0.000000000000000000 ) ) ;
#253=EDGE_CURVE ( 'NONE', #3468, #18406, #1056, .T. ) ;
#254=AXIS2_PLACEMENT_3D ( 'NONE', #16070, #11180, #9791 ) ;
#257=ADVANCED_FACE ( 'NONE', ( #1439 ), #7307, .T. ) ;
#260=CARTESIAN_POINT ( 'NONE',  ( -7.560113746301722060, 42.96559675774617659, 76.25640820822667365 ) ) ;
#262=CARTESIAN_POINT ( 'NONE',  ( -2.939085670389444793, 51.59587639763223166, 75.45433879953088763 ) ) ;
#263=CARTESIAN_POINT ( 'NONE',  ( -5.955451856753751549, 38.00651308716548726, 76.73301527011911105 ) ) ;
#264=VERTEX_POINT ( 'NONE', #11855 ) ;
#267=CARTESIAN_POINT ( 'NONE',  ( -4.517374237173717333, 36.94426307888177519, 76.44623874561141008 ) ) ;
#268=EDGE_CURVE ( 'NONE', #10025, #14733, #19817, .T. ) ;
#271=VERTEX_POINT ( 'NONE', #6526 ) ;
#274=CARTESIAN_POINT ( 'NONE',  ( 1.799688516650707726, 52.86918891857825287, 75.67226899599502588 ) ) ;
#275=VECTOR ( 'NONE', #4873, 1000.000000000000227 ) ;
#277=CARTESIAN_POINT ( 'NONE',  ( 5.035970566151715566, 36.57181739631530348, 75.46362501775257670 ) ) ;
#279=VERTEX_POINT ( 'NONE', #19605 ) ;
#281=CARTESIAN_POINT ( 'NONE',  ( 8.494230864814916515, 42.61589131850842449, 75.57016332177543916 ) ) ;
#283=CARTESIAN_POINT ( 'NONE',  ( 0.6452163281857689059, 52.96132085210302165, 79.54845644658969661 ) ) ;
#286=ORIENTED_EDGE ( 'NONE', *, *, #14335, .T. ) ;
#287=EDGE_CURVE ( 'NONE', #4528, #3672, #19715, .T. ) ;
#288=CARTESIAN_POINT ( 'NONE',  ( 0.8455950101471356728, 52.35579997042385259, 72.45433879953087342 ) ) ;
#289=EDGE_LOOP ( 'NONE', ( #6284, #6972, #19822, #1456 ) ) ;
#290=CARTESIAN_POINT ( 'NONE',  ( -3.522017727535923459, 36.20903332061825353, 77.14704031750767399 ) ) ;
#291=CARTESIAN_POINT ( 'NONE',  ( 6.434241825184708219, 49.81074171462121569, 75.93520998463665705 ) ) ;
#292=CARTESIAN_POINT ( 'NONE',  ( 9.351996896326966180, 42.82225248009945773, 76.45750776978282204 ) ) ;
#294=DIRECTION ( 'NONE',  ( 0.3015081906286096181, -0.9534635866061492715, -1.245503830460495705E-16 ) ) ;
#298=CARTESIAN_POINT ( 'NONE',  ( 6.934807254081542638, 50.36582714328714871, 76.18099276316716839 ) ) ;
#300=LINE ( 'NONE', #12868, #1303 ) ;
#302=CIRCLE ( 'NONE', #9823, 6.000000000000002665 ) ;
#305=CARTESIAN_POINT ( 'NONE',  ( -4.006646489220814011, 48.09791109810387155, 82.45433879953087342 ) ) ;
#306=CARTESIAN_POINT ( 'NONE',  ( 8.949918141112842562, 41.61719694332212072, 78.74360054667872078 ) ) ;
#307=CARTESIAN_POINT ( 'NONE',  ( -4.873991315592625995, 37.20768174929765593, 78.81125587425833601 ) ) ;
#308=CARTESIAN_POINT ( 'NONE',  ( 8.375041524787441460, 41.81431093369050700, 77.18036020728871449 ) ) ;
#309=CARTESIAN_POINT ( 'NONE',  ( -1.883296302981685599, 36.95289499283964574, 72.45432679953087529 ) ) ;
#310=CARTESIAN_POINT ( 'NONE',  ( 9.304727838458644484, 42.68058411497499804, 77.77798975163413786 ) ) ;
#311=ORIENTED_EDGE ( 'NONE', *, *, #5198, .F. ) ;
#313=VECTOR ( 'NONE', #14999, 1000.000000000000114 ) ;
#315=CARTESIAN_POINT ( 'NONE',  ( 6.882736312352589536, 37.89144858414100270, 77.26022115247205591 ) ) ;
#317=CARTESIAN_POINT ( 'NONE',  ( -7.367656984315425817, 48.05973018190410073, 78.32492703482499508 ) ) ;
#318=ORIENTED_EDGE ( 'NONE', *, *, #10196, .T. ) ;
#319=CARTESIAN_POINT ( 'NONE',  ( 8.354092538887906372, 41.75152549397071766, 76.05553801048951357 ) ) ;
#320=CARTESIAN_POINT ( 'NONE',  ( -4.517608495228999210, 36.94443611587072240, 78.61392107264721574 ) ) ;
#322=ORIENTED_EDGE ( 'NONE', *, *, #16808, .F. ) ;
#324=EDGE_CURVE ( 'NONE', #3856, #5035, #17993, .T. ) ;
#325=CARTESIAN_POINT ( 'NONE',  ( 5.561379608955574483, 51.38032281970146897, 76.39036821129558064 ) ) ;
#326=CARTESIAN_POINT ( 'NONE',  ( -3.147752837274839788, 36.84659392771992970, 78.05869123030269918 ) ) ;
#329=VECTOR ( 'NONE', #13331, 1000.000000000000114 ) ;
#335=AXIS2_PLACEMENT_3D ( 'NONE', #10924, #9219, #1536 ) ;
#336=LINE ( 'NONE', #13015, #329 ) ;
#339=DIRECTION ( 'NONE',  ( 1.540237394707284220E-16, 1.793354297423764243E-16, -1.000000000000000000 ) ) ;
#340=CARTESIAN_POINT ( 'NONE',  ( 8.025296824724655664, 41.22723296074632060, 75.38759329643264095 ) ) ;
#341=CARTESIAN_POINT ( 'NONE',  ( 5.829595689320886009, 51.18220240553836931, 75.98827401121828018 ) ) ;
#342=LINE ( 'NONE', #6831, #16623 ) ;
#343=CARTESIAN_POINT ( 'NONE',  ( 0.4259372535303960206, 52.96683778999253178, 78.89168391585492657 ) ) ;
#346=CARTESIAN_POINT ( 'NONE',  ( -4.032216884946988600, 50.97665165413603461, 76.31459635612003467 ) ) ;
#348=CARTESIAN_POINT ( 'NONE',  ( 7.860711257786343609, 47.82081138319720282, 79.44551527011911674 ) ) ;
#350=CARTESIAN_POINT ( 'NONE',  ( -4.615868704430273084, 50.38673528273210422, 75.40305853716382956 ) ) ;
#352=FACE_OUTER_BOUND ( 'NONE', #4295, .T. ) ;
#353=AXIS2_PLACEMENT_3D ( 'NONE', #1504, #7884, #14371 ) ;
#354=EDGE_CURVE ( 'NONE', #13475, #8370, #13216, .T. ) ;
#356=CARTESIAN_POINT ( 'NONE',  ( 8.356924487248303279, 46.61990428187149149, 75.44110882394862472 ) ) ;
#357=CARTESIAN_POINT ( 'NONE',  ( -7.655299514379396264, 47.45321114378259608, 78.28954034321952804 ) ) ;
#358=ORIENTED_EDGE ( 'NONE', *, *, #20772, .T. ) ;
#359=CARTESIAN_POINT ( 'NONE',  ( 1.029933359059799880, 52.96274971666686326, 79.52671882365912381 ) ) ;
#360=CARTESIAN_POINT ( 'NONE',  ( -5.522333806888472196, 37.68658623078928116, 79.43312132436682305 ) ) ;
#362=ORIENTED_EDGE ( 'NONE', *, *, #3216, .T. ) ;
#363=FACE_OUTER_BOUND ( 'NONE', #15901, .T. ) ;
#364=EDGE_CURVE ( 'NONE', #7324, #12818, #18229, .T. ) ;
#367=B_SPLINE_SURFACE_WITH_KNOTS ( 'NONE', 3, 1, ( 
 ( #9391, #8386 ),
 ( #3379, #9895 ),
 ( #13285, #7780 ),
 ( #14663, #17963 ),
 ( #16375, #15875 ),
 ( #88, #1696 ),
 ( #14261, #17467 ),
 ( #2891, #20742 ),
 ( #6177, #12681 ),
 ( #1292, #6570 ),
 ( #2001, #5180 ) ),
 .UNSPECIFIED., .F., .F., .F.,
 ( 4, 1, 1, 1, 1, 1, 1, 1, 4 ),
 ( 2, 2 ),
 ( 0.000000000000000000, 0.1116983415361904319, 0.2084596166200352318, 0.2965296202300037876, 0.3842340601578678183, 0.4893760538913073388, 0.6260801343201788383, 0.7954079187270842732, 1.000000000000000000 ),
 ( 0.000000000000000000, 1.000000000000000000 ),
 .UNSPECIFIED. ) ;
#369=CARTESIAN_POINT ( 'NONE',  ( -6.647464070959230753, 48.14170149837703860, 75.45433879953088763 ) ) ;
#372=CYLINDRICAL_SURFACE ( 'NONE', #19299, 4.200000000000003730 ) ;
#373=CARTESIAN_POINT ( 'NONE',  ( 0.5493427850443924898, 52.96217785025373104, 75.97284715006453837 ) ) ;
#374=VERTEX_POINT ( 'NONE', #1646 ) ;
#375=CARTESIAN_POINT ( 'NONE',  ( -4.311513864721317368, 37.56696343308806973, 77.92992558049613194 ) ) ;
#378=CARTESIAN_POINT ( 'NONE',  ( 0.7854852052231534598, 52.35796933930620156, 77.46569646384521945 ) ) ;
#382=ADVANCED_FACE ( 'NONE', ( #8446 ), #459, .F. ) ;
#383=ADVANCED_FACE ( 'NONE', ( #16643 ), #2062, .T. ) ;
#386=CARTESIAN_POINT ( 'NONE',  ( -7.208272791143412128, 41.42712212161580254, 78.48592181560817949 ) ) ;
#387=ORIENTED_EDGE ( 'NONE', *, *, #17284, .F. ) ;
#391=CARTESIAN_POINT ( 'NONE',  ( 8.392124750090893315, 39.94545476467643397, 78.58253683706189463 ) ) ;
#395=DIRECTION ( 'NONE',  ( -0.3165065846431827645, -0.9485903129789529098, 0.000000000000000000 ) ) ;
#400=CARTESIAN_POINT ( 'NONE',  ( 0.5221537403065015237, 44.16218137147968292, 75.45433879953087342 ) ) ;
#401=ORIENTED_EDGE ( 'NONE', *, *, #18206, .F. ) ;
#402=PLANE ( 'NONE',  #6711 ) ;
#404=CARTESIAN_POINT ( 'NONE',  ( 4.097390034816026372, 51.53687999803451447, 76.58963291717793709 ) ) ;
#405=LINE ( 'NONE', #19960, #8602 ) ;
#407=CARTESIAN_POINT ( 'NONE',  ( 0.8494352808551174361, 52.96349884688018506, 77.70257284945761000 ) ) ;
#408=AXIS2_PLACEMENT_3D ( 'NONE', #16155, #16467, #17952 ) ;
#409=DIRECTION ( 'NONE',  ( -1.540237394707284220E-16, -1.793354297423764243E-16, 1.000000000000000000 ) ) ;
#410=B_SPLINE_CURVE_WITH_KNOTS ( 'NONE', 3,
 ( #6962, #18253, #13567, #3673, #16771, #11880, #20254, #378, #2191, #5261, #14959, #12091, #2405, #20048 ),
 .UNSPECIFIED., .F., .F.,
 ( 4, 2, 2, 2, 2, 2, 4 ),
 ( 0.000000000000000000, 6.529616093792225636E-05, 0.0001305923218758445127, 0.0001958884828137667691, 0.0002611846437516890254, 0.0003917769656275335382, 0.0005223692875033780509 ),
 .UNSPECIFIED. ) ;
#414=VECTOR ( 'NONE', #11198, 1000.000000000000227 ) ;
#417=CARTESIAN_POINT ( 'NONE',  ( 0.5753953112280285609, 52.96564479498633204, 75.97198585835440099 ) ) ;
#418=EDGE_CURVE ( 'NONE', #11233, #17827, #3724, .T. ) ;
#419=CARTESIAN_POINT ( 'NONE',  ( -4.537713647263719174, 36.95928698179384497, 76.12832907849806929 ) ) ;
#421=CARTESIAN_POINT ( 'NONE',  ( 8.525177894392134803, 42.37332589716783104, 75.47260332232873736 ) ) ;
#423=AXIS2_PLACEMENT_3D ( 'NONE', #309, #5407, #15115 ) ;
#424=CARTESIAN_POINT ( 'NONE',  ( 8.330547866859147277, 41.68096061825437459, 77.50814924735175282 ) ) ;
#425=PLANE ( 'NONE',  #423 ) ;
#429=ORIENTED_EDGE ( 'NONE', *, *, #5185, .F. ) ;
#430=EDGE_LOOP ( 'NONE', ( #13284, #4279, #4498, #11595 ) ) ;
#431=CARTESIAN_POINT ( 'NONE',  ( 8.440918477302592038, 42.45611071105919621, 79.41516958226422673 ) ) ;
#433=CARTESIAN_POINT ( 'NONE',  ( 5.543237494533933329, 50.64513746126347371, 78.20513402937135083 ) ) ;
#437=LINE ( 'NONE', #10027, #19359 ) ;
#439=CARTESIAN_POINT ( 'NONE',  ( 2.056690051755801996, 52.94072599914807853, 77.29915700192239569 ) ) ;
#440=CIRCLE ( 'NONE', #3509, 8.199999999999995737 ) ;
#442=CARTESIAN_POINT ( 'NONE',  ( 8.539681987266121155, 42.43459204878987379, 79.42333176336475731 ) ) ;
#444=DIRECTION ( 'NONE',  ( 0.9534635866061470511, 0.3015081906286169455, 2.009271279954808648E-16 ) ) ;
#445=VERTEX_POINT ( 'NONE', #20231 ) ;
#446=DIRECTION ( 'NONE',  ( -0.5954989751681698529, 0.8033560671169786005, 5.234922652618075161E-17 ) ) ;
#448=ORIENTED_EDGE ( 'NONE', *, *, #4183, .T. ) ;
#452=PLANE ( 'NONE',  #15616 ) ;
#453=ORIENTED_EDGE ( 'NONE', *, *, #3759, .T. ) ;
#454=FACE_OUTER_BOUND ( 'NONE', #13979, .T. ) ;
#455=B_SPLINE_CURVE_WITH_KNOTS ( 'NONE', 3,
 ( #16101, #17580, #17484, #9513, #3116, #5991, #4384, #1315, #7797, #14283, #20761, #6195, #8008, #12697, #6292, #11214, #6396, #27, #2128 ),
 .UNSPECIFIED., .F., .F.,
 ( 4, 1, 1, 1, 1, 1, 1, 1, 1, 1, 1, 1, 1, 1, 1, 1, 4 ),
 ( 0.000000000000000000, 0.07819787255609964016, 0.1515336364311310191, 0.2187066978088008651, 0.2814522326392254747, 0.3385163222030129759, 0.3915958516965070690, 0.4406923075239814191, 0.4864642379862412769, 0.5323932679607442653, 0.5831133966729620255, 0.6391356099194271945, 0.6992555458516984679, 0.7657124642625251498, 0.8379597225178306852, 0.9162365097749198828, 1.000000000000000000 ),
 .UNSPECIFIED. ) ;
#458=CARTESIAN_POINT ( 'NONE',  ( -7.575063113447651375, 40.56471555772565551, 77.37311125041073012 ) ) ;
#459=PLANE ( 'NONE',  #12233 ) ;
#460=CARTESIAN_POINT ( 'NONE',  ( 7.860711257786343609, 47.82081138319720282, 79.44551527011911674 ) ) ;
#465=EDGE_LOOP ( 'NONE', ( #9711, #3894, #10452, #803 ) ) ;
#466=CARTESIAN_POINT ( 'NONE',  ( 1.362138928955740402, 52.20745519782975919, 79.45495304649941204 ) ) ;
#467=CARTESIAN_POINT ( 'NONE',  ( 5.472849728943090852, 37.64179392051541839, 78.35708441643889444 ) ) ;
#469=CARTESIAN_POINT ( 'NONE',  ( 8.121917471046002035, 44.10225444150351137, 72.45433879953087342 ) ) ;
#474=CARTESIAN_POINT ( 'NONE',  ( 2.115041367457929589, 52.20598078514408513, 78.16610350541323271 ) ) ;
#475=CARTESIAN_POINT ( 'NONE',  ( -5.493714318389452345, 37.66544616749837360, 75.52011153330033721 ) ) ;
#476=VERTEX_POINT ( 'NONE', #12285 ) ;
#477=CARTESIAN_POINT ( 'NONE',  ( 5.628424039023946612, 51.33079979992434261, 78.86786983087660019 ) ) ;
#478=CARTESIAN_POINT ( 'NONE',  ( 0.3727252375183737754, 52.96094423127976825, 77.03975889764973317 ) ) ;
#480=ORIENTED_EDGE ( 'NONE', *, *, #1486, .F. ) ;
#481=CARTESIAN_POINT ( 'NONE',  ( -4.147711664773192197, 37.44596934634147800, 78.25995115514949418 ) ) ;
#485=CARTESIAN_POINT ( 'NONE',  ( 9.353817388681445522, 42.82770861117572281, 78.41904468188381827 ) ) ;
#487=EDGE_CURVE ( 'NONE', #10540, #2739, #17166, .T. ) ;
#488=CARTESIAN_POINT ( 'NONE',  ( 6.591015671753180705, 50.61977213638343187, 75.57514290624801845 ) ) ;
#489=CARTESIAN_POINT ( 'NONE',  ( 5.581406744796363562, 50.61539444998253856, 76.90580938776616904 ) ) ;
#490=CARTESIAN_POINT ( 'NONE',  ( -2.917199766949189588, 51.60602765227618960, 72.45433879953087342 ) ) ;
#492=VERTEX_POINT ( 'NONE', #14650 ) ;
#494=EDGE_CURVE ( 'NONE', #20602, #3211, #14857, .T. ) ;
#495=CARTESIAN_POINT ( 'NONE',  ( 7.847142571091401564, 40.67652665170315629, 79.34450935619591405 ) ) ;
#496=VERTEX_POINT ( 'NONE', #21015 ) ;
#498=DIRECTION ( 'NONE',  ( 0.3165065846431717178, 0.9485903129789564625, 0.000000000000000000 ) ) ;
#501=PLANE ( 'NONE',  #17443 ) ;
#502=VERTEX_POINT ( 'NONE', #9881 ) ;
#503=CARTESIAN_POINT ( 'NONE',  ( -3.495367959724245299, 36.18934821065389684, 76.68008248600652621 ) ) ;
#505=CARTESIAN_POINT ( 'NONE',  ( -3.382808528096845180, 51.37448915066374155, 79.35174982259798071 ) ) ;
#506=CARTESIAN_POINT ( 'NONE',  ( 8.378637954445377289, 41.81363803720061867, 77.14698585835439815 ) ) ;
#507=CARTESIAN_POINT ( 'NONE',  ( 0.5221537403065005245, 44.16218137147968292, 82.45433879953087342 ) ) ;
#508=CARTESIAN_POINT ( 'NONE',  ( 8.862035351310685982, 41.35380664710483245, 75.97281361087948426 ) ) ;
#511=CARTESIAN_POINT ( 'NONE',  ( 5.210818179720607013, 37.44367253161215103, 77.75193993234761081 ) ) ;
#514=CARTESIAN_POINT ( 'NONE',  ( 0.3418901990080560060, 52.35614732999829357, 76.10778090364108550 ) ) ;
#518=CARTESIAN_POINT ( 'NONE',  ( -4.513346507200660440, 37.69592389900041240, 78.81125587425833601 ) ) ;
#521=CARTESIAN_POINT ( 'NONE',  ( -4.895593109503407092, 37.22363812428621088, 76.38448585835440952 ) ) ;
#522=FACE_OUTER_BOUND ( 'NONE', #11678, .T. ) ;
#523=EDGE_CURVE ( 'NONE', #18140, #20811, #17951, .T. ) ;
#524=CARTESIAN_POINT ( 'NONE',  ( 5.388356174074294458, 50.75501278463794819, 77.94845644658968808 ) ) ;
#525=ORIENTED_EDGE ( 'NONE', *, *, #8421, .T. ) ;
#526=ORIENTED_EDGE ( 'NONE', *, *, #20016, .T. ) ;
#527=CARTESIAN_POINT ( 'NONE',  ( 6.521540251228659990, 49.75211551535583965, 76.74525360924829442 ) ) ;
#529=EDGE_CURVE ( 'NONE', #6977, #4812, #7370, .T. ) ;
#530=CARTESIAN_POINT ( 'NONE',  ( 5.542822135681054085, 50.64549836037226527, 78.13134938951201036 ) ) ;
#532=CARTESIAN_POINT ( 'NONE',  ( 0.3679909894256196412, 52.36076605197753508, 77.03976057311564318 ) ) ;
#534=EDGE_CURVE ( 'NONE', #17146, #7324, #19941, .T. ) ;
#537=CARTESIAN_POINT ( 'NONE',  ( -7.804011829531284583, 41.29348983807560813, 78.85792113001433279 ) ) ;
#541=CARTESIAN_POINT ( 'NONE',  ( -3.245259920192584691, 36.91861848204638363, 77.89282216559597316 ) ) ;
#542=CARTESIAN_POINT ( 'NONE',  ( -7.938266955593502594, 41.73948448446050463, 79.54486073715324324 ) ) ;
#543=ORIENTED_EDGE ( 'NONE', *, *, #8222, .F. ) ;
#544=CARTESIAN_POINT ( 'NONE',  ( 0.8503282811412342657, 52.95606000782371581, 72.45433879953087342 ) ) ;
#552=CARTESIAN_POINT ( 'NONE',  ( -3.477340361660131496, 52.12006153457090818, 79.00686454089694166 ) ) ;
#553=DIRECTION ( 'NONE',  ( 0.9429220365244146418, -0.3330135628418914862, 8.551124769255465366E-17 ) ) ;
#555=EDGE_CURVE ( 'NONE', #18406, #13226, #12465, .T. ) ;
#556=CARTESIAN_POINT ( 'NONE',  ( 3.117507734380599693, 51.94062193790708903, 72.45433879953087342 ) ) ;
#557=VERTEX_POINT ( 'NONE', #590 ) ;
#558=CARTESIAN_POINT ( 'NONE',  ( 8.378637954445377289, 41.81363803720061867, 77.14698585835439815 ) ) ;
#559=VERTEX_POINT ( 'NONE', #18472 ) ;
#561=DIRECTION ( 'NONE',  ( -0.9999689119394086223, 0.007885122365275665235, -1.526048693634353392E-16 ) ) ;
#562=CARTESIAN_POINT ( 'NONE',  ( -8.192078482032012943, 42.93655631659661509, 78.13669174070733447 ) ) ;
#563=FACE_OUTER_BOUND ( 'NONE', #14057, .T. ) ;
#565=CARTESIAN_POINT ( 'NONE',  ( 5.492130682024771282, 37.64468814625064397, 76.33129752952908120 ) ) ;
#566=CIRCLE ( 'NONE', #9426, 6.000000000000002665 ) ;
#567=ORIENTED_EDGE ( 'NONE', *, *, #9336, .T. ) ;
#568=CARTESIAN_POINT ( 'NONE',  ( 8.213883505808539098, 41.33151258250490656, 78.76104738055306598 ) ) ;
#569=ORIENTED_EDGE ( 'NONE', *, *, #6995, .T. ) ;
#573=CARTESIAN_POINT ( 'NONE',  ( -7.163641313832624036, 41.71182641517503953, 77.97272179757899835 ) ) ;
#574=ORIENTED_EDGE ( 'NONE', *, *, #4534, .T. ) ;
#579=CARTESIAN_POINT ( 'NONE',  ( -4.790699304645749557, 51.18158331905331693, 78.75763390087725213 ) ) ;
#582=CARTESIAN_POINT ( 'NONE',  ( 2.115041367457929589, 52.20598078514408513, 78.16610350541323271 ) ) ;
#585=VERTEX_POINT ( 'NONE', #7187 ) ;
#586=CARTESIAN_POINT ( 'NONE',  ( -4.804516487068378083, 51.17171006637344277, 76.41659450085566618 ) ) ;
#587=CARTESIAN_POINT ( 'NONE',  ( 0.5221537403065005245, 44.16218137147968292, 82.45433879953087342 ) ) ;
#589=CARTESIAN_POINT ( 'NONE',  ( -3.603146387903923387, 36.26895979397031056, 78.01078865174693533 ) ) ;
#590=CARTESIAN_POINT ( 'NONE',  ( -4.895593109503407092, 37.22363812428621088, 77.05433879953086773 ) ) ;
#592=VECTOR ( 'NONE', #12454, 1000.000000000000000 ) ;
#593=DIRECTION ( 'NONE',  ( 0.9999542261909885044, 0.009567942452863074584, 1.557325602890291209E-16 ) ) ;
#595=CARTESIAN_POINT ( 'NONE',  ( 0.5221537403065015237, 44.16218137147968292, 75.45433879953088763 ) ) ;
#597=VERTEX_POINT ( 'NONE', #10084 ) ;
#598=CARTESIAN_POINT ( 'NONE',  ( -4.982544207447554108, 38.08376228894968563, 75.45541555965391467 ) ) ;
#600=LINE ( 'NONE', #11898, #16389 ) ;
#601=CARTESIAN_POINT ( 'NONE',  ( -3.358136819263964234, 52.20524002164697208, 76.41354228756682687 ) ) ;
#602=ORIENTED_EDGE ( 'NONE', *, *, #4967, .F. ) ;
#604=LINE ( 'NONE', #5382, #12018 ) ;
#606=CARTESIAN_POINT ( 'NONE',  ( 4.577225057937401864, 52.10727814237509392, 78.46169174070733732 ) ) ;
#607=CARTESIAN_POINT ( 'NONE',  ( 5.833402057135029573, 38.06140832622005377, 75.44618574453703275 ) ) ;
#609=CARTESIAN_POINT ( 'NONE',  ( 9.204112107805267229, 42.37903238726386945, 75.57016332177543916 ) ) ;
#610=CARTESIAN_POINT ( 'NONE',  ( 4.605781907348109883, 52.08618434805546116, 77.30394856433355244 ) ) ;
#613=CARTESIAN_POINT ( 'NONE',  ( 0.6761804647047966466, 52.35351123918825067, 77.39848739855237625 ) ) ;
#615=CARTESIAN_POINT ( 'NONE',  ( 5.939900590116411472, 51.10072461867315496, 76.90580938776616904 ) ) ;
#617=DIRECTION ( 'NONE',  ( -0.9209602848141236198, 0.007262110304243513635, 0.3895887774936765968 ) ) ;
#619=CARTESIAN_POINT ( 'NONE',  ( 0.3790988156517668406, 52.35585392638166979, 76.04467822456393833 ) ) ;
#621=ORIENTED_EDGE ( 'NONE', *, *, #3762, .F. ) ;
#622=CARTESIAN_POINT ( 'NONE',  ( 5.203405869548749507, 50.89463106707474083, 76.94936699987064799 ) ) ;
#625=CARTESIAN_POINT ( 'NONE',  ( -3.405315259844419185, 52.17152803532113126, 78.78030711080756987 ) ) ;
#628=CARTESIAN_POINT ( 'NONE',  ( -7.450195187915191752, 48.08726987376739714, 78.78375056423675460 ) ) ;
#631=PLANE ( 'NONE',  #10880 ) ;
#635=CARTESIAN_POINT ( 'NONE',  ( 6.446408651871711193, 49.83176319091943896, 77.36971804863098612 ) ) ;
#636=DIRECTION ( 'NONE',  ( 0.9485903129789527988, -0.3165065846431829311, 8.934458285744989980E-17 ) ) ;
#637=LINE ( 'NONE', #18411, #13677 ) ;
#639=CARTESIAN_POINT ( 'NONE',  ( -5.510796958474740492, 38.60848837797752964, 78.18375056423674607 ) ) ;
#641=CIRCLE ( 'NONE', #12556, 8.199999999999995737 ) ;
#645=CARTESIAN_POINT ( 'NONE',  ( 2.118841533926105303, 52.94023591187011846, 77.68224048311739693 ) ) ;
#646=CARTESIAN_POINT ( 'NONE',  ( -3.625666805699584216, 36.28559471941820647, 77.96849812480175501 ) ) ;
#647=EDGE_CURVE ( 'NONE', #15434, #225, #16566, .T. ) ;
#650=CARTESIAN_POINT ( 'NONE',  ( -8.174140996651441782, 42.81404400550773914, 78.99660062231663460 ) ) ;
#654=EDGE_CURVE ( 'NONE', #7531, #3376, #7648, .T. ) ;
#655=VECTOR ( 'NONE', #8630, 1000.000000000000114 ) ;
#656=EDGE_LOOP ( 'NONE', ( #3980, #17099, #14768, #7284, #18986, #9998 ) ) ;
#657=CARTESIAN_POINT ( 'NONE',  ( -4.352345764855491517, 50.74789927721977989, 78.91934866582661812 ) ) ;
#660=CARTESIAN_POINT ( 'NONE',  ( 8.281609818839775983, 41.50998675140334626, 78.01310313856961898 ) ) ;
#663=CARTESIAN_POINT ( 'NONE',  ( -4.471346911670678992, 51.40978084683593607, 79.54642512701808243 ) ) ;
#666=CARTESIAN_POINT ( 'NONE',  ( 0.3279354642496041250, 52.35625728194811046, 78.50066232894263862 ) ) ;
#668=CARTESIAN_POINT ( 'NONE',  ( 8.271884794240664363, 41.48202034606706690, 77.51897818627048764 ) ) ;
#669=VECTOR ( 'NONE', #11258, 1000.000000000000000 ) ;
#670=ORIENTED_EDGE ( 'NONE', *, *, #19379, .F. ) ;
#671=DIRECTION ( 'NONE',  ( -0.007885122365275663500, -0.9999689119394085113, -1.805443505845543142E-16 ) ) ;
#672=CARTESIAN_POINT ( 'NONE',  ( 6.931410089129659724, 50.36833649219094866, 77.12327887040382279 ) ) ;
#673=VECTOR ( 'NONE', #16974, 1000.000000000000000 ) ;
#676=CARTESIAN_POINT ( 'NONE',  ( 6.554687423727395768, 50.64660634980899090, 79.34836068132329956 ) ) ;
#677=DIRECTION ( 'NONE',  ( 0.8043570849667761591, -0.5941461771851692664, 1.733862608106489734E-17 ) ) ;
#679=CARTESIAN_POINT ( 'NONE',  ( -5.728661668566965126, 37.83899231081795023, 75.70067668752250256 ) ) ;
#680=CONICAL_SURFACE ( 'NONE', #9184, 6.200000000000020606, 1.047197551196600518 ) ;
#682=VERTEX_POINT ( 'NONE', #13470 ) ;
#683=ADVANCED_FACE ( 'NONE', ( #20262 ), #4587, .T. ) ;
#684=CARTESIAN_POINT ( 'NONE',  ( 8.248434610079064200, 41.43506443388486815, 78.91056401563228917 ) ) ;
#685=B_SPLINE_CURVE_WITH_KNOTS ( 'NONE', 3,
 ( #20191, #622, #6998, #11320, #2227, #14601, #3317, #11922, #10227, #18287 ),
 .UNSPECIFIED., .F., .F.,
 ( 4, 2, 2, 2, 4 ),
 ( 0.000000000000000000, 0.0001306217549985001693, 0.0002612435099970003387, 0.0003918652649955005080, 0.0005224870199940006774 ),
 .UNSPECIFIED. ) ;
#686=ORIENTED_EDGE ( 'NONE', *, *, #5989, .F. ) ;
#687=CARTESIAN_POINT ( 'NONE',  ( -4.217603907031332255, 50.67132072554849742, 75.36022115247205022 ) ) ;
#691=ORIENTED_EDGE ( 'NONE', *, *, #6268, .F. ) ;
#693=DIRECTION ( 'NONE',  ( 0.8136266022444372803, 0.5813877811927012917, 2.295812393977109593E-16 ) ) ;
#694=CARTESIAN_POINT ( 'NONE',  ( 5.471341376803050771, 36.88291743766401254, 75.36841521003546518 ) ) ;
#695=CARTESIAN_POINT ( 'NONE',  ( 0.3821786226492926430, 35.36301154328572949, 76.86610350541323555 ) ) ;
#699=AXIS2_PLACEMENT_3D ( 'NONE', #10681, #862, #6061 ) ;
#700=EDGE_LOOP ( 'NONE', ( #2325, #17366, #15726, #14088 ) ) ;
#701=CARTESIAN_POINT ( 'NONE',  ( -4.450958381679031461, 50.67743431167600932, 76.37148643835737971 ) ) ;
#702=DIRECTION ( 'NONE',  ( 0.007885122365275663500, 0.9999689119394085113, 1.805443505845543142E-16 ) ) ;
#705=CARTESIAN_POINT ( 'NONE',  ( -4.534767414998234436, 37.71174666070368175, 76.36316342150684022 ) ) ;
#707=CARTESIAN_POINT ( 'NONE',  ( 0.4269670398180140936, 52.96169137011722228, 78.89164370455331721 ) ) ;
#708=FACE_OUTER_BOUND ( 'NONE', #9864, .T. ) ;
#710=CARTESIAN_POINT ( 'NONE',  ( 0.5922593966368500107, 52.21352501355296738, 75.36022115247205022 ) ) ;
#711=ORIENTED_EDGE ( 'NONE', *, *, #20025, .F. ) ;
#716=CARTESIAN_POINT ( 'NONE',  ( 6.924055141134583202, 50.37376929599953712, 78.48669174070734300 ) ) ;
#717=ORIENTED_EDGE ( 'NONE', *, *, #15127, .T. ) ;
#722=LINE ( 'NONE', #4010, #13169 ) ;
#723=DIRECTION ( 'NONE',  ( 1.540237394707284220E-16, 1.793354297423764243E-16, -1.000000000000000000 ) ) ;
#725=CARTESIAN_POINT ( 'NONE',  ( 8.792356959002002981, 41.14497608504091630, 76.18655208513948196 ) ) ;
#727=CARTESIAN_POINT ( 'NONE',  ( 4.439499113014429454, 51.28417780296363304, 75.58280986828056314 ) ) ;
#730=CARTESIAN_POINT ( 'NONE',  ( 1.658154530501163570, 36.04125148601230677, 76.86610350541322134 ) ) ;
#732=FACE_OUTER_BOUND ( 'NONE', #13452, .T. ) ;
#733=AXIS2_PLACEMENT_3D ( 'NONE', #10034, #6712, #11945 ) ;
#736=CARTESIAN_POINT ( 'NONE',  ( -4.007802336140563249, 51.74101282905964894, 79.45569801420249689 ) ) ;
#738=CARTESIAN_POINT ( 'NONE',  ( -4.850396850989173281, 37.19025346873809923, 77.31947969467269388 ) ) ;
#740=CARTESIAN_POINT ( 'NONE',  ( 0.5838706545074757726, 52.36194911346490954, 78.93669174070734584 ) ) ;
#741=EDGE_CURVE ( 'NONE', #19585, #19846, #11459, .T. ) ;
#744=ORIENTED_EDGE ( 'NONE', *, *, #6572, .T. ) ;
#745=AXIS2_PLACEMENT_3D ( 'NONE', #16885, #20171, #18584 ) ;
#746=CARTESIAN_POINT ( 'NONE',  ( 8.553273006160548420, 42.79284436168489947, 79.20437336408532758 ) ) ;
#748=CARTESIAN_POINT ( 'NONE',  ( 8.930560609631596591, 41.55918119345393080, 76.05553801048951357 ) ) ;
#751=LINE ( 'NONE', #13732, #1966 ) ;
#755=EDGE_CURVE ( 'NONE', #2672, #14271, #8781, .T. ) ;
#756=CARTESIAN_POINT ( 'NONE',  ( -7.720740609617425143, 47.25708002984855227, 78.10358362899698648 ) ) ;
#759=CARTESIAN_POINT ( 'NONE',  ( 6.851319717782478946, 37.86899943589613571, 76.12774863075016185 ) ) ;
#760=CARTESIAN_POINT ( 'NONE',  ( 5.791714832554497150, 51.21018346849771063, 78.93490712750880789 ) ) ;
#763=EDGE_CURVE ( 'NONE', #2000, #9068, #9535, .T. ) ;
#772=CARTESIAN_POINT ( 'NONE',  ( -4.274069566951154364, 51.55074801458793132, 79.52610421797659512 ) ) ;
#774=CARTESIAN_POINT ( 'NONE',  ( -8.192078482032012943, 42.93655631659661509, 75.45433879953087342 ) ) ;
#777=CARTESIAN_POINT ( 'NONE',  ( 5.327855396560547518, 50.80644620442382831, 77.95494770374325810 ) ) ;
#778=VECTOR ( 'NONE', #3824, 1000.000000000000000 ) ;
#781=CARTESIAN_POINT ( 'NONE',  ( 4.973101328672442811, 51.81486028805201727, 77.67439681936272677 ) ) ;
#784=DIRECTION ( 'NONE',  ( 1.540237394707284220E-16, 1.793354297423764243E-16, -1.000000000000000000 ) ) ;
#785=CARTESIAN_POINT ( 'NONE',  ( 5.807634474669838731, 51.19842427014940967, 79.54761434581399726 ) ) ;
#789=ORIENTED_EDGE ( 'NONE', *, *, #20431, .T. ) ;
#790=CARTESIAN_POINT ( 'NONE',  ( 8.804944317620234884, 41.18270119734690837, 78.86399424569901839 ) ) ;
#795=CARTESIAN_POINT ( 'NONE',  ( -8.068594480573938910, 42.12297466537643942, 77.08187429197492690 ) ) ;
#800=CARTESIAN_POINT ( 'NONE',  ( 0.5221537403065010796, 44.16218137147968292, 78.32492703482499508 ) ) ;
#803=ORIENTED_EDGE ( 'NONE', *, *, #2329, .T. ) ;
#804=FACE_BOUND ( 'NONE', #6425, .T. ) ;
#811=EDGE_CURVE ( 'NONE', #2938, #15510, #6634, .T. ) ;
#812=AXIS2_PLACEMENT_3D ( 'NONE', #507, #5716, #3806 ) ;
#814=CARTESIAN_POINT ( 'NONE',  ( -4.523256899386018937, 37.70324430649279179, 76.12782976279942204 ) ) ;
#816=CARTESIAN_POINT ( 'NONE',  ( -7.280826702657820171, 41.64048047902432614, 78.01850061686013760 ) ) ;
#817=CARTESIAN_POINT ( 'NONE',  ( 1.767938056577025741, 52.20425435525031332, 75.65494847458032268 ) ) ;
#819=CARTESIAN_POINT ( 'NONE',  ( 6.398363615859712361, 50.76207644957375464, 75.46588380158773646 ) ) ;
#820=CARTESIAN_POINT ( 'NONE',  ( 2.108290839596759003, 51.34989793853182505, 77.84551527011910821 ) ) ;
#823=CARTESIAN_POINT ( 'NONE',  ( 6.923174433796239313, 50.37441983903331533, 78.52964612251847143 ) ) ;
#825=DIRECTION ( 'NONE',  ( -0.9429220365244121993, 0.3330135628418984250, -8.551124769255302663E-17 ) ) ;
#826=CARTESIAN_POINT ( 'NONE',  ( 0.5221537403065008576, 44.16218137147968292, 80.45433879953087342 ) ) ;
#829=CARTESIAN_POINT ( 'NONE',  ( -7.359991238862622076, 41.90117226254449179, 78.84683685324785074 ) ) ;
#830=CARTESIAN_POINT ( 'NONE',  ( -7.531346616919285530, 42.61233131736031510, 79.37808970707625633 ) ) ;
#832=CARTESIAN_POINT ( 'NONE',  ( -6.210882734309923769, 46.73118581782181025, 75.45433879953087342 ) ) ;
#833=CARTESIAN_POINT ( 'NONE',  ( 8.817118105929894867, 41.21918681320168787, 76.01674029036281866 ) ) ;
#834=FACE_OUTER_BOUND ( 'NONE', #13780, .T. ) ;
#835=DIRECTION ( 'NONE',  ( 0.5954989751681698529, -0.8033560671169786005, -5.234922652618075161E-17 ) ) ;
#837=CARTESIAN_POINT ( 'NONE',  ( -7.945066593710369496, 41.73949022789241781, 78.79490040793942285 ) ) ;
#838=ORIENTED_EDGE ( 'NONE', *, *, #17686, .F. ) ;
#839=CARTESIAN_POINT ( 'NONE',  ( 8.950958007118590132, 41.62031348770922534, 78.64183653779139149 ) ) ;
#840=ORIENTED_EDGE ( 'NONE', *, *, #1689, .T. ) ;
#845=CARTESIAN_POINT ( 'NONE',  ( -4.718161399584266391, 37.09257646755418847, 75.97198585835440099 ) ) ;
#846=FACE_OUTER_BOUND ( 'NONE', #4937, .T. ) ;
#849=CARTESIAN_POINT ( 'NONE',  ( 5.524900579399185219, 50.65415293276860353, 78.06587361566768379 ) ) ;
#853=CARTESIAN_POINT ( 'NONE',  ( 8.162892682119435861, 41.62284976526770208, 79.54845644658969661 ) ) ;
#854=CARTESIAN_POINT ( 'NONE',  ( -4.074436747594614161, 36.61708299794013044, 75.46341390175899733 ) ) ;
#856=CARTESIAN_POINT ( 'NONE',  ( 0.5838706545074757726, 52.36194911346490954, 78.93669174070734584 ) ) ;
#857=CARTESIAN_POINT ( 'NONE',  ( 5.561379608955574483, 51.38032281970146897, 76.90580938776616904 ) ) ;
#858=CARTESIAN_POINT ( 'NONE',  ( 9.155505153612395475, 42.23335426198017473, 78.07975471416389723 ) ) ;
#861=CARTESIAN_POINT ( 'NONE',  ( -7.670684956156135215, 47.40709999874347602, 78.27541057140679470 ) ) ;
#862=DIRECTION ( 'NONE',  ( 1.540237394707284220E-16, 1.793354297423764243E-16, -1.000000000000000000 ) ) ;
#863=EDGE_CURVE ( 'NONE', #9302, #16784, #3241, .T. ) ;
#865=ORIENTED_EDGE ( 'NONE', *, *, #3090, .T. ) ;
#866=CARTESIAN_POINT ( 'NONE',  ( 5.410205795499257064, 50.73735288404611055, 77.28904345712264501 ) ) ;
#867=VERTEX_POINT ( 'NONE', #3450 ) ;
#868=CARTESIAN_POINT ( 'NONE',  ( -4.796459876899764829, 51.17746702502860501, 78.71090438869831019 ) ) ;
#870=ORIENTED_EDGE ( 'NONE', *, *, #20402, .T. ) ;
#872=DIRECTION ( 'NONE',  ( -0.5941461771851691553, -0.8043570849667760481, -2.357623395011396791E-16 ) ) ;
#874=CARTESIAN_POINT ( 'NONE',  ( -3.572718533232662530, 51.13213220290453620, 79.45569801420249689 ) ) ;
#875=CARTESIAN_POINT ( 'NONE',  ( -6.792737292293177909, 47.86790251333490431, 72.45433879953087342 ) ) ;
#876=CARTESIAN_POINT ( 'NONE',  ( 5.201148050424325042, 50.89177541897332446, 76.94115191089467487 ) ) ;
#878=ORIENTED_EDGE ( 'NONE', *, *, #3983, .T. ) ;
#879=LINE ( 'NONE', #2373, #10565 ) ;
#882=CARTESIAN_POINT ( 'NONE',  ( 4.539372959821318609, 52.13523796247791608, 76.58963291717793709 ) ) ;
#883=CARTESIAN_POINT ( 'NONE',  ( 6.828109521384686076, 50.44464046038347504, 77.45110917081549928 ) ) ;
#885=CARTESIAN_POINT ( 'NONE',  ( -7.833107574997801414, 41.39546341374030902, 76.33867328066237690 ) ) ;
#886=CARTESIAN_POINT ( 'NONE',  ( 8.868817592801745420, 41.37413345511091478, 75.97198585835440099 ) ) ;
#887=CARTESIAN_POINT ( 'NONE',  ( -4.174946515328806562, 37.44075729451967760, 78.12452307498179493 ) ) ;
#888=CARTESIAN_POINT ( 'NONE',  ( 6.489847418355314979, 49.78593742637539776, 78.48669174070734300 ) ) ;
#889=VERTEX_POINT ( 'NONE', #9743 ) ;
#890=CARTESIAN_POINT ( 'NONE',  ( 8.787829143201873805, 41.13140593384864729, 78.45948585835439815 ) ) ;
#894=CARTESIAN_POINT ( 'NONE',  ( -7.364103761167730688, 42.34575162834247664, 77.08187429197492690 ) ) ;
#897=LINE ( 'NONE', #15589, #7222 ) ;
#898=CARTESIAN_POINT ( 'NONE',  ( 0.3326973149608335456, 52.96014171822455552, 77.76169174070734869 ) ) ;
#900=DIRECTION ( 'NONE',  ( -0.3165065846431170393, -0.9485903129789747812, 0.000000000000000000 ) ) ;
#902=FACE_OUTER_BOUND ( 'NONE', #1834, .T. ) ;
#903=ORIENTED_EDGE ( 'NONE', *, *, #17975, .F. ) ;
#906=ORIENTED_EDGE ( 'NONE', *, *, #9778, .F. ) ;
#909=AXIS2_PLACEMENT_3D ( 'NONE', #9327, #1226, #1330 ) ;
#911=CARTESIAN_POINT ( 'NONE',  ( -3.568560454108619773, 36.24341255788211669, 78.11242031084098869 ) ) ;
#912=CARTESIAN_POINT ( 'NONE',  ( 5.428282431822193388, 36.85214909206928269, 76.61095391776262886 ) ) ;
#913=EDGE_CURVE ( 'NONE', #16685, #14370, #19197, .T. ) ;
#914=CYLINDRICAL_SURFACE ( 'NONE', #4488, 6.000000000000002665 ) ;
#915=EDGE_CURVE ( 'NONE', #7365, #682, #8745, .T. ) ;
#917=CARTESIAN_POINT ( 'NONE',  ( 1.478628313566038077, 52.95937378012966690, 75.49332451037695080 ) ) ;
#918=ORIENTED_EDGE ( 'NONE', *, *, #10957, .F. ) ;
#919=FACE_BOUND ( 'NONE', #656, .T. ) ;
#920=EDGE_CURVE ( 'NONE', #6129, #19774, #17602, .T. ) ;
#921=CARTESIAN_POINT ( 'NONE',  ( 1.652727357819364418, 35.35299279957455099, 76.16022115247204738 ) ) ;
#923=ADVANCED_FACE ( 'NONE', ( #3145 ), #3031, .F. ) ;
#924=ORIENTED_EDGE ( 'NONE', *, *, #9750, .F. ) ;
#925=CIRCLE ( 'NONE', #3632, 8.199999999999995737 ) ;
#926=CARTESIAN_POINT ( 'NONE',  ( -4.383323755399650246, 50.73378672401133826, 75.36197610833401939 ) ) ;
#928=FACE_OUTER_BOUND ( 'NONE', #9385, .T. ) ;
#929=DIRECTION ( 'NONE',  ( 1.540237394707284220E-16, 1.793354297423764243E-16, -1.000000000000000000 ) ) ;
#931=CARTESIAN_POINT ( 'NONE',  ( -5.412716252285424190, 48.91899944357702879, 72.45433879953087342 ) ) ;
#932=CARTESIAN_POINT ( 'NONE',  ( -7.018774656858025374, 41.28963458989208846, 79.50989352969267543 ) ) ;
#936=AXIS2_PLACEMENT_3D ( 'NONE', #5717, #18816, #20979 ) ;
#937=CARTESIAN_POINT ( 'NONE',  ( -5.271099104061234719, 49.91853162867187166, 75.88700421999355683 ) ) ;
#938=CARTESIAN_POINT ( 'NONE',  ( 5.080928206799192992, 51.73521291671138300, 75.47011219584838670 ) ) ;
#941=CARTESIAN_POINT ( 'NONE',  ( -7.590962929491896105, 40.75019128785367428, 79.42781143817570921 ) ) ;
#943=CARTESIAN_POINT ( 'NONE',  ( 8.336228674048411946, 41.69800626661804444, 78.91042349786003740 ) ) ;
#944=ORIENTED_EDGE ( 'NONE', *, *, #19238, .F. ) ;
#945=CARTESIAN_POINT ( 'NONE',  ( -7.610866399937288307, 43.11623716858539979, 75.65823358996551917 ) ) ;
#947=EDGE_CURVE ( 'NONE', #4394, #14370, #1546, .T. ) ;
#948=CARTESIAN_POINT ( 'NONE',  ( -3.713457647669470063, 51.95134076679423174, 79.29276450469329518 ) ) ;
#949=SURFACE_STYLE_USAGE ( .BOTH. , #20520 ) ;
#951=CARTESIAN_POINT ( 'NONE',  ( 0.5221537403065010796, 44.16218137147968292, 78.25433879953088478 ) ) ;
#952=CARTESIAN_POINT ( 'NONE',  ( -8.289887965425112526, 42.82811778982430440, 78.89751519991851580 ) ) ;
#953=CARTESIAN_POINT ( 'NONE',  ( 0.5221537403065011906, 44.16218137147968292, 77.43080938776617472 ) ) ;
#954=CARTESIAN_POINT ( 'NONE',  ( -4.196599071979020046, 37.46195532796716776, 76.05537227506185616 ) ) ;
#955=ORIENTED_EDGE ( 'NONE', *, *, #12761, .T. ) ;
#957=B_SPLINE_CURVE_WITH_KNOTS ( 'NONE', 3,
 ( #8213, #3213, #17789, #20957, #4896, #16196, #6391, #19271, #20859, #1410, #4684, #11207 ),
 .UNSPECIFIED., .F., .F.,
 ( 4, 2, 2, 2, 2, 4 ),
 ( 0.000000000000000000, 0.0001994714521133825950, 0.0003989429042267651901, 0.0007978858084534908067, 0.001196828712680216749, 0.001595771616906942365 ),
 .UNSPECIFIED. ) ;
#958=CARTESIAN_POINT ( 'NONE',  ( 8.288346550782289768, 41.53027563821294166, 78.93576830848654424 ) ) ;
#962=CARTESIAN_POINT ( 'NONE',  ( 5.599756831756513620, 51.35197511114724733, 78.21422674182478829 ) ) ;
#963=CARTESIAN_POINT ( 'NONE',  ( 8.370724156415352724, 42.24573387831544835, 78.12791555553386047 ) ) ;
#966=CARTESIAN_POINT ( 'NONE',  ( -4.572866156349838285, 51.33723891144499163, 75.97260225988416948 ) ) ;
#967=CARTESIAN_POINT ( 'NONE',  ( -7.727022169037351063, 47.23825379777235156, 77.78596583901244799 ) ) ;
#969=CARTESIAN_POINT ( 'NONE',  ( 6.880792506138228681, 37.89005961138749967, 76.49840989696882332 ) ) ;
#971=CARTESIAN_POINT ( 'NONE',  ( 5.929557977968517690, 51.10836428964097422, 77.10005730845655592 ) ) ;
#977=AXIS2_PLACEMENT_3D ( 'NONE', #6001, #1220, #20666 ) ;
#978=CARTESIAN_POINT ( 'NONE',  ( -0.9388773962491537839, 52.84004908296358849, 72.45433879953087342 ) ) ;
#981=CARTESIAN_POINT ( 'NONE',  ( 0.3849377270197763545, 52.36105381785655055, 77.46089079190313953 ) ) ;
#982=CARTESIAN_POINT ( 'NONE',  ( -3.532917577324401925, 36.21708460058427193, 78.46683879953087626 ) ) ;
#984=CARTESIAN_POINT ( 'NONE',  ( 4.048141534226263438, 36.75897868094575216, 79.45433879953087342 ) ) ;
#985=EDGE_CURVE ( 'NONE', #165, #15850, #4155, .T. ) ;
#987=ORIENTED_EDGE ( 'NONE', *, *, #14448, .T. ) ;
#988=CARTESIAN_POINT ( 'NONE',  ( -4.047219024143313248, 37.35069009299581211, 75.37207009874634878 ) ) ;
#989=PLANE ( 'NONE',  #4341 ) ;
#990=CARTESIAN_POINT ( 'NONE',  ( -7.149724537181753270, 47.05990690267743304, 79.05973021912267029 ) ) ;
#991=FACE_OUTER_BOUND ( 'NONE', #3571, .T. ) ;
#992=CARTESIAN_POINT ( 'NONE',  ( -4.432998774651716545, 37.62853090491852015, 77.91271439283131883 ) ) ;
#993=CARTESIAN_POINT ( 'NONE',  ( 6.352851448254905442, 49.92817053755964452, 79.12994158702615266 ) ) ;
#995=ORIENTED_EDGE ( 'NONE', *, *, #8965, .F. ) ;
#996=CARTESIAN_POINT ( 'NONE',  ( 4.621588727139584130, 51.26391586304784198, 77.68963291717793140 ) ) ;
#999=CARTESIAN_POINT ( 'NONE',  ( -4.652687709939232086, 51.28020135170361016, 75.36022115247205022 ) ) ;
#1001=CARTESIAN_POINT ( 'NONE',  ( -7.933076142375738549, 41.69442312082315993, 77.67112630499640602 ) ) ;
#1002=EDGE_LOOP ( 'NONE', ( #17060, #19303, #20211, #3071 ) ) ;
#1003=VECTOR ( 'NONE', #13053, 1000.000000000000000 ) ;
#1007=CARTESIAN_POINT ( 'NONE',  ( 4.597212664172372953, 36.25829706351294135, 75.77524573853747825 ) ) ;
#1009=ADVANCED_FACE ( 'NONE', ( #7454 ), #4426, .F. ) ;
#1017=CARTESIAN_POINT ( 'NONE',  ( 5.094470189521428161, 37.35527774201511875, 76.21970569554892450 ) ) ;
#1019=VECTOR ( 'NONE', #11103, 1000.000000000000000 ) ;
#1021=CARTESIAN_POINT ( 'NONE',  ( 5.125405977158137283, 37.38264009880134608, 76.06572720930677178 ) ) ;
#1022=CARTESIAN_POINT ( 'NONE',  ( 5.289916459460165754, 50.82772623642982524, 78.90029747732744170 ) ) ;
#1023=CARTESIAN_POINT ( 'NONE',  ( 8.868817592801743643, 41.37413345511091478, 75.97198585835440099 ) ) ;
#1026=CARTESIAN_POINT ( 'NONE',  ( 1.555492715512752255, 52.20592956483955760, 75.52862058684291924 ) ) ;
#1031=CARTESIAN_POINT ( 'NONE',  ( 0.6404851603139647409, 52.36132752672286017, 79.54845644658969661 ) ) ;
#1034=B_SPLINE_SURFACE_WITH_KNOTS ( 'NONE', 3, 1, ( 
 ( #5879, #17362 ),
 ( #2892, #14065 ),
 ( #18851, #10789 ),
 ( #6178, #2792 ),
 ( #20444, #9293 ),
 ( #1196, #7681 ),
 ( #6071, #9392 ),
 ( #20849, #14374 ),
 ( #15876, #12682 ),
 ( #9183, #17564 ),
 ( #15673, #19162 ),
 ( #12377, #11096 ),
 ( #1093, #9495 ),
 ( #17155, #15981 ),
 ( #7888, #6276 ),
 ( #12778, #10693 ),
 ( #7467, #17256 ),
 ( #11305, #8095 ),
 ( #4779, #14688 ),
 ( #17877, #19469 ),
 ( #7993, #3299 ),
 ( #19677, #10321 ),
 ( #5386, #1610 ),
 ( #4886, #14584 ),
 ( #9807, #11906 ),
 ( #112, #18381 ),
 ( #11, #19570 ) ),
 .UNSPECIFIED., .F., .F., .F.,
 ( 4, 1, 1, 1, 1, 1, 1, 1, 1, 1, 1, 1, 1, 1, 1, 1, 1, 1, 1, 1, 1, 1, 1, 1, 4 ),
 ( 2, 2 ),
 ( 0.000000000000000000, 0.05996724504547770729, 0.1145758167962369900, 0.1640861619357650014, 0.2084987699952417783, 0.2475617630034998851, 0.2815348823686551483, 0.3104252079858747515, 0.3342443525417332362, 0.3765838217147600697, 0.4197110765771541185, 0.4650989620513389933, 0.5135994637417293784, 0.5388633206098475403, 0.5643363709942800233, 0.5903657223275191601, 0.6168353869529757949, 0.6439286963540884479, 0.6717746256502626911, 0.7005904770003053006, 0.7303719928790673999, 0.7923444005162998405, 0.8574606674909915904, 0.9267280696664335071, 1.000000000000000000 ),
 ( 0.000000000000000000, 1.000000000000000000 ),
 .UNSPECIFIED. ) ;
#1036=ORIENTED_EDGE ( 'NONE', *, *, #17255, .F. ) ;
#1037=AXIS2_PLACEMENT_3D ( 'NONE', #12828, #8146, #14742 ) ;
#1038=EDGE_CURVE ( 'NONE', #476, #10886, #8836, .T. ) ;
#1039=CARTESIAN_POINT ( 'NONE',  ( 5.593371404305700345, 50.44267676395632805, 79.53335372712579954 ) ) ;
#1041=FACE_OUTER_BOUND ( 'NONE', #16159, .T. ) ;
#1043=LINE ( 'NONE', #7201, #19684 ) ;
#1044=CARTESIAN_POINT ( 'NONE',  ( 8.385738467910485383, 39.92631467184355643, 77.08252479744105301 ) ) ;
#1046=ORIENTED_EDGE ( 'NONE', *, *, #5178, .T. ) ;
#1047=CARTESIAN_POINT ( 'NONE',  ( -4.578768572918463953, 36.98961260158171882, 78.00876120161012750 ) ) ;
#1048=CARTESIAN_POINT ( 'NONE',  ( -7.570753287668954279, 40.54925684501983341, 79.32598559883581402 ) ) ;
#1049=CARTESIAN_POINT ( 'NONE',  ( -7.497174307679370209, 42.44115768106999553, 79.44947929565324785 ) ) ;
#1053=CARTESIAN_POINT ( 'NONE',  ( 5.712782733624313103, 51.26848743039855094, 75.36064185147203887 ) ) ;
#1054=ADVANCED_FACE ( 'NONE', ( #8945 ), #19050, .T. ) ;
#1056=B_SPLINE_CURVE_WITH_KNOTS ( 'NONE', 3,
 ( #6216, #17218, #7822, #20286, #17599, #14305, #9536, #3027, #4709, #2643, #3237, #12923, #5831, #17709 ),
 .UNSPECIFIED., .F., .F.,
 ( 4, 2, 2, 2, 2, 2, 4 ),
 ( 0.000000000000000000, 0.0001389608718179012755, 0.0002779217436358025510, 0.0003474021795447532158, 0.0004168826154537039349, 0.0004863630513626545997, 0.0005558434872716053188 ),
 .UNSPECIFIED. ) ;
#1057=VECTOR ( 'NONE', #18086, 1000.000000000000000 ) ;
#1058=DIRECTION ( 'NONE',  ( 1.540237394707284220E-16, 1.793354297423764243E-16, -1.000000000000000000 ) ) ;
#1060=CARTESIAN_POINT ( 'NONE',  ( 6.691294758883309157, 37.75465145915448062, 79.45433879953087342 ) ) ;
#1062=CARTESIAN_POINT ( 'NONE',  ( -4.574316323987747346, 51.33620267474496757, 79.54845644658969661 ) ) ;
#1064=CARTESIAN_POINT ( 'NONE',  ( -7.343158166839156564, 42.28655005559638624, 79.49764826322659417 ) ) ;
#1065=CARTESIAN_POINT ( 'NONE',  ( 5.534247820986439415, 36.92786807952553119, 77.73906448345020692 ) ) ;
#1067=CARTESIAN_POINT ( 'NONE',  ( 9.353718648869055130, 42.82741268169404947, 78.44945682776121032 ) ) ;
#1069=EDGE_CURVE ( 'NONE', #18879, #5725, #3926, .T. ) ;
#1070=CARTESIAN_POINT ( 'NONE',  ( 8.940907051378230719, 41.59019013573462331, 76.11674899411023887 ) ) ;
#1071=CARTESIAN_POINT ( 'NONE',  ( 5.939849532777430774, 51.10076233267274404, 76.96076274685535168 ) ) ;
#1073=B_SPLINE_CURVE_WITH_KNOTS ( 'NONE', 3,
 ( #18568, #4089, #5681, #13993, #15493, #20478, #10506, #12408, #16769, #9006, #16871, #2189, #2401, #20153, #15168, #13778, #5475, #7177, #2609, #582 ),
 .UNSPECIFIED., .F., .F.,
 ( 4, 2, 2, 2, 2, 2, 2, 2, 2, 4 ),
 ( 0.000000000000000000, 0.0002954762126916160841, 0.0005909524253832317345, 0.0008864286380748474933, 0.001181904850766463252, 0.001477381063458079119, 0.001625119169803869489, 0.001772857276149659858, 0.002068333488841280713, 0.002363809701532901784 ),
 .UNSPECIFIED. ) ;
#1077=ADVANCED_FACE ( 'NONE', ( #16915 ), #631, .T. ) ;
#1078=VECTOR ( 'NONE', #6501, 1000.000000000000114 ) ;
#1079=CARTESIAN_POINT ( 'NONE',  ( -0.9223058776520068891, 52.84282348712751798, 78.54073599580733855 ) ) ;
#1082=CARTESIAN_POINT ( 'NONE',  ( -5.955451856753751549, 38.00651308716548726, 78.53742703482498655 ) ) ;
#1083=CARTESIAN_POINT ( 'NONE',  ( 0.6073277304985209568, 52.36177255988537382, 78.93565971576092011 ) ) ;
#1085=CARTESIAN_POINT ( 'NONE',  ( 1.794851674890223459, 52.26306568748834991, 75.67222655803806219 ) ) ;
#1091=VERTEX_POINT ( 'NONE', #5531 ) ;
#1093=CARTESIAN_POINT ( 'NONE',  ( -0.7867047173639660773, 52.21826805272613115, 75.89928829349869943 ) ) ;
#1094=CARTESIAN_POINT ( 'NONE',  ( 8.946756316568102108, 41.60772075457913388, 78.11862058389174024 ) ) ;
#1096=CARTESIAN_POINT ( 'NONE',  ( -4.409036544953043979, 47.67330854490502645, 72.45432679953087529 ) ) ;
#1097=CARTESIAN_POINT ( 'NONE',  ( -3.887033836373874784, 37.39267102169923618, 79.51042285023450518 ) ) ;
#1099=CARTESIAN_POINT ( 'NONE',  ( 5.838531714063069700, 37.14529820897372758, 77.55803991379978868 ) ) ;
#1101=ORIENTED_EDGE ( 'NONE', *, *, #4826, .T. ) ;
#1104=CARTESIAN_POINT ( 'NONE',  ( -7.320717484398829633, 46.55579181444844750, 79.45433879953087342 ) ) ;
#1108=CARTESIAN_POINT ( 'NONE',  ( -5.157025508368711542, 37.41674770618861601, 75.39928922905468767 ) ) ;
#1111=CARTESIAN_POINT ( 'NONE',  ( 8.215319998344366326, 41.32401173211437850, 76.31063117824747621 ) ) ;
#1112=ORIENTED_EDGE ( 'NONE', *, *, #5848, .F. ) ;
#1115=CARTESIAN_POINT ( 'NONE',  ( -7.080934810785074696, 41.45028247878327221, 78.59694605312716931 ) ) ;
#1116=VERTEX_POINT ( 'NONE', #13414 ) ;
#1120=CARTESIAN_POINT ( 'NONE',  ( -4.156963686837030103, 37.43267826557348599, 78.61392107264721574 ) ) ;
#1122=CARTESIAN_POINT ( 'NONE',  ( 5.205681390936892861, 50.88842682295077680, 76.21945306000542075 ) ) ;
#1123=VECTOR ( 'NONE', #10142, 1000.000000000000227 ) ;
#1124=EDGE_LOOP ( 'NONE', ( #8653, #3076, #5632, #3231 ) ) ;
#1127=EDGE_LOOP ( 'NONE', ( #16, #17882, #8412, #15082, #6611, #1732 ) ) ;
#1129=LINE ( 'NONE', #14304, #11229 ) ;
#1132=CARTESIAN_POINT ( 'NONE',  ( 5.464930624430781592, 36.87833654873140432, 76.10043865634602867 ) ) ;
#1133=CARTESIAN_POINT ( 'NONE',  ( 8.792356959002002981, 41.14497608504091630, 76.18655208513948196 ) ) ;
#1136=ADVANCED_FACE ( 'NONE', ( #6910 ), #5733, .T. ) ;
#1137=CARTESIAN_POINT ( 'NONE',  ( 2.114670974380917112, 52.20152023876698166, 76.45922371407752394 ) ) ;
#1139=CARTESIAN_POINT ( 'NONE',  ( 6.695638642021790155, 50.54249136271632636, 75.66183449524544358 ) ) ;
#1140=CARTESIAN_POINT ( 'NONE',  ( 5.495239211387634271, 37.64690938752282534, 77.40928489470421425 ) ) ;
#1142=CARTESIAN_POINT ( 'NONE',  ( -4.138842527380969472, 50.91175009559962916, 75.36205588254068743 ) ) ;
#1146=CARTESIAN_POINT ( 'NONE',  ( -3.580888326837075475, 36.25251866086962593, 75.96390267329995538 ) ) ;
#1147=CARTESIAN_POINT ( 'NONE',  ( -4.909077168075741682, 50.30854671200530959, 75.47180400867900119 ) ) ;
#1148=ORIENTED_EDGE ( 'NONE', *, *, #11269, .T. ) ;
#1149=CARTESIAN_POINT ( 'NONE',  ( 4.174832730680089199, 51.49049413994026025, 78.81874598975664981 ) ) ;
#1150=PLANE ( 'NONE',  #7800 ) ;
#1152=VECTOR ( 'NONE', #18705, 1000.000000000000114 ) ;
#1153=EDGE_CURVE ( 'NONE', #14867, #8763, #4842, .T. ) ;
#1154=ORIENTED_EDGE ( 'NONE', *, *, #10571, .F. ) ;
#1155=CARTESIAN_POINT ( 'NONE',  ( 6.520305832453487049, 49.75344699685330596, 76.44686420531779447 ) ) ;
#1156=CARTESIAN_POINT ( 'NONE',  ( -6.705005553477274560, 40.29739814665693132, 78.50801527011910252 ) ) ;
#1157=CARTESIAN_POINT ( 'NONE',  ( -5.509791672390228712, 38.60739634041024715, 78.62262977491066351 ) ) ;
#1160=CARTESIAN_POINT ( 'NONE',  ( 5.008928291858447679, 51.78839635354462700, 75.50506468444432073 ) ) ;
#1162=EDGE_CURVE ( 'NONE', #19108, #5214, #13598, .T. ) ;
#1163=CARTESIAN_POINT ( 'NONE',  ( 9.026838159693451047, 41.84773111872319618, 78.13669174070733447 ) ) ;
#1164=CARTESIAN_POINT ( 'NONE',  ( 8.946998292058729874, 41.60844597047518789, 78.80177617112552468 ) ) ;
#1166=CARTESIAN_POINT ( 'NONE',  ( -4.006646489220814011, 48.09791109810387155, 82.45433879953087342 ) ) ;
#1170=DIRECTION ( 'NONE',  ( 0.5813877811927011807, -0.8136266022444372803, -5.636455622144619183E-17 ) ) ;
#1171=CARTESIAN_POINT ( 'NONE',  ( 5.561379608955574483, 51.38032281970146897, 76.39036821129558064 ) ) ;
#1173=LINE ( 'NONE', #7333, #12306 ) ;
#1174=VERTEX_POINT ( 'NONE', #21000 ) ;
#1175=CARTESIAN_POINT ( 'NONE',  ( 8.215457551141771120, 41.32437277815750321, 78.72120140517411357 ) ) ;
#1176=CARTESIAN_POINT ( 'NONE',  ( -3.964734524320789877, 36.53605038468285215, 79.39152984579853012 ) ) ;
#1177=CARTESIAN_POINT ( 'NONE',  ( 0.3821786226492924210, 35.36301154328572949, 78.57639762306027365 ) ) ;
#1178=DIRECTION ( 'NONE',  ( 0.6080936526121289987, 0.7938652969193448206, 2.360290325043240801E-16 ) ) ;
#1184=EDGE_CURVE ( 'NONE', #20695, #4844, #6435, .T. ) ;
#1186=EDGE_CURVE ( 'NONE', #15454, #9664, #12945, .T. ) ;
#1187=DIRECTION ( 'NONE',  ( -0.3165065846431824870, -0.9485903129789529098, 0.000000000000000000 ) ) ;
#1188=B_SPLINE_CURVE_WITH_KNOTS ( 'NONE', 3,
 ( #283, #6355, #16164, #4649, #13174, #11170, #19334, #19648, #86, #8383, #4753, #11486, #3183, #4964, #13073, #5073, #19548, #11591, #3486, #8068 ),
 .UNSPECIFIED., .F., .F.,
 ( 4, 2, 2, 2, 2, 2, 2, 2, 2, 4 ),
 ( 0.000000000000000000, 0.0002953950361844887278, 0.0005907900723689777809, 0.0008861851085534668340, 0.001181580144737955779, 0.001476975180922444940, 0.001624672699014688328, 0.001772370217106931283, 0.002067765253291418710, 0.002363160289475906353 ),
 .UNSPECIFIED. ) ;
#1189=ORIENTED_EDGE ( 'NONE', *, *, #1153, .T. ) ;
#1191=EDGE_CURVE ( 'NONE', #3376, #9436, #6232, .T. ) ;
#1195=ADVANCED_FACE ( 'NONE', ( #20899 ), #19423, .F. ) ;
#1196=CARTESIAN_POINT ( 'NONE',  ( -0.9375027607463610746, 52.21945715071739613, 76.61976384666378692 ) ) ;
#1200=LINE ( 'NONE', #13102, #414 ) ;
#1202=CARTESIAN_POINT ( 'NONE',  ( 8.887668352622405621, 41.43063037816333605, 75.36022115247205022 ) ) ;
#1207=LINE ( 'NONE', #4489, #17796 ) ;
#1208=DIRECTION ( 'NONE',  ( 0.3165065846431826535, 0.9485903129789529098, 2.188653791613874008E-16 ) ) ;
#1210=CARTESIAN_POINT ( 'NONE',  ( 8.227529334238381509, 41.35732131334246731, 76.09516292429817952 ) ) ;
#1212=CARTESIAN_POINT ( 'NONE',  ( -3.061196554867672948, 51.49764708062921414, 75.88277413867518817 ) ) ;
#1215=CARTESIAN_POINT ( 'NONE',  ( -7.081455809225041698, 41.45193003946861410, 78.55785233681892521 ) ) ;
#1216=ORIENTED_EDGE ( 'NONE', *, *, #418, .T. ) ;
#1218=DIRECTION ( 'NONE',  ( -1.540237394707284467E-16, -1.793354297423764243E-16, 1.000000000000000000 ) ) ;
#1219=ORIENTED_EDGE ( 'NONE', *, *, #3797, .F. ) ;
#1220=DIRECTION ( 'NONE',  ( -1.540237394707284220E-16, -1.793354297423764243E-16, 1.000000000000000000 ) ) ;
#1221=CARTESIAN_POINT ( 'NONE',  ( 5.619974078175711263, 51.33704144561774996, 76.01203914421944319 ) ) ;
#1222=ORIENTED_EDGE ( 'NONE', *, *, #654, .T. ) ;
#1223=CARTESIAN_POINT ( 'NONE',  ( 0.5221537403065009686, 44.16218137147968292, 79.45433879953087342 ) ) ;
#1224=CARTESIAN_POINT ( 'NONE',  ( 0.7188031343443799237, 52.96453286013366579, 78.90093525964157095 ) ) ;
#1225=ORIENTED_EDGE ( 'NONE', *, *, #9336, .F. ) ;
#1226=DIRECTION ( 'NONE',  ( -1.540237394707283727E-16, -1.793354297423763257E-16, 1.000000000000000000 ) ) ;
#1227=CARTESIAN_POINT ( 'NONE',  ( 0.5221537403065013017, 44.16218137147968292, 76.86610350541323555 ) ) ;
#1229=CARTESIAN_POINT ( 'NONE',  ( 5.102094394548418954, 37.36598249535994398, 76.14053225265315916 ) ) ;
#1230=CARTESIAN_POINT ( 'NONE',  ( 5.427780505986065762, 36.85179043424346190, 76.70433879953087342 ) ) ;
#1231=CARTESIAN_POINT ( 'NONE',  ( -3.798187483714133172, 36.41302879471073339, 77.61986069475027250 ) ) ;
#1233=CARTESIAN_POINT ( 'NONE',  ( 2.120636086428073774, 52.95414912482170422, 78.26636343789274974 ) ) ;
#1235=LINE ( 'NONE', #9547, #13257 ) ;
#1236=CARTESIAN_POINT ( 'NONE',  ( 5.377879434019748217, 37.56304838743142227, 77.74321050730907245 ) ) ;
#1238=CARTESIAN_POINT ( 'NONE',  ( -2.917199766949189588, 51.60602765227618960, 76.69845644658968808 ) ) ;
#1239=ORIENTED_EDGE ( 'NONE', *, *, #4663, .T. ) ;
#1241=CARTESIAN_POINT ( 'NONE',  ( -4.067689360272797039, 37.53693192171343185, 75.36838243422435824 ) ) ;
#1242=CARTESIAN_POINT ( 'NONE',  ( -6.752712905682232147, 40.37832409722801685, 78.03977571741488362 ) ) ;
#1243=APPLICATION_CONTEXT ( 'automotive_design' ) ;
#1245=CARTESIAN_POINT ( 'NONE',  ( 4.639020460657009792, 52.06163236765677738, 78.92424046551381878 ) ) ;
#1246=CARTESIAN_POINT ( 'NONE',  ( 8.806278593017598411, 41.18670010535765869, 77.44807837618913027 ) ) ;
#1247=CARTESIAN_POINT ( 'NONE',  ( 8.387827792284632267, 39.93257650953714943, 76.58175473889373563 ) ) ;
#1248=VECTOR ( 'NONE', #173, 1000.000000000000000 ) ;
#1249=ORIENTED_EDGE ( 'NONE', *, *, #13683, .T. ) ;
#1250=CARTESIAN_POINT ( 'NONE',  ( 6.508108282020931057, 49.76650363545953581, 76.25652011681395948 ) ) ;
#1251=CARTESIAN_POINT ( 'NONE',  ( 5.761154613439540384, 51.23275707131721646, 77.94923276678728996 ) ) ;
#1254=ADVANCED_FACE ( 'NONE', ( #3048 ), #18871, .F. ) ;
#1256=CARTESIAN_POINT ( 'NONE',  ( 6.348731048540022570, 38.39225852662888627, 77.99342907322302665 ) ) ;
#1257=DIRECTION ( 'NONE',  ( -1.540237394707284220E-16, -1.793354297423764243E-16, 1.000000000000000000 ) ) ;
#1258=CARTESIAN_POINT ( 'NONE',  ( 8.527988662190095326, 48.03182059810101379, 79.44551527011911674 ) ) ;
#1259=EDGE_CURVE ( 'NONE', #3817, #16083, #10291, .T. ) ;
#1260=CARTESIAN_POINT ( 'NONE',  ( -0.9435164075001931661, 52.21748252032886484, 77.82884852524264829 ) ) ;
#1261=VECTOR ( 'NONE', #7367, 1000.000000000000227 ) ;
#1262=CARTESIAN_POINT ( 'NONE',  ( 7.680032241523796266, 40.16158449578585277, 72.45433879953087342 ) ) ;
#1263=CARTESIAN_POINT ( 'NONE',  ( 8.604143167063659448, 40.58088741054138637, 79.41216397796385706 ) ) ;
#1266=CARTESIAN_POINT ( 'NONE',  ( -8.305235601612645624, 42.87665183533326996, 78.69093640348562246 ) ) ;
#1267=CARTESIAN_POINT ( 'NONE',  ( 5.317402881116432667, 37.51983405691463958, 75.97247164366282846 ) ) ;
#1269=CARTESIAN_POINT ( 'NONE',  ( -4.535380886826608560, 37.70757786157348335, 78.71874188495704061 ) ) ;
#1270=CARTESIAN_POINT ( 'NONE',  ( -4.811608766808348037, 37.16160227343304712, 79.54845644658969661 ) ) ;
#1271=CARTESIAN_POINT ( 'NONE',  ( -4.753421688333184569, 37.11862182248194131, 78.93508260432024315 ) ) ;
#1273=CARTESIAN_POINT ( 'NONE',  ( 5.605612954821764582, 51.34764942893797013, 78.13212606300182017 ) ) ;
#1274=AXIS2_PLACEMENT_3D ( 'NONE', #5713, #8813, #15307 ) ;
#1276=CARTESIAN_POINT ( 'NONE',  ( 8.582646700885783630, 42.88087918820886557, 77.82525376769920911 ) ) ;
#1279=( BOUNDED_CURVE ( )  B_SPLINE_CURVE ( 3, ( #1312, #9509, #3215, #7901 ),
 .UNSPECIFIED., .F., .F. ) 
 B_SPLINE_CURVE_WITH_KNOTS ( ( 4, 4 ),
 ( 4.605568300160951090, 4.721714797055254209 ),
 .UNSPECIFIED. ) 
 CURVE ( )  GEOMETRIC_REPRESENTATION_ITEM ( )  RATIONAL_B_SPLINE_CURVE ( ( 1.000000000000000000, 0.9988761485075002833, 0.9988761485075002833, 1.000000000000000000 ) ) 
 REPRESENTATION_ITEM ( '' )  );
#1284=CARTESIAN_POINT ( 'NONE',  ( 0.7995893671964704463, 52.35749147831580075, 78.82132991813820411 ) ) ;
#1285=CARTESIAN_POINT ( 'NONE',  ( -3.473388836350903119, 37.00066556884812030, 77.65937392779746062 ) ) ;
#1286=EDGE_CURVE ( 'NONE', #6210, #10787, #11772, .T. ) ;
#1289=DIRECTION ( 'NONE',  ( 0.9999689119394086223, -0.007885122365274166434, 1.526048693634355610E-16 ) ) ;
#1292=CARTESIAN_POINT ( 'NONE',  ( 5.901851037876958195, 51.12883029018298231, 78.62249727093715990 ) ) ;
#1294=CARTESIAN_POINT ( 'NONE',  ( 4.719835101441633540, 52.00193784792148222, 79.11209812681292419 ) ) ;
#1296=CARTESIAN_POINT ( 'NONE',  ( 0.7200154223361650008, 52.35315281306618829, 75.99814205791308552 ) ) ;
#1297=DIRECTION ( 'NONE',  ( -0.007885122365275663500, -0.9999689119394085113, -1.805443505845543142E-16 ) ) ;
#1298=EDGE_CURVE ( 'NONE', #13246, #3817, #8302, .T. ) ;
#1300=EDGE_CURVE ( 'NONE', #13048, #19006, #5153, .T. ) ;
#1301=CARTESIAN_POINT ( 'NONE',  ( 8.868817592801743643, 41.37413345511091478, 75.97198585835440099 ) ) ;
#1303=VECTOR ( 'NONE', #3193, 1000.000000000000227 ) ;
#1304=ORIENTED_EDGE ( 'NONE', *, *, #14130, .F. ) ;
#1306=CARTESIAN_POINT ( 'NONE',  ( -2.083470957239373256, 47.45622447009557021, 82.45433879953087342 ) ) ;
#1307=CARTESIAN_POINT ( 'NONE',  ( -0.02883801100815608018, 35.36625256049322275, 79.45433879953087342 ) ) ;
#1308=DIRECTION ( 'NONE',  ( 1.540237394707284220E-16, 1.793354297423764243E-16, -1.000000000000000000 ) ) ;
#1312=CARTESIAN_POINT ( 'NONE',  ( 8.559588968570775336, 45.78687671259945802, 75.44992703482499508 ) ) ;
#1314=EDGE_LOOP ( 'NONE', ( #18437, #9465, #7349, #17556 ) ) ;
#1315=CARTESIAN_POINT ( 'NONE',  ( 4.623413712694776301, 52.07316044369832042, 78.06776350345396054 ) ) ;
#1317=EDGE_LOOP ( 'NONE', ( #15615, #5320, #19697, #944 ) ) ;
#1318=CARTESIAN_POINT ( 'NONE',  ( -2.961117163336547620, 51.56916014967697492, 76.13050287850805375 ) ) ;
#1320=CARTESIAN_POINT ( 'NONE',  ( -7.150160440251022820, 41.66919565927783253, 78.04033446252860529 ) ) ;
#1321=EDGE_LOOP ( 'NONE', ( #12087, #10715, #13866, #4940 ) ) ;
#1322=CARTESIAN_POINT ( 'NONE',  ( -5.352023103366428280, 49.86053488430150793, 78.79017217825926878 ) ) ;
#1324=CARTESIAN_POINT ( 'NONE',  ( 6.663926478743484871, 37.73509508818325031, 78.14418354478426920 ) ) ;
#1325=CARTESIAN_POINT ( 'NONE',  ( 5.363666972247387754, 50.77172923808412008, 75.97249762499970416 ) ) ;
#1330=DIRECTION ( 'NONE',  ( 0.3165065846431826535, 0.9485903129789529098, 2.188653791613874008E-16 ) ) ;
#1331=DIRECTION ( 'NONE',  ( -0.3015081906286226077, 0.9534635866061452747, 1.245503830460468341E-16 ) ) ;
#1332=EDGE_CURVE ( 'NONE', #16083, #4532, #2463, .T. ) ;
#1333=VECTOR ( 'NONE', #1915, 1000.000000000000114 ) ;
#1334=DIRECTION ( 'NONE',  ( -0.5813877811927011807, 0.8136266022444372803, 5.636455622144619183E-17 ) ) ;
#1336=CARTESIAN_POINT ( 'NONE',  ( 5.655950003444441876, 37.76811099897118851, 78.37198585835440667 ) ) ;
#1338=DIRECTION ( 'NONE',  ( 1.540237394707284220E-16, 1.793354297423764243E-16, -1.000000000000000000 ) ) ;
#1339=CARTESIAN_POINT ( 'NONE',  ( 5.543757954317092285, 50.63870328413648991, 76.06909773771320715 ) ) ;
#1340=ORIENTED_EDGE ( 'NONE', *, *, #12820, .F. ) ;
#1341=CARTESIAN_POINT ( 'NONE',  ( -7.036662486785782988, 47.34139391789577189, 78.30609472687723382 ) ) ;
#1344=CARTESIAN_POINT ( 'NONE',  ( -0.3452625352290130678, 52.31683812620389062, 75.52989945841051167 ) ) ;
#1346=CARTESIAN_POINT ( 'NONE',  ( -8.080465354403331801, 46.01554175503538602, 79.45433879953087342 ) ) ;
#1348=VECTOR ( 'NONE', #3895, 1000.000000000000114 ) ;
#1350=ORIENTED_EDGE ( 'NONE', *, *, #15478, .F. ) ;
#1351=CARTESIAN_POINT ( 'NONE',  ( -3.934466035114216442, 36.51369227099507242, 75.53057231289058393 ) ) ;
#1352=CARTESIAN_POINT ( 'NONE',  ( -4.256347323304533248, 37.50608895441494894, 75.99117330331094422 ) ) ;
#1354=ORIENTED_EDGE ( 'NONE', *, *, #15753, .T. ) ;
#1355=CARTESIAN_POINT ( 'NONE',  ( 4.579592178280777581, 52.10552964593085790, 78.58658920843723195 ) ) ;
#1356=FACE_OUTER_BOUND ( 'NONE', #10590, .T. ) ;
#1358=VECTOR ( 'NONE', #6848, 1000.000000000000114 ) ;
#1359=VECTOR ( 'NONE', #409, 1000.000000000000000 ) ;
#1360=ORIENTED_EDGE ( 'NONE', *, *, #20955, .F. ) ;
#1361=CARTESIAN_POINT ( 'NONE',  ( 8.443422548343662015, 42.04239353520513589, 78.13669174070733447 ) ) ;
#1366=AXIS2_PLACEMENT_3D ( 'NONE', #7617, #14410, #12614 ) ;
#1368=CARTESIAN_POINT ( 'NONE',  ( -7.496435415918218048, 40.53612117468122733, 79.30582264914816903 ) ) ;
#1369=CARTESIAN_POINT ( 'NONE',  ( 0.6326014232273523552, 51.36153429190470376, 79.54845644658969661 ) ) ;
#1370=CARTESIAN_POINT ( 'NONE',  ( -0.6022041793465181536, 52.97723187893011954, 79.21387586705148465 ) ) ;
#1371=AXIS2_PLACEMENT_3D ( 'NONE', #13854, #12279, #18326 ) ;
#1372=VERTEX_POINT ( 'NONE', #695 ) ;
#1373=CARTESIAN_POINT ( 'NONE',  ( -4.314207556397965604, 37.54021473506075068, 75.97461220940198245 ) ) ;
#1375=CARTESIAN_POINT ( 'NONE',  ( 0.5706356501935867520, 52.36203804732553380, 75.97198585835440099 ) ) ;
#1376=ORIENTED_EDGE ( 'NONE', *, *, #9773, .F. ) ;
#1377=VERTEX_POINT ( 'NONE', #13991 ) ;
#1379=CARTESIAN_POINT ( 'NONE',  ( -4.879976564110344306, 37.21210281127716968, 78.77850703318271997 ) ) ;
#1381=B_SPLINE_SURFACE_WITH_KNOTS ( 'NONE', 3, 1, ( 
 ( #17108, #14117 ),
 ( #10847, #12526 ),
 ( #19121, #12327 ),
 ( #2632, #8923 ),
 ( #17315, #18807 ),
 ( #14016, #20499 ),
 ( #5931, #6136 ),
 ( #19013, #16997 ),
 ( #12214, #2532 ),
 ( #2845, #15411 ),
 ( #9027, #15514 ),
 ( #4219, #12428 ),
 ( #17419, #7528 ),
 ( #1245, #9348 ),
 ( #2740, #1149 ),
 ( #7738, #12639 ),
 ( #1355, #71 ),
 ( #16146, #4533 ),
 ( #17619, #3163 ) ),
 .UNSPECIFIED., .F., .F., .F.,
 ( 4, 1, 1, 1, 1, 1, 1, 1, 1, 1, 1, 1, 1, 1, 1, 1, 4 ),
 ( 2, 2 ),
 ( 0.000000000000000000, 0.09548257688036490554, 0.1831260162920692325, 0.2638843215906733763, 0.3377405854367836469, 0.4051287172156797234, 0.4664893278449969150, 0.5228337310946251648, 0.5750047063118850499, 0.6251976803793458659, 0.6747285784134858799, 0.7246222549260739054, 0.7756163566473811555, 0.8279184090424840381, 0.8823814665238148836, 0.9394578349448057253, 1.000000000000000000 ),
 ( 0.000000000000000000, 1.000000000000000000 ),
 .UNSPECIFIED. ) ;
#1383=VECTOR ( 'NONE', #14886, 1000.000000000000114 ) ;
#1384=CARTESIAN_POINT ( 'NONE',  ( 8.623636628666181636, 43.00372860211926707, 77.60952670463396430 ) ) ;
#1386=LINE ( 'NONE', #11291, #19153 ) ;
#1389=B_SPLINE_CURVE_WITH_KNOTS ( 'NONE', 3,
 ( #3693, #19863, #2317, #829, #8502, #12114, #6890, #2115 ),
 .UNSPECIFIED., .F., .F.,
 ( 4, 2, 2, 4 ),
 ( 0.000000000000000000, 0.0002990918838428522860, 0.0004486378257642822508, 0.0005981837676857122699 ),
 .UNSPECIFIED. ) ;
#1392=CARTESIAN_POINT ( 'NONE',  ( 2.029186242314200861, 35.35002428291939225, 76.86610350541323555 ) ) ;
#1396=VERTEX_POINT ( 'NONE', #18460 ) ;
#1398=CARTESIAN_POINT ( 'NONE',  ( 8.324322233486002531, 41.69710151208300175, 78.09303657357962436 ) ) ;
#1401=ORIENTED_EDGE ( 'NONE', *, *, #11885, .F. ) ;
#1405=EDGE_CURVE ( 'NONE', #15226, #4372, #4197, .T. ) ;
#1408=B_SPLINE_CURVE_WITH_KNOTS ( 'NONE', 3,
 ( #6514, #16210, #8547, #20969, #18120, #11534, #136, #1635, #6404, #6615, #12911, #19392, #4808, #3637, #3226, #5016, #4909, #11329, #1851 ),
 .UNSPECIFIED., .F., .F.,
 ( 4, 1, 1, 1, 1, 1, 1, 1, 1, 1, 1, 1, 1, 1, 1, 1, 4 ),
 ( 0.000000000000000000, 0.07046818618994758754, 0.1352139183126853383, 0.1951004221781245107, 0.2505542266086520642, 0.3026661728221104464, 0.3524186183690131702, 0.4011907228821319227, 0.4500572973727005044, 0.5012199576353847386, 0.5567639849620312775, 0.6168130928284528691, 0.6819767269214894734, 0.7529340711039560485, 0.8292206168931396393, 0.9117786016023526896, 1.000000000000000000 ),
 .UNSPECIFIED. ) ;
#1410=CARTESIAN_POINT ( 'NONE',  ( -7.480639693313347216, 47.82437745672348228, 78.83519423975563711 ) ) ;
#1412=CARTESIAN_POINT ( 'NONE',  ( -5.943920255163962274, 37.99799515759236357, 76.35020017089209432 ) ) ;
#1414=AXIS2_PLACEMENT_3D ( 'NONE', #9438, #15825, #11140 ) ;
#1417=VECTOR ( 'NONE', #14612, 1000.000000000000114 ) ;
#1420=ORIENTED_EDGE ( 'NONE', *, *, #13310, .F. ) ;
#1425=DIRECTION ( 'NONE',  ( -0.9534635866061451637, -0.3015081906286224411, -2.009271279954815058E-16 ) ) ;
#1427=CARTESIAN_POINT ( 'NONE',  ( 4.556677822976353376, 36.22933235006951946, 75.83703142516586126 ) ) ;
#1430=CARTESIAN_POINT ( 'NONE',  ( 5.074809179647884250, 37.34648547976750166, 77.45531005930804724 ) ) ;
#1431=ORIENTED_EDGE ( 'NONE', *, *, #12448, .F. ) ;
#1433=DIRECTION ( 'NONE',  ( -0.9534635866061451637, -0.3015081906286224411, -2.009271279954815058E-16 ) ) ;
#1434=AXIS2_PLACEMENT_3D ( 'NONE', #5372, #13689, #8597 ) ;
#1437=DIRECTION ( 'NONE',  ( -0.9534635866061452747, -0.3015081906286225522, -2.009271279954815797E-16 ) ) ;
#1438=VECTOR ( 'NONE', #17781, 1000.000000000000114 ) ;
#1439=FACE_OUTER_BOUND ( 'NONE', #700, .T. ) ;
#1441=FACE_OUTER_BOUND ( 'NONE', #11776, .T. ) ;
#1443=CARTESIAN_POINT ( 'NONE',  ( -3.053385034718948177, 36.78770617509731267, 76.68008248600652621 ) ) ;
#1444=ORIENTED_EDGE ( 'NONE', *, *, #9410, .F. ) ;
#1445=CARTESIAN_POINT ( 'NONE',  ( 2.050960264585806936, 52.82843088445552837, 77.27574491810834445 ) ) ;
#1446=CARTESIAN_POINT ( 'NONE',  ( -3.539401246598059991, 43.09270903039240608, 79.40903933791013003 ) ) ;
#1448=ORIENTED_EDGE ( 'NONE', *, *, #12563, .F. ) ;
#1451=EDGE_CURVE ( 'NONE', #12015, #6821, #5227, .T. ) ;
#1453=CARTESIAN_POINT ( 'NONE',  ( 9.201390675156970289, 42.37087608097247227, 79.34093170394821470 ) ) ;
#1454=CIRCLE ( 'NONE', #13345, 8.199999999999995737 ) ;
#1456=ORIENTED_EDGE ( 'NONE', *, *, #7029, .T. ) ;
#1457=CARTESIAN_POINT ( 'NONE',  ( 5.627315617218822119, 51.33161854646183997, 78.02054163389647101 ) ) ;
#1459=CARTESIAN_POINT ( 'NONE',  ( -3.674734132037355661, 36.32183877683144857, 75.77010869825431882 ) ) ;
#1460=CARTESIAN_POINT ( 'NONE',  ( 8.296628936784257391, 41.55497301399228149, 78.93669174070734584 ) ) ;
#1461=EDGE_CURVE ( 'NONE', #264, #4065, #10399, .T. ) ;
#1462=CARTESIAN_POINT ( 'NONE',  ( 4.393996117251955269, 36.11308595931626542, 76.73963291717792856 ) ) ;
#1464=CARTESIAN_POINT ( 'NONE',  ( -4.436679849166036860, 37.65941850380397682, 77.31392376534303423 ) ) ;
#1469=DIRECTION ( 'NONE',  ( 1.540237394707284220E-16, 1.793354297423764243E-16, -1.000000000000000000 ) ) ;
#1475=DIRECTION ( 'NONE',  ( -0.9534635866061451637, -0.3015081906286224411, -2.009271279954815058E-16 ) ) ;
#1476=CARTESIAN_POINT ( 'NONE',  ( -7.774959294756113692, 41.22996117453095621, 78.61536821129558916 ) ) ;
#1477=CARTESIAN_POINT ( 'NONE',  ( -0.9388773962491546721, 52.84004908296358138, 77.21536821129558348 ) ) ;
#1478=CARTESIAN_POINT ( 'NONE',  ( -0.7827652907628513956, 52.97865566965094786, 79.01146473771775902 ) ) ;
#1481=CARTESIAN_POINT ( 'NONE',  ( 0.5221537403065015237, 44.16218137147968292, 75.45433879953088763 ) ) ;
#1482=CARTESIAN_POINT ( 'NONE',  ( 0.6277305834145071595, 52.36170047174137210, 75.97329779118079784 ) ) ;
#1483=FACE_OUTER_BOUND ( 'NONE', #4375, .T. ) ;
#1484=ORIENTED_EDGE ( 'NONE', *, *, #18701, .T. ) ;
#1486=EDGE_CURVE ( 'NONE', #8055, #5056, #5581, .T. ) ;
#1487=B_SPLINE_CURVE_WITH_KNOTS ( 'NONE', 3,
 ( #9600, #12991, #11192, #12880, #9704, #17874, #4777, #9916, #16498, #16183, #8410, #8198, #18093, #110, #19567, #17775, #16401, #14685, #13199, #3296, #6587, #7991, #1824, #19362, #3097, #17980, #16287, #17664, #1608, #19673, #6693 ),
 .UNSPECIFIED., .F., .F.,
 ( 4, 1, 1, 1, 1, 1, 1, 1, 1, 1, 1, 1, 1, 1, 1, 1, 1, 1, 1, 1, 1, 1, 1, 1, 1, 1, 1, 1, 4 ),
 ( 0.000000000000000000, 0.04402879139878041609, 0.08604540006880039005, 0.1260521755942069777, 0.1641511405281330660, 0.2003442918647115323, 0.2347805632357193584, 0.2676267374383518027, 0.2986515534027265328, 0.3283031585252670914, 0.3570062744687346745, 0.3846398569069188755, 0.4113091075058319390, 0.4372322170293685417, 0.4625237182236557887, 0.4872935253130181721, 0.5115235732650775802, 0.5580727247437320404, 0.6018864549903041317, 0.6437727082467282758, 0.6848253805047307408, 0.7076001045990409910, 0.7352252901417971609, 0.7674583008524621386, 0.8043075748156178761, 0.8460289209228792906, 0.8926357087385640154, 0.9438729761760307202, 1.000000000000000000 ),
 .UNSPECIFIED. ) ;
#1488=LINE ( 'NONE', #18073, #11449 ) ;
#1490=CARTESIAN_POINT ( 'NONE',  ( 5.085125551764789087, 37.34896360483502775, 77.63600869567171969 ) ) ;
#1491=CARTESIAN_POINT ( 'NONE',  ( -6.354755732003290802, 42.02918051195119631, 76.16022115247204738 ) ) ;
#1493=CARTESIAN_POINT ( 'NONE',  ( 6.284457548606577681, 49.99629437706096979, 77.78632772248469962 ) ) ;
#1494=CARTESIAN_POINT ( 'NONE',  ( -4.792503378000012582, 37.91763016944491227, 72.45433879953085921 ) ) ;
#1495=CARTESIAN_POINT ( 'NONE',  ( 9.353187571392870936, 42.82582100880699016, 77.22643688620827618 ) ) ;
#1496=DIRECTION ( 'NONE',  ( 0.9534635866061470511, 0.3015081906286169455, 2.009271279954808648E-16 ) ) ;
#1497=CARTESIAN_POINT ( 'NONE',  ( 6.961907239250668233, 50.34580947589670075, 76.63889762306028786 ) ) ;
#1498=VECTOR ( 'NONE', #8770, 1000.000000000000000 ) ;
#1500=ADVANCED_FACE ( 'NONE', ( #902 ), #15166, .T. ) ;
#1501=CARTESIAN_POINT ( 'NONE',  ( -4.740836738068939127, 51.21721328354402658, 79.54427050475041483 ) ) ;
#1502=CARTESIAN_POINT ( 'NONE',  ( 5.244278063348997598, 50.86602667680485723, 78.70784175427819207 ) ) ;
#1503=EDGE_LOOP ( 'NONE', ( #15950, #6051, #18646, #9291 ) ) ;
#1504=CARTESIAN_POINT ( 'NONE',  ( 0.5221537403065015237, 44.16218137147968292, 75.45433879953088763 ) ) ;
#1506=ORIENTED_EDGE ( 'NONE', *, *, #13097, .T. ) ;
#1507=CARTESIAN_POINT ( 'NONE',  ( 5.397982717164803823, 37.75027360759684569, 75.36337631951366234 ) ) ;
#1508=CARTESIAN_POINT ( 'NONE',  ( 5.086801335794131518, 51.73087467290688579, 79.44143248960128290 ) ) ;
#1510=CARTESIAN_POINT ( 'NONE',  ( 0.8383241538550171290, 52.35221990523898938, 76.16511824318942558 ) ) ;
#1512=ORIENTED_EDGE ( 'NONE', *, *, #9923, .T. ) ;
#1513=CARTESIAN_POINT ( 'NONE',  ( 5.847824973458005005, 37.15193883188941015, 77.47236191065434241 ) ) ;
#1518=CARTESIAN_POINT ( 'NONE',  ( -0.001084937681666381338, 35.97658959305408644, 77.43518796918013436 ) ) ;
#1520=CARTESIAN_POINT ( 'NONE',  ( -7.940942381894581459, 41.72644817493324609, 78.82529883526802905 ) ) ;
#1521=ORIENTED_EDGE ( 'NONE', *, *, #6169, .F. ) ;
#1522=CARTESIAN_POINT ( 'NONE',  ( 8.214799251806553571, 41.32260305165857517, 76.40801527011910821 ) ) ;
#1523=ADVANCED_FACE ( 'NONE', ( #14189 ), #9551, .T. ) ;
#1525=CARTESIAN_POINT ( 'NONE',  ( -5.838428831739583380, 50.43291415881836315, 78.10580938776615767 ) ) ;
#1528=CARTESIAN_POINT ( 'NONE',  ( -7.098692764276762546, 41.50643870456164564, 78.36017682096837689 ) ) ;
#1530=CARTESIAN_POINT ( 'NONE',  ( 8.527988662190095326, 48.03182059810101379, 79.44551527011911674 ) ) ;
#1533=CARTESIAN_POINT ( 'NONE',  ( 5.215133383782184495, 50.88144501658546659, 76.13411024644928204 ) ) ;
#1534=CARTESIAN_POINT ( 'NONE',  ( 5.467161035934759994, 36.87993031913157438, 77.68578589458712713 ) ) ;
#1536=DIRECTION ( 'NONE',  ( 0.9534635866061452747, 0.3015081906286224966, 2.009271279954815304E-16 ) ) ;
#1537=CARTESIAN_POINT ( 'NONE',  ( 1.011011570371347812, 52.34791438083374260, 76.77344599742670539 ) ) ;
#1538=ORIENTED_EDGE ( 'NONE', *, *, #1461, .F. ) ;
#1542=CARTESIAN_POINT ( 'NONE',  ( 5.848951923618479931, 37.15274410921379911, 77.37492703482499223 ) ) ;
#1545=B_SPLINE_CURVE_WITH_KNOTS ( 'NONE', 3,
 ( #1702, #19243, #19342, #4558, #14461, #1490, #16169, #12665, #94, #9373 ),
 .UNSPECIFIED., .F., .F.,
 ( 4, 2, 2, 2, 4 ),
 ( 0.000000000000000000, 0.0001199900948641854036, 0.0002399801897283708072, 0.0003599702845925562109, 0.0004799603794567416145 ),
 .UNSPECIFIED. ) ;
#1546=LINE ( 'NONE', #8030, #12564 ) ;
#1547=CARTESIAN_POINT ( 'NONE',  ( -3.165502623679720795, 36.87052292169065737, 77.44024473021482891 ) ) ;
#1548=B_SPLINE_CURVE_WITH_KNOTS ( 'NONE', 3,
 ( #4535, #17523, #19014, #9349, #3052, #16249, #17835, #7637, #14540, #15835, #11262, #1567, #20697, #14118, #14433, #17733 ),
 .UNSPECIFIED., .F., .F.,
 ( 4, 2, 2, 2, 2, 2, 2, 4 ),
 ( 0.000000000000000000, 0.0001316607980626216534, 0.0002633215961252433068, 0.0005266431922504869389, 0.0007899647883757306794, 0.001053286384500974312, 0.001579929576751444662, 0.002106572769001915230 ),
 .UNSPECIFIED. ) ;
#1549=VERTEX_POINT ( 'NONE', #20575 ) ;
#1550=CARTESIAN_POINT ( 'NONE',  ( -7.132598987128367263, 47.10241527675634643, 78.19896882776124869 ) ) ;
#1551=CARTESIAN_POINT ( 'NONE',  ( -3.955205046931959068, 36.52901134360648427, 77.68963291717793140 ) ) ;
#1552=EDGE_LOOP ( 'NONE', ( #11027, #2531, #7948, #10259 ) ) ;
#1553=DIRECTION ( 'NONE',  ( -0.9429220365244147528, 0.3330135628418914862, -8.551124769255465366E-17 ) ) ;
#1555=CARTESIAN_POINT ( 'NONE',  ( -0.6451721385307191969, 52.27904522445349045, 75.73030909034207525 ) ) ;
#1557=B_SPLINE_SURFACE_WITH_KNOTS ( 'NONE', 3, 1, ( 
 ( #9147, #14033 ),
 ( #10861, #15747 ),
 ( #12541, #19030 ),
 ( #15527, #13714 ),
 ( #18919, #16904 ),
 ( #839, #2757 ),
 ( #20514, #20189 ),
 ( #15639, #4018 ),
 ( #9260, #5619 ),
 ( #7325, #4335 ),
 ( #1164, #18606 ),
 ( #12229, #7650 ),
 ( #9041, #14129 ),
 ( #10541, #17012 ),
 ( #13814, #943 ),
 ( #7431, #20292 ),
 ( #4126, #10655 ),
 ( #17120, #2544 ),
 ( #13925, #20407 ) ),
 .UNSPECIFIED., .F., .F., .F.,
 ( 4, 1, 1, 1, 1, 1, 1, 1, 1, 1, 1, 1, 1, 1, 1, 1, 4 ),
 ( 2, 2 ),
 ( 0.000000000000000000, 0.09472651553281030701, 0.1809448578637775085, 0.2575849355004761199, 0.3257111939256314703, 0.3842597268839244573, 0.4332657528852557616, 0.4727039292014991179, 0.5037345896081361074, 0.5551104982754543338, 0.6060435029138766527, 0.6590687186606726256, 0.7172582036121251114, 0.7797016678215834551, 0.8463570695623257034, 0.9189979831805518140, 1.000000000000000000 ),
 ( 0.000000000000000000, 1.000000000000000000 ),
 .UNSPECIFIED. ) ;
#1558=CARTESIAN_POINT ( 'NONE',  ( -3.012672749018421747, 51.56125195451731003, 76.00197347997514896 ) ) ;
#1559=ORIENTED_EDGE ( 'NONE', *, *, #5348, .T. ) ;
#1560=CARTESIAN_POINT ( 'NONE',  ( 5.599231707071657738, 51.35236299959863970, 78.30875056423674607 ) ) ;
#1561=ORIENTED_EDGE ( 'NONE', *, *, #13796, .T. ) ;
#1563=CARTESIAN_POINT ( 'NONE',  ( -4.158450310422142415, 37.43377637453095730, 76.36459416792565946 ) ) ;
#1566=CARTESIAN_POINT ( 'NONE',  ( -5.135517778528634558, 37.40086081253993910, 77.33633635728615729 ) ) ;
#1567=CARTESIAN_POINT ( 'NONE',  ( -7.016336539762185076, 40.93177535399939160, 79.42775612813471753 ) ) ;
#1572=CARTESIAN_POINT ( 'NONE',  ( -5.260605497331073188, 38.34791887000096722, 79.35384852091290497 ) ) ;
#1573=ADVANCED_FACE ( 'NONE', ( #11332 ), #20893, .T. ) ;
#1577=CARTESIAN_POINT ( 'NONE',  ( 5.885001432003880595, 37.95852707458993081, 78.35303564028859569 ) ) ;
#1578=FACE_OUTER_BOUND ( 'NONE', #13552, .T. ) ;
#1579=EDGE_CURVE ( 'NONE', #2109, #17272, #1672, .T. ) ;
#1580=CARTESIAN_POINT ( 'NONE',  ( 5.632375035844972899, 36.99798619459680538, 75.36061873398452349 ) ) ;
#1581=EDGE_CURVE ( 'NONE', #3682, #18429, #16956, .T. ) ;
#1585=CARTESIAN_POINT ( 'NONE',  ( 8.638892188706073227, 43.04945048335348901, 76.30013550906805619 ) ) ;
#1586=CARTESIAN_POINT ( 'NONE',  ( 5.566326199328858415, 51.37666897265353327, 76.21945306000542075 ) ) ;
#1587=CARTESIAN_POINT ( 'NONE',  ( 6.487242172018640396, 49.78241043515765085, 78.48669174070734300 ) ) ;
#1588=EDGE_CURVE ( 'NONE', #13986, #8211, #7083, .T. ) ;
#1591=ORIENTED_EDGE ( 'NONE', *, *, #5839, .T. ) ;
#1592=CARTESIAN_POINT ( 'NONE',  ( 7.770520676892109790, 40.32783022416316498, 75.85744100972826232 ) ) ;
#1594=CARTESIAN_POINT ( 'NONE',  ( 4.144921371010943822, 51.51850920521359001, 78.55031972648716021 ) ) ;
#1597=LINE ( 'NONE', #19072, #17222 ) ;
#1598=CARTESIAN_POINT ( 'NONE',  ( 6.862151516847506016, 50.41949500963030317, 77.39285358288198324 ) ) ;
#1599=CARTESIAN_POINT ( 'NONE',  ( 8.617838889373357958, 45.46597658821364263, 78.74919174070734584 ) ) ;
#1604=CARTESIAN_POINT ( 'NONE',  ( -4.981196848641174846, 38.22287665415147018, 79.46937556254052026 ) ) ;
#1605=CARTESIAN_POINT ( 'NONE',  ( -5.802311964739910621, 50.45872194965342317, 78.71528818263502103 ) ) ;
#1606=DIRECTION ( 'NONE',  ( 0.9999689119394086223, -0.007885122365275665235, 1.526048693634353392E-16 ) ) ;
#1607=CARTESIAN_POINT ( 'NONE',  ( 8.789147962602239517, 47.20595287382010241, 75.43669174070734584 ) ) ;
#1608=CARTESIAN_POINT ( 'NONE',  ( 8.385851074499695912, 39.92665216093506331, 76.98031643592585738 ) ) ;
#1610=CARTESIAN_POINT ( 'NONE',  ( 0.006406757820996506793, 52.97120749765745273, 75.41772606587693417 ) ) ;
#1612=CARTESIAN_POINT ( 'NONE',  ( 0.3970485124631613627, 52.20691167326921800, 79.54130260543404063 ) ) ;
#1613=CARTESIAN_POINT ( 'NONE',  ( 6.853565520360258567, 37.87060420419414442, 77.68698088877128782 ) ) ;
#1615=LINE ( 'NONE', #11309, #1438 ) ;
#1616=ORIENTED_EDGE ( 'NONE', *, *, #16806, .T. ) ;
#1620=VECTOR ( 'NONE', #2773, 1000.000000000000227 ) ;
#1621=CARTESIAN_POINT ( 'NONE',  ( 0.5706356501935867520, 52.36203804732553380, 75.97198585835440099 ) ) ;
#1623=CARTESIAN_POINT ( 'NONE',  ( 6.531299583006453524, 48.82481648921748274, 72.45432679953087529 ) ) ;
#1627=CARTESIAN_POINT ( 'NONE',  ( -4.616992131696500579, 37.01784680471219247, 75.99117330331094422 ) ) ;
#1628=ORIENTED_EDGE ( 'NONE', *, *, #523, .T. ) ;
#1634=CARTESIAN_POINT ( 'NONE',  ( 2.106992520703838689, 52.20762236682631396, 77.55786177449368779 ) ) ;
#1635=CARTESIAN_POINT ( 'NONE',  ( -5.803682309770399783, 37.89440703645915676, 79.21211992218960063 ) ) ;
#1636=CIRCLE ( 'NONE', #18628, 6.000000000000002665 ) ;
#1638=CARTESIAN_POINT ( 'NONE',  ( -4.035675179171060556, 50.97418048369974031, 78.65149807507090429 ) ) ;
#1639=CARTESIAN_POINT ( 'NONE',  ( 5.435172323252741577, 36.85707235623052469, 77.60331851759366373 ) ) ;
#1641=CARTESIAN_POINT ( 'NONE',  ( -4.030452273627614268, 50.97791258077830889, 76.38961819735682468 ) ) ;
#1646=CARTESIAN_POINT ( 'NONE',  ( -7.075244453723417593, 44.52209897503762193, 75.45433879953087342 ) ) ;
#1651=AXIS2_PLACEMENT_3D ( 'NONE', #3553, #677, #20020 ) ;
#1652=CARTESIAN_POINT ( 'NONE',  ( 5.568159709253909462, 50.62067869072730275, 76.16996516156804375 ) ) ;
#1654=CARTESIAN_POINT ( 'NONE',  ( 1.641182446559612318, 52.20525483714327208, 79.33873778842219338 ) ) ;
#1656=CARTESIAN_POINT ( 'NONE',  ( -4.225462782839600528, 50.84799750334796187, 79.54845644658969661 ) ) ;
#1659=CARTESIAN_POINT ( 'NONE',  ( 2.115041367457930033, 52.20598078514408513, 76.48963291717792856 ) ) ;
#1660=CARTESIAN_POINT ( 'NONE',  ( -7.515910409428084193, 42.82581192461235986, 76.44005692701139765 ) ) ;
#1662=DIRECTION ( 'NONE',  ( -0.8043570849667760481, 0.5941461771851693774, -1.733862608106482338E-17 ) ) ;
#1663=LINE ( 'NONE', #8147, #11664 ) ;
#1666=CARTESIAN_POINT ( 'NONE',  ( 8.375284547952256631, 41.80244594815106751, 78.79373795524233515 ) ) ;
#1670=LINE ( 'NONE', #2085, #11217 ) ;
#1672=CIRCLE ( 'NONE', #21018, 4.200000000000003730 ) ;
#1673=EDGE_LOOP ( 'NONE', ( #17517, #15759, #16528, #10336 ) ) ;
#1676=PLANE ( 'NONE',  #11562 ) ;
#1679=UNCERTAINTY_MEASURE_WITH_UNIT (LENGTH_MEASURE( 1.000000000000000082E-05 ), #18708, 'distance_accuracy_value', 'NONE');
#1680=EDGE_CURVE ( 'NONE', #10288, #12015, #16432, .T. ) ;
#1681=CARTESIAN_POINT ( 'NONE',  ( -5.838255805151811195, 50.43303779728307745, 76.65235776097600251 ) ) ;
#1682=CARTESIAN_POINT ( 'NONE',  ( 0.4501203527806490468, 52.96713143748286257, 76.95466777776533718 ) ) ;
#1685=CARTESIAN_POINT ( 'NONE',  ( 7.870074787697994623, 40.74525595966579772, 79.37958223971880045 ) ) ;
#1686=ORIENTED_EDGE ( 'NONE', *, *, #4099, .T. ) ;
#1689=EDGE_CURVE ( 'NONE', #13226, #14563, #13229, .T. ) ;
#1690=LINE ( 'NONE', #14764, #8252 ) ;
#1691=CARTESIAN_POINT ( 'NONE',  ( 6.924055141134583202, 50.37376929599953712, 78.48669174070734300 ) ) ;
#1692=EDGE_CURVE ( 'NONE', #4602, #7376, #342, .T. ) ;
#1694=ORIENTED_EDGE ( 'NONE', *, *, #11419, .F. ) ;
#1696=CARTESIAN_POINT ( 'NONE',  ( 5.513895972565329373, 50.66228159254415431, 78.86250487280319987 ) ) ;
#1697=ORIENTED_EDGE ( 'NONE', *, *, #19263, .F. ) ;
#1701=ADVANCED_FACE ( 'NONE', ( #8549 ), #452, .F. ) ;
#1702=CARTESIAN_POINT ( 'NONE',  ( 5.282950423531485917, 37.48574407745871895, 77.76022115247205591 ) ) ;
#1704=FACE_OUTER_BOUND ( 'NONE', #12263, .T. ) ;
#1705=VECTOR ( 'NONE', #4961, 1000.000000000000227 ) ;
#1706=CARTESIAN_POINT ( 'NONE',  ( 6.518026314581760516, 49.74885348734871116, 76.80946857459053945 ) ) ;
#1707=CARTESIAN_POINT ( 'NONE',  ( 4.553522022787977797, 51.30320697278853004, 77.72474235116990826 ) ) ;
#1708=CARTESIAN_POINT ( 'NONE',  ( -1.598719209087999138, 36.85794301744668644, 75.45433879953087342 ) ) ;
#1709=AXIS2_PLACEMENT_3D ( 'NONE', #6936, #13441, #14615 ) ;
#1711=ORIENTED_EDGE ( 'NONE', *, *, #6470, .T. ) ;
#1712=CARTESIAN_POINT ( 'NONE',  ( -5.510796958474739604, 38.60848837797752964, 72.45433879953085921 ) ) ;
#1713=CARTESIAN_POINT ( 'NONE',  ( 8.871704507997348443, 41.38278572309461367, 78.93627637315103129 ) ) ;
#1716=VECTOR ( 'NONE', #16757, 1000.000000000000000 ) ;
#1719=CARTESIAN_POINT ( 'NONE',  ( 9.026838159693451047, 41.84773111872319618, 78.13669174070733447 ) ) ;
#1720=ORIENTED_EDGE ( 'NONE', *, *, #8592, .T. ) ;
#1721=ORIENTED_EDGE ( 'NONE', *, *, #6470, .F. ) ;
#1722=CARTESIAN_POINT ( 'NONE',  ( 6.447530045045036573, 38.50024170171982973, 76.65924029158320252 ) ) ;
#1723=VECTOR ( 'NONE', #10551, 1000.000000000000000 ) ;
#1725=CARTESIAN_POINT ( 'NONE',  ( 7.680615469065380729, 40.16262800804438626, 77.93428071991040440 ) ) ;
#1726=DIRECTION ( 'NONE',  ( -1.540237394707284220E-16, -1.793354297423764243E-16, 1.000000000000000000 ) ) ;
#1727=ADVANCED_FACE ( 'NONE', ( #19497 ), #6471, .T. ) ;
#1730=CARTESIAN_POINT ( 'NONE',  ( -4.385374315297738690, 51.47121371654639432, 78.59092584394873882 ) ) ;
#1731=EDGE_CURVE ( 'NONE', #2631, #8069, #7143, .T. ) ;
#1732=ORIENTED_EDGE ( 'NONE', *, *, #8303, .F. ) ;
#1735=CARTESIAN_POINT ( 'NONE',  ( 1.257148372430989092, 52.94703067912596595, 76.78082255713043480 ) ) ;
#1737=CARTESIAN_POINT ( 'NONE',  ( 8.299662904660788598, 41.56403757284476796, 75.97198585835440099 ) ) ;
#1738=B_SPLINE_SURFACE_WITH_KNOTS ( 'NONE', 3, 1, ( 
 ( #19513, #6419 ),
 ( #4925, #12928 ),
 ( #18390, #16698 ),
 ( #15103, #511 ),
 ( #3811, #10330 ),
 ( #3967, #7161 ),
 ( #1534, #20874 ),
 ( #17700, #16214 ),
 ( #1639, #1752 ),
 ( #19395, #13123 ),
 ( #14719, #3329 ),
 ( #4601, #1430 ),
 ( #8121, #19288 ) ),
 .UNSPECIFIED., .F., .F., .F.,
 ( 4, 1, 1, 1, 1, 1, 1, 1, 1, 1, 4 ),
 ( 2, 2 ),
 ( 0.000000000000000000, 0.08953921432355217702, 0.1742669454086417657, 0.2528767480256390865, 0.3294736160795620483, 0.4632125218299475988, 0.5712501803543521550, 0.6337422670347153675, 0.7254863994935087934, 0.8484041168876338412, 0.9999999999999998890 ),
 ( 0.000000000000000000, 1.000000000000000000 ),
 .UNSPECIFIED. ) ;
#1739=LINE ( 'NONE', #11735, #7865 ) ;
#1741=ORIENTED_EDGE ( 'NONE', *, *, #5248, .F. ) ;
#1742=B_SPLINE_CURVE_WITH_KNOTS ( 'NONE', 3,
 ( #15260, #15687, #20236, #10601, #8885, #1108, #2384, #14080, #3965, #20562, #17070, #2495, #10491, #679, #7158, #5987, #13660, #20134, #5569, #9308, #3002, #14491, #1412, #13009, #16097, #9404, #4687 ),
 .UNSPECIFIED., .F., .F.,
 ( 4, 1, 1, 1, 1, 1, 1, 1, 1, 1, 1, 1, 1, 1, 1, 1, 1, 1, 1, 1, 1, 1, 1, 1, 4 ),
 ( 0.000000000000000000, 0.06156270711109813193, 0.1195928175617291256, 0.1747495234496604655, 0.2265549029623682431, 0.2754357869405233972, 0.3212504303641821046, 0.3646692690278454108, 0.4055209537250142326, 0.4439801712034092684, 0.4803226396643038298, 0.5144678959723257838, 0.5464657104125147935, 0.5769957197620103617, 0.6058640933454703115, 0.6335754242279014736, 0.6604510950290067850, 0.6887476664015759198, 0.7209157586619387992, 0.7570169132788651112, 0.7970502319830404803, 0.8414026928090143631, 0.8898175437432860324, 0.9426652073923825759, 1.000000000000000000 ),
 .UNSPECIFIED. ) ;
#1745=FACE_OUTER_BOUND ( 'NONE', #15464, .T. ) ;
#1747=CARTESIAN_POINT ( 'NONE',  ( 1.227438297423749880, 52.33307690334542173, 76.77372445804466849 ) ) ;
#1748=LINE ( 'NONE', #9729, #14028 ) ;
#1749=DIRECTION ( 'NONE',  ( 0.3165065846431827645, 0.9485903129789529098, 0.000000000000000000 ) ) ;
#1752=CARTESIAN_POINT ( 'NONE',  ( 5.081857000512829181, 37.35152159452039911, 77.60331851759366373 ) ) ;
#1754=CARTESIAN_POINT ( 'NONE',  ( -1.123656915330052408, 35.37488560990637865, 76.86610350541323555 ) ) ;
#1757=CARTESIAN_POINT ( 'NONE',  ( 4.597613975033692846, 52.09221767063174013, 78.17666347917207759 ) ) ;
#1759=CARTESIAN_POINT ( 'NONE',  ( -4.313560930641144431, 37.53965589074172016, 77.26981739744707056 ) ) ;
#1764=CARTESIAN_POINT ( 'NONE',  ( 7.992712741985108060, 47.55532711652816147, 77.53155195043741799 ) ) ;
#1765=CARTESIAN_POINT ( 'NONE',  ( 5.939788499136119171, 51.10080741576499719, 76.32243632687685420 ) ) ;
#1768=CARTESIAN_POINT ( 'NONE',  ( 5.051595465965247556, 37.34078104729439218, 78.11840496518735222 ) ) ;
#1769=VERTEX_POINT ( 'NONE', #13647 ) ;
#1770=CARTESIAN_POINT ( 'NONE',  ( 5.581406744796363562, 50.61539444998253856, 76.90580938776616904 ) ) ;
#1776=CARTESIAN_POINT ( 'NONE',  ( -5.561099455747295472, 37.71522085402569502, 75.56266266290518274 ) ) ;
#1783=CARTESIAN_POINT ( 'NONE',  ( -4.517072128342576320, 36.94403992325788977, 76.81463291717793140 ) ) ;
#1784=CARTESIAN_POINT ( 'NONE',  ( -4.608953993764375312, 37.01190935601762533, 77.97288938838477179 ) ) ;
#1786=ORIENTED_EDGE ( 'NONE', *, *, #13000, .F. ) ;
#1788=DIRECTION ( 'NONE',  ( 0.3014919283324601351, -0.9534121601185491235, 0.01038605259262642688 ) ) ;
#1791=CARTESIAN_POINT ( 'NONE',  ( 6.149032746747884026, 50.02141417194002315, 75.57514290624801845 ) ) ;
#1792=ADVANCED_FACE ( 'NONE', ( #3740 ), #8006, .T. ) ;
#1794=CARTESIAN_POINT ( 'NONE',  ( 1.082972178424195242, 52.33928642596643499, 76.77198585835439815 ) ) ;
#1795=CARTESIAN_POINT ( 'NONE',  ( 4.884665026186969961, 36.46369999710588417, 75.53067132529541539 ) ) ;
#1797=CARTESIAN_POINT ( 'NONE',  ( 8.458367304687495647, 40.14398790315176058, 79.09910503406773330 ) ) ;
#1798=ORIENTED_EDGE ( 'NONE', *, *, #11244, .F. ) ;
#1799=CYLINDRICAL_SURFACE ( 'NONE', #10885, 6.200000000000000178 ) ;
#1800=CARTESIAN_POINT ( 'NONE',  ( 9.343936824499609273, 42.79809593351145480, 76.16967972087822147 ) ) ;
#1803=EDGE_CURVE ( 'NONE', #6003, #3218, #4264, .T. ) ;
#1807=AXIS2_PLACEMENT_3D ( 'NONE', #11485, #13282, #395 ) ;
#1810=CARTESIAN_POINT ( 'NONE',  ( 5.658108625003792191, 37.01637447524286273, 75.97198585835440099 ) ) ;
#1815=PLANE ( 'NONE',  #12513 ) ;
#1816=CARTESIAN_POINT ( 'NONE',  ( -4.766817752550178255, 37.12851695549264974, 75.97348137399042400 ) ) ;
#1818=ORIENTED_EDGE ( 'NONE', *, *, #1038, .T. ) ;
#1819=CARTESIAN_POINT ( 'NONE',  ( 0.3329282460686175393, 52.96755673690322652, 76.41414202728766725 ) ) ;
#1820=AXIS2_PLACEMENT_3D ( 'NONE', #8022, #9735, #16326 ) ;
#1821=CARTESIAN_POINT ( 'NONE',  ( 8.950841833175557483, 41.61996530703199682, 78.68229860608910542 ) ) ;
#1824=CARTESIAN_POINT ( 'NONE',  ( 8.392716226808454749, 39.94722745792154939, 76.30598982719874357 ) ) ;
#1825=ORIENTED_EDGE ( 'NONE', *, *, #15179, .T. ) ;
#1826=CARTESIAN_POINT ( 'NONE',  ( 6.445708703230327963, 38.49894023754261241, 76.49840989696882332 ) ) ;
#1827=CARTESIAN_POINT ( 'NONE',  ( -0.01650830115698442499, 52.97261345168382007, 79.48573486738433758 ) ) ;
#1829=CARTESIAN_POINT ( 'NONE',  ( -3.522342774269682675, 36.20927341954680401, 76.21065298426071877 ) ) ;
#1830=CARTESIAN_POINT ( 'NONE',  ( 0.5753667321910650445, 52.96202048236657589, 75.97198585835440099 ) ) ;
#1832=CARTESIAN_POINT ( 'NONE',  ( 8.333395564809045197, 41.68949534966480996, 76.00786757613292366 ) ) ;
#1834=EDGE_LOOP ( 'NONE', ( #17200, #10352, #12724, #6542 ) ) ;
#1837=CARTESIAN_POINT ( 'NONE',  ( 2.113017254819833379, 52.20161731206520273, 77.68224048311739693 ) ) ;
#1843=CARTESIAN_POINT ( 'NONE',  ( 9.353817388681445522, 42.82770861117572281, 76.74257409364852833 ) ) ;
#1845=CARTESIAN_POINT ( 'NONE',  ( -7.423951210289297720, 47.94363824867885171, 78.32492703482499508 ) ) ;
#1846=CARTESIAN_POINT ( 'NONE',  ( 3.212180877488374886, 51.27651577472676792, 72.45433879953087342 ) ) ;
#1848=EDGE_CURVE ( 'NONE', #17827, #15970, #19163, .T. ) ;
#1850=LINE ( 'NONE', #3847, #13372 ) ;
#1851=CARTESIAN_POINT ( 'NONE',  ( -4.811608766808348037, 37.16160227343304712, 79.54845644658969661 ) ) ;
#1852=CARTESIAN_POINT ( 'NONE',  ( 5.921589662822362321, 51.11425016305613411, 76.13071926429850578 ) ) ;
#1854=VERTEX_POINT ( 'NONE', #17363 ) ;
#1857=CARTESIAN_POINT ( 'NONE',  ( 4.355143591211044551, 51.35730577063056046, 77.83360891957636341 ) ) ;
#1858=CARTESIAN_POINT ( 'NONE',  ( -6.705246719490330243, 40.29814987666313186, 78.47931198110067896 ) ) ;
#1861=DIRECTION ( 'NONE',  ( 0.5800177190770278157, 0.8146038580541354879, 2.354238310054624259E-16 ) ) ;
#1862=LINE ( 'NONE', #16443, #15009 ) ;
#1864=B_SPLINE_CURVE_WITH_KNOTS ( 'NONE', 3,
 ( #14878, #17971, #16176, #19350, #16487, #16276, #14777, #100, #1707, #6579 ),
 .UNSPECIFIED., .F., .F.,
 ( 4, 2, 2, 2, 4 ),
 ( 0.000000000000000000, 0.0002556600934737911549, 0.0005113201869475823098, 0.0007669802804213734105, 0.001022640373895164620 ),
 .UNSPECIFIED. ) ;
#1866=EDGE_CURVE ( 'NONE', #3490, #18561, #4520, .T. ) ;
#1867=CARTESIAN_POINT ( 'NONE',  ( 5.231589412277350526, 37.46939813133004549, 78.26671861549210973 ) ) ;
#1868=VERTEX_POINT ( 'NONE', #9603 ) ;
#1872=VERTEX_POINT ( 'NONE', #10998 ) ;
#1874=CARTESIAN_POINT ( 'NONE',  ( -5.113776628078608333, 38.32080799658261583, 75.56266266290518274 ) ) ;
#1875=ORIENTED_EDGE ( 'NONE', *, *, #2222, .F. ) ;
#1876=CARTESIAN_POINT ( 'NONE',  ( 5.753005855668248181, 51.23877623043087937, 78.93669174070734584 ) ) ;
#1877=CARTESIAN_POINT ( 'NONE',  ( 0.3548969944630057660, 52.96060458516934233, 76.08537024512065727 ) ) ;
#1879=VERTEX_POINT ( 'NONE', #17469 ) ;
#1881=ORIENTED_EDGE ( 'NONE', *, *, #9105, .T. ) ;
#1883=CARTESIAN_POINT ( 'NONE',  ( 5.426454583374004770, 50.73403188498316041, 78.93531119083770875 ) ) ;
#1887=CARTESIAN_POINT ( 'NONE',  ( 5.963693060521315203, 51.08315007920423056, 75.36814786694185386 ) ) ;
#1888=PLANE ( 'NONE',  #16052 ) ;
#1889=CARTESIAN_POINT ( 'NONE',  ( 5.471341376803050771, 36.88291743766401254, 75.36841521003546518 ) ) ;
#1890=CARTESIAN_POINT ( 'NONE',  ( 8.385938212755766230, 39.92691331981644254, 77.86095545630369941 ) ) ;
#1891=EDGE_LOOP ( 'NONE', ( #6937, #16639, #1239, #20060 ) ) ;
#1892=DIRECTION ( 'NONE',  ( -1.540237394707284220E-16, -1.793354297423764243E-16, 1.000000000000000000 ) ) ;
#1893=CARTESIAN_POINT ( 'NONE',  ( 9.332226353535185481, 42.76299890913265500, 76.00948821603452643 ) ) ;
#1894=CARTESIAN_POINT ( 'NONE',  ( -5.888748219722875987, 40.55551840971140365, 78.50801527011910252 ) ) ;
#1896=EDGE_LOOP ( 'NONE', ( #13114, #18259, #1616, #5276 ) ) ;
#1898=CARTESIAN_POINT ( 'NONE',  ( 5.544276951911416340, 50.64433212932689088, 78.59183879953087626 ) ) ;
#1900=CARTESIAN_POINT ( 'NONE',  ( -3.752498811055295924, 36.37928041266965806, 77.59103917682324436 ) ) ;
#1901=EDGE_CURVE ( 'NONE', #10941, #9206, #18999, .T. ) ;
#1904=CARTESIAN_POINT ( 'NONE',  ( -0.6408505906039995148, 52.88534186852020014, 75.73072098668157537 ) ) ;
#1906=CARTESIAN_POINT ( 'NONE',  ( 4.119841024906783389, 51.52029635603552293, 76.17419329630023128 ) ) ;
#1907=CARTESIAN_POINT ( 'NONE',  ( -3.510185363184280316, 36.20029322970840724, 76.30596599901106458 ) ) ;
#1910=ORIENTED_EDGE ( 'NONE', *, *, #11885, .T. ) ;
#1911=CARTESIAN_POINT ( 'NONE',  ( 4.045888121501547197, 36.75785668915397508, 76.03652549193961363 ) ) ;
#1913=CARTESIAN_POINT ( 'NONE',  ( 5.362953798781178172, 50.78084096341162024, 78.93369693484829952 ) ) ;
#1914=CARTESIAN_POINT ( 'NONE',  ( 0.3201111382462867860, 51.36399839264385037, 77.10139762306027933 ) ) ;
#1915=DIRECTION ( 'NONE',  ( -0.9485903129789527988, 0.3165065846431829311, -8.934458285744989980E-17 ) ) ;
#1917=EDGE_CURVE ( 'NONE', #2886, #14804, #14891, .T. ) ;
#1918=CARTESIAN_POINT ( 'NONE',  ( 9.353817388681445522, 42.82770861117572281, 77.06316232894263862 ) ) ;
#1919=CARTESIAN_POINT ( 'NONE',  ( 8.004281444754417052, 40.80494971592259645, 79.42365263778002316 ) ) ;
#1920=CARTESIAN_POINT ( 'NONE',  ( -3.815104224344752382, 36.42552450956669929, 75.61442449207443417 ) ) ;
#1921=CARTESIAN_POINT ( 'NONE',  ( 5.421101980426652922, 50.73801848575102014, 77.95022289312436214 ) ) ;
#1922=EDGE_LOOP ( 'NONE', ( #4715, #10698, #8890, #840, #7355, #19426 ) ) ;
#1923=CARTESIAN_POINT ( 'NONE',  ( 8.921551879414991504, 41.53218145749156776, 76.03029119948048731 ) ) ;
#1926=EDGE_LOOP ( 'NONE', ( #18975, #6201, #1697, #9756 ) ) ;
#1929=B_SPLINE_CURVE_WITH_KNOTS ( 'NONE', 3,
 ( #20504, #19125, #4439, #9138, #17112, #10853, #7640, #2637, #2948, #14121, #2535, #17425, #1047, #20603, #2850, #9030, #15517, #12330, #6031 ),
 .UNSPECIFIED., .F., .F.,
 ( 4, 1, 1, 1, 1, 1, 1, 1, 1, 1, 1, 1, 1, 1, 1, 1, 4 ),
 ( 0.000000000000000000, 0.1026547437176949656, 0.1953110930976798554, 0.2773242249590897601, 0.3493914542831295655, 0.4108068724308638342, 0.4622887491528899773, 0.5032980238437735343, 0.5345418472720404601, 0.5847168530758872773, 0.6322731508218554231, 0.6775315938118185999, 0.7246750034944897667, 0.7779009386454487363, 0.8408031781967141294, 0.9146367246678260843, 1.000000000000000000 ),
 .UNSPECIFIED. ) ;
#1933=DIRECTION ( 'NONE',  ( 0.007885122365275663500, 0.9999689119394085113, 1.805443505845543142E-16 ) ) ;
#1934=ORIENTED_EDGE ( 'NONE', *, *, #1069, .F. ) ;
#1936=ORIENTED_EDGE ( 'NONE', *, *, #9256, .F. ) ;
#1937=CARTESIAN_POINT ( 'NONE',  ( -7.519011464410084500, 47.73881877701913368, 78.32326252082832241 ) ) ;
#1939=DIRECTION ( 'NONE',  ( 0.007885122365275663500, 0.9999689119394085113, 1.805443505845543142E-16 ) ) ;
#1940=ORIENTED_EDGE ( 'NONE', *, *, #14592, .F. ) ;
#1941=EDGE_CURVE ( 'NONE', #9093, #14083, #18312, .T. ) ;
#1943=EDGE_CURVE ( 'NONE', #20669, #9230, #12884, .T. ) ;
#1944=CARTESIAN_POINT ( 'NONE',  ( 8.059489980808651310, 41.32971201870342526, 75.37437276336991943 ) ) ;
#1945=CARTESIAN_POINT ( 'NONE',  ( -5.667418469993653396, 43.80274312437727247, 78.25433879953087057 ) ) ;
#1947=ADVANCED_FACE ( 'NONE', ( #13099 ), #17687, .F. ) ;
#1950=CARTESIAN_POINT ( 'NONE',  ( -4.486751758304120763, 51.39877310743911210, 75.98707017319573254 ) ) ;
#1953=CARTESIAN_POINT ( 'NONE',  ( -6.705008690618248224, 40.29739715461727201, 78.50801527011910252 ) ) ;
#1956=CARTESIAN_POINT ( 'NONE',  ( 6.924055141134583202, 50.37376929599953712, 78.48669174070734300 ) ) ;
#1957=PLANE ( 'NONE',  #20657 ) ;
#1961=CARTESIAN_POINT ( 'NONE',  ( -7.712300854543705952, 47.28237451121256640, 78.18191347276355430 ) ) ;
#1963=CARTESIAN_POINT ( 'NONE',  ( 0.8357988670611854465, 52.21160558265095375, 79.54553221853565503 ) ) ;
#1965=B_SPLINE_CURVE_WITH_KNOTS ( 'NONE', 3,
 ( #19750, #5273, #16681, #5171, #15182, #20061, #12206, #15506, #14009, #7303, #9124, #5814, #5599, #18583, #6018, #1031 ),
 .UNSPECIFIED., .F., .F.,
 ( 4, 2, 2, 2, 2, 2, 2, 4 ),
 ( 0.000000000000000000, 0.0007061632881199156157, 0.0008827041101498631862, 0.001059244932179810757, 0.001412326576239666650, 0.001765408220299522542, 0.002118489864359378218, 0.002824653152479090004 ),
 .UNSPECIFIED. ) ;
#1966=VECTOR ( 'NONE', #12254, 1000.000000000000227 ) ;
#1968=CARTESIAN_POINT ( 'NONE',  ( 7.691771551572207599, 40.18266124458227750, 75.45433879953088763 ) ) ;
#1971=ORIENTED_EDGE ( 'NONE', *, *, #11662, .F. ) ;
#1973=CARTESIAN_POINT ( 'NONE',  ( -5.907462774012225637, 37.97106548486248556, 76.06004113464240390 ) ) ;
#1976=CARTESIAN_POINT ( 'NONE',  ( 0.4461516307629347367, 52.96189878203579582, 76.96012881851619625 ) ) ;
#1979=ORIENTED_EDGE ( 'NONE', *, *, #9383, .T. ) ;
#1980=LINE ( 'NONE', #6758, #8511 ) ;
#1981=EDGE_LOOP ( 'NONE', ( #9342, #8226, #9610, #11212 ) ) ;
#1982=CARTESIAN_POINT ( 'NONE',  ( -4.795362370604993707, 51.17825126284458293, 76.19771883405211099 ) ) ;
#1987=CARTESIAN_POINT ( 'NONE',  ( 5.712959422672630794, 50.34352397032943571, 75.39427037473855364 ) ) ;
#1988=CARTESIAN_POINT ( 'NONE',  ( 5.433321616587456049, 50.72893591270732827, 77.28832074152185783 ) ) ;
#1989=CARTESIAN_POINT ( 'NONE',  ( -3.479253321868470916, 37.00426859223156129, 79.33569596569910232 ) ) ;
#1991=CARTESIAN_POINT ( 'NONE',  ( 4.393996117251955269, 36.11308595931626542, 76.73963291717792856 ) ) ;
#1992=CARTESIAN_POINT ( 'NONE',  ( 8.496565932950701949, 40.25847161533236829, 79.21682452846883393 ) ) ;
#1993=ORIENTED_EDGE ( 'NONE', *, *, #6250, .T. ) ;
#1994=CARTESIAN_POINT ( 'NONE',  ( 0.5221537403065019678, 44.16218137147968292, 72.45433879953087342 ) ) ;
#1995=CARTESIAN_POINT ( 'NONE',  ( 9.115819689944924420, 42.11441440976988559, 75.45386443748748206 ) ) ;
#1996=CARTESIAN_POINT ( 'NONE',  ( 2.643026689701002407, 51.46641972551267941, 72.45433879953087342 ) ) ;
#1998=ORIENTED_EDGE ( 'NONE', *, *, #1803, .T. ) ;
#2000=VERTEX_POINT ( 'NONE', #1166 ) ;
#2001=CARTESIAN_POINT ( 'NONE',  ( 5.902048492000326441, 51.12868443877599134, 78.59183879953087626 ) ) ;
#2003=CARTESIAN_POINT ( 'NONE',  ( 5.581406744796362673, 50.61539444998253856, 76.38301527011910252 ) ) ;
#2005=CARTESIAN_POINT ( 'NONE',  ( 4.629792079547915939, 52.06844900104020013, 77.37197156638603701 ) ) ;
#2006=CARTESIAN_POINT ( 'NONE',  ( -2.582283693828128168, 37.50405593653111680, 78.46683879953087626 ) ) ;
#2008=CARTESIAN_POINT ( 'NONE',  ( 8.787869161997047485, 41.13152587271654426, 76.34522901481825841 ) ) ;
#2012=VECTOR ( 'NONE', #19910, 1000.000000000000000 ) ;
#2015=CARTESIAN_POINT ( 'NONE',  ( 0.3467105299092503312, 52.96744805853006710, 76.10778090364108550 ) ) ;
#2017=CARTESIAN_POINT ( 'NONE',  ( 0.5221537403065019678, 44.16218137147968292, 72.45433879953087342 ) ) ;
#2018=CARTESIAN_POINT ( 'NONE',  ( -5.721665869871382704, 50.51634869640449210, 78.97495844722888592 ) ) ;
#2019=CARTESIAN_POINT ( 'NONE',  ( 8.432571228970111576, 41.99999248199843294, 75.38373313750008720 ) ) ;
#2022=CARTESIAN_POINT ( 'NONE',  ( 8.374750565220676179, 41.81343890941077746, 77.24172240072661566 ) ) ;
#2026=ORIENTED_EDGE ( 'NONE', *, *, #9076, .F. ) ;
#2028=B_SPLINE_CURVE_WITH_KNOTS ( 'NONE', 3,
 ( #2140, #433, #530, #3413, #8641, #18198, #1921, #16408 ),
 .UNSPECIFIED., .F., .F.,
 ( 4, 2, 2, 4 ),
 ( 0.000000000000000000, 0.0002181616706891221331, 0.0003272425060336631554, 0.0004363233413782042591 ),
 .UNSPECIFIED. ) ;
#2029=CARTESIAN_POINT ( 'NONE',  ( 9.335797811945472091, 42.77370279655738017, 78.83313045764568017 ) ) ;
#2030=LINE ( 'NONE', #6594, #13481 ) ;
#2038=CARTESIAN_POINT ( 'NONE',  ( 1.874180992794621803, 52.20350062376504496, 77.04052575557504667 ) ) ;
#2041=VECTOR ( 'NONE', #13553, 1000.000000000000114 ) ;
#2045=ORIENTED_EDGE ( 'NONE', *, *, #14164, .T. ) ;
#2046=AXIS2_PLACEMENT_3D ( 'NONE', #12940, #1662, #7943 ) ;
#2047=CARTESIAN_POINT ( 'NONE',  ( -7.723575267056036253, 47.23593929668128766, 77.80994480216610043 ) ) ;
#2050=CARTESIAN_POINT ( 'NONE',  ( 8.424733569470319594, 41.97255615673255846, 78.13519505141211141 ) ) ;
#2051=CARTESIAN_POINT ( 'NONE',  ( 8.677276008184190204, 40.80007117484056067, 75.42295143068700725 ) ) ;
#2055=CARTESIAN_POINT ( 'NONE',  ( 0.3655949440400476647, 52.96731361127903170, 78.79918605040184332 ) ) ;
#2056=VERTEX_POINT ( 'NONE', #6768 ) ;
#2058=VERTEX_POINT ( 'NONE', #12958 ) ;
#2059=DIRECTION ( 'NONE',  ( -1.540237394707284220E-16, -1.793354297423764243E-16, 1.000000000000000000 ) ) ;
#2060=CARTESIAN_POINT ( 'NONE',  ( -7.521768377761679503, 40.39618086641783634, 77.60658645233600339 ) ) ;
#2061=ADVANCED_FACE ( 'NONE', ( #9991 ), #9375, .T. ) ;
#2062=PLANE ( 'NONE',  #11553 ) ;
#2066=CARTESIAN_POINT ( 'NONE',  ( 5.839584039462725862, 37.14605016217623046, 76.11636564480957645 ) ) ;
#2068=ORIENTED_EDGE ( 'NONE', *, *, #7854, .T. ) ;
#2071=CARTESIAN_POINT ( 'NONE',  ( 5.831313177393474767, 37.14014010695713353, 78.35708441643889444 ) ) ;
#2072=ORIENTED_EDGE ( 'NONE', *, *, #12976, .F. ) ;
#2074=EDGE_CURVE ( 'NONE', #17824, #13387, #20801, .T. ) ;
#2075=CARTESIAN_POINT ( 'NONE',  ( -3.539401246598059991, 43.09270903039240608, 82.45433879953087342 ) ) ;
#2077=B_SPLINE_SURFACE_WITH_KNOTS ( 'NONE', 3, 1, ( 
 ( #5486, #7296 ),
 ( #705, #8298 ),
 ( #5690, #3989 ),
 ( #11607, #15284 ),
 ( #10511, #19663 ),
 ( #16388, #16777 ),
 ( #814, #17972 ),
 ( #12199, #7185 ),
 ( #19560, #18679 ),
 ( #12096, #13686 ),
 ( #12000, #13571 ),
 ( #10626, #3394 ),
 ( #9908, #1816 ),
 ( #18471, #10408 ),
 ( #3783, #17095 ) ),
 .UNSPECIFIED., .F., .F., .F.,
 ( 4, 1, 1, 1, 1, 1, 1, 1, 1, 1, 1, 1, 4 ),
 ( 2, 2 ),
 ( 0.000000000000000000, 0.1167597168375007488, 0.2214683318549902913, 0.3169846747733736647, 0.4005759510517727939, 0.4723184013547362947, 0.5354911787873812834, 0.5872921887835030885, 0.6299408870648134373, 0.7051993628396346914, 0.7869278594151544182, 0.8829706743529757151, 1.000000000000000000 ),
 ( 0.000000000000000000, 1.000000000000000000 ),
 .UNSPECIFIED. ) ;
#2078=ORIENTED_EDGE ( 'NONE', *, *, #17255, .T. ) ;
#2080=CARTESIAN_POINT ( 'NONE',  ( -5.441628559556528799, 38.56297901168398568, 75.98496980016291502 ) ) ;
#2081=ORIENTED_EDGE ( 'NONE', *, *, #4414, .T. ) ;
#2082=CARTESIAN_POINT ( 'NONE',  ( 5.404201196092212278, 50.75047497752489534, 79.54845644658969661 ) ) ;
#2083=CARTESIAN_POINT ( 'NONE',  ( -4.519095118814112411, 36.94553422482819371, 76.36459416792565946 ) ) ;
#2085=CARTESIAN_POINT ( 'NONE',  ( -3.055882809522131094, 36.78399362325244937, 72.45433879953085921 ) ) ;
#2089=DIRECTION ( 'NONE',  ( -0.3165065846431826535, -0.9485903129789529098, -2.188653791613874008E-16 ) ) ;
#2090=AXIS2_PLACEMENT_3D ( 'NONE', #3293, #14884, #8405 ) ;
#2093=CARTESIAN_POINT ( 'NONE',  ( 6.154942347677927472, 50.94188193477284443, 75.39427037473855364 ) ) ;
#2094=CARTESIAN_POINT ( 'NONE',  ( 5.579861850767188436, 50.61660611302658452, 76.99230741551831159 ) ) ;
#2097=ORIENTED_EDGE ( 'NONE', *, *, #1579, .T. ) ;
#2098=EDGE_CURVE ( 'NONE', #4990, #3211, #9636, .T. ) ;
#2099=ORIENTED_EDGE ( 'NONE', *, *, #13357, .T. ) ;
#2100=CARTESIAN_POINT ( 'NONE',  ( 4.260580622453801425, 36.93752771366491316, 75.66510065906194882 ) ) ;
#2101=CARTESIAN_POINT ( 'NONE',  ( 7.805461224862361824, 40.55160501283941699, 79.26294543469528264 ) ) ;
#2102=ORIENTED_EDGE ( 'NONE', *, *, #8192, .F. ) ;
#2103=VECTOR ( 'NONE', #7409, 1000.000000000000000 ) ;
#2104=CARTESIAN_POINT ( 'NONE',  ( -4.909608826887576605, 38.01840769510402396, 75.43005142596166479 ) ) ;
#2105=EDGE_CURVE ( 'NONE', #18429, #5501, #12826, .T. ) ;
#2108=AXIS2_PLACEMENT_3D ( 'NONE', #14350, #10864, #12443 ) ;
#2109=VERTEX_POINT ( 'NONE', #6127 ) ;
#2112=VERTEX_POINT ( 'NONE', #1346 ) ;
#2115=CARTESIAN_POINT ( 'NONE',  ( -7.294472080575377326, 41.68420623513899415, 78.93669174070734584 ) ) ;
#2116=LINE ( 'NONE', #5285, #18784 ) ;
#2118=CARTESIAN_POINT ( 'NONE',  ( 8.272882475523552159, 41.50813378219739036, 75.97436175383765544 ) ) ;
#2119=VECTOR ( 'NONE', #3701, 1000.000000000000000 ) ;
#2125=VERTEX_POINT ( 'NONE', #14320 ) ;
#2126=CARTESIAN_POINT ( 'NONE',  ( 0.4078721606605034689, 52.35562703798189688, 76.01942718764288998 ) ) ;
#2127=EDGE_LOOP ( 'NONE', ( #8859, #6030, #16934, #14120 ) ) ;
#2128=CARTESIAN_POINT ( 'NONE',  ( 5.008975552073978932, 51.78836144432716537, 77.68963291717794561 ) ) ;
#2129=ADVANCED_FACE ( 'NONE', ( #20894 ), #2733, .F. ) ;
#2130=CARTESIAN_POINT ( 'NONE',  ( -4.534820675463383743, 37.71178600206382470, 78.55727908454632313 ) ) ;
#2133=CARTESIAN_POINT ( 'NONE',  ( -7.154059339130676598, 47.04588606493869918, 72.45433879953087342 ) ) ;
#2134=CARTESIAN_POINT ( 'NONE',  ( 7.753636062665578699, 48.02814353133176439, 72.45433879953087342 ) ) ;
#2135=CARTESIAN_POINT ( 'NONE',  ( 5.509674309642067058, 50.66539996488663178, 78.02050120841747116 ) ) ;
#2138=CARTESIAN_POINT ( 'NONE',  ( 8.412752068583754905, 42.37169419728517994, 79.44701590970058191 ) ) ;
#2139=LINE ( 'NONE', #12141, #4304 ) ;
#2140=CARTESIAN_POINT ( 'NONE',  ( 5.544276951911416340, 50.64433212932689088, 78.27786821129558348 ) ) ;
#2141=ORIENTED_EDGE ( 'NONE', *, *, #6732, .T. ) ;
#2142=CARTESIAN_POINT ( 'NONE',  ( 0.8450648237196969337, 52.96353724031100541, 78.65078808693101564 ) ) ;
#2148=B_SPLINE_CURVE_WITH_KNOTS ( 'NONE', 3,
 ( #19060, #17658, #3094, #9595, #12566, #2885, #8091, #11299, #2982, #4468, #4881 ),
 .UNSPECIFIED., .F., .F.,
 ( 4, 1, 1, 1, 1, 1, 1, 1, 4 ),
 ( 0.000000000000000000, 0.1208544691022559597, 0.2402546218586821825, 0.3598696579477268509, 0.4809300011950208842, 0.6037041574249993880, 0.7308714335393303729, 0.8631644367168944676, 0.9999999999999998890 ),
 .UNSPECIFIED. ) ;
#2151=CARTESIAN_POINT ( 'NONE',  ( 4.432284427945813121, 36.14044538431356557, 77.43080938776617472 ) ) ;
#2152=ORIENTED_EDGE ( 'NONE', *, *, #1461, .T. ) ;
#2154=ORIENTED_EDGE ( 'NONE', *, *, #16533, .F. ) ;
#2159=VECTOR ( 'NONE', #4458, 1000.000000000000000 ) ;
#2161=CARTESIAN_POINT ( 'NONE',  ( 8.787829143201870252, 41.13140593384865440, 77.80727997600146750 ) ) ;
#2164=VERTEX_POINT ( 'NONE', #19281 ) ;
#2169=CARTESIAN_POINT ( 'NONE',  ( -6.932661394073498684, 41.01730649666358630, 77.07900976289242578 ) ) ;
#2171=CARTESIAN_POINT ( 'NONE',  ( 5.430500802020164386, 37.59341706865419042, 76.00983965925686903 ) ) ;
#2173=EDGE_CURVE ( 'NONE', #279, #18072, #8618, .T. ) ;
#2181=ORIENTED_EDGE ( 'NONE', *, *, #4678, .F. ) ;
#2182=CARTESIAN_POINT ( 'NONE',  ( -4.209923912819722780, 38.70632820095286775, 77.90139762306027649 ) ) ;
#2184=VERTEX_POINT ( 'NONE', #5997 ) ;
#2185=B_SPLINE_CURVE_WITH_KNOTS ( 'NONE', 3,
 ( #5206, #3303, #12996, #16294, #213, #1829, #16503, #17987, #3616, #3412, #14792, #9922, #3519, #10023, #1920, #5738, #7231, #2344, #854, #10672, #4034, #12248, #17135, #13729, #18730, #8735, #11823 ),
 .UNSPECIFIED., .F., .F.,
 ( 4, 1, 1, 1, 1, 1, 1, 1, 1, 1, 1, 1, 1, 1, 1, 1, 1, 1, 1, 1, 1, 1, 1, 1, 4 ),
 ( 0.000000000000000000, 0.04981064803454772483, 0.09714544705284619552, 0.1414600528990057893, 0.1834992459999073566, 0.2227657660311612720, 0.2600403684493295953, 0.2949019026928859644, 0.3281718573768891978, 0.3602550803352915776, 0.3926260793274650163, 0.4253773651182169435, 0.4592860034499685606, 0.4939555262694102500, 0.5299277977440765008, 0.5677681756169172811, 0.6073809588441169138, 0.6486765994917140787, 0.6919144726687150859, 0.7374495574558619371, 0.7851062196494249523, 0.8349986418379958808, 0.8875444209637680659, 0.9425288195084158271, 1.000000000000000000 ),
 .UNSPECIFIED. ) ;
#2186=CARTESIAN_POINT ( 'NONE',  ( 5.750640099535992533, 51.24052371918730842, 75.36022115247205022 ) ) ;
#2189=CARTESIAN_POINT ( 'NONE',  ( 1.997688547473374099, 52.22837930658135264, 78.99477371038418028 ) ) ;
#2190=ORIENTED_EDGE ( 'NONE', *, *, #19409, .F. ) ;
#2191=CARTESIAN_POINT ( 'NONE',  ( 0.7971746217111946864, 52.35757360625640189, 77.48431181218198560 ) ) ;
#2192=LINE ( 'NONE', #13998, #673 ) ;
#2194=CARTESIAN_POINT ( 'NONE',  ( -3.533185125431080653, 36.21728222759318072, 78.38559710128819802 ) ) ;
#2195=CARTESIAN_POINT ( 'NONE',  ( -5.661408436751226070, 39.74363423441516829, 72.45433879953085921 ) ) ;
#2196=CARTESIAN_POINT ( 'NONE',  ( 6.450247442662826458, 38.49669771550791353, 76.69330938776616335 ) ) ;
#2197=EDGE_CURVE ( 'NONE', #4469, #16470, #10915, .T. ) ;
#2198=VERTEX_POINT ( 'NONE', #12601 ) ;
#2200=VERTEX_POINT ( 'NONE', #15900 ) ;
#2201=CARTESIAN_POINT ( 'NONE',  ( 8.787829143201870252, 41.13140593384865440, 77.80727997600146750 ) ) ;
#2204=CARTESIAN_POINT ( 'NONE',  ( -3.496280357775573222, 52.10652770678432688, 75.88277413867518817 ) ) ;
#2205=ORIENTED_EDGE ( 'NONE', *, *, #15377, .F. ) ;
#2206=CARTESIAN_POINT ( 'NONE',  ( 6.921466148593897749, 50.37568168049836714, 78.61296362383696135 ) ) ;
#2208=DIRECTION ( 'NONE',  ( 0.3165065846431930341, 0.9485903129789495791, 2.188653791613884362E-16 ) ) ;
#2210=CARTESIAN_POINT ( 'NONE',  ( 5.701723800661059549, 37.96731586519243251, 75.40772603260481333 ) ) ;
#2212=PLANE ( 'NONE',  #17884 ) ;
#2213=CARTESIAN_POINT ( 'NONE',  ( 4.097638513832391638, 51.53669645659447696, 76.64209438045911327 ) ) ;
#2214=EDGE_CURVE ( 'NONE', #14909, #13986, #7781, .T. ) ;
#2215=LINE ( 'NONE', #4973, #5167 ) ;
#2216=LINE ( 'NONE', #10751, #7952 ) ;
#2217=CARTESIAN_POINT ( 'NONE',  ( 0.6017860623987091317, 52.35409786639082341, 77.38437845781280089 ) ) ;
#2219=CARTESIAN_POINT ( 'NONE',  ( -4.517072128342570991, 36.94403992325788977, 76.81463291717793140 ) ) ;
#2220=EDGE_CURVE ( 'NONE', #1879, #18554, #5121, .T. ) ;
#2222=EDGE_CURVE ( 'NONE', #11233, #557, #8432, .T. ) ;
#2223=CARTESIAN_POINT ( 'NONE',  ( -1.123656915330052408, 35.37488560990637865, 76.86610350541323555 ) ) ;
#2225=LINE ( 'NONE', #3916, #12943 ) ;
#2226=ORIENTED_EDGE ( 'NONE', *, *, #9928, .F. ) ;
#2227=CARTESIAN_POINT ( 'NONE',  ( 5.216235101676203634, 50.88570979358116375, 77.12281451049645398 ) ) ;
#2229=CARTESIAN_POINT ( 'NONE',  ( -3.349688636638950889, 52.21127678364309332, 78.10580938776615767 ) ) ;
#2231=CARTESIAN_POINT ( 'NONE',  ( -4.895412223390202655, 37.22350451100091817, 76.36316342150684022 ) ) ;
#2235=ORIENTED_EDGE ( 'NONE', *, *, #6169, .T. ) ;
#2237=B_SPLINE_CURVE_WITH_KNOTS ( 'NONE', 3,
 ( #2509, #15387, #18352, #694, #7174, #9002, #15489, #17492, #13990, #18983, #12404, #18884, #9417, #9629, #11225, #1007, #1427, #10819, #4598, #16007, #14092, #12605, #17590, #14295, #19092, #7609, #12498 ),
 .UNSPECIFIED., .F., .F.,
 ( 4, 1, 1, 1, 1, 1, 1, 1, 1, 1, 1, 1, 1, 1, 1, 1, 1, 1, 1, 1, 1, 1, 1, 1, 4 ),
 ( 0.000000000000000000, 0.04992685941337848821, 0.09871136507264777205, 0.1457954968408328167, 0.1915776562037285746, 0.2364429891513756543, 0.2798905081306632403, 0.3226114784840122263, 0.3640369619956516645, 0.4040931382756795531, 0.4423864865660626644, 0.4791244981183566676, 0.5145420102664520767, 0.5484747442263178119, 0.5814193454185596632, 0.6141157465626525536, 0.6462545211269067336, 0.6795390940691592441, 0.7156628256359011120, 0.7545220547839790459, 0.7966562418723396322, 0.8423152836035615598, 0.8912945236129800053, 0.9437207944264596193, 1.000000000000000000 ),
 .UNSPECIFIED. ) ;
#2238=CARTESIAN_POINT ( 'NONE',  ( 9.201390675156970289, 42.37087608097247227, 79.34093170394821470 ) ) ;
#2239=CARTESIAN_POINT ( 'NONE',  ( 8.787829143201870252, 41.13140593384865440, 77.14698585835439815 ) ) ;
#2246=EDGE_CURVE ( 'NONE', #4602, #14794, #3429, .T. ) ;
#2247=CARTESIAN_POINT ( 'NONE',  ( -7.199075288064514133, 41.41206959199826088, 78.61536821129558916 ) ) ;
#2251=VERTEX_POINT ( 'NONE', #9941 ) ;
#2256=ORIENTED_EDGE ( 'NONE', *, *, #534, .F. ) ;
#2257=CARTESIAN_POINT ( 'NONE',  ( -4.283496025856503131, 47.84326572019833179, 72.45433879953087342 ) ) ;
#2260=CARTESIAN_POINT ( 'NONE',  ( -3.926839636664805511, 51.79886580987140832, 79.42193487995672285 ) ) ;
#2261=CARTESIAN_POINT ( 'NONE',  ( 4.393996117251955269, 36.11308595931626542, 76.96022115247204454 ) ) ;
#2264=ORIENTED_EDGE ( 'NONE', *, *, #11861, .F. ) ;
#2269=CARTESIAN_POINT ( 'NONE',  ( 5.309255083855641821, 37.50457964663987553, 75.97198585835440099 ) ) ;
#2271=CARTESIAN_POINT ( 'NONE',  ( 6.573693162767834330, 44.00881163587200717, 75.45433879953087342 ) ) ;
#2273=CARTESIAN_POINT ( 'NONE',  ( -4.387981331227590154, 51.46935083841186298, 75.37146543928014353 ) ) ;
#2274=ORIENTED_EDGE ( 'NONE', *, *, #13438, .F. ) ;
#2276=ADVANCED_FACE ( 'NONE', ( #1745 ), #8225, .T. ) ;
#2277=ORIENTED_EDGE ( 'NONE', *, *, #16165, .F. ) ;
#2281=CARTESIAN_POINT ( 'NONE',  ( -8.007168758255900798, 41.92872724082349123, 77.34580771017452605 ) ) ;
#2288=VERTEX_POINT ( 'NONE', #14711 ) ;
#2289=CARTESIAN_POINT ( 'NONE',  ( -7.609845089999874190, 43.10833364818387992, 76.06610350541322418 ) ) ;
#2293=CARTESIAN_POINT ( 'NONE',  ( -4.804644443005473775, 51.17161863374556674, 76.44036821129557779 ) ) ;
#2298=AXIS2_PLACEMENT_3D ( 'NONE', #15629, #17708, #4819 ) ;
#2301=ORIENTED_EDGE ( 'NONE', *, *, #10196, .F. ) ;
#2303=CARTESIAN_POINT ( 'NONE',  ( 2.002180786195896900, 52.20240726524163932, 75.93722239247614425 ) ) ;
#2304=VECTOR ( 'NONE', #18591, 1000.000000000000000 ) ;
#2306=FACE_BOUND ( 'NONE', #1922, .T. ) ;
#2307=CARTESIAN_POINT ( 'NONE',  ( 0.3594029150778950688, 52.35600914658472504, 77.51213090161979835 ) ) ;
#2309=ORIENTED_EDGE ( 'NONE', *, *, #1184, .T. ) ;
#2310=LINE ( 'NONE', #10421, #15056 ) ;
#2311=ORIENTED_EDGE ( 'NONE', *, *, #4534, .F. ) ;
#2317=CARTESIAN_POINT ( 'NONE',  ( -7.375807652561674033, 41.95680328822960092, 78.70894555753855570 ) ) ;
#2320=CARTESIAN_POINT ( 'NONE',  ( 0.7603968142568129363, 52.96420094791147903, 77.43909148762901395 ) ) ;
#2322=CARTESIAN_POINT ( 'NONE',  ( 5.089266475819410829, 50.80422082628552261, 75.36789977960694387 ) ) ;
#2324=DIRECTION ( 'NONE',  ( -0.3855022007253699479, 0.1286266402413967502, -0.9136975652020240535 ) ) ;
#2325=ORIENTED_EDGE ( 'NONE', *, *, #15698, .F. ) ;
#2329=EDGE_CURVE ( 'NONE', #6705, #502, #19256, .T. ) ;
#2336=CARTESIAN_POINT ( 'NONE',  ( -4.517072128342570991, 36.94403992325788977, 76.81463291717793140 ) ) ;
#2337=DIRECTION ( 'NONE',  ( -0.3165065846431826535, -0.9485903129789527988, 0.000000000000000000 ) ) ;
#2339=EDGE_CURVE ( 'NONE', #19914, #10724, #11510, .T. ) ;
#2341=EDGE_LOOP ( 'NONE', ( #11895, #5818, #19485, #17485, #7605, #7895 ) ) ;
#2342=VERTEX_POINT ( 'NONE', #8093 ) ;
#2343=CARTESIAN_POINT ( 'NONE',  ( 9.263154249150899133, 42.55598543044034443, 79.20437336408532758 ) ) ;
#2344=CARTESIAN_POINT ( 'NONE',  ( -4.002011967609276688, 36.56358573041305249, 75.49480657079904233 ) ) ;
#2346=CARTESIAN_POINT ( 'NONE',  ( 5.799728954038464224, 51.20426375978601641, 77.28794373216803137 ) ) ;
#2347=LINE ( 'NONE', #20727, #1620 ) ;
#2348=VECTOR ( 'NONE', #11097, 1000.000000000000227 ) ;
#2349=CARTESIAN_POINT ( 'NONE',  ( -8.190409139795066906, 42.92474528817020740, 76.06610350541322418 ) ) ;
#2351=CARTESIAN_POINT ( 'NONE',  ( -0.2933318293205740002, 52.92496007935942259, 79.40378080832554986 ) ) ;
#2352=CARTESIAN_POINT ( 'NONE',  ( -7.701322689919003039, 47.31527676703458951, 78.22140724958771330 ) ) ;
#2354=CARTESIAN_POINT ( 'NONE',  ( 6.774925554820337759, 37.81441096401221102, 75.87985893138584004 ) ) ;
#2355=ORIENTED_EDGE ( 'NONE', *, *, #4557, .F. ) ;
#2356=EDGE_CURVE ( 'NONE', #5798, #4528, #1487, .T. ) ;
#2357=CARTESIAN_POINT ( 'NONE',  ( 1.309422257521039024, 52.32623752027490127, 75.43140154991867519 ) ) ;
#2361=ADVANCED_FACE ( 'NONE', ( #16082 ), #13094, .T. ) ;
#2365=EDGE_CURVE ( 'NONE', #16412, #20669, #5266, .T. ) ;
#2368=CARTESIAN_POINT ( 'NONE',  ( -3.425442721482995445, 52.15714568814760810, 78.86270620133520026 ) ) ;
#2370=CARTESIAN_POINT ( 'NONE',  ( 0.8505931169942170245, 52.96356605174086951, 76.42615000023204175 ) ) ;
#2371=CARTESIAN_POINT ( 'NONE',  ( 0.5672115121316617659, 52.96572379054431678, 78.93584868477675798 ) ) ;
#2373=CARTESIAN_POINT ( 'NONE',  ( -7.617292153972126556, 43.16748516956134551, 72.45433879953085921 ) ) ;
#2374=VECTOR ( 'NONE', #12084, 1000.000000000000114 ) ;
#2375=ORIENTED_EDGE ( 'NONE', *, *, #17785, .T. ) ;
#2377=CARTESIAN_POINT ( 'NONE',  ( -3.099028042286850138, 36.80507306568591019, 78.38160280800818214 ) ) ;
#2378=DIRECTION ( 'NONE',  ( -0.3165065846431826535, -0.9485903129789527988, 0.000000000000000000 ) ) ;
#2379=VECTOR ( 'NONE', #13162, 1000.000000000000000 ) ;
#2380=VECTOR ( 'NONE', #19902, 1000.000000000000114 ) ;
#2381=CARTESIAN_POINT ( 'NONE',  ( 6.467578312573260213, 50.71095034124950729, 79.40187404227555135 ) ) ;
#2382=DIRECTION ( 'NONE',  ( -0.9996789974703352843, 0.02533578529877050789, -1.494306935163143217E-16 ) ) ;
#2384=CARTESIAN_POINT ( 'NONE',  ( -5.251100579623896536, 37.48623717174979220, 75.42164981362142839 ) ) ;
#2386=VERTEX_POINT ( 'NONE', #3005 ) ;
#2387=CARTESIAN_POINT ( 'NONE',  ( 8.865792162213244509, 41.36506604770743678, 78.93669174070734584 ) ) ;
#2388=ORIENTED_EDGE ( 'NONE', *, *, #14063, .F. ) ;
#2390=EDGE_CURVE ( 'NONE', #10307, #1377, #14391, .T. ) ;
#2396=CARTESIAN_POINT ( 'NONE',  ( 0.5472186751089482826, 52.96225730869564075, 77.38586825451125151 ) ) ;
#2397=ORIENTED_EDGE ( 'NONE', *, *, #3532, .T. ) ;
#2398=CARTESIAN_POINT ( 'NONE',  ( 1.851481395807867303, 48.14626068599128672, 79.40903933791013003 ) ) ;
#2400=EDGE_LOOP ( 'NONE', ( #7586, #711, #14166, #3451 ) ) ;
#2401=CARTESIAN_POINT ( 'NONE',  ( 2.021724605155154286, 52.22392082761901122, 78.95144739612317153 ) ) ;
#2404=ORIENTED_EDGE ( 'NONE', *, *, #14317, .T. ) ;
#2405=CARTESIAN_POINT ( 'NONE',  ( 0.8448918989077306430, 52.35582772558348097, 77.71799948569541527 ) ) ;
#2410=CARTESIAN_POINT ( 'NONE',  ( 0.5886017282102210535, 52.96193049659134999, 78.93669174070734584 ) ) ;
#2411=B_SPLINE_CURVE_WITH_KNOTS ( 'NONE', 3,
 ( #12264, #18531, #17356, #20541, #5870, #13742, #17247, #1085, #5548, #8861, #2357, #20212, #12463, #2671, #20322, #9175 ),
 .UNSPECIFIED., .F., .F.,
 ( 4, 2, 2, 2, 2, 2, 2, 4 ),
 ( 0.000000000000000000, 0.0002719588327788573625, 0.0005439176655577147249, 0.0008158764983365720874, 0.001087835331115429450, 0.001631752996673123575, 0.001903711829451970854, 0.002175670662230817700 ),
 .UNSPECIFIED. ) ;
#2412=CARTESIAN_POINT ( 'NONE',  ( 5.241460166982749413, 50.86801069014953924, 72.45433879953087342 ) ) ;
#2413=EDGE_CURVE ( 'NONE', #9137, #15270, #302, .T. ) ;
#2416=CARTESIAN_POINT ( 'NONE',  ( 1.383856401949368875, 52.20728298024938141, 75.46169036918907125 ) ) ;
#2417=ORIENTED_EDGE ( 'NONE', *, *, #16993, .T. ) ;
#2418=FACE_OUTER_BOUND ( 'NONE', #18268, .T. ) ;
#2419=FACE_OUTER_BOUND ( 'NONE', #3614, .T. ) ;
#2421=ORIENTED_EDGE ( 'NONE', *, *, #10000, .F. ) ;
#2423=CARTESIAN_POINT ( 'NONE',  ( 6.467578312573260213, 50.71095034124950729, 79.40187404227555135 ) ) ;
#2426=LINE ( 'NONE', #4111, #13508 ) ;
#2427=DIRECTION ( 'NONE',  ( -1.540237394707284220E-16, -1.793354297423764243E-16, 1.000000000000000000 ) ) ;
#2429=CARTESIAN_POINT ( 'NONE',  ( -4.142301312995646079, 50.90705069304581087, 79.54681934798814780 ) ) ;
#2430=CARTESIAN_POINT ( 'NONE',  ( -7.594845318933780121, 42.99712684704532961, 78.99675904272704940 ) ) ;
#2432=B_SPLINE_SURFACE_WITH_KNOTS ( 'NONE', 3, 1, ( 
 ( #14715, #14815 ),
 ( #6721, #18219 ),
 ( #13227, #13335 ),
 ( #19704, #10045 ),
 ( #16524, #1944 ),
 ( #14915, #340 ),
 ( #5229, #16630 ),
 ( #2051, #11797 ),
 ( #3691, #15093 ),
 ( #13485, #19956 ),
 ( #5387, #3802 ),
 ( #15193, #18492 ),
 ( #10426, #16893 ),
 ( #20179, #5609 ),
 ( #14119, #4113 ),
 ( #20501, #7638 ),
 ( #19123, #20394 ),
 ( #4322, #2847 ),
 ( #4221, #5933 ),
 ( #18810, #4536 ),
 ( #10747, #13909 ),
 ( #9029, #12430 ),
 ( #10849, #7314 ),
 ( #15836, #17209 ),
 ( #9350, #2634 ),
 ( #1247, #10643 ),
 ( #9135, #7416 ),
 ( #7740, #17110 ),
 ( #15622, #5824 ),
 ( #1044, #7530 ),
 ( #4437, #6029 ) ),
 .UNSPECIFIED., .F., .F., .F.,
 ( 4, 1, 1, 1, 1, 1, 1, 1, 1, 1, 1, 1, 1, 1, 1, 1, 1, 1, 1, 1, 1, 1, 1, 1, 1, 1, 1, 1, 4 ),
 ( 2, 2 ),
 ( 0.000000000000000000, 0.04402879139878041609, 0.08604540006880039005, 0.1260521755942069777, 0.1641511405281330660, 0.2003442918647115323, 0.2347805632357193584, 0.2676267374383518027, 0.2986515534027265328, 0.3283031585252670914, 0.3570062744687346745, 0.3846398569069188755, 0.4113091075058319390, 0.4372322170293685417, 0.4625237182236557887, 0.4872935253130181721, 0.5115235732650775802, 0.5580727247437320404, 0.6018864549903041317, 0.6437727082467282758, 0.6848253805047307408, 0.7076001045990409910, 0.7352252901417971609, 0.7674583008524621386, 0.8043075748156178761, 0.8460289209228792906, 0.8926357087385640154, 0.9438729761760307202, 1.000000000000000000 ),
 ( 0.000000000000000000, 1.000000000000000000 ),
 .UNSPECIFIED. ) ;
#2433=CARTESIAN_POINT ( 'NONE',  ( 0.8452388978709587386, 52.35217815131273511, 77.74134350746754762 ) ) ;
#2434=EDGE_CURVE ( 'NONE', #1854, #17442, #641, .T. ) ;
#2436=PLANE ( 'NONE',  #12586 ) ;
#2439=CARTESIAN_POINT ( 'NONE',  ( -7.955859814585196865, 41.77362178188068498, 78.62287654527649750 ) ) ;
#2441=VECTOR ( 'NONE', #10969, 1000.000000000000000 ) ;
#2445=CARTESIAN_POINT ( 'NONE',  ( 5.750640099535992533, 51.24052371918730842, 75.36022115247205022 ) ) ;
#2448=CARTESIAN_POINT ( 'NONE',  ( -5.135517778528630117, 37.40086081253994621, 77.33633635728615729 ) ) ;
#2449=CARTESIAN_POINT ( 'NONE',  ( -7.607193028824243086, 43.12151120863332920, 78.28007409364852265 ) ) ;
#2450=CARTESIAN_POINT ( 'NONE',  ( 5.564133502460520297, 36.94922329332227662, 77.75193993234761081 ) ) ;
#2452=ORIENTED_EDGE ( 'NONE', *, *, #324, .T. ) ;
#2455=CARTESIAN_POINT ( 'NONE',  ( 6.519648887156654915, 49.75415655210358068, 76.85154547133247149 ) ) ;
#2456=CARTESIAN_POINT ( 'NONE',  ( -5.667418469993653396, 43.80274312437727247, 80.45433879953087342 ) ) ;
#2457=CARTESIAN_POINT ( 'NONE',  ( 8.951667845840693971, 41.62244091939069790, 76.38301527011910252 ) ) ;
#2459=CARTESIAN_POINT ( 'NONE',  ( 5.936990147225109204, 51.10287444559717329, 77.01219674908871582 ) ) ;
#2460=PLANE ( 'NONE',  #17589 ) ;
#2461=CARTESIAN_POINT ( 'NONE',  ( 9.080605399405701661, 42.00887494707089331, 78.12791555553386047 ) ) ;
#2463=B_SPLINE_CURVE_WITH_KNOTS ( 'NONE', 3,
 ( #13365, #18150, #9976, #16457, #6956, #14846, #1877, #19934, #3569, #10075, #8469, #14952, #373, #6858 ),
 .UNSPECIFIED., .F., .F.,
 ( 4, 2, 2, 2, 2, 2, 4 ),
 ( 0.000000000000000000, 0.0001566759795594400181, 0.0003133519591188800362, 0.0003916899488986000724, 0.0004700279386783201086, 0.0005483659284580401447, 0.0006267039182377599641 ),
 .UNSPECIFIED. ) ;
#2465=CARTESIAN_POINT ( 'NONE',  ( -6.879319821983923333, 47.65235040223281260, 78.32456649736994336 ) ) ;
#2467=VECTOR ( 'NONE', #6966, 1000.000000000000114 ) ;
#2468=EDGE_CURVE ( 'NONE', #16604, #12459, #6783, .T. ) ;
#2469=CARTESIAN_POINT ( 'NONE',  ( -7.912665105161496903, 41.65176285775086029, 79.54689059276779517 ) ) ;
#2470=CARTESIAN_POINT ( 'NONE',  ( 5.853612939038055352, 51.16446183064613251, 78.89719962956496602 ) ) ;
#2471=VECTOR ( 'NONE', #6575, 1000.000000000000000 ) ;
#2473=ORIENTED_EDGE ( 'NONE', *, *, #8472, .F. ) ;
#2474=CARTESIAN_POINT ( 'NONE',  ( -4.766891056059167298, 51.19859582181767621, 78.86176377286571437 ) ) ;
#2476=ORIENTED_EDGE ( 'NONE', *, *, #17478, .T. ) ;
#2479=CARTESIAN_POINT ( 'NONE',  ( -3.387980870927748800, 52.18391455498849751, 78.68920376838389075 ) ) ;
#2480=CARTESIAN_POINT ( 'NONE',  ( 0.5915428171209280439, 52.96190779654647685, 77.38375056423674891 ) ) ;
#2482=LINE ( 'NONE', #8977, #8934 ) ;
#2483=ORIENTED_EDGE ( 'NONE', *, *, #3782, .T. ) ;
#2485=CARTESIAN_POINT ( 'NONE',  ( 5.360476111768327279, 50.78276677175456655, 77.95007283232945383 ) ) ;
#2486=VECTOR ( 'NONE', #10396, 1000.000000000000000 ) ;
#2487=ORIENTED_EDGE ( 'NONE', *, *, #11341, .T. ) ;
#2488=CARTESIAN_POINT ( 'NONE',  ( 6.485595322925789219, 49.79047067704939877, 78.31989234064305094 ) ) ;
#2489=CARTESIAN_POINT ( 'NONE',  ( 4.546108750497564799, 52.13026250523957827, 76.88467537290178200 ) ) ;
#2490=ADVANCED_FACE ( 'NONE', ( #7599 ), #9406, .T. ) ;
#2491=CARTESIAN_POINT ( 'NONE',  ( 0.3201111382462868971, 51.36399839264385037, 76.44919174070734869 ) ) ;
#2492=CARTESIAN_POINT ( 'NONE',  ( -7.437180633310755518, 40.40796476851179619, 77.62507288737846523 ) ) ;
#2494=CARTESIAN_POINT ( 'NONE',  ( 5.807735516834878986, 37.12329237395520920, 76.04105433551922033 ) ) ;
#2495=CARTESIAN_POINT ( 'NONE',  ( -5.623541984526490012, 37.76134463469641389, 75.60525969576029581 ) ) ;
#2497=EDGE_CURVE ( 'NONE', #9206, #17046, #455, .T. ) ;
#2499=CARTESIAN_POINT ( 'NONE',  ( 8.211482387076870282, 41.32431627734197832, 78.55826321071354812 ) ) ;
#2500=ORIENTED_EDGE ( 'NONE', *, *, #7029, .F. ) ;
#2502=CARTESIAN_POINT ( 'NONE',  ( -4.126251043470592350, 50.73659813720719569, 75.36123162944792853 ) ) ;
#2504=ORIENTED_EDGE ( 'NONE', *, *, #19447, .T. ) ;
#2507=CARTESIAN_POINT ( 'NONE',  ( 5.561379608955574483, 51.38032281970146897, 76.39036821129558064 ) ) ;
#2509=CARTESIAN_POINT ( 'NONE',  ( 5.665287683258889651, 37.02150436742986273, 75.36022115247205022 ) ) ;
#2514=CARTESIAN_POINT ( 'NONE',  ( -5.405939962049822967, 49.82766502745145232, 78.10580938776615767 ) ) ;
#2515=DIRECTION ( 'NONE',  ( -0.3165065846431827090, -0.9485903129789527988, 0.000000000000000000 ) ) ;
#2518=DIRECTION ( 'NONE',  ( 0.5813877811927011807, -0.8136266022444372803, -5.636455622144619183E-17 ) ) ;
#2520=CARTESIAN_POINT ( 'NONE',  ( 5.393087686338805753, 50.75151780712509009, 78.93669174070734584 ) ) ;
#2523=CARTESIAN_POINT ( 'NONE',  ( -6.850209527372854268, 47.75220363455441230, 78.32492703482499508 ) ) ;
#2526=LINE ( 'NONE', #921, #2103 ) ;
#2528=CARTESIAN_POINT ( 'NONE',  ( -3.373440834332912086, 52.19430433279444514, 76.25796290525131838 ) ) ;
#2530=CARTESIAN_POINT ( 'NONE',  ( -7.333990156426536622, 40.19720935722482125, 75.45433879953087342 ) ) ;
#2531=ORIENTED_EDGE ( 'NONE', *, *, #6063, .T. ) ;
#2532=CARTESIAN_POINT ( 'NONE',  ( 4.468221962074742315, 51.27377933314817682, 79.33697856897433098 ) ) ;
#2535=CARTESIAN_POINT ( 'NONE',  ( -4.645483384943265293, 37.03889214578788369, 77.94562699264550076 ) ) ;
#2536=CARTESIAN_POINT ( 'NONE',  ( -7.068211413017330358, 41.44596913834843122, 79.53187240040659844 ) ) ;
#2537=CARTESIAN_POINT ( 'NONE',  ( 6.882736312352589536, 37.89144858414100270, 77.26022115247205591 ) ) ;
#2538=FACE_OUTER_BOUND ( 'NONE', #6775, .T. ) ;
#2539=CARTESIAN_POINT ( 'NONE',  ( -4.848575437813097189, 50.22045157099402957, 75.48294376282896678 ) ) ;
#2540=( NAMED_UNIT ( * ) PLANE_ANGLE_UNIT ( ) SI_UNIT ( $, .RADIAN. ) );
#2543=EDGE_LOOP ( 'NONE', ( #20116, #7012, #11650, #5179 ) ) ;
#2544=CARTESIAN_POINT ( 'NONE',  ( 8.295230459923363497, 41.57513201800704650, 78.93627637315103129 ) ) ;
#2546=DIRECTION ( 'NONE',  ( -0.3165065846431829311, -0.9485903129789527988, -2.188653791613874255E-16 ) ) ;
#2548=CARTESIAN_POINT ( 'NONE',  ( -4.370691255933373931, 51.48170569318705247, 79.53937015691786883 ) ) ;
#2549=CARTESIAN_POINT ( 'NONE',  ( -4.453436368711327198, 50.68011839687689957, 76.44036821129557779 ) ) ;
#2551=CARTESIAN_POINT ( 'NONE',  ( -4.842431058766297980, 37.18436945890474021, 76.00936707281648808 ) ) ;
#2552=CARTESIAN_POINT ( 'NONE',  ( -7.498699170063192199, 42.77841955502557170, 79.26478910100486530 ) ) ;
#2553=CARTESIAN_POINT ( 'NONE',  ( 8.480805917192030918, 42.18208851247151614, 78.13498589288056451 ) ) ;
#2554=CARTESIAN_POINT ( 'NONE',  ( -4.338703338798237219, 37.56692202555748139, 75.97299512023676016 ) ) ;
#2556=CARTESIAN_POINT ( 'NONE',  ( 8.214799251806553571, 41.32260305165857517, 78.45948585835439815 ) ) ;
#2557=CARTESIAN_POINT ( 'NONE',  ( 0.5221537403065010796, 44.16218137147968292, 78.25433879953088478 ) ) ;
#2558=CARTESIAN_POINT ( 'NONE',  ( 8.945167944750011202, 41.60296030347588214, 76.15680935856015310 ) ) ;
#2559=CARTESIAN_POINT ( 'NONE',  ( -5.955451856753747109, 38.00651308716548726, 77.05433879953086773 ) ) ;
#2561=CARTESIAN_POINT ( 'NONE',  ( -4.101343092926645895, 50.93446548159070630, 78.88986109003506897 ) ) ;
#2563=CARTESIAN_POINT ( 'NONE',  ( -4.536263512923754959, 51.36339382032895884, 75.97373057797423712 ) ) ;
#2564=CARTESIAN_POINT ( 'NONE',  ( -7.517776057030331138, 47.86537766978320718, 78.32456649736994336 ) ) ;
#2565=CARTESIAN_POINT ( 'NONE',  ( -5.492848774261456235, 38.60081332101042051, 78.80728580974474085 ) ) ;
#2566=CARTESIAN_POINT ( 'NONE',  ( 5.991756872021341884, 37.25478729691962343, 75.38041148603002739 ) ) ;
#2567=ORIENTED_EDGE ( 'NONE', *, *, #17772, .T. ) ;
#2568=CARTESIAN_POINT ( 'NONE',  ( 5.799728954038464224, 51.20426375978601641, 77.28794373216803137 ) ) ;
#2571=DIRECTION ( 'NONE',  ( 1.540237394707283727E-16, 1.793354297423763257E-16, -1.000000000000000000 ) ) ;
#2573=ORIENTED_EDGE ( 'NONE', *, *, #20426, .F. ) ;
#2574=CARTESIAN_POINT ( 'NONE',  ( 6.522560395309022319, 49.75102024682771429, 76.63889762306028786 ) ) ;
#2576=CARTESIAN_POINT ( 'NONE',  ( -4.007802336140563249, 51.74101282905964894, 79.45569801420249689 ) ) ;
#2577=LINE ( 'NONE', #15564, #3997 ) ;
#2578=CARTESIAN_POINT ( 'NONE',  ( 5.755371611800503828, 51.23702874167446453, 77.28963291717792572 ) ) ;
#2581=CARTESIAN_POINT ( 'NONE',  ( 5.599231707071657738, 51.35236299959863970, 78.59183879953087626 ) ) ;
#2583=EDGE_CURVE ( 'NONE', #10346, #4844, #12893, .T. ) ;
#2584=ORIENTED_EDGE ( 'NONE', *, *, #16663, .T. ) ;
#2586=DIRECTION ( 'NONE',  ( -0.3164955768080224829, -0.9485573217986537076, 0.008340091313796951095 ) ) ;
#2588=CARTESIAN_POINT ( 'NONE',  ( 8.214799251806553571, 41.32260305165857517, 76.40801527011910821 ) ) ;
#2589=EDGE_CURVE ( 'NONE', #14804, #7531, #685, .T. ) ;
#2591=CARTESIAN_POINT ( 'NONE',  ( 5.658108625003792191, 37.01637447524286273, 75.97198585835440099 ) ) ;
#2592=DIRECTION ( 'NONE',  ( -0.9485903129789527988, 0.3165065846431829311, -8.934458285744989980E-17 ) ) ;
#2593=ORIENTED_EDGE ( 'NONE', *, *, #10000, .T. ) ;
#2594=CARTESIAN_POINT ( 'NONE',  ( -1.117719678584871090, 36.12782917792895176, 76.86610350541323555 ) ) ;
#2597=ADVANCED_FACE ( 'NONE', ( #16596 ), #10443, .T. ) ;
#2598=EDGE_LOOP ( 'NONE', ( #13106, #7378, #18979, #1998 ) ) ;
#2599=CIRCLE ( 'NONE', #18221, 4.200000000000003730 ) ;
#2600=CARTESIAN_POINT ( 'NONE',  ( -4.561334846378493069, 51.34547876336230843, 75.36123162944792853 ) ) ;
#2602=ORIENTED_EDGE ( 'NONE', *, *, #19010, .T. ) ;
#2604=LINE ( 'NONE', #12187, #12335 ) ;
#2606=CARTESIAN_POINT ( 'NONE',  ( -4.804644443005473775, 51.17161863374555963, 78.45066232894264147 ) ) ;
#2607=EDGE_CURVE ( 'NONE', #11628, #26, #8722, .T. ) ;
#2608=VERTEX_POINT ( 'NONE', #20084 ) ;
#2609=CARTESIAN_POINT ( 'NONE',  ( 2.114739078132396255, 52.20604064652322762, 78.26567215968707103 ) ) ;
#2612=CARTESIAN_POINT ( 'NONE',  ( -5.357560295633086334, 49.87790279705807706, 78.82253136475043220 ) ) ;
#2613=CARTESIAN_POINT ( 'NONE',  ( 5.098362185591304829, 37.35789059091872133, 76.18266185049213846 ) ) ;
#2614=APPLICATION_CONTEXT ( 'automotive_design' ) ;
#2616=SHAPE_DEFINITION_REPRESENTATION ( #20075, #9739 ) ;
#2617=CARTESIAN_POINT ( 'NONE',  ( 5.089995120079088942, 37.35733679680688368, 76.23948081211554495 ) ) ;
#2618=CARTESIAN_POINT ( 'NONE',  ( 5.497686461428984650, 36.90174267058258550, 76.03636210503219672 ) ) ;
#2621=CARTESIAN_POINT ( 'NONE',  ( 1.086229506649126764, 52.96246798893113805, 75.39315892328370694 ) ) ;
#2623=CARTESIAN_POINT ( 'NONE',  ( 6.532049803590284753, 50.66332784790530752, 75.53514883118299394 ) ) ;
#2624=EDGE_CURVE ( 'NONE', #16845, #682, #5521, .T. ) ;
#2625=PLANE ( 'NONE',  #18408 ) ;
#2628=AXIS2_PLACEMENT_3D ( 'NONE', #7555, #14043, #5952 ) ;
#2629=EDGE_CURVE ( 'NONE', #17396, #13246, #16906, .T. ) ;
#2631=VERTEX_POINT ( 'NONE', #15110 ) ;
#2632=CARTESIAN_POINT ( 'NONE',  ( 5.455102971993217587, 51.45882509034149166, 79.53290755650829169 ) ) ;
#2633=LINE ( 'NONE', #5823, #4713 ) ;
#2634=CARTESIAN_POINT ( 'NONE',  ( 7.674368124774328948, 40.17547738449357553, 76.47636794762235013 ) ) ;
#2637=CARTESIAN_POINT ( 'NONE',  ( -4.753731435370070812, 37.11885062014071934, 77.91594000873737969 ) ) ;
#2638=CARTESIAN_POINT ( 'NONE',  ( 5.894623494294806143, 51.13416898548390321, 78.12411320240556734 ) ) ;
#2640=CARTESIAN_POINT ( 'NONE',  ( 1.658154530501163793, 36.04125148601230677, 75.45433879953087342 ) ) ;
#2641=LINE ( 'NONE', #7644, #9458 ) ;
#2643=CARTESIAN_POINT ( 'NONE',  ( 0.7004076996470288696, 52.96039943697842745, 78.90962015830227472 ) ) ;
#2644=DIRECTION ( 'NONE',  ( -0.2741027427660463478, -0.8215033088236058934, -0.4999999999999977240 ) ) ;
#2645=EDGE_CURVE ( 'NONE', #12080, #3841, #20018, .T. ) ;
#2647=VECTOR ( 'NONE', #17448, 1000.000000000000114 ) ;
#2648=CARTESIAN_POINT ( 'NONE',  ( -7.465935398647475907, 40.46964184340244230, 79.25534888921224308 ) ) ;
#2649=DIRECTION ( 'NONE',  ( 0.5813877811925719508, -0.8136266022445296509, 1.938039666723524832E-13 ) ) ;
#2652=LINE ( 'NONE', #9152, #12310 ) ;
#2654=VECTOR ( 'NONE', #10381, 1000.000000000000000 ) ;
#2655=CARTESIAN_POINT ( 'NONE',  ( 1.652727357819364418, 35.35299279957455099, 76.86610350541323555 ) ) ;
#2656=CARTESIAN_POINT ( 'NONE',  ( -7.047195691697199393, 47.09221404848518944, 79.02985774836469091 ) ) ;
#2658=FACE_OUTER_BOUND ( 'NONE', #1926, .T. ) ;
#2659=CARTESIAN_POINT ( 'NONE',  ( -3.533668833548938348, 36.21763952329489200, 78.50831005042292077 ) ) ;
#2663=LINE ( 'NONE', #20206, #14273 ) ;
#2667=ORIENTED_EDGE ( 'NONE', *, *, #3090, .F. ) ;
#2669=CARTESIAN_POINT ( 'NONE',  ( 0.8336586891988152503, 52.35626390271237085, 78.71056005854129012 ) ) ;
#2670=ORIENTED_EDGE ( 'NONE', *, *, #10386, .T. ) ;
#2671=CARTESIAN_POINT ( 'NONE',  ( 0.7746764342352833177, 52.35878496689903017, 75.36252188568599308 ) ) ;
#2672=VERTEX_POINT ( 'NONE', #8936 ) ;
#2673=CARTESIAN_POINT ( 'NONE',  ( -4.437383981905837160, 50.68713408076344251, 78.75763390087725213 ) ) ;
#2677=AXIS2_PLACEMENT_3D ( 'NONE', #15887, #1308, #16095 ) ;
#2678=CARTESIAN_POINT ( 'NONE',  ( -6.647464070959230753, 48.14170149837703860, 72.45433879953087342 ) ) ;
#2679=CARTESIAN_POINT ( 'NONE',  ( -5.004817973257477348, 39.29348442311233214, 77.05433879953086773 ) ) ;
#2682=CARTESIAN_POINT ( 'NONE',  ( -4.811608766808351589, 37.16160227343304712, 79.54845644658969661 ) ) ;
#2683=ORIENTED_EDGE ( 'NONE', *, *, #811, .F. ) ;
#2685=ORIENTED_EDGE ( 'NONE', *, *, #18602, .F. ) ;
#2687=DIRECTION ( 'NONE',  ( 1.540237394707283727E-16, 1.793354297423763257E-16, -1.000000000000000000 ) ) ;
#2691=DIRECTION ( 'NONE',  ( 0.9485903129789527988, -0.3165065846431829311, 8.934458285744989980E-17 ) ) ;
#2692=CARTESIAN_POINT ( 'NONE',  ( -4.396013154037729187, 37.60064804164377250, 77.91526691179548436 ) ) ;
#2693=CARTESIAN_POINT ( 'NONE',  ( 5.601728273810613778, 37.72457639632248316, 78.37032190549847144 ) ) ;
#2696=CARTESIAN_POINT ( 'NONE',  ( 9.353599821682333726, 42.82705654907719151, 77.11956464767864361 ) ) ;
#2698=VECTOR ( 'NONE', #3068, 1000.000000000000114 ) ;
#2702=CARTESIAN_POINT ( 'NONE',  ( -7.840586881915256434, 41.40194303324297920, 78.11653805097020609 ) ) ;
#2703=ORIENTED_EDGE ( 'NONE', *, *, #3654, .T. ) ;
#2704=VECTOR ( 'NONE', #3356, 1000.000000000000000 ) ;
#2706=CARTESIAN_POINT ( 'NONE',  ( -4.826313235042861471, 50.23618790873877060, 79.40394833312912226 ) ) ;
#2707=DIRECTION ( 'NONE',  ( -1.540237394707284220E-16, -1.793354297423764243E-16, 1.000000000000000000 ) ) ;
#2709=CARTESIAN_POINT ( 'NONE',  ( 6.882736312352589536, 37.89144858414100270, 77.26022115247205591 ) ) ;
#2710=CARTESIAN_POINT ( 'NONE',  ( 5.561379608955574483, 51.38032281970146897, 76.39036821129558064 ) ) ;
#2711=ADVANCED_FACE ( 'NONE', ( #9042 ), #5841, .T. ) ;
#2717=CARTESIAN_POINT ( 'NONE',  ( -3.055882809522131094, 36.78399362325244937, 75.45433879953087342 ) ) ;
#2719=VECTOR ( 'NONE', #15596, 1000.000000000000000 ) ;
#2720=CARTESIAN_POINT ( 'NONE',  ( 5.316416202095706645, 37.50973464508803801, 75.36022115247205022 ) ) ;
#2722=CARTESIAN_POINT ( 'NONE',  ( 8.787829143201870252, 41.13140593384865440, 76.40801527011910821 ) ) ;
#2724=FACE_OUTER_BOUND ( 'NONE', #8996, .T. ) ;
#2725=ORIENTED_EDGE ( 'NONE', *, *, #14942, .F. ) ;
#2726=CARTESIAN_POINT ( 'NONE',  ( 2.058288634170412745, 52.20196483424038547, 76.07541412571639228 ) ) ;
#2730=DIRECTION ( 'NONE',  ( 1.540237394707283727E-16, 1.793354297423763257E-16, -1.000000000000000000 ) ) ;
#2731=CARTESIAN_POINT ( 'NONE',  ( 5.416600712022146880, 37.59071719501547193, 77.71701144737939160 ) ) ;
#2733=B_SPLINE_SURFACE_WITH_KNOTS ( 'NONE', 3, 1, ( 
 ( #4722, #12730 ),
 ( #4836, #16237 ),
 ( #260, #13255 ),
 ( #1660, #6749 ),
 ( #10284, #8995 ),
 ( #3766, #15483 ),
 ( #15586, #10393 ),
 ( #894, #795 ),
 ( #11980, #7382 ),
 ( #10718, #2281 ),
 ( #13872, #16963 ),
 ( #8895, #12297 ),
 ( #17176, #1001 ),
 ( #15382, #20035 ),
 ( #16761, #7279 ),
 ( #19928, #15162 ),
 ( #573, #4695 ),
 ( #1320, #20867 ),
 ( #7804, #2702 ),
 ( #7704, #6297 ),
 ( #11017, #5902 ),
 ( #1528, #19089 ),
 ( #11117, #13985 ),
 ( #14290, #11221 ),
 ( #1215, #17385 ),
 ( #1115, #7908 ),
 ( #18878, #12798 ) ),
 .UNSPECIFIED., .F., .F., .F.,
 ( 4, 1, 1, 1, 1, 1, 1, 1, 1, 1, 1, 1, 1, 1, 1, 1, 1, 1, 1, 1, 1, 1, 1, 1, 4 ),
 ( 2, 2 ),
 ( 0.000000000000000000, 0.07935366776402412448, 0.1548335512306962258, 0.2264778788879675819, 0.2937702508597817563, 0.3573743676598307717, 0.4169588998156444348, 0.4725242949814433824, 0.5240711055231918047, 0.5716000239151953766, 0.6154428185654550187, 0.6549388753896664417, 0.6907509128113638042, 0.7224122923534581631, 0.7502020185738895730, 0.7741815239783794711, 0.7939676610466723794, 0.8283228184009381323, 0.8602605685341977448, 0.8894181639262210837, 0.9162808273808505932, 0.9404180486131810124, 0.9623203467589012128, 0.9822441917195737782, 0.9999999999999998890 ),
 ( 0.000000000000000000, 1.000000000000000000 ),
 .UNSPECIFIED. ) ;
#2734=CARTESIAN_POINT ( 'NONE',  ( -3.715078426196892991, 51.18328438983323281, 75.42494517787103803 ) ) ;
#2735=ORIENTED_EDGE ( 'NONE', *, *, #14052, .T. ) ;
#2736=VECTOR ( 'NONE', #13308, 1000.000000000000000 ) ;
#2737=CARTESIAN_POINT ( 'NONE',  ( -3.815104224344752382, 36.42552450956669219, 75.61442449207443417 ) ) ;
#2738=CARTESIAN_POINT ( 'NONE',  ( -5.395897241545734246, 49.83815834233242015, 76.36688022495927441 ) ) ;
#2739=VERTEX_POINT ( 'NONE', #6043 ) ;
#2740=CARTESIAN_POINT ( 'NONE',  ( 4.611645699796032893, 52.08185300078213942, 78.81874598975664981 ) ) ;
#2744=CARTESIAN_POINT ( 'NONE',  ( 5.481509524342429884, 37.63185606553125240, 77.59973382626697003 ) ) ;
#2745=CARTESIAN_POINT ( 'NONE',  ( -6.721170549555291807, 40.34851694082927764, 78.82487260570216847 ) ) ;
#2746=CARTESIAN_POINT ( 'NONE',  ( -0.9376663952598962570, 52.84025806911358103, 76.73514787659645719 ) ) ;
#2749=DIRECTION ( 'NONE',  ( -1.540237394707283727E-16, -1.793354297423763257E-16, 1.000000000000000000 ) ) ;
#2750=EDGE_CURVE ( 'NONE', #5849, #14686, #9689, .T. ) ;
#2753=ADVANCED_FACE ( 'NONE', ( #14132 ), #10758, .T. ) ;
#2755=CARTESIAN_POINT ( 'NONE',  ( -4.964211958109541634, 43.56811128349716000, 78.65179900065426466 ) ) ;
#2756=ADVANCED_FACE ( 'NONE', ( #7544 ), #17223, .T. ) ;
#2757=CARTESIAN_POINT ( 'NONE',  ( 8.374483959044606962, 41.81265978262165817, 78.64183653779139149 ) ) ;
#2761=LINE ( 'NONE', #13817, #4382 ) ;
#2763=CARTESIAN_POINT ( 'NONE',  ( 8.388854304654358884, 39.93565303222995055, 78.40165754912887053 ) ) ;
#2766=CARTESIAN_POINT ( 'NONE',  ( -7.889836807277443853, 41.56303039276833289, 79.54845644658969661 ) ) ;
#2769=CARTESIAN_POINT ( 'NONE',  ( 8.632693788391325285, 43.03087348439100879, 78.75800315165874110 ) ) ;
#2770=CARTESIAN_POINT ( 'NONE',  ( -4.032264951078912141, 50.98107207184723677, 76.47051527011910821 ) ) ;
#2771=CARTESIAN_POINT ( 'NONE',  ( -5.004817973257478236, 39.29348442311233214, 78.53742703482498655 ) ) ;
#2773=DIRECTION ( 'NONE',  ( 0.5813877811927011807, -0.8136266022444372803, -5.636455622144619183E-17 ) ) ;
#2774=CIRCLE ( 'NONE', #17047, 4.200000000000003730 ) ;
#2776=DIRECTION ( 'NONE',  ( -0.5941461771851693774, -0.8043570849667760481, -2.357623395011396791E-16 ) ) ;
#2779=ORIENTED_EDGE ( 'NONE', *, *, #1332, .T. ) ;
#2780=EDGE_CURVE ( 'NONE', #13982, #19239, #2761, .T. ) ;
#2783=CARTESIAN_POINT ( 'NONE',  ( 5.766510840975054286, 51.22880064179873472, 78.93606911575150775 ) ) ;
#2784=CARTESIAN_POINT ( 'NONE',  ( 5.579255781724441476, 50.61248246897039138, 76.90580938776616904 ) ) ;
#2787=CARTESIAN_POINT ( 'NONE',  ( 5.748274343403736886, 51.24227120794373747, 77.94845644658968808 ) ) ;
#2792=CARTESIAN_POINT ( 'NONE',  ( -0.9367543186758918727, 52.97864466936303529, 76.89011419028814487 ) ) ;
#2795=FACE_OUTER_BOUND ( 'NONE', #6961, .T. ) ;
#2796=CARTESIAN_POINT ( 'NONE',  ( -3.597291554029906191, 36.26463506403467107, 78.92082147625116306 ) ) ;
#2798=DIRECTION ( 'NONE',  ( 0.2741027427660463478, 0.8215033088236062264, -0.4999999999999973910 ) ) ;
#2800=CARTESIAN_POINT ( 'NONE',  ( -7.244367111870785081, 46.79357224500207479, 79.23461367391459476 ) ) ;
#2803=DIRECTION ( 'NONE',  ( -0.8136266022444372803, -0.5813877811927012917, -2.295812393977109100E-16 ) ) ;
#2804=LINE ( 'NONE', #1623, #7883 ) ;
#2805=AXIS2_PLACEMENT_3D ( 'NONE', #14505, #6619, #20973 ) ;
#2807=CARTESIAN_POINT ( 'NONE',  ( 9.348820989215322896, 42.81273408501008504, 77.37738884012668450 ) ) ;
#2808=ORIENTED_EDGE ( 'NONE', *, *, #3654, .F. ) ;
#2809=CARTESIAN_POINT ( 'NONE',  ( -2.918372561058340864, 51.59970387748519727, 76.50206692849373269 ) ) ;
#2812=ORIENTED_EDGE ( 'NONE', *, *, #3395, .T. ) ;
#2814=CARTESIAN_POINT ( 'NONE',  ( -5.435385416347992660, 50.72091422709593189, 79.30596685730465367 ) ) ;
#2816=CARTESIAN_POINT ( 'NONE',  ( -4.517608495229000098, 36.94443611587072240, 78.61392107264721574 ) ) ;
#2817=CARTESIAN_POINT ( 'NONE',  ( 5.581171587375775900, 51.36570328251199413, 76.09992453055346573 ) ) ;
#2819=ORIENTED_EDGE ( 'NONE', *, *, #2214, .T. ) ;
#2827=CARTESIAN_POINT ( 'NONE',  ( 5.085584811987322595, 37.35418535211618263, 76.29939265556315320 ) ) ;
#2829=VECTOR ( 'NONE', #14914, 1000.000000000000000 ) ;
#2830=CARTESIAN_POINT ( 'NONE',  ( -3.847049756032941303, 36.44912138698024506, 77.64672866243046201 ) ) ;
#2832=FACE_OUTER_BOUND ( 'NONE', #20366, .T. ) ;
#2835=CARTESIAN_POINT ( 'NONE',  ( -0.7999275206693371443, 52.25527902654923906, 75.91237294090058185 ) ) ;
#2837=B_SPLINE_CURVE_WITH_KNOTS ( 'NONE', 3,
 ( #6820, #13326, #19798, #3315, #15025, #3422, #442, #6924, #11634, #9821, #18110, #16308, #8217, #127, #13112, #3530 ),
 .UNSPECIFIED., .F., .F.,
 ( 4, 2, 2, 2, 2, 2, 2, 4 ),
 ( 0.000000000000000000, 0.0002686153547044001721, 0.0005372307094088003441, 0.001074461418817601989, 0.001343076773521993976, 0.001611692128226385962, 0.001880307482930778165, 0.002148922837635170151 ),
 .UNSPECIFIED. ) ;
#2838=CARTESIAN_POINT ( 'NONE',  ( -3.970323366337335180, 51.02496109656326695, 75.37033317797633458 ) ) ;
#2839=ORIENTED_EDGE ( 'NONE', *, *, #6356, .T. ) ;
#2840=EDGE_LOOP ( 'NONE', ( #15503, #3531, #2152, #19912 ) ) ;
#2841=EDGE_CURVE ( 'NONE', #279, #17248, #12232, .T. ) ;
#2842=CARTESIAN_POINT ( 'NONE',  ( -4.320790804570143528, 36.79905481608120965, 75.39293290059653430 ) ) ;
#2843=CARTESIAN_POINT ( 'NONE',  ( -6.828828674771580509, 40.52810780656849943, 77.72183404180550781 ) ) ;
#2844=ORIENTED_EDGE ( 'NONE', *, *, #4355, .T. ) ;
#2845=CARTESIAN_POINT ( 'NONE',  ( 4.833451453752482863, 51.91801402521529241, 79.26957207196610966 ) ) ;
#2847=CARTESIAN_POINT ( 'NONE',  ( 7.741105926769938250, 40.37549481084163716, 75.80967849220077426 ) ) ;
#2850=CARTESIAN_POINT ( 'NONE',  ( -4.537329489133271387, 36.95900321965770985, 78.11020518223413944 ) ) ;
#2851=CARTESIAN_POINT ( 'NONE',  ( 5.847431522242757751, 51.16902779423016767, 77.98758453411963387 ) ) ;
#2852=PLANE ( 'NONE',  #12243 ) ;
#2854=EDGE_CURVE ( 'NONE', #10889, #15617, #12898, .T. ) ;
#2855=CARTESIAN_POINT ( 'NONE',  ( 6.198133899858643936, 38.24375437806406808, 78.20706894449375568 ) ) ;
#2856=ADVANCED_FACE ( 'NONE', ( #4750 ), #1799, .F. ) ;
#2858=CARTESIAN_POINT ( 'NONE',  ( 0.5221537403065015237, 44.16218137147968292, 75.45433879953088763 ) ) ;
#2859=CARTESIAN_POINT ( 'NONE',  ( -0.9273978588864755235, 52.97979615060394565, 78.43306491891449639 ) ) ;
#2860=ORIENTED_EDGE ( 'NONE', *, *, #17431, .F. ) ;
#2862=CARTESIAN_POINT ( 'NONE',  ( 0.5868117437017631444, 52.36192644938283536, 77.38375056423674891 ) ) ;
#2863=CARTESIAN_POINT ( 'NONE',  ( 8.807144941123576487, 41.18929660559136607, 79.54516904849367620 ) ) ;
#2865=EDGE_CURVE ( 'NONE', #13992, #10817, #3072, .T. ) ;
#2868=CARTESIAN_POINT ( 'NONE',  ( -8.299466572873484438, 42.85840835471202581, 78.79856413697085316 ) ) ;
#2871=VERTEX_POINT ( 'NONE', #4550 ) ;
#2872=CARTESIAN_POINT ( 'NONE',  ( 8.643936145691096584, 43.06456754242027074, 78.41904468188381827 ) ) ;
#2873=CARTESIAN_POINT ( 'NONE',  ( -3.736319852780221495, 36.36732966792005328, 79.18890841331918296 ) ) ;
#2874=EDGE_CURVE ( 'NONE', #20695, #6977, #11889, .T. ) ;
#2876=CARTESIAN_POINT ( 'NONE',  ( -3.539401246598059991, 43.09270903039240608, 82.45433879953087342 ) ) ;
#2879=CARTESIAN_POINT ( 'NONE',  ( 9.054037327392332912, 41.92924874979977545, 78.13567616980381558 ) ) ;
#2880=CARTESIAN_POINT ( 'NONE',  ( 2.538045550429134600, 49.87014351810298507, 72.45432679953087529 ) ) ;
#2881=CARTESIAN_POINT ( 'NONE',  ( 6.961907239250668233, 50.34580947589670075, 76.63889762306028786 ) ) ;
#2884=CARTESIAN_POINT ( 'NONE',  ( -5.171864905379679023, 50.90921633613218944, 79.44348587025405095 ) ) ;
#2885=CARTESIAN_POINT ( 'NONE',  ( 5.666494898543479763, 37.02236699927324537, 78.30432351818811298 ) ) ;
#2886=VERTEX_POINT ( 'NONE', #19442 ) ;
#2890=ORIENTED_EDGE ( 'NONE', *, *, #7439, .T. ) ;
#2891=CARTESIAN_POINT ( 'NONE',  ( 5.895605937740185709, 51.13344329408603528, 78.75475733230618403 ) ) ;
#2892=CARTESIAN_POINT ( 'NONE',  ( -0.9434902559443921755, 52.21950436431747278, 77.15777051809955367 ) ) ;
#2893=CARTESIAN_POINT ( 'NONE',  ( 5.196643236000038080, 51.64973888592641771, 79.48101422306089603 ) ) ;
#2894=LINE ( 'NONE', #15879, #18233 ) ;
#2895=CARTESIAN_POINT ( 'NONE',  ( 0.5892521710836133852, 52.35418392935860510, 75.97241503363285631 ) ) ;
#2897=CARTESIAN_POINT ( 'NONE',  ( -4.069601230858995500, 36.61351119651401120, 79.44037905412795908 ) ) ;
#2900=LINE ( 'NONE', #11200, #8496 ) ;
#2901=B_SPLINE_CURVE_WITH_KNOTS ( 'NONE', 3,
 ( #19037, #14134, #12754, #16060, #20616, #7756, #6045, #19233, #9365, #6153, #1586, #12658, #14235, #4752, #19141 ),
 .UNSPECIFIED., .F., .F.,
 ( 4, 1, 1, 1, 1, 1, 1, 1, 1, 1, 1, 1, 4 ),
 ( 0.000000000000000000, 0.1100843045400305420, 0.2037028897711227471, 0.2865965782701816456, 0.3664837514983516065, 0.4113922274074651164, 0.4651658430714658010, 0.5281943374952151604, 0.6014928947756199573, 0.6850328536222562992, 0.7789954854465236389, 0.8848457782734755472, 1.000000000000000000 ),
 .UNSPECIFIED. ) ;
#2907=CARTESIAN_POINT ( 'NONE',  ( -7.361413977510151696, 41.92405526712225594, 78.79490040793942285 ) ) ;
#2908=B_SPLINE_SURFACE_WITH_KNOTS ( 'NONE', 3, 1, ( 
 ( #1953, #4919 ),
 ( #1858, #146 ),
 ( #19816, #6625 ),
 ( #6731, #19604 ),
 ( #10054, #13235 ),
 ( #10159, #8445 ),
 ( #5238, #13129 ),
 ( #3549, #14925 ),
 ( #11854, #8343 ),
 ( #14825, #3648 ),
 ( #19714, #16641 ),
 ( #16329, #5132 ),
 ( #8238, #2060 ),
 ( #8555, #15043 ),
 ( #11652, #11440 ),
 ( #6939, #458 ),
 ( #13444, #6524 ),
 ( #17912, #3335 ),
 ( #2169, #3748 ),
 ( #19916, #9840 ),
 ( #5340, #18130 ),
 ( #18330, #10270 ),
 ( #16746, #46 ),
 ( #13031, #19505 ),
 ( #13655, #16951 ),
 ( #7264, #7044 ),
 ( #4068, #8668 ) ),
 .UNSPECIFIED., .F., .F., .F.,
 ( 4, 1, 1, 1, 1, 1, 1, 1, 1, 1, 1, 1, 1, 1, 1, 1, 1, 1, 1, 1, 1, 1, 1, 1, 4 ),
 ( 2, 2 ),
 ( 0.000000000000000000, 0.03008419796516914949, 0.06086558711599211746, 0.09255548834448126816, 0.1250230453031442313, 0.1589818606095132758, 0.1938610318241761332, 0.2303980278329116893, 0.2682253880681681468, 0.2893299372400329750, 0.3134124272828068825, 0.3409194378824745297, 0.3718003620435414991, 0.4059162288623138770, 0.4432730987006598955, 0.4838755806815719374, 0.5280884695239720372, 0.5753551328988536495, 0.6260749037380917148, 0.6800510712237001210, 0.7372563232514290910, 0.7979168342633055078, 0.8620069649650062837, 0.9293841258006002581, 1.000000000000000000 ),
 ( 0.000000000000000000, 1.000000000000000000 ),
 .UNSPECIFIED. ) ;
#2909=ORIENTED_EDGE ( 'NONE', *, *, #16136, .F. ) ;
#2910=CARTESIAN_POINT ( 'NONE',  ( 9.353817388681445522, 42.82770861117572281, 77.06316232894263862 ) ) ;
#2912=CARTESIAN_POINT ( 'NONE',  ( -2.923053016356064404, 51.59635939549185935, 76.41354228756682687 ) ) ;
#2914=CARTESIAN_POINT ( 'NONE',  ( 5.080928206799192992, 51.73521291671138300, 75.47011219584838670 ) ) ;
#2915=ORIENTED_EDGE ( 'NONE', *, *, #12953, .T. ) ;
#2918=CARTESIAN_POINT ( 'NONE',  ( -4.427139072037590495, 51.44137015048543304, 78.85744209785094938 ) ) ;
#2921=CARTESIAN_POINT ( 'NONE',  ( 0.5978773219678675810, 52.35412866480164951, 78.93607282253582014 ) ) ;
#2926=CARTESIAN_POINT ( 'NONE',  ( 5.304793302263878907, 37.51082371353273714, 75.97198585835440099 ) ) ;
#2927=CARTESIAN_POINT ( 'NONE',  ( 8.831661421392389855, 41.26277405225351202, 75.98994273744924044 ) ) ;
#2928=CARTESIAN_POINT ( 'NONE',  ( -3.356204558708832053, 37.01138675915414922, 77.61986069475027250 ) ) ;
#2930=CARTESIAN_POINT ( 'NONE',  ( -7.079104428204942678, 47.23853788948614607, 78.28573025590448253 ) ) ;
#2932=ORIENTED_EDGE ( 'NONE', *, *, #12363, .T. ) ;
#2934=CARTESIAN_POINT ( 'NONE',  ( 5.848554534127551108, 37.15246014923294382, 77.40928489470421425 ) ) ;
#2936=CARTESIAN_POINT ( 'NONE',  ( -3.628814973742291894, 51.23455773969688920, 75.44858973835683003 ) ) ;
#2938=VERTEX_POINT ( 'NONE', #16058 ) ;
#2939=CARTESIAN_POINT ( 'NONE',  ( -3.115596136743314482, 36.83365901014666122, 76.03954924220039402 ) ) ;
#2940=CARTESIAN_POINT ( 'NONE',  ( -4.303842671124285424, 37.54117185462008877, 75.97486526700035370 ) ) ;
#2941=CARTESIAN_POINT ( 'NONE',  ( -4.691270138005329216, 50.49220747607777326, 75.40225920472202858 ) ) ;
#2942=EDGE_LOOP ( 'NONE', ( #13176, #3890, #11751, #3746, #429, #16731, #1444, #19901 ) ) ;
#2943=CARTESIAN_POINT ( 'NONE',  ( -4.148395103613341739, 37.44647417508210197, 76.91875223014945107 ) ) ;
#2944=CARTESIAN_POINT ( 'NONE',  ( 6.450247442662826458, 38.49669771550791353, 77.26022115247205591 ) ) ;
#2947=ORIENTED_EDGE ( 'NONE', *, *, #4287, .T. ) ;
#2948=CARTESIAN_POINT ( 'NONE',  ( -4.717426356068883386, 37.09203352051872571, 77.92182307551118470 ) ) ;
#2949=CARTESIAN_POINT ( 'NONE',  ( -7.466141682373640620, 40.21844209608204324, 79.01214282451080351 ) ) ;
#2950=CARTESIAN_POINT ( 'NONE',  ( -5.094963349914481299, 38.18624571745164076, 79.46021242174440147 ) ) ;
#2952=EDGE_CURVE ( 'NONE', #6298, #8901, #14451, .T. ) ;
#2953=CARTESIAN_POINT ( 'NONE',  ( -5.569494948991628114, 50.62508446513216143, 75.69846806870741318 ) ) ;
#2956=CARTESIAN_POINT ( 'NONE',  ( -0.9083001327017958815, 52.97964555801444675, 78.68934297065942474 ) ) ;
#2958=ORIENTED_EDGE ( 'NONE', *, *, #4670, .T. ) ;
#2959=CARTESIAN_POINT ( 'NONE',  ( 0.5221537403065015237, 44.16218137147968292, 75.45433879953087342 ) ) ;
#2965=ORIENTED_EDGE ( 'NONE', *, *, #18293, .F. ) ;
#2966=CARTESIAN_POINT ( 'NONE',  ( 8.643644394765681582, 43.06369314638848778, 78.50890480505780999 ) ) ;
#2967=LINE ( 'NONE', #11176, #8063 ) ;
#2968=CARTESIAN_POINT ( 'NONE',  ( -4.705149740856862550, 37.08296527939383935, 78.93669174070734584 ) ) ;
#2970=EDGE_CURVE ( 'NONE', #6925, #17824, #9853, .T. ) ;
#2971=DIRECTION ( 'NONE',  ( -1.540237394707284220E-16, -1.793354297423764243E-16, 1.000000000000000000 ) ) ;
#2973=CARTESIAN_POINT ( 'NONE',  ( 6.420168591842209338, 49.82113704518689445, 77.39285358288198324 ) ) ;
#2976=EDGE_CURVE ( 'NONE', #13351, #16624, #19676, .T. ) ;
#2977=EDGE_CURVE ( 'NONE', #2342, #19757, #6767, .T. ) ;
#2978=CARTESIAN_POINT ( 'NONE',  ( 8.824963465026481657, 41.24269985211446254, 78.91056401563228917 ) ) ;
#2980=CARTESIAN_POINT ( 'NONE',  ( 0.8434211303427824324, 52.35588695112656410, 78.61836880615196321 ) ) ;
#2982=CARTESIAN_POINT ( 'NONE',  ( 5.920503277122149299, 37.20387208676527280, 78.36928251986560667 ) ) ;
#2983=VERTEX_POINT ( 'NONE', #18166 ) ;
#2984=CARTESIAN_POINT ( 'NONE',  ( 3.099655065065782367, 37.00631057046153671, 72.45432679953087529 ) ) ;
#2988=FACE_OUTER_BOUND ( 'NONE', #6607, .T. ) ;
#2989=CARTESIAN_POINT ( 'NONE',  ( -4.423487203781090393, 50.70288581026932917, 76.07809204575713125 ) ) ;
#2991=CARTESIAN_POINT ( 'NONE',  ( 0.5221537403065015237, 44.16218137147968292, 75.45433879953088763 ) ) ;
#2993=CARTESIAN_POINT ( 'NONE',  ( 2.484494565094238716, 50.04344131194920919, 78.25433879953088478 ) ) ;
#2998=CARTESIAN_POINT ( 'NONE',  ( 8.648170029844120421, 43.06315486489794608, 72.45433879953087342 ) ) ;
#2999=FACE_OUTER_BOUND ( 'NONE', #15063, .T. ) ;
#3001=EDGE_CURVE ( 'NONE', #2198, #20811, #19949, .T. ) ;
#3002=CARTESIAN_POINT ( 'NONE',  ( -5.921523028668191913, 37.98145122859525458, 76.14635491738357587 ) ) ;
#3005=CARTESIAN_POINT ( 'NONE',  ( -5.486992102393413617, 39.49954625374182626, 75.45433879953087342 ) ) ;
#3007=ADVANCED_FACE ( 'NONE', ( #11690, #2306 ), #5070, .T. ) ;
#3010=B_SPLINE_CURVE_WITH_KNOTS ( 'NONE', 3,
 ( #5732, #2553, #5847, #13824, #14137, #20303, #12447, #13934, #9048, #7550, #15536, #10553 ),
 .UNSPECIFIED., .F., .F.,
 ( 4, 2, 2, 2, 2, 4 ),
 ( 0.000000000000000000, 0.0004293312658746052364, 0.0008586625317492104729, 0.001073328164686520843, 0.001287993797623830997, 0.001717325063498451520 ),
 .UNSPECIFIED. ) ;
#3011=CARTESIAN_POINT ( 'NONE',  ( -3.353456363966241138, 52.20858450364031000, 76.50206692849373269 ) ) ;
#3013=CARTESIAN_POINT ( 'NONE',  ( 5.243485048422129147, 51.61513872599351771, 75.41617184184443090 ) ) ;
#3015=CARTESIAN_POINT ( 'NONE',  ( -5.787187992231675793, 50.46952898668384790, 78.79017217825926878 ) ) ;
#3017=CARTESIAN_POINT ( 'NONE',  ( -4.526015856129117942, 36.95064629469847972, 78.75608284215286403 ) ) ;
#3018=CARTESIAN_POINT ( 'NONE',  ( 5.220526778983810345, 50.87746113280923765, 76.09992453055346573 ) ) ;
#3019=LINE ( 'NONE', #3129, #1417 ) ;
#3022=CARTESIAN_POINT ( 'NONE',  ( 0.8455664302218980355, 52.35217554515582350, 78.52566232894263010 ) ) ;
#3023=ORIENTED_EDGE ( 'NONE', *, *, #8303, .T. ) ;
#3024=DIRECTION ( 'NONE',  ( -1.540237394707284220E-16, -1.793354297423764243E-16, 1.000000000000000000 ) ) ;
#3026=VECTOR ( 'NONE', #7581, 1000.000000000000227 ) ;
#3027=CARTESIAN_POINT ( 'NONE',  ( 0.7608161506431847521, 52.95895884780778573, 78.87528306474457906 ) ) ;
#3031=PLANE ( 'NONE',  #9852 ) ;
#3032=CARTESIAN_POINT ( 'NONE',  ( 5.829595689320886009, 51.18220240553836931, 75.98827401121828018 ) ) ;
#3033=ORIENTED_EDGE ( 'NONE', *, *, #14335, .F. ) ;
#3035=CARTESIAN_POINT ( 'NONE',  ( 2.069300872037923789, 52.82512215700846525, 77.34613596266348168 ) ) ;
#3036=DIRECTION ( 'NONE',  ( -0.5941461771851693774, -0.8043570849667760481, -2.357623395011396791E-16 ) ) ;
#3038=ORIENTED_EDGE ( 'NONE', *, *, #10403, .F. ) ;
#3039=CARTESIAN_POINT ( 'NONE',  ( -8.144617840030331735, 42.60233705719735298, 76.47068638765421156 ) ) ;
#3040=CARTESIAN_POINT ( 'NONE',  ( -0.9190990356458662580, 52.23452979981542654, 76.25498568266576171 ) ) ;
#3042=CARTESIAN_POINT ( 'NONE',  ( 8.850491666625398324, 41.31920949178531544, 79.54734031390459847 ) ) ;
#3043=ORIENTED_EDGE ( 'NONE', *, *, #106, .T. ) ;
#3046=ORIENTED_EDGE ( 'NONE', *, *, #2098, .T. ) ;
#3047=CARTESIAN_POINT ( 'NONE',  ( -4.716387082485074878, 37.09126585098686490, 75.36022115247205022 ) ) ;
#3048=FACE_OUTER_BOUND ( 'NONE', #16544, .T. ) ;
#3049=CARTESIAN_POINT ( 'NONE',  ( -6.859512391284826371, 40.59060452047487644, 77.62511654548754336 ) ) ;
#3050=ORIENTED_EDGE ( 'NONE', *, *, #6872, .F. ) ;
#3051=CARTESIAN_POINT ( 'NONE',  ( -4.518657848439222136, 36.94521123081658232, 76.91875223014945107 ) ) ;
#3052=CARTESIAN_POINT ( 'NONE',  ( -6.721036008677163665, 40.31817738747478330, 78.72633731078545338 ) ) ;
#3054=CIRCLE ( 'NONE', #13243, 8.199999999999995737 ) ;
#3056=ORIENTED_EDGE ( 'NONE', *, *, #7272, .F. ) ;
#3057=CARTESIAN_POINT ( 'NONE',  ( -7.782451534811345439, 41.25123178438806093, 78.77893168383444333 ) ) ;
#3061=DIRECTION ( 'NONE',  ( 1.000000000000000000, 0.000000000000000000, 0.000000000000000000 ) ) ;
#3063=CARTESIAN_POINT ( 'NONE',  ( 6.393340659266161019, 38.43765720549087206, 77.85582082558342165 ) ) ;
#3065=CARTESIAN_POINT ( 'NONE',  ( 9.271561067608034890, 45.68041113525027441, 79.47125056423675460 ) ) ;
#3066=VECTOR ( 'NONE', #18774, 1000.000000000000000 ) ;
#3067=CARTESIAN_POINT ( 'NONE',  ( 1.042984815895136252, 52.96245648330992140, 76.77289608131282250 ) ) ;
#3068=DIRECTION ( 'NONE',  ( 0.003037711714694931939, -0.009606198427078794025, -0.9999492453416412019 ) ) ;
#3069=CARTESIAN_POINT ( 'NONE',  ( -0.6082159309068581043, 52.21483855284596132, 79.21387586705148465 ) ) ;
#3070=AXIS2_PLACEMENT_3D ( 'NONE', #13652, #20124, #12064 ) ;
#3071=ORIENTED_EDGE ( 'NONE', *, *, #19129, .F. ) ;
#3072=LINE ( 'NONE', #21021, #1705 ) ;
#3074=CARTESIAN_POINT ( 'NONE',  ( 8.436128353966983795, 40.07733635702963682, 79.00897045670630803 ) ) ;
#3076=ORIENTED_EDGE ( 'NONE', *, *, #19255, .T. ) ;
#3081=CARTESIAN_POINT ( 'NONE',  ( -4.853223633226589229, 37.19234149890713326, 78.86751516113972116 ) ) ;
#3083=LINE ( 'NONE', #14570, #18611 ) ;
#3084=VECTOR ( 'NONE', #19462, 1000.000000000000000 ) ;
#3085=CARTESIAN_POINT ( 'NONE',  ( -3.069519124378985886, 36.79039167325804272, 76.24341621876634179 ) ) ;
#3086=CARTESIAN_POINT ( 'NONE',  ( 8.567695763276095278, 42.83607027972283987, 77.86785210695053649 ) ) ;
#3087=CARTESIAN_POINT ( 'NONE',  ( 5.599231707071657738, 51.35236299959863970, 78.30875056423674607 ) ) ;
#3088=CARTESIAN_POINT ( 'NONE',  ( 5.228220230638878974, 50.87731552598469875, 76.07147373344933783 ) ) ;
#3090=EDGE_CURVE ( 'NONE', #476, #889, #1965, .T. ) ;
#3094=CARTESIAN_POINT ( 'NONE',  ( 5.450944860649778789, 36.86834283398499679, 78.16244716952144245 ) ) ;
#3095=ORIENTED_EDGE ( 'NONE', *, *, #6187, .T. ) ;
#3096=LINE ( 'NONE', #14475, #11586 ) ;
#3097=CARTESIAN_POINT ( 'NONE',  ( 8.389283321988518338, 39.93693882439677623, 76.47636794762235013 ) ) ;
#3098=ORIENTED_EDGE ( 'NONE', *, *, #15241, .F. ) ;
#3099=CARTESIAN_POINT ( 'NONE',  ( 5.556673069113441166, 37.86366792307473617, 75.38041148603002739 ) ) ;
#3100=CARTESIAN_POINT ( 'NONE',  ( -4.429894154275758389, 50.69802490680864082, 76.10363940379099290 ) ) ;
#3102=CARTESIAN_POINT ( 'NONE',  ( 0.6249198533375087683, 52.35390267657594165, 75.97323462179006981 ) ) ;
#3106=CARTESIAN_POINT ( 'NONE',  ( 5.848951923618479931, 37.15274410921379911, 77.37492703482499223 ) ) ;
#3110=CARTESIAN_POINT ( 'NONE',  ( -0.1944850259765472933, 35.99355670886600933, 76.86610350541323555 ) ) ;
#3111=CARTESIAN_POINT ( 'NONE',  ( 5.846647460608473956, 37.15109742431862827, 76.40678776405631822 ) ) ;
#3113=CARTESIAN_POINT ( 'NONE',  ( -7.908203753683241466, 41.62291835105061466, 78.91811502121268518 ) ) ;
#3116=CARTESIAN_POINT ( 'NONE',  ( 4.588242150565980282, 52.09914025984591746, 78.23954818826248925 ) ) ;
#3117=VECTOR ( 'NONE', #6905, 1000.000000000000227 ) ;
#3118=ORIENTED_EDGE ( 'NONE', *, *, #418, .F. ) ;
#3119=LINE ( 'NONE', #9622, #19045 ) ;
#3121=CARTESIAN_POINT ( 'NONE',  ( 4.552447320970152589, 52.12558045856467004, 76.26690125110441443 ) ) ;
#3122=ORIENTED_EDGE ( 'NONE', *, *, #17021, .T. ) ;
#3124=CARTESIAN_POINT ( 'NONE',  ( -5.802311964739910621, 50.45872194965342317, 78.71528818263502103 ) ) ;
#3126=CARTESIAN_POINT ( 'NONE',  ( -4.260738562919781813, 37.50933258622881539, 78.92211507803222048 ) ) ;
#3127=CARTESIAN_POINT ( 'NONE',  ( 5.561486116954087677, 51.38024414653337146, 76.36928804473561172 ) ) ;
#3129=CARTESIAN_POINT ( 'NONE',  ( -0.02883801100815608018, 35.36625256049322275, 79.45433879953087342 ) ) ;
#3132=PLANE ( 'NONE',  #1820 ) ;
#3133=VECTOR ( 'NONE', #4125, 1000.000000000000000 ) ;
#3135=CARTESIAN_POINT ( 'NONE',  ( 4.715683878568929011, 52.00500418903608590, 77.90619853385557292 ) ) ;
#3139=VECTOR ( 'NONE', #7662, 1000.000000000000227 ) ;
#3140=ADVANCED_FACE ( 'NONE', ( #919, #2418 ), #4312, .F. ) ;
#3141=CARTESIAN_POINT ( 'NONE',  ( -6.210882734309923769, 46.73118581782181025, 77.58227997600145898 ) ) ;
#3144=EDGE_CURVE ( 'NONE', #18072, #16704, #20225, .T. ) ;
#3145=FACE_OUTER_BOUND ( 'NONE', #64, .T. ) ;
#3147=ORIENTED_EDGE ( 'NONE', *, *, #19459, .F. ) ;
#3148=CARTESIAN_POINT ( 'NONE',  ( 2.046000312423422507, 52.20206269949791533, 78.89969410769322167 ) ) ;
#3150=VECTOR ( 'NONE', #1218, 1000.000000000000000 ) ;
#3152=DIRECTION ( 'NONE',  ( 1.540237394707284220E-16, 1.793354297423764243E-16, -1.000000000000000000 ) ) ;
#3154=AXIS2_PLACEMENT_3D ( 'NONE', #8615, #294, #16380 ) ;
#3156=ORIENTED_EDGE ( 'NONE', *, *, #11419, .T. ) ;
#3157=LINE ( 'NONE', #2655, #16332 ) ;
#3159=CARTESIAN_POINT ( 'NONE',  ( -7.866550369700228806, 41.50330127738815378, 78.93669174070734584 ) ) ;
#3160=CARTESIAN_POINT ( 'NONE',  ( 8.378483041054197500, 41.81311971792333537, 78.53442867677860306 ) ) ;
#3162=VERTEX_POINT ( 'NONE', #20381 ) ;
#3163=CARTESIAN_POINT ( 'NONE',  ( 4.140412088821458170, 51.51591928153320765, 78.46169174070733732 ) ) ;
#3164=CARTESIAN_POINT ( 'NONE',  ( 8.833159395675938441, 41.26726357621102181, 77.50846324053436831 ) ) ;
#3166=AXIS2_PLACEMENT_3D ( 'NONE', #15274, #20361, #13675 ) ;
#3167=ORIENTED_EDGE ( 'NONE', *, *, #6198, .F. ) ;
#3168=FACE_OUTER_BOUND ( 'NONE', #1552, .T. ) ;
#3169=CARTESIAN_POINT ( 'NONE',  ( -5.395909702104524364, 38.48590459560077903, 79.18739798713926348 ) ) ;
#3172=VECTOR ( 'NONE', #19858, 1000.000000000000000 ) ;
#3174=CARTESIAN_POINT ( 'NONE',  ( -4.484214873741871443, 37.66782333187624943, 76.00985440664865678 ) ) ;
#3175=CARTESIAN_POINT ( 'NONE',  ( 0.5234091789269255113, 52.34369878586026203, 76.89772265631788173 ) ) ;
#3177=LINE ( 'NONE', #11378, #12559 ) ;
#3178=CARTESIAN_POINT ( 'NONE',  ( -0.4185253612809345936, 52.97578350394660163, 79.34012451928875009 ) ) ;
#3181=DIRECTION ( 'NONE',  ( -1.540237394707283727E-16, -1.793354297423763257E-16, 1.000000000000000000 ) ) ;
#3182=CARTESIAN_POINT ( 'NONE',  ( 0.8448466153661705613, 52.35582950748954545, 76.37320713360470847 ) ) ;
#3183=CARTESIAN_POINT ( 'NONE',  ( 2.026641451580078357, 52.83264100297040500, 78.95121740658819931 ) ) ;
#3185=CARTESIAN_POINT ( 'NONE',  ( 7.688925413721245050, 40.17753638632645163, 76.35905954771017434 ) ) ;
#3188=CARTESIAN_POINT ( 'NONE',  ( 5.263499222790406051, 50.85473774294745652, 79.54645054556618788 ) ) ;
#3191=CARTESIAN_POINT ( 'NONE',  ( -4.895593109503407092, 37.22363812428621088, 76.38448585835440952 ) ) ;
#3192=CARTESIAN_POINT ( 'NONE',  ( 6.127581622321778276, 50.03725925344959080, 77.67636243622263237 ) ) ;
#3193=DIRECTION ( 'NONE',  ( -0.5813877811927011807, 0.8136266022444372803, 5.636455622144619183E-17 ) ) ;
#3194=VECTOR ( 'NONE', #4830, 1000.000000000000114 ) ;
#3195=ORIENTED_EDGE ( 'NONE', *, *, #8884, .T. ) ;
#3196=CARTESIAN_POINT ( 'NONE',  ( -4.364285939139664450, 37.76718941598996082, 79.54845644658969661 ) ) ;
#3199=CARTESIAN_POINT ( 'NONE',  ( 8.951691408152598228, 41.62251153713423690, 78.44085888008430629 ) ) ;
#3202=CARTESIAN_POINT ( 'NONE',  ( 9.131267103411046193, 42.16071128789349132, 78.09998440036279987 ) ) ;
#3204=CARTESIAN_POINT ( 'NONE',  ( 6.146933156575338231, 38.28544617077390200, 75.62429547252081363 ) ) ;
#3206=CARTESIAN_POINT ( 'NONE',  ( 6.032012598193956521, 38.20332814726474879, 78.28436300994860630 ) ) ;
#3210=CARTESIAN_POINT ( 'NONE',  ( 8.375199775097005528, 41.81478521990748476, 76.38301527011910252 ) ) ;
#3211=VERTEX_POINT ( 'NONE', #7937 ) ;
#3213=CARTESIAN_POINT ( 'NONE',  ( -7.876156483970349953, 46.79098802322403117, 79.40730115154055113 ) ) ;
#3214=DIRECTION ( 'NONE',  ( 0.007885122365275663500, 0.9999689119394085113, 1.805443505845543142E-16 ) ) ;
#3215=CARTESIAN_POINT ( 'NONE',  ( 8.415751671997487193, 46.40539568610629573, 77.63812446857940586 ) ) ;
#3216=EDGE_CURVE ( 'NONE', #13955, #17982, #6512, .T. ) ;
#3217=EDGE_CURVE ( 'NONE', #5430, #9093, #1235, .T. ) ;
#3218=VERTEX_POINT ( 'NONE', #1656 ) ;
#3219=CARTESIAN_POINT ( 'NONE',  ( -4.525716193177017566, 36.95042494574692427, 76.22840587216694530 ) ) ;
#3221=CARTESIAN_POINT ( 'NONE',  ( -3.350440871817599753, 52.21073926392551812, 76.59793576264409865 ) ) ;
#3223=CARTESIAN_POINT ( 'NONE',  ( 0.5221537403065010796, 44.16218137147968292, 78.25433879953088478 ) ) ;
#3225=CARTESIAN_POINT ( 'NONE',  ( 9.273778039597953438, 45.67340037358405169, 78.74919174070734584 ) ) ;
#3226=CARTESIAN_POINT ( 'NONE',  ( -5.210464978622034060, 37.45622129019157853, 79.52089765539699329 ) ) ;
#3231=ORIENTED_EDGE ( 'NONE', *, *, #4933, .F. ) ;
#3233=CARTESIAN_POINT ( 'NONE',  ( 0.5920942507238189378, 52.36215724832370455, 76.86006382792197655 ) ) ;
#3237=CARTESIAN_POINT ( 'NONE',  ( 0.6794293633488347472, 52.96080299881479192, 78.91894504275920497 ) ) ;
#3241=LINE ( 'NONE', #19406, #19023 ) ;
#3244=EDGE_CURVE ( 'NONE', #12818, #2386, #9338, .T. ) ;
#3245=CARTESIAN_POINT ( 'NONE',  ( -3.495367959724249296, 36.18934821065389684, 76.68008248600652621 ) ) ;
#3246=ORIENTED_EDGE ( 'NONE', *, *, #2074, .F. ) ;
#3247=CARTESIAN_POINT ( 'NONE',  ( 1.859207995029386495, 52.95621058139879267, 79.18222496875146987 ) ) ;
#3251=CARTESIAN_POINT ( 'NONE',  ( -7.600593896485820622, 45.28511094584521146, 75.45433879953088763 ) ) ;
#3252=CARTESIAN_POINT ( 'NONE',  ( 9.177137044501376906, 42.29818641127601353, 79.38025142445083304 ) ) ;
#3253=B_SPLINE_SURFACE_WITH_KNOTS ( 'NONE', 3, 1, ( 
 ( #12706, #15701 ),
 ( #1120, #2816 ),
 ( #10920, #9320 ),
 ( #15807, #3017 ),
 ( #9523, #6302 ),
 ( #12802, #19286 ),
 ( #4699, #17698 ),
 ( #3126, #8016 ),
 ( #6405, #12912 ),
 ( #3638, #5230 ),
 ( #16525, #4809 ) ),
 .UNSPECIFIED., .F., .F., .F.,
 ( 4, 1, 1, 1, 1, 1, 1, 1, 4 ),
 ( 2, 2 ),
 ( 0.000000000000000000, 0.2014779019512820402, 0.3683355476270177564, 0.4986267722911685296, 0.6014797591950403755, 0.6911751734036410966, 0.7846115128848750730, 0.8848135988872103397, 1.000000000000000000 ),
 ( 0.000000000000000000, 1.000000000000000000 ),
 .UNSPECIFIED. ) ;
#3254=VERTEX_POINT ( 'NONE', #4719 ) ;
#3256=CARTESIAN_POINT ( 'NONE',  ( -5.507966265829200125, 38.61198000306179523, 76.68644156968609593 ) ) ;
#3257=ORIENTED_EDGE ( 'NONE', *, *, #2468, .T. ) ;
#3259=CARTESIAN_POINT ( 'NONE',  ( 8.362247588757593775, 41.75942743809601865, 78.86713471249643703 ) ) ;
#3261=ORIENTED_EDGE ( 'NONE', *, *, #14174, .T. ) ;
#3262=CARTESIAN_POINT ( 'NONE',  ( -4.570740025688050601, 36.98368223715221603, 77.15538146413656762 ) ) ;
#3263=CARTESIAN_POINT ( 'NONE',  ( -5.072433652944437377, 37.35426311015444867, 77.90218689189877921 ) ) ;
#3266=CARTESIAN_POINT ( 'NONE',  ( -4.783040473602117260, 51.18705603930939674, 76.11505395997643575 ) ) ;
#3267=PLANE ( 'NONE',  #13843 ) ;
#3269=CARTESIAN_POINT ( 'NONE',  ( -4.536720638049474452, 37.70867145396312026, 76.33888740947983820 ) ) ;
#3270=CARTESIAN_POINT ( 'NONE',  ( -4.158578283022523969, 37.42937009194850617, 78.34992703482498655 ) ) ;
#3271=ADVANCED_FACE ( 'NONE', ( #13045 ), #11248, .T. ) ;
#3273=CARTESIAN_POINT ( 'NONE',  ( 8.557023814081752278, 40.43966772045860125, 79.34450935619591405 ) ) ;
#3274=ORIENTED_EDGE ( 'NONE', *, *, #18070, .T. ) ;
#3275=CARTESIAN_POINT ( 'NONE',  ( -4.158578283022523081, 37.42937009194850617, 76.53375056423675460 ) ) ;
#3276=CARTESIAN_POINT ( 'NONE',  ( 9.353817388681445522, 42.82770861117572281, 76.74257409364852833 ) ) ;
#3278=CARTESIAN_POINT ( 'NONE',  ( 5.391786323697940198, 50.75965653268888644, 77.94845644658968808 ) ) ;
#3279=CARTESIAN_POINT ( 'NONE',  ( 6.832223124813663340, 50.44160190723654580, 77.98033120372964788 ) ) ;
#3280=EDGE_CURVE ( 'NONE', #2125, #4394, #5, .T. ) ;
#3282=AXIS2_PLACEMENT_3D ( 'NONE', #8812, #16795, #18382 ) ;
#3283=CYLINDRICAL_SURFACE ( 'NONE', #20922, 8.199999999999995737 ) ;
#3284=CARTESIAN_POINT ( 'NONE',  ( -5.955451856753747109, 38.00651308716548726, 76.73301527011911105 ) ) ;
#3287=CARTESIAN_POINT ( 'NONE',  ( 8.605722098886982252, 42.95003761989442381, 77.73063109826868811 ) ) ;
#3288=CARTESIAN_POINT ( 'NONE',  ( -3.495065479208315562, 36.18912478048144266, 76.62933879953087057 ) ) ;
#3291=ORIENTED_EDGE ( 'NONE', *, *, #16384, .F. ) ;
#3292=CARTESIAN_POINT ( 'NONE',  ( -4.763142150953350473, 38.06180843274848513, 79.52089765539699329 ) ) ;
#3293=CARTESIAN_POINT ( 'NONE',  ( 5.427780505986065762, 36.85179043424346190, 76.96022115247204454 ) ) ;
#3294=CARTESIAN_POINT ( 'NONE',  ( 5.319138446618715044, 50.81266539351954492, 78.91899942818734814 ) ) ;
#3295=CARTESIAN_POINT ( 'NONE',  ( -7.949137504989496783, 41.77948864320536160, 72.45433879953085921 ) ) ;
#3296=CARTESIAN_POINT ( 'NONE',  ( 8.415472958870040543, 40.01543082757027747, 76.00709785348774972 ) ) ;
#3297=ORIENTED_EDGE ( 'NONE', *, *, #3144, .F. ) ;
#3298=VERTEX_POINT ( 'NONE', #15824 ) ;
#3299=CARTESIAN_POINT ( 'NONE',  ( -0.2483056323647954422, 52.97321599846241469, 75.49651412033875886 ) ) ;
#3301=CARTESIAN_POINT ( 'NONE',  ( -0.1138099061810181750, 52.21093997964378985, 79.46489189366771200 ) ) ;
#3302=CARTESIAN_POINT ( 'NONE',  ( 6.363981487871726905, 38.44054096167169376, 77.90902863000688683 ) ) ;
#3303=CARTESIAN_POINT ( 'NONE',  ( -3.495392342740026415, 36.18936622140545012, 76.59109406773794149 ) ) ;
#3304=CARTESIAN_POINT ( 'NONE',  ( 6.924055141134583202, 50.37376929599953712, 78.48669174070734300 ) ) ;
#3306=CARTESIAN_POINT ( 'NONE',  ( 8.368699874006322759, 41.79530460399266900, 76.15680935856015310 ) ) ;
#3307=ORIENTED_EDGE ( 'NONE', *, *, #7433, .T. ) ;
#3310=CARTESIAN_POINT ( 'NONE',  ( -6.613032277150674432, 45.52591812603678534, 79.45433879953087342 ) ) ;
#3312=EDGE_CURVE ( 'NONE', #10226, #9748, #3561, .T. ) ;
#3313=CARTESIAN_POINT ( 'NONE',  ( 8.375221590814755146, 41.80223450334851520, 76.19888858912942453 ) ) ;
#3315=CARTESIAN_POINT ( 'NONE',  ( 8.410029692550303082, 41.91954370998553969, 79.53253037310241780 ) ) ;
#3316=ORIENTED_EDGE ( 'NONE', *, *, #19236, .T. ) ;
#3317=CARTESIAN_POINT ( 'NONE',  ( 5.264787936635038967, 50.85164499159836282, 77.24089811989679788 ) ) ;
#3320=CARTESIAN_POINT ( 'NONE',  ( -7.702335971347676669, 47.29235430678204466, 78.19878669242514491 ) ) ;
#3324=CARTESIAN_POINT ( 'NONE',  ( 1.575197090673905009, 52.29457635664441284, 76.85862500479365167 ) ) ;
#3325=PLANE ( 'NONE',  #4500 ) ;
#3326=VECTOR ( 'NONE', #20857, 1000.000000000000000 ) ;
#3327=CARTESIAN_POINT ( 'NONE',  ( 5.939862031672385356, 51.10075310024252815, 76.36217657474753651 ) ) ;
#3328=CARTESIAN_POINT ( 'NONE',  ( -4.040577624441578308, 50.97067737579940427, 78.70491066849456274 ) ) ;
#3329=CARTESIAN_POINT ( 'NONE',  ( 5.075432096899075596, 37.34693059362874834, 77.49967648550449439 ) ) ;
#3333=ORIENTED_EDGE ( 'NONE', *, *, #17772, .F. ) ;
#3334=PLANE ( 'NONE',  #6336 ) ;
#3335=CARTESIAN_POINT ( 'NONE',  ( -7.620684125509877838, 40.70898352502287310, 77.18350490445806145 ) ) ;
#3336=DIRECTION ( 'NONE',  ( -0.9485903129789527988, 0.3165065846431829311, -8.934458285744989980E-17 ) ) ;
#3339=DIRECTION ( 'NONE',  ( 0.5954989751681698529, -0.8033560671169786005, -5.234922652618076394E-17 ) ) ;
#3342=CARTESIAN_POINT ( 'NONE',  ( 5.426594447001382271, 50.72524724735664847, 75.97375991483075097 ) ) ;
#3345=CARTESIAN_POINT ( 'NONE',  ( 1.509564537322647615, 52.20629269272797757, 79.40139704896512285 ) ) ;
#3346=LINE ( 'NONE', #14835, #3428 ) ;
#3352=DIRECTION ( 'NONE',  ( -0.3165065846431826535, -0.9485903129789529098, -2.188653791613874008E-16 ) ) ;
#3353=CARTESIAN_POINT ( 'NONE',  ( -5.841826873769424111, 37.92258288932846710, 75.85972562479176418 ) ) ;
#3355=CARTESIAN_POINT ( 'NONE',  ( 5.739147447831700610, 51.24901287804902239, 78.93590013629759028 ) ) ;
#3356=DIRECTION ( 'NONE',  ( -1.540237394707284467E-16, -1.793354297423764243E-16, 1.000000000000000000 ) ) ;
#3358=ORIENTED_EDGE ( 'NONE', *, *, #7772, .T. ) ;
#3359=CARTESIAN_POINT ( 'NONE',  ( -4.603341302083757469, 37.00776348676620131, 77.20593245741272881 ) ) ;
#3362=ORIENTED_EDGE ( 'NONE', *, *, #741, .T. ) ;
#3363=CARTESIAN_POINT ( 'NONE',  ( -4.739054262994943478, 51.21848697497132719, 76.01646854312687651 ) ) ;
#3364=CARTESIAN_POINT ( 'NONE',  ( 5.543189085303068531, 50.64520219118831079, 78.74294592654759128 ) ) ;
#3367=CARTESIAN_POINT ( 'NONE',  ( 8.850663652843866913, 41.31972494539268581, 77.52203278780699236 ) ) ;
#3368=CARTESIAN_POINT ( 'NONE',  ( 4.381145549518540072, 37.02367899638166193, 75.57109918664292536 ) ) ;
#3370=CARTESIAN_POINT ( 'NONE',  ( 7.675887208068574274, 40.16326346448608575, 77.75090705316073070 ) ) ;
#3371=EDGE_LOOP ( 'NONE', ( #12774, #602, #12488, #6282, #1721, #15892, #11760, #9578, #3815, #9887, #1112, #8148, #838, #19267, #2102, #13880, #6079, #2205, #10620 ) ) ;
#3374=CARTESIAN_POINT ( 'NONE',  ( -4.463792963332828378, 40.72925446781975722, 75.45433879953087342 ) ) ;
#3375=CARTESIAN_POINT ( 'NONE',  ( 6.395410155697720533, 49.85024304639465953, 77.98033120372964788 ) ) ;
#3376=VERTEX_POINT ( 'NONE', #1770 ) ;
#3377=AXIS2_PLACEMENT_3D ( 'NONE', #10063, #5141, #11660 ) ;
#3378=VECTOR ( 'NONE', #19540, 1000.000000000000000 ) ;
#3379=CARTESIAN_POINT ( 'NONE',  ( 5.766510840975054286, 51.22880064179873472, 78.93606911575150775 ) ) ;
#3383=CARTESIAN_POINT ( 'NONE',  ( -2.802060903037110862, 47.69598914657549216, 79.04308574771191331 ) ) ;
#3386=CARTESIAN_POINT ( 'NONE',  ( 2.091368541865485486, 52.21063245889818916, 72.45433879953087342 ) ) ;
#3390=CARTESIAN_POINT ( 'NONE',  ( 5.239500195294445994, 50.86496669987803187, 78.27515171461519117 ) ) ;
#3391=AXIS2_PLACEMENT_3D ( 'NONE', #12421, #2730, #10738 ) ;
#3392=DIRECTION ( 'NONE',  ( -0.5941461771851691553, -0.8043570849667760481, -2.357623395011396791E-16 ) ) ;
#3393=CARTESIAN_POINT ( 'NONE',  ( 1.652727357819364418, 35.35299279957455099, 76.16022115247204738 ) ) ;
#3394=CARTESIAN_POINT ( 'NONE',  ( -4.808920012916951592, 37.15961619924308934, 75.98775578934684916 ) ) ;
#3395=EDGE_CURVE ( 'NONE', #5130, #9664, #5247, .T. ) ;
#3399=CARTESIAN_POINT ( 'NONE',  ( 8.860816794629819526, 41.35015455542848173, 78.93613448519710118 ) ) ;
#3400=EDGE_CURVE ( 'NONE', #19191, #4192, #18239, .T. ) ;
#3402=CARTESIAN_POINT ( 'NONE',  ( -4.705149740856858998, 37.08296527939383935, 78.93669174070734584 ) ) ;
#3404=CARTESIAN_POINT ( 'NONE',  ( 8.293280423777593668, 41.56926772713645590, 77.52492703482499792 ) ) ;
#3406=VERTEX_POINT ( 'NONE', #1968 ) ;
#3407=EDGE_LOOP ( 'NONE', ( #3038, #4261, #7934, #18607 ) ) ;
#3408=CARTESIAN_POINT ( 'NONE',  ( 6.379311811789950326, 38.45149544986467305, 75.97427057108799886 ) ) ;
#3409=AXIS2_PLACEMENT_3D ( 'NONE', #18631, #15446, #18739 ) ;
#3410=CARTESIAN_POINT ( 'NONE',  ( 4.639020460657009792, 52.06163236765677738, 78.92424046551381878 ) ) ;
#3411=CARTESIAN_POINT ( 'NONE',  ( 6.445631799257238725, 38.49888528477907812, 77.41265765549051991 ) ) ;
#3412=CARTESIAN_POINT ( 'NONE',  ( -3.607357127890973292, 36.27207009797979254, 75.89423958357750166 ) ) ;
#3413=CARTESIAN_POINT ( 'NONE',  ( 5.515973886530674442, 50.66617152567425109, 78.02711337524276303 ) ) ;
#3416=DIRECTION ( 'NONE',  ( -1.540237394707284220E-16, -1.793354297423764243E-16, 1.000000000000000000 ) ) ;
#3420=CARTESIAN_POINT ( 'NONE',  ( 1.487944053602040295, 52.20654624397499788, 76.82903323957145858 ) ) ;
#3422=CARTESIAN_POINT ( 'NONE',  ( 8.500816298777042590, 42.26161455596683680, 79.47732676628994852 ) ) ;
#3423=ORIENTED_EDGE ( 'NONE', *, *, #12651, .F. ) ;
#3424=LINE ( 'NONE', #11636, #9919 ) ;
#3426=LINE ( 'NONE', #3736, #16658 ) ;
#3428=VECTOR ( 'NONE', #8355, 1000.000000000000114 ) ;
#3429=LINE ( 'NONE', #3634, #19664 ) ;
#3431=LINE ( 'NONE', #2257, #7588 ) ;
#3439=CARTESIAN_POINT ( 'NONE',  ( 0.8453367053598014325, 52.35217735662078553, 78.54797669815580718 ) ) ;
#3441=CARTESIAN_POINT ( 'NONE',  ( 4.278870909452986204, 51.41364532819419964, 77.90619853385557292 ) ) ;
#3443=DIRECTION ( 'NONE',  ( -1.540237394707284467E-16, -1.793354297423764243E-16, 1.000000000000000000 ) ) ;
#3447=CARTESIAN_POINT ( 'NONE',  ( 5.486268716722809025, 37.64049940046611198, 76.11636564480957645 ) ) ;
#3450=CARTESIAN_POINT ( 'NONE',  ( 5.599231707071657738, 51.35236299959863970, 78.30875056423674607 ) ) ;
#3451=ORIENTED_EDGE ( 'NONE', *, *, #12458, .T. ) ;
#3453=CYLINDRICAL_SURFACE ( 'NONE', #51, 8.199999999999995737 ) ;
#3458=CARTESIAN_POINT ( 'NONE',  ( 8.299312890679575005, 42.03170978465910679, 75.38196330830126612 ) ) ;
#3461=CARTESIAN_POINT ( 'NONE',  ( -4.972333685589229724, 38.21632979263497987, 75.48149882193594351 ) ) ;
#3462=ORIENTED_EDGE ( 'NONE', *, *, #15634, .F. ) ;
#3464=CARTESIAN_POINT ( 'NONE',  ( 5.599231707071657738, 51.35236299959863970, 78.59183879953087626 ) ) ;
#3465=CARTESIAN_POINT ( 'NONE',  ( 0.9437382761187699254, 52.95236866523615760, 76.77576213461180998 ) ) ;
#3467=AXIS2_PLACEMENT_3D ( 'NONE', #19140, #11067, #12545 ) ;
#3468=VERTEX_POINT ( 'NONE', #8461 ) ;
#3470=CARTESIAN_POINT ( 'NONE',  ( -4.184856022532954078, 37.47340638715262173, 78.05402056118774112 ) ) ;
#3473=CARTESIAN_POINT ( 'NONE',  ( -7.816538853785817587, 41.35010719132777979, 78.90520654368830833 ) ) ;
#3476=VECTOR ( 'NONE', #18077, 1000.000000000000000 ) ;
#3478=CARTESIAN_POINT ( 'NONE',  ( 4.597212664172372953, 36.25829706351294135, 75.77524573853747825 ) ) ;
#3479=AXIS2_PLACEMENT_3D ( 'NONE', #2991, #19574, #14267 ) ;
#3480=CARTESIAN_POINT ( 'NONE',  ( 8.400787919062072007, 39.97141883166423781, 78.77723610448765612 ) ) ;
#3481=ADVANCED_FACE ( 'NONE', ( #363, #7053, #16450 ), #6851, .T. ) ;
#3483=CARTESIAN_POINT ( 'NONE',  ( -5.217375104949212528, 38.30559640794556486, 75.60320319432446468 ) ) ;
#3486=CARTESIAN_POINT ( 'NONE',  ( 2.119548831151183421, 52.81598568046361919, 78.26563523839334380 ) ) ;
#3489=LINE ( 'NONE', #18173, #17111 ) ;
#3490=VERTEX_POINT ( 'NONE', #10171 ) ;
#3491=VECTOR ( 'NONE', #15005, 1000.000000000000000 ) ;
#3493=CARTESIAN_POINT ( 'NONE',  ( 7.726125090393122008, 40.24513420275368247, 76.01001584831250568 ) ) ;
#3494=DIRECTION ( 'NONE',  ( 0.8146038580541355989, -0.5800177190770277047, 2.145060549590874096E-17 ) ) ;
#3499=EDGE_CURVE ( 'NONE', #1377, #1091, #13453, .T. ) ;
#3504=ORIENTED_EDGE ( 'NONE', *, *, #2854, .T. ) ;
#3505=EDGE_CURVE ( 'NONE', #2000, #13846, #9855, .T. ) ;
#3506=CARTESIAN_POINT ( 'NONE',  ( 4.648737399797364667, 37.07553919738725057, 75.46805039548223704 ) ) ;
#3509=AXIS2_PLACEMENT_3D ( 'NONE', #400, #10996, #16579 ) ;
#3511=EDGE_CURVE ( 'NONE', #1769, #10226, #11976, .T. ) ;
#3512=CARTESIAN_POINT ( 'NONE',  ( -4.886362818588788848, 37.21682008020638222, 78.74088963820604192 ) ) ;
#3513=CARTESIAN_POINT ( 'NONE',  ( 8.951509595531131680, 41.62196663317372725, 77.18036020728871449 ) ) ;
#3515=CARTESIAN_POINT ( 'NONE',  ( 9.201306621205869618, 42.37062416594873326, 78.02362291919803283 ) ) ;
#3517=CARTESIAN_POINT ( 'NONE',  ( 4.591414450663933167, 52.09679700955160797, 78.70655549710109256 ) ) ;
#3518=CARTESIAN_POINT ( 'NONE',  ( 6.880715602165139444, 37.89000465862396538, 77.41265765549051991 ) ) ;
#3519=CARTESIAN_POINT ( 'NONE',  ( -3.716790732209381165, 36.35290429323533345, 75.71473766112499959 ) ) ;
#3520=CARTESIAN_POINT ( 'NONE',  ( 0.8503282811412335995, 52.95606000782370870, 76.48963291717792856 ) ) ;
#3522=DIRECTION ( 'NONE',  ( -0.5941461771851693774, -0.8043570849667760481, -2.357623395011396791E-16 ) ) ;
#3524=DIRECTION ( 'NONE',  ( -0.9485903129789527988, 0.3165065846431829311, -8.934458285744989980E-17 ) ) ;
#3525=EDGE_LOOP ( 'NONE', ( #4754, #3946, #2844, #14312 ) ) ;
#3527=CARTESIAN_POINT ( 'NONE',  ( 1.638828243247879790, 52.94402099307490772, 76.88486154722851040 ) ) ;
#3530=CARTESIAN_POINT ( 'NONE',  ( 8.648170029844118645, 43.06315486489794608, 78.41904468188381827 ) ) ;
#3531=ORIENTED_EDGE ( 'NONE', *, *, #11507, .T. ) ;
#3532=EDGE_CURVE ( 'NONE', #11879, #11628, #13870, .T. ) ;
#3534=ORIENTED_EDGE ( 'NONE', *, *, #17686, .T. ) ;
#3539=ORIENTED_EDGE ( 'NONE', *, *, #3868, .F. ) ;
#3542=CARTESIAN_POINT ( 'NONE',  ( -3.495065479208315562, 36.18912478048144266, 76.62933879953087057 ) ) ;
#3543=CARTESIAN_POINT ( 'NONE',  ( -4.032058992557826294, 50.97676447825651991, 78.59092584394873882 ) ) ;
#3544=CARTESIAN_POINT ( 'NONE',  ( 0.5223315597379962760, 52.35472439729344529, 78.93427191990714675 ) ) ;
#3546=CARTESIAN_POINT ( 'NONE',  ( -4.030157702633146322, 50.97812307042602953, 76.47051527011910821 ) ) ;
#3548=CARTESIAN_POINT ( 'NONE',  ( -3.098709854545130593, 36.80491647020841128, 78.46683879953087626 ) ) ;
#3549=CARTESIAN_POINT ( 'NONE',  ( -6.743140149339597933, 40.41798080217650835, 77.97023824993468111 ) ) ;
#3551=CARTESIAN_POINT ( 'NONE',  ( -4.158578283022522193, 37.42937009194850617, 76.81463291717793140 ) ) ;
#3553=CARTESIAN_POINT ( 'NONE',  ( -4.209923912819721892, 38.70632820095286775, 77.33669174070733732 ) ) ;
#3555=CARTESIAN_POINT ( 'NONE',  ( 5.807735516834878986, 37.12329237395520920, 76.04105433551922033 ) ) ;
#3556=CARTESIAN_POINT ( 'NONE',  ( -6.910121556090746076, 47.56003565108909470, 78.32234914140835258 ) ) ;
#3557=ORIENTED_EDGE ( 'NONE', *, *, #17672, .F. ) ;
#3560=ORIENTED_EDGE ( 'NONE', *, *, #16758, .T. ) ;
#3561=LINE ( 'NONE', #6640, #1716 ) ;
#3562=CARTESIAN_POINT ( 'NONE',  ( 5.427780505986065762, 36.85179043424346190, 76.96022115247204454 ) ) ;
#3566=CARTESIAN_POINT ( 'NONE',  ( -5.921523028668194577, 37.98145122859525458, 76.14635491738357587 ) ) ;
#3567=ORIENTED_EDGE ( 'NONE', *, *, #14800, .F. ) ;
#3569=CARTESIAN_POINT ( 'NONE',  ( 0.4048777997643838167, 52.96142680216856746, 76.02501977270890166 ) ) ;
#3570=CARTESIAN_POINT ( 'NONE',  ( -6.711723140599398896, 40.30068868319698083, 78.38758635656873253 ) ) ;
#3571=EDGE_LOOP ( 'NONE', ( #20587, #18476, #4451, #20878 ) ) ;
#3572=CARTESIAN_POINT ( 'NONE',  ( -4.547183694812711785, 37.74104324321675108, 77.90454030471208569 ) ) ;
#3573=ORIENTED_EDGE ( 'NONE', *, *, #16514, .T. ) ;
#3574=CARTESIAN_POINT ( 'NONE',  ( -4.239546901740170348, 50.82850121497202167, 75.97198585835440099 ) ) ;
#3575=CARTESIAN_POINT ( 'NONE',  ( 5.316416202095706645, 37.50973464508803801, 75.36022115247205022 ) ) ;
#3578=CARTESIAN_POINT ( 'NONE',  ( 6.203825325419909831, 49.98094110125470024, 75.61685692759286326 ) ) ;
#3579=CARTESIAN_POINT ( 'NONE',  ( 0.3700437505152531781, 52.96086955526534013, 78.81268084498510973 ) ) ;
#3580=CARTESIAN_POINT ( 'NONE',  ( 4.816229352426441679, 36.41479837022654920, 75.57109918664292536 ) ) ;
#3581=CARTESIAN_POINT ( 'NONE',  ( 7.680169873459327334, 40.17609888434939336, 78.49952087821802138 ) ) ;
#3583=CARTESIAN_POINT ( 'NONE',  ( 0.5221537403065019678, 44.16218137147968292, 72.45433879953087342 ) ) ;
#3584=CARTESIAN_POINT ( 'NONE',  ( 8.354770124117221641, 42.19791863141301036, 75.41143022427675646 ) ) ;
#3585=CARTESIAN_POINT ( 'NONE',  ( -1.202011496911927990, 49.96493122755408223, 72.45432679953087529 ) ) ;
#3587=ORIENTED_EDGE ( 'NONE', *, *, #11328, .T. ) ;
#3588=ORIENTED_EDGE ( 'NONE', *, *, #19324, .F. ) ;
#3590=ORIENTED_EDGE ( 'NONE', *, *, #364, .T. ) ;
#3591=CARTESIAN_POINT ( 'NONE',  ( -3.501255140781824426, 36.19369683415101946, 76.91456057462045237 ) ) ;
#3593=CARTESIAN_POINT ( 'NONE',  ( 4.286460013181947915, 51.39722162121891103, 77.51131257087278925 ) ) ;
#3594=CARTESIAN_POINT ( 'NONE',  ( 0.4776854187739327795, 52.96289371955013081, 75.36214535001711567 ) ) ;
#3595=EDGE_CURVE ( 'NONE', #15970, #557, #7602, .T. ) ;
#3598=CARTESIAN_POINT ( 'NONE',  ( 0.6066065119434701502, 52.96541364096408699, 77.38437845781280089 ) ) ;
#3600=CARTESIAN_POINT ( 'NONE',  ( 4.539819439306699955, 52.13490816606735478, 76.55090572632929025 ) ) ;
#3603=VERTEX_POINT ( 'NONE', #15379 ) ;
#3606=CARTESIAN_POINT ( 'NONE',  ( -5.811565481342516826, 50.45210972548208161, 78.65111229433956908 ) ) ;
#3607=CARTESIAN_POINT ( 'NONE',  ( 8.647902309851698277, 43.06067594696713030, 76.34338796316330900 ) ) ;
#3609=CARTESIAN_POINT ( 'NONE',  ( -5.529385682154831727, 44.31555110708731604, 72.45433879953085921 ) ) ;
#3610=LINE ( 'NONE', #3712, #778 ) ;
#3613=ORIENTED_EDGE ( 'NONE', *, *, #7724, .T. ) ;
#3614=EDGE_LOOP ( 'NONE', ( #16476, #11946, #14823, #2072 ) ) ;
#3615=DIRECTION ( 'NONE',  ( 1.540237394707284220E-16, 1.793354297423764243E-16, -1.000000000000000000 ) ) ;
#3616=CARTESIAN_POINT ( 'NONE',  ( -3.580888326837074587, 36.25251866086962593, 75.96390267329995538 ) ) ;
#3617=DIRECTION ( 'NONE',  ( -0.5941461771851727081, -0.8043570849667734945, -2.357623395011397284E-16 ) ) ;
#3619=EDGE_CURVE ( 'NONE', #6827, #5214, #13983, .T. ) ;
#3620=CARTESIAN_POINT ( 'NONE',  ( -4.388990501910972952, 51.46862972198961472, 78.65149807507090429 ) ) ;
#3625=CARTESIAN_POINT ( 'NONE',  ( 1.880005271900893948, 52.94211922356995359, 77.04052575557504667 ) ) ;
#3628=LINE ( 'NONE', #13011, #8889 ) ;
#3630=CARTESIAN_POINT ( 'NONE',  ( 8.872773925109784798, 41.38599083402314704, 79.54845644658969661 ) ) ;
#3631=ORIENTED_EDGE ( 'NONE', *, *, #20629, .F. ) ;
#3632=AXIS2_PLACEMENT_3D ( 'NONE', #19787, #1726, #13315 ) ;
#3633=CARTESIAN_POINT ( 'NONE',  ( 6.282717385696039436, 38.32643750394947801, 79.45433879953087342 ) ) ;
#3634=CARTESIAN_POINT ( 'NONE',  ( 2.115041367457930477, 52.20598078514409224, 72.45433879953087342 ) ) ;
#3637=CARTESIAN_POINT ( 'NONE',  ( -5.324466712459395623, 37.54042977870726361, 79.49842882144521639 ) ) ;
#3638=CARTESIAN_POINT ( 'NONE',  ( -4.329272046085858250, 37.55995550954649786, 78.93589701864812014 ) ) ;
#3640=DIRECTION ( 'NONE',  ( 1.540237394707284220E-16, 1.793354297423764243E-16, -1.000000000000000000 ) ) ;
#3643=CARTESIAN_POINT ( 'NONE',  ( -4.388425821632080392, 51.46903322184264340, 76.24813767079230331 ) ) ;
#3648=CARTESIAN_POINT ( 'NONE',  ( -7.484136228611396824, 40.27717619252914716, 77.79645048995966761 ) ) ;
#3649=CARTESIAN_POINT ( 'NONE',  ( -4.497956288874163100, 37.67830001658522576, 77.32061371610187450 ) ) ;
#3652=DIRECTION ( 'NONE',  ( -0.9485903129789527988, 0.3165065846431829311, -8.934458285744989980E-17 ) ) ;
#3653=ADVANCED_FACE ( 'NONE', ( #4190 ), #12592, .T. ) ;
#3654=EDGE_CURVE ( 'NONE', #8370, #20845, #6295, .T. ) ;
#3655=ORIENTED_EDGE ( 'NONE', *, *, #9722, .T. ) ;
#3656=DIRECTION ( 'NONE',  ( -0.3165065846431827645, -0.9485903129789529098, 0.000000000000000000 ) ) ;
#3659=ORIENTED_EDGE ( 'NONE', *, *, #16750, .T. ) ;
#3664=CARTESIAN_POINT ( 'NONE',  ( 9.026838159693451047, 41.84773111872319618, 78.13669174070733447 ) ) ;
#3665=CARTESIAN_POINT ( 'NONE',  ( -5.157025508368715094, 37.41674770618860890, 75.39928922905468767 ) ) ;
#3666=ORIENTED_EDGE ( 'NONE', *, *, #6710, .F. ) ;
#3669=VERTEX_POINT ( 'NONE', #4591 ) ;
#3672=VERTEX_POINT ( 'NONE', #20659 ) ;
#3673=CARTESIAN_POINT ( 'NONE',  ( 0.6728307876203661886, 52.36082399497195894, 77.39742102862167883 ) ) ;
#3675=AXIS2_PLACEMENT_3D ( 'NONE', #19705, #6616, #1749 ) ;
#3680=CARTESIAN_POINT ( 'NONE',  ( 4.029718316871106154, 36.77256196250399256, 76.05895398371444571 ) ) ;
#3681=CARTESIAN_POINT ( 'NONE',  ( 7.786684689960352124, 40.49533054657691622, 79.21682452846883393 ) ) ;
#3682=VERTEX_POINT ( 'NONE', #8010 ) ;
#3685=CARTESIAN_POINT ( 'NONE',  ( -7.282021299424333627, 41.64493098333839072, 78.93502118727992922 ) ) ;
#3687=ORIENTED_EDGE ( 'NONE', *, *, #18315, .T. ) ;
#3688=CARTESIAN_POINT ( 'NONE',  ( 6.264934721967925668, 49.94661999341979453, 79.21482656134288902 ) ) ;
#3689=ORIENTED_EDGE ( 'NONE', *, *, #268, .T. ) ;
#3691=CARTESIAN_POINT ( 'NONE',  ( 8.648380609495486482, 40.71346983188059454, 75.44378286633819641 ) ) ;
#3693=CARTESIAN_POINT ( 'NONE',  ( -7.376743071288318632, 41.96049357349896525, 78.50654468188380974 ) ) ;
#3696=CARTESIAN_POINT ( 'NONE',  ( 0.7195706321513085646, 52.35316909177178246, 77.41791596341448667 ) ) ;
#3698=CARTESIAN_POINT ( 'NONE',  ( 4.110464395964859463, 51.52722249412126843, 76.26690125110441443 ) ) ;
#3701=DIRECTION ( 'NONE',  ( 0.9585804129707224952, 0.2848220354341972071, 1.987228219138359305E-16 ) ) ;
#3702=CARTESIAN_POINT ( 'NONE',  ( 5.384092268968043271, 50.76532863195453160, 75.97198585835440099 ) ) ;
#3703=AXIS2_PLACEMENT_3D ( 'NONE', #14553, #8165, #15947 ) ;
#3705=CARTESIAN_POINT ( 'NONE',  ( -4.546230963980875117, 36.96557838055436207, 76.09208750614521932 ) ) ;
#3709=EDGE_CURVE ( 'NONE', #5644, #14094, #3119, .T. ) ;
#3711=LINE ( 'NONE', #2133, #1723 ) ;
#3712=CARTESIAN_POINT ( 'NONE',  ( 6.282717385696040324, 38.32643750394948512, 72.45433879953087342 ) ) ;
#3714=ORIENTED_EDGE ( 'NONE', *, *, #14708, .F. ) ;
#3715=ORIENTED_EDGE ( 'NONE', *, *, #14712, .T. ) ;
#3717=CARTESIAN_POINT ( 'NONE',  ( 8.350753804761280819, 42.18588146751271495, 79.49775514261133935 ) ) ;
#3721=CARTESIAN_POINT ( 'NONE',  ( 5.583914945631950566, 51.36367687427735973, 77.16202479023476712 ) ) ;
#3722=EDGE_CURVE ( 'NONE', #8200, #15454, #8114, .T. ) ;
#3724=CIRCLE ( 'NONE', #9185, 8.199999999999995737 ) ;
#3727=CARTESIAN_POINT ( 'NONE',  ( -7.199302705971482474, 41.41278875884007959, 78.64066830726386570 ) ) ;
#3735=AXIS2_PLACEMENT_3D ( 'NONE', #9156, #17613, #3352 ) ;
#3736=CARTESIAN_POINT ( 'NONE',  ( 2.337612517491833408, 49.93701999136722947, 75.45433879953087342 ) ) ;
#3739=DIRECTION ( 'NONE',  ( -1.540237394707284220E-16, -1.793354297423764243E-16, 1.000000000000000000 ) ) ;
#3740=FACE_OUTER_BOUND ( 'NONE', #1891, .T. ) ;
#3742=ORIENTED_EDGE ( 'NONE', *, *, #20609, .F. ) ;
#3746=ORIENTED_EDGE ( 'NONE', *, *, #4414, .F. ) ;
#3747=CARTESIAN_POINT ( 'NONE',  ( -6.354755732003290802, 42.02918051195119631, 76.16022115247204738 ) ) ;
#3748=CARTESIAN_POINT ( 'NONE',  ( -7.646773700855245437, 40.79148695562606264, 77.07900976289242578 ) ) ;
#3749=CARTESIAN_POINT ( 'NONE',  ( 8.385679600361122255, 39.92613824206362949, 77.13595644658970230 ) ) ;
#3750=CARTESIAN_POINT ( 'NONE',  ( 5.408052348349806415, 37.57667531233130376, 75.99391262232927602 ) ) ;
#3751=VECTOR ( 'NONE', #13193, 1000.000000000000000 ) ;
#3754=ORIENTED_EDGE ( 'NONE', *, *, #14500, .T. ) ;
#3757=CARTESIAN_POINT ( 'NONE',  ( 0.5221537403065019678, 44.16218137147968292, 72.45433879953087342 ) ) ;
#3758=EDGE_CURVE ( 'NONE', #15539, #16083, #16520, .T. ) ;
#3759=EDGE_CURVE ( 'NONE', #11768, #13622, #9939, .T. ) ;
#3760=ORIENTED_EDGE ( 'NONE', *, *, #3312, .F. ) ;
#3762=EDGE_CURVE ( 'NONE', #16089, #5649, #12725, .T. ) ;
#3766=CARTESIAN_POINT ( 'NONE',  ( -7.435220081765090860, 42.57064376796103744, 76.77997794206987692 ) ) ;
#3772=CARTESIAN_POINT ( 'NONE',  ( -4.517072128342572768, 36.94403992325788977, 76.53375056423675460 ) ) ;
#3775=EDGE_LOOP ( 'NONE', ( #20646, #6854, #2483, #20438, #4129 ) ) ;
#3776=CARTESIAN_POINT ( 'NONE',  ( -4.645483384943289273, 37.03889214578785527, 77.94562699264550076 ) ) ;
#3777=CIRCLE ( 'NONE', #7178, 8.799999999999998934 ) ;
#3778=ORIENTED_EDGE ( 'NONE', *, *, #8058, .T. ) ;
#3779=CARTESIAN_POINT ( 'NONE',  ( -4.798777446476682584, 51.17581097466058537, 76.24916814194597237 ) ) ;
#3781=VECTOR ( 'NONE', #15426, 1000.000000000000000 ) ;
#3782=EDGE_CURVE ( 'NONE', #19006, #4385, #336, .T. ) ;
#3783=CARTESIAN_POINT ( 'NONE',  ( -4.357516591192297284, 37.58081861725695205, 75.97198585835440099 ) ) ;
#3786=ORIENTED_EDGE ( 'NONE', *, *, #10571, .T. ) ;
#3788=DIRECTION ( 'NONE',  ( 1.540237394707284220E-16, 1.793354297423764243E-16, -1.000000000000000000 ) ) ;
#3792=CARTESIAN_POINT ( 'NONE',  ( 0.5706633979203369345, 52.96569706562746660, 77.38474949312757190 ) ) ;
#3794=AXIS2_PLACEMENT_3D ( 'NONE', #8231, #11334, #17805 ) ;
#3795=ORIENTED_EDGE ( 'NONE', *, *, #6981, .T. ) ;
#3796=ORIENTED_EDGE ( 'NONE', *, *, #3762, .T. ) ;
#3797=EDGE_CURVE ( 'NONE', #557, #10826, #5224, .T. ) ;
#3798=CARTESIAN_POINT ( 'NONE',  ( 6.853523395152754105, 50.42586825556427499, 78.95155228521747404 ) ) ;
#3799=ORIENTED_EDGE ( 'NONE', *, *, #13796, .F. ) ;
#3800=CARTESIAN_POINT ( 'NONE',  ( 5.581238861929509909, 50.61552606843185487, 76.29031835629793079 ) ) ;
#3801=CARTESIAN_POINT ( 'NONE',  ( 6.814395614697851933, 37.84261482370956031, 75.97427057108799886 ) ) ;
#3802=CARTESIAN_POINT ( 'NONE',  ( 7.881290621023779863, 40.79563723267156661, 75.50010622114506020 ) ) ;
#3805=CARTESIAN_POINT ( 'NONE',  ( 8.314648285358305912, 41.60894804291065441, 77.52294762828243790 ) ) ;
#3806=DIRECTION ( 'NONE',  ( -0.3165065846431824870, -0.9485903129789529098, 0.000000000000000000 ) ) ;
#3807=CARTESIAN_POINT ( 'NONE',  ( 0.7243910816960694721, 52.96448486634505315, 77.41791596341448667 ) ) ;
#3808=VECTOR ( 'NONE', #1257, 1000.000000000000000 ) ;
#3810=CARTESIAN_POINT ( 'NONE',  ( 4.540684532156292086, 52.13426915682742901, 76.47586842453881673 ) ) ;
#3811=CARTESIAN_POINT ( 'NONE',  ( 5.534247820986439415, 36.92786807952553119, 77.73906448345020692 ) ) ;
#3814=CARTESIAN_POINT ( 'NONE',  ( -7.953953629696516536, 41.76759382663043141, 78.67381781145438424 ) ) ;
#3815=ORIENTED_EDGE ( 'NONE', *, *, #5529, .F. ) ;
#3816=CARTESIAN_POINT ( 'NONE',  ( 4.185959258523188176, 36.82597263316856129, 75.77243029545449815 ) ) ;
#3817=VERTEX_POINT ( 'NONE', #8221 ) ;
#3820=CARTESIAN_POINT ( 'NONE',  ( 8.318328750355229673, 41.62059619433301094, 75.36022115247205022 ) ) ;
#3824=DIRECTION ( 'NONE',  ( 1.540237394707284220E-16, 1.793354297423764243E-16, -1.000000000000000000 ) ) ;
#3825=CARTESIAN_POINT ( 'NONE',  ( 5.819883890974968388, 51.18937611976139834, 77.96367690144739981 ) ) ;
#3827=EDGE_LOOP ( 'NONE', ( #11575, #2190, #19726, #14940 ) ) ;
#3829=LINE ( 'NONE', #10350, #18262 ) ;
#3830=CARTESIAN_POINT ( 'NONE',  ( 6.813511439209503529, 39.88797755036236481, 72.45432679953087529 ) ) ;
#3831=ORIENTED_EDGE ( 'NONE', *, *, #1579, .F. ) ;
#3833=DIRECTION ( 'NONE',  ( 0.8043570849667760481, -0.5941461771851693774, 1.733862608106482338E-17 ) ) ;
#3837=CARTESIAN_POINT ( 'NONE',  ( 1.493768332708312441, 52.94516484377990651, 76.82903323957145858 ) ) ;
#3838=VECTOR ( 'NONE', #15780, 1000.000000000000000 ) ;
#3840=LINE ( 'NONE', #10362, #5820 ) ;
#3841=VERTEX_POINT ( 'NONE', #3633 ) ;
#3842=CARTESIAN_POINT ( 'NONE',  ( 8.303614452336031349, 41.57589654819728509, 79.54845644658969661 ) ) ;
#3843=ORIENTED_EDGE ( 'NONE', *, *, #19899, .T. ) ;
#3844=CARTESIAN_POINT ( 'NONE',  ( -4.785381074711875016, 51.18538353145122954, 78.79723525346945223 ) ) ;
#3847=CARTESIAN_POINT ( 'NONE',  ( -5.478128554961354091, 38.57320898139802523, 72.45433879953085921 ) ) ;
#3848=VECTOR ( 'NONE', #18676, 1000.000000000000227 ) ;
#3849=DIRECTION ( 'NONE',  ( -0.5670994908670430323, 0.8236492988270800453, 6.036271672687320902E-17 ) ) ;
#3850=CARTESIAN_POINT ( 'NONE',  ( 8.200913038183980319, 41.32723632482947806, 77.80727997600146750 ) ) ;
#3851=CARTESIAN_POINT ( 'NONE',  ( 0.7565349869329739407, 52.95907566945976441, 77.43632499672374081 ) ) ;
#3852=CARTESIAN_POINT ( 'NONE',  ( 0.8503874818422292314, 52.96356767324962078, 76.48963291717792856 ) ) ;
#3853=CARTESIAN_POINT ( 'NONE',  ( 0.3279640439667346752, 52.35988168082470651, 77.10139762306027933 ) ) ;
#3854=EDGE_LOOP ( 'NONE', ( #12920, #87, #6116, #11038 ) ) ;
#3856=VERTEX_POINT ( 'NONE', #19489 ) ;
#3860=CARTESIAN_POINT ( 'NONE',  ( 6.152864644243832615, 50.94341665060460400, 79.51305506302354331 ) ) ;
#3862=CARTESIAN_POINT ( 'NONE',  ( 5.848563030374239524, 37.15246622033975399, 76.55482881315118959 ) ) ;
#3863=AXIS2_PLACEMENT_3D ( 'NONE', #11037, #19517, #4929 ) ;
#3865=CARTESIAN_POINT ( 'NONE',  ( 4.394187631985148279, 51.39056414810583817, 77.57533925735273783 ) ) ;
#3867=DIRECTION ( 'NONE',  ( 0.8043570849667761591, -0.5941461771851690443, 1.733862608106491891E-17 ) ) ;
#3868=EDGE_CURVE ( 'NONE', #4394, #18879, #18006, .T. ) ;
#3876=CARTESIAN_POINT ( 'NONE',  ( -4.799400614414246036, 51.17536568166803335, 78.65631888207801126 ) ) ;
#3877=ORIENTED_EDGE ( 'NONE', *, *, #3400, .T. ) ;
#3880=ORIENTED_EDGE ( 'NONE', *, *, #11484, .T. ) ;
#3881=CARTESIAN_POINT ( 'NONE',  ( -4.451201164328465687, 50.67726082808356836, 76.41659450085566618 ) ) ;
#3883=EDGE_CURVE ( 'NONE', #12307, #4579, #3426, .T. ) ;
#3887=CARTESIAN_POINT ( 'NONE',  ( -3.584565806390782594, 36.25523506687804343, 78.05869123030269918 ) ) ;
#3888=DIRECTION ( 'NONE',  ( 1.540237394707284220E-16, 1.793354297423764243E-16, -1.000000000000000000 ) ) ;
#3890=ORIENTED_EDGE ( 'NONE', *, *, #6992, .F. ) ;
#3892=ADVANCED_FACE ( 'NONE', ( #16935 ), #5955, .T. ) ;
#3893=CARTESIAN_POINT ( 'NONE',  ( 1.966680432375413012, 52.20268719857811135, 75.87378281519762879 ) ) ;
#3894=ORIENTED_EDGE ( 'NONE', *, *, #11826, .F. ) ;
#3895=DIRECTION ( 'NONE',  ( -0.9485903129789527988, 0.3165065846431829311, -8.934458285744989980E-17 ) ) ;
#3896=FACE_OUTER_BOUND ( 'NONE', #16141, .T. ) ;
#3899=DIRECTION ( 'NONE',  ( -0.5941461771851691553, -0.8043570849667760481, -2.357623395011396791E-16 ) ) ;
#3901=DIRECTION ( 'NONE',  ( 0.9485903129789495791, -0.3165065846431930341, 8.934458285744763183E-17 ) ) ;
#3902=DIRECTION ( 'NONE',  ( -0.3165065846431828200, -0.9485903129789529098, 0.000000000000000000 ) ) ;
#3903=B_SPLINE_CURVE_WITH_KNOTS ( 'NONE', 3,
 ( #1375, #1482, #11169, #14453, #20919, #6354, #12855, #19444, #11277, #3182, #17439, #9684 ),
 .UNSPECIFIED., .F., .F.,
 ( 4, 2, 2, 2, 2, 4 ),
 ( 4.336808689942017736E-19, 0.0001693000378404274555, 0.0003386000756808544773, 0.0004232500946010679882, 0.0005079001135212814991, 0.0006772001513616680802 ),
 .UNSPECIFIED. ) ;
#3905=CARTESIAN_POINT ( 'NONE',  ( -2.917199766949190476, 51.60602765227618960, 78.10580938776615767 ) ) ;
#3908=CARTESIAN_POINT ( 'NONE',  ( 8.218197382629700343, 41.34423908963691474, 76.14505377247542128 ) ) ;
#3910=DIRECTION ( 'NONE',  ( -1.540237394707283727E-16, -1.793354297423763257E-16, 1.000000000000000000 ) ) ;
#3911=ADVANCED_FACE ( 'NONE', ( #10687 ), #15350, .F. ) ;
#3913=CARTESIAN_POINT ( 'NONE',  ( 8.373001147486398565, 41.79479491692730164, 76.15241572602435838 ) ) ;
#3916=CARTESIAN_POINT ( 'NONE',  ( -7.333990156426534845, 40.19720935722482835, 72.45433879953085921 ) ) ;
#3918=ORIENTED_EDGE ( 'NONE', *, *, #13471, .T. ) ;
#3919=CARTESIAN_POINT ( 'NONE',  ( 8.789147962602239517, 47.20595287382010241, 75.43669174070734584 ) ) ;
#3920=DIRECTION ( 'NONE',  ( -0.3165065846431827645, -0.9485903129789529098, 0.000000000000000000 ) ) ;
#3921=CARTESIAN_POINT ( 'NONE',  ( -4.337246640924047547, 50.76736814398887532, 78.93151080536149777 ) ) ;
#3923=DIRECTION ( 'NONE',  ( -0.3165065846431826535, -0.9485903129789529098, -2.188653791613874008E-16 ) ) ;
#3924=DIRECTION ( 'NONE',  ( 1.540237394707284220E-16, 1.793354297423764243E-16, -1.000000000000000000 ) ) ;
#3925=DIRECTION ( 'NONE',  ( -1.540237394707284467E-16, -1.793354297423764243E-16, 1.000000000000000000 ) ) ;
#3926=LINE ( 'NONE', #10121, #9172 ) ;
#3929=CARTESIAN_POINT ( 'NONE',  ( 6.153536035488349043, 50.12267912296926653, 77.68963291717793140 ) ) ;
#3931=CARTESIAN_POINT ( 'NONE',  ( 8.951454296033540814, 41.62180089707131003, 76.31823237213514233 ) ) ;
#3934=CARTESIAN_POINT ( 'NONE',  ( 5.633915549615357676, 51.32674344226200702, 77.24912405724838038 ) ) ;
#3935=CARTESIAN_POINT ( 'NONE',  ( -4.526015856129116166, 36.95064629469848683, 78.75608284215286403 ) ) ;
#3937=CARTESIAN_POINT ( 'NONE',  ( -0.7639737096562715379, 52.86806976190393215, 79.04649434735723901 ) ) ;
#3938=CARTESIAN_POINT ( 'NONE',  ( -3.554968601118880134, 36.23337280359183410, 78.17158301229430606 ) ) ;
#3939=CARTESIAN_POINT ( 'NONE',  ( -7.622107932457680590, 47.55268842043668087, 78.30768265673681583 ) ) ;
#3940=ADVANCED_FACE ( 'NONE', ( #7028 ), #10366, .F. ) ;
#3944=ORIENTED_EDGE ( 'NONE', *, *, #12353, .T. ) ;
#3945=CARTESIAN_POINT ( 'NONE',  ( 5.839579929017896021, 51.17482744986389775, 77.27318761637275202 ) ) ;
#3946=ORIENTED_EDGE ( 'NONE', *, *, #15853, .T. ) ;
#3947=CARTESIAN_POINT ( 'NONE',  ( -4.705661087595403025, 51.24234851550965431, 78.91934866582661812 ) ) ;
#3953=CARTESIAN_POINT ( 'NONE',  ( -3.415291652819150592, 51.24462368788206845, 79.38294305353919356 ) ) ;
#3955=CARTESIAN_POINT ( 'NONE',  ( 5.427780505986065762, 36.85179043424346190, 76.96022115247204454 ) ) ;
#3956=CARTESIAN_POINT ( 'NONE',  ( 0.3400554298508484674, 52.96751499973433397, 78.67509294885779525 ) ) ;
#3957=EDGE_LOOP ( 'NONE', ( #17378, #10605, #2703, #18252 ) ) ;
#3958=CARTESIAN_POINT ( 'NONE',  ( 8.644901377098815232, 43.03925179711409754, 72.45433879953087342 ) ) ;
#3962=FACE_OUTER_BOUND ( 'NONE', #11065, .T. ) ;
#3963=CARTESIAN_POINT ( 'NONE',  ( 5.496261972130637830, 37.64311312718927383, 76.46034384425426822 ) ) ;
#3965=CARTESIAN_POINT ( 'NONE',  ( -5.419656513257913311, 37.61074265007807327, 75.48149882193594351 ) ) ;
#3966=CIRCLE ( 'NONE', #8742, 8.799999999999995381 ) ;
#3967=CARTESIAN_POINT ( 'NONE',  ( 5.500237024828340537, 36.90356520980568433, 77.71779572520892998 ) ) ;
#3968=ORIENTED_EDGE ( 'NONE', *, *, #13386, .F. ) ;
#3970=CARTESIAN_POINT ( 'NONE',  ( -3.722637431614235659, 51.02500564700225993, 75.40660817806873695 ) ) ;
#3974=EDGE_CURVE ( 'NONE', #8922, #9137, #9598, .T. ) ;
#3976=FACE_OUTER_BOUND ( 'NONE', #6855, .T. ) ;
#3977=CARTESIAN_POINT ( 'NONE',  ( -0.1994209430448784792, 35.36759766960258844, 76.86610350541323555 ) ) ;
#3980=ORIENTED_EDGE ( 'NONE', *, *, #2413, .T. ) ;
#3983=EDGE_CURVE ( 'NONE', #6157, #12496, #14258, .T. ) ;
#3984=ORIENTED_EDGE ( 'NONE', *, *, #11293, .F. ) ;
#3989=CARTESIAN_POINT ( 'NONE',  ( -4.895069120933020379, 37.22325107503680641, 76.32271929704664615 ) ) ;
#3991=CARTESIAN_POINT ( 'NONE',  ( 0.3329060540236485899, 52.96014621323875815, 78.59782805397716743 ) ) ;
#3996=CARTESIAN_POINT ( 'NONE',  ( 0.7219634870551158157, 52.21250224913298155, 75.36169494263242541 ) ) ;
#3997=VECTOR ( 'NONE', #553, 1000.000000000000000 ) ;
#3998=EDGE_LOOP ( 'NONE', ( #8038, #11363, #17206, #18751 ) ) ;
#4003=ORIENTED_EDGE ( 'NONE', *, *, #9244, .T. ) ;
#4004=CARTESIAN_POINT ( 'NONE',  ( 6.554687423727395768, 50.64660634980899090, 79.34836068132329956 ) ) ;
#4006=CARTESIAN_POINT ( 'NONE',  ( 6.531299583006453524, 48.82481648921748274, 75.45433879953087342 ) ) ;
#4007=DIRECTION ( 'NONE',  ( 0.2848220354341971516, -0.9585804129707224952, -1.280380753214897429E-16 ) ) ;
#4008=VECTOR ( 'NONE', #17372, 1000.000000000000000 ) ;
#4010=CARTESIAN_POINT ( 'NONE',  ( -2.544431595712045358, 37.47609611642828753, 76.62933879953087057 ) ) ;
#4012=CARTESIAN_POINT ( 'NONE',  ( -3.754515857360592346, 38.36993661534067712, 78.93669174070734584 ) ) ;
#4013=CARTESIAN_POINT ( 'NONE',  ( 0.7871607343966636749, 52.96398990456528111, 77.46299673659909502 ) ) ;
#4017=PLANE ( 'NONE',  #20795 ) ;
#4018=CARTESIAN_POINT ( 'NONE',  ( 8.373815933025275271, 41.81065766626294788, 78.71610475470291135 ) ) ;
#4021=CARTESIAN_POINT ( 'NONE',  ( 8.385679600361122255, 39.92613824206362949, 77.13595644658970230 ) ) ;
#4023=CARTESIAN_POINT ( 'NONE',  ( -3.373742936343101739, 52.19408846175863204, 78.58955347608575437 ) ) ;
#4027=CARTESIAN_POINT ( 'NONE',  ( -7.587684248800459663, 47.67520643615086584, 78.88364539996459257 ) ) ;
#4028=DIRECTION ( 'NONE',  ( 1.540237394707284220E-16, 1.793354297423764243E-16, -1.000000000000000000 ) ) ;
#4030=CARTESIAN_POINT ( 'NONE',  ( 5.748274343403736886, 51.24227120794373747, 77.94845644658968808 ) ) ;
#4032=ORIENTED_EDGE ( 'NONE', *, *, #2356, .F. ) ;
#4033=CARTESIAN_POINT ( 'NONE',  ( 9.279665234200917823, 42.60546990007262025, 79.15097751326614173 ) ) ;
#4034=CARTESIAN_POINT ( 'NONE',  ( -4.233737104609305746, 36.73475175465707565, 75.41196988111011024 ) ) ;
#4035=EDGE_CURVE ( 'NONE', #8763, #1377, #7676, .T. ) ;
#4040=CARTESIAN_POINT ( 'NONE',  ( -0.9199438314403624029, 52.23437776363726215, 72.45433879953087342 ) ) ;
#4045=CARTESIAN_POINT ( 'NONE',  ( 6.882736312352589536, 37.89144858414100270, 76.69330938776616335 ) ) ;
#4048=AXIS2_PLACEMENT_3D ( 'NONE', #1994, #10417, #18063 ) ;
#4049=VERTEX_POINT ( 'NONE', #4668 ) ;
#4050=CARTESIAN_POINT ( 'NONE',  ( -4.449342498592997686, 50.67858896256802836, 78.59458524649963351 ) ) ;
#4051=B_SPLINE_CURVE_WITH_KNOTS ( 'NONE', 3,
 ( #10673, #18731, #6054, #13942, #12452, #15542, #748, #10769, #1070, #2558, #18932, #12250, #3931, #15335, #2457 ),
 .UNSPECIFIED., .F., .F.,
 ( 4, 1, 1, 1, 1, 1, 1, 1, 1, 1, 1, 1, 4 ),
 ( 0.000000000000000000, 0.07577303389073718198, 0.1558117613168219784, 0.2417361372947465226, 0.3357870204060591224, 0.3882587240527491379, 0.4455552461494497463, 0.5113167710153618817, 0.5866953322903324386, 0.6731791507778834838, 0.7705825181721650541, 0.8794626622360116608, 1.000000000000000000 ),
 .UNSPECIFIED. ) ;
#4053=EDGE_LOOP ( 'NONE', ( #286, #3613, #1559, #16718, #8157, #19812, #1720, #7299 ) ) ;
#4056=CIRCLE ( 'NONE', #17653, 8.199999999999995737 ) ;
#4057=AXIS2_PLACEMENT_3D ( 'NONE', #9842, #15045, #5027 ) ;
#4058=CARTESIAN_POINT ( 'NONE',  ( -4.370691255933373931, 51.48170569318705247, 79.53937015691786883 ) ) ;
#4060=CARTESIAN_POINT ( 'NONE',  ( 5.308257127890501970, 50.81265825806588055, 77.27261723006257910 ) ) ;
#4063=ORIENTED_EDGE ( 'NONE', *, *, #2624, .F. ) ;
#4064=CARTESIAN_POINT ( 'NONE',  ( 8.234060390202110113, 41.37527878033370854, 77.44800974218487966 ) ) ;
#4065=VERTEX_POINT ( 'NONE', #18949 ) ;
#4067=CARTESIAN_POINT ( 'NONE',  ( 1.658154530501163126, 36.04125148601230677, 79.45433879953087342 ) ) ;
#4068=CARTESIAN_POINT ( 'NONE',  ( -7.171016202898661263, 41.77105925685706467, 76.16022115247204738 ) ) ;
#4071=CARTESIAN_POINT ( 'NONE',  ( 6.761793986577667503, 50.49362507459272820, 79.13556070921569585 ) ) ;
#4075=B_SPLINE_SURFACE_WITH_KNOTS ( 'NONE', 3, 1, ( 
 ( #5511, #13398 ),
 ( #2433, #11912 ),
 ( #16799, #407 ),
 ( #5614, #5188 ),
 ( #18387, #7093 ),
 ( #8929, #12118 ),
 ( #15418, #13709 ),
 ( #15099, #6894 ),
 ( #15311, #4013 ),
 ( #12023, #2320 ),
 ( #3696, #3807 ),
 ( #613, #11705 ),
 ( #18599, #13596 ),
 ( #2217, #3598 ),
 ( #16588, #8816 ) ),
 .UNSPECIFIED., .F., .F., .F.,
 ( 4, 1, 1, 1, 1, 1, 1, 1, 1, 1, 1, 1, 4 ),
 ( 2, 2 ),
 ( 0.000000000000000000, 0.1162067238869137348, 0.2214153483095009645, 0.3146488149876708329, 0.3978441427673392039, 0.4713237328820706895, 0.5351740646982715566, 0.5914750994871406098, 0.6429785647885755129, 0.7385262294747835243, 0.8287699788399466305, 0.9143335036940697380, 1.000000000000000000 ),
 ( 0.000000000000000000, 1.000000000000000000 ),
 .UNSPECIFIED. ) ;
#4076=AXIS2_PLACEMENT_3D ( 'NONE', #239, #8123, #13026 ) ;
#4077=ORIENTED_EDGE ( 'NONE', *, *, #9773, .T. ) ;
#4078=CARTESIAN_POINT ( 'NONE',  ( 4.271559758984892596, 51.45486941304334749, 77.47147465385867804 ) ) ;
#4079=VERTEX_POINT ( 'NONE', #20637 ) ;
#4089=CARTESIAN_POINT ( 'NONE',  ( 0.7398053571154690200, 52.35989412137791277, 79.54697819541583215 ) ) ;
#4091=VECTOR ( 'NONE', #12366, 1000.000000000000000 ) ;
#4092=VERTEX_POINT ( 'NONE', #19254 ) ;
#4097=LINE ( 'NONE', #13784, #10692 ) ;
#4098=CARTESIAN_POINT ( 'NONE',  ( 5.599231707071657738, 51.35236299959863970, 78.59183879953087626 ) ) ;
#4099=EDGE_CURVE ( 'NONE', #8069, #1372, #12467, .T. ) ;
#4101=ORIENTED_EDGE ( 'NONE', *, *, #5348, .F. ) ;
#4102=CARTESIAN_POINT ( 'NONE',  ( 2.084502445282489624, 52.95459623993866671, 76.15080458372598571 ) ) ;
#4104=CARTESIAN_POINT ( 'NONE',  ( 6.961592395446249526, 50.34604203833234237, 76.59575135851817151 ) ) ;
#4107=EDGE_LOOP ( 'NONE', ( #4101, #9897, #9705, #15167 ) ) ;
#4110=ORIENTED_EDGE ( 'NONE', *, *, #4617, .F. ) ;
#4111=CARTESIAN_POINT ( 'NONE',  ( 2.538045550429134600, 49.87014351810298507, 75.45433879953087342 ) ) ;
#4113=CARTESIAN_POINT ( 'NONE',  ( 7.795054281054241585, 40.53718145105147386, 75.64968528315669971 ) ) ;
#4116=CARTESIAN_POINT ( 'NONE',  ( -7.313565574299385474, 41.74526126053015673, 79.54845644658969661 ) ) ;
#4120=CARTESIAN_POINT ( 'NONE',  ( -5.364198675898909308, 49.85200608322956128, 76.15119298917683466 ) ) ;
#4121=CARTESIAN_POINT ( 'NONE',  ( 4.987469076889843755, 50.87941446422544090, 75.37972891991934432 ) ) ;
#4125=DIRECTION ( 'NONE',  ( 1.540237394707284220E-16, 1.793354297423764243E-16, -1.000000000000000000 ) ) ;
#4126=CARTESIAN_POINT ( 'NONE',  ( 8.882918921757626762, 41.41639603256331981, 78.93548851266230315 ) ) ;
#4129=ORIENTED_EDGE ( 'NONE', *, *, #12758, .F. ) ;
#4132=CARTESIAN_POINT ( 'NONE',  ( -3.778837258911088792, 51.90462289030131160, 79.34012906335151172 ) ) ;
#4136=DIRECTION ( 'NONE',  ( 1.540237394707284220E-16, 1.793354297423764243E-16, -1.000000000000000000 ) ) ;
#4137=ADVANCED_FACE ( 'NONE', ( #9490 ), #20846, .T. ) ;
#4138=DIRECTION ( 'NONE',  ( -0.3165065846431826535, -0.9485903129789529098, -2.188653791613874008E-16 ) ) ;
#4142=CARTESIAN_POINT ( 'NONE',  ( 8.617743499586005385, 42.98606652041282672, 78.90414333341678343 ) ) ;
#4145=AXIS2_PLACEMENT_3D ( 'NONE', #6595, #6701, #16717 ) ;
#4148=DIRECTION ( 'NONE',  ( -1.540237394707284220E-16, -1.793354297423764243E-16, 1.000000000000000000 ) ) ;
#4151=EDGE_CURVE ( 'NONE', #12841, #18903, #6174, .T. ) ;
#4153=EDGE_CURVE ( 'NONE', #10457, #14370, #20728, .T. ) ;
#4155=LINE ( 'NONE', #18840, #10193 ) ;
#4156=CARTESIAN_POINT ( 'NONE',  ( -5.403476264047557542, 38.53479744785971661, 79.12851299606570876 ) ) ;
#4158=CARTESIAN_POINT ( 'NONE',  ( 6.268485860042931179, 37.45252770006494103, 75.44618574453703275 ) ) ;
#4162=CARTESIAN_POINT ( 'NONE',  ( 4.048141534226263438, 36.75897868094575216, 79.45433879953087342 ) ) ;
#4167=LINE ( 'NONE', #12470, #12689 ) ;
#4169=CARTESIAN_POINT ( 'NONE',  ( -3.042256558752230777, 51.51118090841579544, 79.00686454089694166 ) ) ;
#4171=CARTESIAN_POINT ( 'NONE',  ( 5.201902455060544384, 50.89121817065782238, 77.00567114208729436 ) ) ;
#4172=CARTESIAN_POINT ( 'NONE',  ( -4.200570128010908455, 37.62426765031928966, 79.54612747205591461 ) ) ;
#4174=LINE ( 'NONE', #9082, #19698 ) ;
#4175=AXIS2_PLACEMENT_3D ( 'NONE', #8409, #8728, #19780 ) ;
#4176=ORIENTED_EDGE ( 'NONE', *, *, #19769, .F. ) ;
#4178=LINE ( 'NONE', #1494, #14158 ) ;
#4179=DIRECTION ( 'NONE',  ( 0.007885122365275663500, 0.9999689119394085113, 1.805443505845543142E-16 ) ) ;
#4180=CARTESIAN_POINT ( 'NONE',  ( 6.907457231639352102, 50.38602950313908480, 78.73390793106847241 ) ) ;
#4181=FACE_OUTER_BOUND ( 'NONE', #1981, .T. ) ;
#4182=CARTESIAN_POINT ( 'NONE',  ( -4.722163902562435567, 37.85776514764631173, 77.90206145538023463 ) ) ;
#4183=EDGE_CURVE ( 'NONE', #6991, #7247, #3096, .T. ) ;
#4184=CARTESIAN_POINT ( 'NONE',  ( 5.037341483232629535, 37.31725042616477594, 78.09625056423675460 ) ) ;
#4187=CARTESIAN_POINT ( 'NONE',  ( 8.211813679349305062, 41.32530918129923947, 78.64407474691132904 ) ) ;
#4188=ORIENTED_EDGE ( 'NONE', *, *, #494, .T. ) ;
#4190=FACE_OUTER_BOUND ( 'NONE', #6183, .T. ) ;
#4192=VERTEX_POINT ( 'NONE', #8092 ) ;
#4194=CARTESIAN_POINT ( 'NONE',  ( -4.305671849203691615, 50.60821918116168661, 79.54427050475041483 ) ) ;
#4197=LINE ( 'NONE', #12189, #8831 ) ;
#4200=DIRECTION ( 'NONE',  ( -1.540237394707284220E-16, -1.793354297423764243E-16, 1.000000000000000000 ) ) ;
#4201=CARTESIAN_POINT ( 'NONE',  ( 0.6026978026911212760, 52.96544839334315924, 78.93607282253582014 ) ) ;
#4203=CARTESIAN_POINT ( 'NONE',  ( -4.787608953476067519, 50.41169371076171046, 79.45199527959816521 ) ) ;
#4207=CARTESIAN_POINT ( 'NONE',  ( 5.265323063642338930, 37.48261972611145865, 75.97391373086902888 ) ) ;
#4208=CARTESIAN_POINT ( 'NONE',  ( 5.438900134727234992, 36.85973611382630821, 76.29939265556315320 ) ) ;
#4209=DIRECTION ( 'NONE',  ( -1.540237394707284467E-16, -1.793354297423764243E-16, 1.000000000000000000 ) ) ;
#4211=CARTESIAN_POINT ( 'NONE',  ( -6.899669779797631186, 47.65063352677621822, 78.32453850483534552 ) ) ;
#4213=CARTESIAN_POINT ( 'NONE',  ( 6.241727703577843123, 50.87777708829695200, 75.41423045364997790 ) ) ;
#4216=ORIENTED_EDGE ( 'NONE', *, *, #6101, .F. ) ;
#4219=CARTESIAN_POINT ( 'NONE',  ( 4.719835101441633540, 52.00193784792148222, 79.11209812681292419 ) ) ;
#4221=CARTESIAN_POINT ( 'NONE',  ( 8.435567168294131335, 40.07565444796716747, 75.89798363837520867 ) ) ;
#4223=CARTESIAN_POINT ( 'NONE',  ( -6.705289424168793921, 40.29829583493234679, 78.54487611535471103 ) ) ;
#4224=CARTESIAN_POINT ( 'NONE',  ( -7.413538919509569780, 42.09506629875884443, 79.52729148488525368 ) ) ;
#4226=CARTESIAN_POINT ( 'NONE',  ( 5.902048492000326441, 51.12868443877599134, 78.27786821129558348 ) ) ;
#4227=CARTESIAN_POINT ( 'NONE',  ( -6.850209527372854268, 47.75220363455441230, 78.32492703482499508 ) ) ;
#4228=CARTESIAN_POINT ( 'NONE',  ( 5.333527369480803415, 51.54862809055342154, 75.39573407869305299 ) ) ;
#4230=CARTESIAN_POINT ( 'NONE',  ( -2.083470957239373256, 47.45622447009557021, 82.45433879953087342 ) ) ;
#4232=DIRECTION ( 'NONE',  ( 0.5813877811927012917, -0.8136266022444372803, -5.636455622144620416E-17 ) ) ;
#4234=CARTESIAN_POINT ( 'NONE',  ( -4.410496611078632334, 50.71268463827564688, 78.87432127096172962 ) ) ;
#4237=CARTESIAN_POINT ( 'NONE',  ( -7.945817805444411519, 41.74005988965458869, 79.54527856538405217 ) ) ;
#4238=CARTESIAN_POINT ( 'NONE',  ( 5.428124502387796646, 36.85203624147762724, 77.45531005930804724 ) ) ;
#4239=EDGE_CURVE ( 'NONE', #10226, #13351, #13410, .T. ) ;
#4241=PLANE ( 'NONE',  #2628 ) ;
#4243=CARTESIAN_POINT ( 'NONE',  ( 5.839579929017896021, 51.17482744986389775, 77.27318761637275202 ) ) ;
#4244=B_SPLINE_SURFACE_WITH_KNOTS ( 'NONE', 3, 1, ( 
 ( #10225, #417 ),
 ( #16807, #15108 ),
 ( #16702, #18503 ),
 ( #15207, #11612 ),
 ( #5095, #16594 ),
 ( #2126, #11920 ),
 ( #619, #7099 ),
 ( #13605, #13498 ),
 ( #514, #2015 ),
 ( #19873, #19971 ),
 ( #20081, #8514 ),
 ( #10441, #10014 ),
 ( #5294, #5398 ),
 ( #5519, #1819 ),
 ( #8301, #16491 ) ),
 .UNSPECIFIED., .F., .F., .F.,
 ( 4, 1, 1, 1, 1, 1, 1, 1, 1, 1, 1, 1, 4 ),
 ( 2, 2 ),
 ( 0.000000000000000000, 0.07541797170168144937, 0.1450771083642982684, 0.2121257487690652588, 0.2760806684033449421, 0.3377115757710241750, 0.3948710521788694749, 0.4527877999541435883, 0.5116051076384522389, 0.5882781613054922643, 0.6941869364785798746, 0.8318120212073902842, 1.000000000000000000 ),
 ( 0.000000000000000000, 1.000000000000000000 ),
 .UNSPECIFIED. ) ;
#4245=LINE ( 'NONE', #7872, #592 ) ;
#4246=CARTESIAN_POINT ( 'NONE',  ( -4.032264951078913029, 50.98107207184723677, 78.45066232894264147 ) ) ;
#4247=DIRECTION ( 'NONE',  ( 0.3330135628418984250, 0.9429220365244121993, 2.203913228770417655E-16 ) ) ;
#4250=CARTESIAN_POINT ( 'NONE',  ( -4.383767596367525776, 51.47236181906818331, 76.38961819735682468 ) ) ;
#4251=ADVANCED_FACE ( 'NONE', ( #19672 ), #13764, .T. ) ;
#4252=CARTESIAN_POINT ( 'NONE',  ( -7.084038296528465395, 47.03879614692494471, 78.06303731277932911 ) ) ;
#4256=CARTESIAN_POINT ( 'NONE',  ( 5.579238239244114439, 50.61249542689395042, 76.92469047792664583 ) ) ;
#4257=EDGE_CURVE ( 'NONE', #13330, #16250, #13093, .T. ) ;
#4258=ORIENTED_EDGE ( 'NONE', *, *, #10583, .T. ) ;
#4259=CARTESIAN_POINT ( 'NONE',  ( -4.790699304645749557, 51.18158331905331693, 78.75763390087725213 ) ) ;
#4261=ORIENTED_EDGE ( 'NONE', *, *, #15524, .F. ) ;
#4264=LINE ( 'NONE', #7994, #3026 ) ;
#4266=CARTESIAN_POINT ( 'NONE',  ( 0.8504581424305197590, 52.96356711606490819, 76.46781884397893236 ) ) ;
#4267=CARTESIAN_POINT ( 'NONE',  ( -3.098319451127027335, 36.81007947667079350, 78.58910375170351870 ) ) ;
#4268=EDGE_LOOP ( 'NONE', ( #6912, #17885, #18094, #12090 ) ) ;
#4271=ORIENTED_EDGE ( 'NONE', *, *, #7673, .F. ) ;
#4275=CARTESIAN_POINT ( 'NONE',  ( -7.012702200122923557, 47.39982587559282479, 78.90834094864484882 ) ) ;
#4279=ORIENTED_EDGE ( 'NONE', *, *, #4880, .F. ) ;
#4280=CARTESIAN_POINT ( 'NONE',  ( -4.804644443005473775, 51.17161863374556674, 76.44036821129557779 ) ) ;
#4286=ORIENTED_EDGE ( 'NONE', *, *, #19058, .T. ) ;
#4287=EDGE_CURVE ( 'NONE', #10061, #26, #19566, .T. ) ;
#4289=CARTESIAN_POINT ( 'NONE',  ( -4.466244978593272741, 50.49347950185737943, 79.52300236340988704 ) ) ;
#4291=ORIENTED_EDGE ( 'NONE', *, *, #2365, .F. ) ;
#4292=CARTESIAN_POINT ( 'NONE',  ( 6.853565520360258567, 37.87060420419414442, 77.68698088877128782 ) ) ;
#4294=EDGE_CURVE ( 'NONE', #11222, #7247, #9914, .T. ) ;
#4295=EDGE_LOOP ( 'NONE', ( #8513, #2476, #6850, #7737 ) ) ;
#4296=CARTESIAN_POINT ( 'NONE',  ( 4.393996117251955269, 36.11308595931626542, 76.73963291717792856 ) ) ;
#4303=EDGE_CURVE ( 'NONE', #16845, #18638, #14786, .T. ) ;
#4304=VECTOR ( 'NONE', #7118, 1000.000000000000000 ) ;
#4306=ADVANCED_FACE ( 'NONE', ( #207 ), #19779, .F. ) ;
#4307=CARTESIAN_POINT ( 'NONE',  ( 5.434476177758928550, 36.85657491614816195, 76.36627918048426977 ) ) ;
#4309=ORIENTED_EDGE ( 'NONE', *, *, #4153, .F. ) ;
#4310=CARTESIAN_POINT ( 'NONE',  ( 1.631982057795271501, 52.20532641826535780, 75.56770918405875648 ) ) ;
#4312=PLANE ( 'NONE',  #3391 ) ;
#4313=CARTESIAN_POINT ( 'NONE',  ( 5.801534520520057470, 37.11886136902160160, 77.67950998295866327 ) ) ;
#4317=CARTESIAN_POINT ( 'NONE',  ( -3.638656433990026695, 36.29518963458221492, 75.82994300095940332 ) ) ;
#4318=CARTESIAN_POINT ( 'NONE',  ( 5.760694563098077481, 51.23309689197249384, 79.54845644658969661 ) ) ;
#4319=ORIENTED_EDGE ( 'NONE', *, *, #1191, .T. ) ;
#4320=DIRECTION ( 'NONE',  ( -0.9534635866061452747, -0.3015081906286225522, -2.009271279954815797E-16 ) ) ;
#4321=CARTESIAN_POINT ( 'NONE',  ( 6.705715917364262424, 48.58072850854415492, 72.45432679953087529 ) ) ;
#4322=CARTESIAN_POINT ( 'NONE',  ( 8.456021123984127641, 40.13695625074483786, 75.80967849220077426 ) ) ;
#4324=CARTESIAN_POINT ( 'NONE',  ( 6.351167193117434273, 49.92987544885872353, 75.73266097293476662 ) ) ;
#4325=CARTESIAN_POINT ( 'NONE',  ( -7.539150955374725349, 40.44932034567779056, 79.25635544885822981 ) ) ;
#4329=PLANE ( 'NONE',  #13180 ) ;
#4331=CARTESIAN_POINT ( 'NONE',  ( 5.429452001895136881, 51.47777242866884251, 75.37972891991934432 ) ) ;
#4335=CARTESIAN_POINT ( 'NONE',  ( 8.372590497971586387, 41.80698495966687034, 78.77153038569251464 ) ) ;
#4336=CARTESIAN_POINT ( 'NONE',  ( -0.9221579532582926397, 52.97975483202236546, 78.52473566685461037 ) ) ;
#4337=EDGE_LOOP ( 'NONE', ( #2808, #8604, #2309, #12193 ) ) ;
#4338=DIRECTION ( 'NONE',  ( -0.9485903129789527988, 0.3165065846431829311, -8.934458285744989980E-17 ) ) ;
#4339=CARTESIAN_POINT ( 'NONE',  ( 8.661599634585135377, 45.15687757339797059, 75.45433879953088763 ) ) ;
#4340=CARTESIAN_POINT ( 'NONE',  ( -4.274069566951154364, 51.55074801458793132, 79.52610421797659512 ) ) ;
#4341=AXIS2_PLACEMENT_3D ( 'NONE', #18443, #12284, #2586 ) ;
#4342=CARTESIAN_POINT ( 'NONE',  ( -8.256031663946394872, 42.72105353206794831, 79.08626245367327101 ) ) ;
#4343=DIRECTION ( 'NONE',  ( -0.8043570849667502909, 0.5941461771852041274, -1.733862608105461749E-17 ) ) ;
#4344=ORIENTED_EDGE ( 'NONE', *, *, #16750, .F. ) ;
#4352=VECTOR ( 'NONE', #12287, 1000.000000000000114 ) ;
#4355=EDGE_CURVE ( 'NONE', #18944, #3817, #16496, .T. ) ;
#4358=CARTESIAN_POINT ( 'NONE',  ( 5.512699119566887518, 50.66164519424028612, 77.25083512729199242 ) ) ;
#4360=CARTESIAN_POINT ( 'NONE',  ( -5.590960105440975880, 48.67769231808699715, 72.45432679953087529 ) ) ;
#4363=EDGE_LOOP ( 'NONE', ( #15598, #13789, #4891, #16765, #6511, #6968, #9812, #11787 ) ) ;
#4366=ADVANCED_FACE ( 'NONE', ( #11719 ), #20415, .T. ) ;
#4370=CARTESIAN_POINT ( 'NONE',  ( 0.8408802816388469825, 52.35219974923202102, 76.19252767286178596 ) ) ;
#4371=LINE ( 'NONE', #10897, #10637 ) ;
#4372=VERTEX_POINT ( 'NONE', #10665 ) ;
#4373=LINE ( 'NONE', #6077, #7468 ) ;
#4375=EDGE_LOOP ( 'NONE', ( #12959, #17072, #7176, #1825 ) ) ;
#4379=CARTESIAN_POINT ( 'NONE',  ( -7.507604988220667686, 45.82440120099734315, 79.45433879953087342 ) ) ;
#4380=CARTESIAN_POINT ( 'NONE',  ( 5.848951923618479931, 37.15274410921379911, 76.58742703482498371 ) ) ;
#4381=CARTESIAN_POINT ( 'NONE',  ( 6.388020695587198539, 49.89220557922158861, 79.05872268769354605 ) ) ;
#4382=VECTOR ( 'NONE', #15749, 1000.000000000000000 ) ;
#4383=EDGE_LOOP ( 'NONE', ( #17540, #1940, #20503, #543, #18171, #19708 ) ) ;
#4384=CARTESIAN_POINT ( 'NONE',  ( 4.609531566588798590, 52.08341462581984871, 78.11943565213420015 ) ) ;
#4385=VERTEX_POINT ( 'NONE', #10447 ) ;
#4386=VECTOR ( 'NONE', #10167, 1000.000000000000000 ) ;
#4387=CARTESIAN_POINT ( 'NONE',  ( -3.373440834332912086, 52.19430433279444514, 76.25796290525131838 ) ) ;
#4392=CARTESIAN_POINT ( 'NONE',  ( -5.000220527482744259, 50.11192012471359192, 79.30596685730465367 ) ) ;
#4394=VERTEX_POINT ( 'NONE', #18721 ) ;
#4395=CARTESIAN_POINT ( 'NONE',  ( 6.046986631774924348, 37.29425246114896453, 78.37121987722640881 ) ) ;
#4397=CARTESIAN_POINT ( 'NONE',  ( -4.598246518171406727, 51.31910303412165320, 78.93669174070734584 ) ) ;
#4399=CARTESIAN_POINT ( 'NONE',  ( -1.883296302981686043, 36.95289499283964574, 75.45433879953087342 ) ) ;
#4400=VECTOR ( 'NONE', #18717, 1000.000000000000000 ) ;
#4401=LINE ( 'NONE', #15705, #6220 ) ;
#4402=EDGE_CURVE ( 'NONE', #20886, #14909, #11256, .T. ) ;
#4404=DIRECTION ( 'NONE',  ( 0.9999689119394085113, -0.007885122365275719011, 1.526048693634352652E-16 ) ) ;
#4407=CIRCLE ( 'NONE', #8847, 8.199999999999995737 ) ;
#4408=CARTESIAN_POINT ( 'NONE',  ( -3.936224163802635179, 36.51499092983547001, 77.70026928173652436 ) ) ;
#4409=VECTOR ( 'NONE', #8481, 999.9999999999998863 ) ;
#4410=CARTESIAN_POINT ( 'NONE',  ( 8.801580714196775901, 41.17262026450377022, 76.07953452682116335 ) ) ;
#4413=CARTESIAN_POINT ( 'NONE',  ( -3.936408902674057853, 36.51512738899804589, 77.68304435440727218 ) ) ;
#4414=EDGE_CURVE ( 'NONE', #17910, #14291, #3711, .T. ) ;
#4416=LINE ( 'NONE', #14522, #19336 ) ;
#4420=ORIENTED_EDGE ( 'NONE', *, *, #16540, .T. ) ;
#4422=EDGE_CURVE ( 'NONE', #10826, #10346, #7088, .T. ) ;
#4423=CARTESIAN_POINT ( 'NONE',  ( 0.5934291639749685876, 52.36187159818830850, 75.36022115247205022 ) ) ;
#4426=B_SPLINE_SURFACE_WITH_KNOTS ( 'NONE', 3, 1, ( 
 ( #5543, #7345 ),
 ( #15342, #13837 ),
 ( #8960, #5640 ),
 ( #12259, #967 ),
 ( #14933, #17039 ),
 ( #13242, #14831 ),
 ( #10777, #13737 ),
 ( #4252, #20105 ),
 ( #7129, #756 ),
 ( #18135, #20208 ),
 ( #16929, #1961 ),
 ( #12149, #2352 ),
 ( #18738, #17143 ),
 ( #6736, #861 ),
 ( #18630, #357 ),
 ( #19721, #13630 ),
 ( #18526, #3939 ),
 ( #8854, #16541 ),
 ( #12365, #10464 ),
 ( #3556, #8453 ),
 ( #2465, #2564 ),
 ( #20316, #10060 ),
 ( #7242, #13952 ) ),
 .UNSPECIFIED., .F., .F., .F.,
 ( 4, 1, 1, 1, 1, 1, 1, 1, 1, 1, 1, 1, 1, 1, 1, 1, 1, 1, 1, 1, 4 ),
 ( 2, 2 ),
 ( 0.000000000000000000, 0.08067270264552857395, 0.1526829783898679127, 0.2165906325091179196, 0.2718813074182493406, 0.3185216544617175960, 0.3571485182974105665, 0.3872397186037628281, 0.4089098634073701777, 0.4447579376399536377, 0.4819898389264800631, 0.5235943582205320190, 0.5710910199931596987, 0.5998727328596447084, 0.6352309269333883401, 0.6779581688328760736, 0.7280061531568029487, 0.7849809541712158278, 0.8494662260529197706, 0.9209515060471785697, 0.9999999999999998890 ),
 ( 0.000000000000000000, 1.000000000000000000 ),
 .UNSPECIFIED. ) ;
#4427=CARTESIAN_POINT ( 'NONE',  ( -3.236474689574856622, 51.45049332321921298, 75.68338214653230978 ) ) ;
#4429=EDGE_LOOP ( 'NONE', ( #13041, #2045, #3043, #12420 ) ) ;
#4430=VECTOR ( 'NONE', #9803, 1000.000000000000227 ) ;
#4431=CARTESIAN_POINT ( 'NONE',  ( -3.522342774269683563, 36.20927341954680401, 76.21065298426071877 ) ) ;
#4432=CARTESIAN_POINT ( 'NONE',  ( -6.951684312017277989, 40.78766315881389204, 77.34121496451329847 ) ) ;
#4434=EDGE_CURVE ( 'NONE', #20845, #14379, #8389, .T. ) ;
#4436=DIRECTION ( 'NONE',  ( 1.540237394707284220E-16, 1.793354297423764243E-16, -1.000000000000000000 ) ) ;
#4437=CARTESIAN_POINT ( 'NONE',  ( 8.385679600361122255, 39.92613824206362949, 77.13595644658970230 ) ) ;
#4439=CARTESIAN_POINT ( 'NONE',  ( -5.072433652944413396, 37.35426311015447709, 77.90218689189877921 ) ) ;
#4440=CARTESIAN_POINT ( 'NONE',  ( -7.420489402526318834, 40.07407525022878048, 78.61740305894309699 ) ) ;
#4441=CARTESIAN_POINT ( 'NONE',  ( 1.964251312053307830, 36.08998497932209659, 75.45433879953088763 ) ) ;
#4443=LINE ( 'NONE', #4226, #10818 ) ;
#4444=CARTESIAN_POINT ( 'NONE',  ( 8.484205517248936346, 46.29100619283276785, 79.46269805960562849 ) ) ;
#4450=LINE ( 'NONE', #6459, #18062 ) ;
#4451=ORIENTED_EDGE ( 'NONE', *, *, #14847, .T. ) ;
#4453=CARTESIAN_POINT ( 'NONE',  ( 5.760549983993971779, 37.08957531975971023, 75.99604373986946371 ) ) ;
#4455=CARTESIAN_POINT ( 'NONE',  ( 8.214904837957266892, 41.32288909301291113, 78.51180775816763457 ) ) ;
#4456=CARTESIAN_POINT ( 'NONE',  ( -3.597291554029903526, 36.26463506403467107, 78.92082147625116306 ) ) ;
#4457=LINE ( 'NONE', #3284, #19113 ) ;
#4458=DIRECTION ( 'NONE',  ( -1.540237394707284220E-16, -1.793354297423764243E-16, 1.000000000000000000 ) ) ;
#4460=VECTOR ( 'NONE', #18003, 1000.000000000000114 ) ;
#4461=CARTESIAN_POINT ( 'NONE',  ( -4.062845822180057631, 50.96055957082182175, 78.82314076797449331 ) ) ;
#4466=CARTESIAN_POINT ( 'NONE',  ( -5.940171601930143375, 37.99522617845349970, 78.80728580974474085 ) ) ;
#4467=CARTESIAN_POINT ( 'NONE',  ( -5.052695833059940078, 50.99437019215367428, 79.48628414162533318 ) ) ;
#4468=CARTESIAN_POINT ( 'NONE',  ( 5.981342461385748877, 37.24734554037533485, 78.37107466246847309 ) ) ;
#4469=VERTEX_POINT ( 'NONE', #16035 ) ;
#4474=ORIENTED_EDGE ( 'NONE', *, *, #3868, .T. ) ;
#4476=LINE ( 'NONE', #2678, #8454 ) ;
#4477=CARTESIAN_POINT ( 'NONE',  ( 5.455102971993217587, 51.45882509034149166, 79.53290755650829169 ) ) ;
#4478=CARTESIAN_POINT ( 'NONE',  ( -5.510796958474740492, 38.60848837797752964, 78.53742703482498655 ) ) ;
#4479=FACE_BOUND ( 'NONE', #18657, .T. ) ;
#4480=CARTESIAN_POINT ( 'NONE',  ( -3.798798875594518787, 36.41348040526440144, 79.26586447293077242 ) ) ;
#4482=LINE ( 'NONE', #9608, #1019 ) ;
#4484=EDGE_LOOP ( 'NONE', ( #7351, #8363, #20767, #20462 ) ) ;
#4485=CARTESIAN_POINT ( 'NONE',  ( 6.705715917364262424, 48.58072850854415492, 72.45433879953087342 ) ) ;
#4487=CARTESIAN_POINT ( 'NONE',  ( -5.955451856753747109, 38.00651308716548726, 76.73301527011911105 ) ) ;
#4488=AXIS2_PLACEMENT_3D ( 'NONE', #7516, #13891, #15607 ) ;
#4489=CARTESIAN_POINT ( 'NONE',  ( -6.360298161978083620, 42.04670741611674600, 79.54845644658969661 ) ) ;
#4490=CARTESIAN_POINT ( 'NONE',  ( -7.350415620663316218, 41.88927500876809518, 78.85747680284711691 ) ) ;
#4491=VECTOR ( 'NONE', #17233, 1000.000000000000227 ) ;
#4492=EDGE_LOOP ( 'NONE', ( #11743, #2735, #13617, #14146, #14525, #3316 ) ) ;
#4495=CARTESIAN_POINT ( 'NONE',  ( -3.496280357775573222, 52.10652770678432688, 75.88277413867518817 ) ) ;
#4498=ORIENTED_EDGE ( 'NONE', *, *, #15944, .T. ) ;
#4499=CARTESIAN_POINT ( 'NONE',  ( 4.004906909697989015, 36.73854140438177041, 77.43080938776617472 ) ) ;
#4500=AXIS2_PLACEMENT_3D ( 'NONE', #17903, #9831, #8334 ) ;
#4502=B_SPLINE_CURVE_WITH_KNOTS ( 'NONE', 3,
 ( #10676, #6057, #15767, #2561, #20530, #4461, #12557, #17349, #12455, #18936, #15860, #4246 ),
 .UNSPECIFIED., .F., .F.,
 ( 4, 2, 2, 2, 2, 4 ),
 ( 0.000000000000000000, 0.0001618041688235931916, 0.0002427062532353941649, 0.0003236083376471951653, 0.0004854125064707999850, 0.0006472166752944048590 ),
 .UNSPECIFIED. ) ;
#4503=CARTESIAN_POINT ( 'NONE',  ( 5.563409226749892689, 51.37882362279480475, 76.27120023672567584 ) ) ;
#4504=AXIS2_PLACEMENT_3D ( 'NONE', #10364, #15028, #444 ) ;
#4505=ADVANCED_FACE ( 'NONE', ( #16140 ), #6431, .T. ) ;
#4507=LINE ( 'NONE', #4399, #6794 ) ;
#4510=CARTESIAN_POINT ( 'NONE',  ( -5.246808833622705670, 49.98991590973655263, 79.09052234626923905 ) ) ;
#4513=CARTESIAN_POINT ( 'NONE',  ( 5.549530740019891439, 36.93878869392346331, 75.99415254657458263 ) ) ;
#4514=CARTESIAN_POINT ( 'NONE',  ( 8.787842894572216679, 41.13144714757795128, 76.38644048143638088 ) ) ;
#4517=ADVANCED_FACE ( 'NONE', ( #6326 ), #18829, .T. ) ;
#4519=DIRECTION ( 'NONE',  ( -0.9585804129707224952, -0.2848220354341972071, -1.987228219138359305E-16 ) ) ;
#4520=B_SPLINE_CURVE_WITH_KNOTS ( 'NONE', 3,
 ( #9294, #15783, #9186, #17566, #7682, #2989, #3100, #14159, #20642, #6072 ),
 .UNSPECIFIED., .F., .F.,
 ( 4, 2, 2, 2, 4 ),
 ( 0.000000000000000000, 0.0001564258200695812736, 0.0002346387301043621797, 0.0003128516401391430858, 0.0006257032802783057956 ),
 .UNSPECIFIED. ) ;
#4522=CARTESIAN_POINT ( 'NONE',  ( -7.962931747100077118, 41.82371769612938550, 77.49347059784275871 ) ) ;
#4526=CARTESIAN_POINT ( 'NONE',  ( 2.108290839596759447, 51.34989793853182505, 76.48963291717792856 ) ) ;
#4528=VERTEX_POINT ( 'NONE', #17724 ) ;
#4529=CARTESIAN_POINT ( 'NONE',  ( -3.232751207032058094, 36.92019674127485729, 75.77010869825431882 ) ) ;
#4530=CARTESIAN_POINT ( 'NONE',  ( 8.378694375505322256, 41.81382678022286115, 78.47674047826052401 ) ) ;
#4531=CARTESIAN_POINT ( 'NONE',  ( 5.716051675127889808, 50.35205778976271773, 79.51305506302354331 ) ) ;
#4532=VERTEX_POINT ( 'NONE', #19309 ) ;
#4533=CARTESIAN_POINT ( 'NONE',  ( 4.141216478295206116, 51.51532511143173565, 78.50413411530853125 ) ) ;
#4534=EDGE_CURVE ( 'NONE', #11768, #6129, #3157, .T. ) ;
#4535=CARTESIAN_POINT ( 'NONE',  ( -6.709242558049761662, 40.29605830358345031, 78.50801527011910252 ) ) ;
#4536=CARTESIAN_POINT ( 'NONE',  ( 7.700557761655851152, 40.25396938766707677, 76.00709785348774972 ) ) ;
#4539=ORIENTED_EDGE ( 'NONE', *, *, #6835, .T. ) ;
#4541=CARTESIAN_POINT ( 'NONE',  ( 5.902048492000326441, 51.12868443877599134, 78.27786821129558348 ) ) ;
#4545=ADVANCED_FACE ( 'NONE', ( #7840 ), #11460, .T. ) ;
#4547=LINE ( 'NONE', #20710, #14008 ) ;
#4548=FACE_OUTER_BOUND ( 'NONE', #5380, .T. ) ;
#4549=CARTESIAN_POINT ( 'NONE',  ( -0.3473626758238653744, 52.97522236001905327, 79.37504392981026058 ) ) ;
#4550=CARTESIAN_POINT ( 'NONE',  ( 0.3279640439667345642, 52.35988168082470651, 77.76169174070734869 ) ) ;
#4552=DIRECTION ( 'NONE',  ( 0.007885122365275663500, 0.9999689119394085113, 1.805443505845543142E-16 ) ) ;
#4555=CARTESIAN_POINT ( 'NONE',  ( 2.447781712115294273, 38.42313889284341144, 72.45432679953087529 ) ) ;
#4557=EDGE_CURVE ( 'NONE', #6157, #867, #10170, .T. ) ;
#4558=CARTESIAN_POINT ( 'NONE',  ( 5.155652520773657876, 37.39667442584504897, 77.72325690743420523 ) ) ;
#4559=CARTESIAN_POINT ( 'NONE',  ( -5.004817973257477348, 39.29348442311233214, 76.73301527011911105 ) ) ;
#4560=CARTESIAN_POINT ( 'NONE',  ( 5.245694785492322154, 50.86039100563218085, 78.13212606300182017 ) ) ;
#4561=CARTESIAN_POINT ( 'NONE',  ( 6.507463592229761673, 49.75665574485773135, 76.97234655072247733 ) ) ;
#4564=EDGE_CURVE ( 'NONE', #9068, #19085, #16667, .T. ) ;
#4566=CARTESIAN_POINT ( 'NONE',  ( -5.075010979219785057, 38.29217337334619486, 79.43312132436682305 ) ) ;
#4567=DIRECTION ( 'NONE',  ( 0.2999031954727301441, 0.9539696396349547358, 2.172727669310452375E-16 ) ) ;
#4568=CARTESIAN_POINT ( 'NONE',  ( 5.332873941910801108, 50.80275800021833277, 78.92693817761565356 ) ) ;
#4569=ORIENTED_EDGE ( 'NONE', *, *, #12563, .T. ) ;
#4573=CARTESIAN_POINT ( 'NONE',  ( -6.613032277150673544, 45.52591812603678534, 75.45433879953087342 ) ) ;
#4574=DIRECTION ( 'NONE',  ( 0.3165065846431827645, 0.9485903129789529098, 0.000000000000000000 ) ) ;
#4576=CARTESIAN_POINT ( 'NONE',  ( -5.405939962049822078, 49.82766502745145942, 76.76022115247205591 ) ) ;
#4579=VERTEX_POINT ( 'NONE', #262 ) ;
#4580=DIRECTION ( 'NONE',  ( 1.540237394707284220E-16, 1.793354297423764243E-16, -1.000000000000000000 ) ) ;
#4584=CARTESIAN_POINT ( 'NONE',  ( 1.087774996680691109, 52.94836625043949851, 76.77198585835439815 ) ) ;
#4585=CARTESIAN_POINT ( 'NONE',  ( -4.792503378000012582, 37.91763016944491227, 77.90139762306027649 ) ) ;
#4587=B_SPLINE_SURFACE_WITH_KNOTS ( 'NONE', 3, 1, ( 
 ( #4098, #17096 ),
 ( #12617, #17196 ),
 ( #14202, #20485 ),
 ( #19104, #9016 ),
 ( #12201, #10627 ),
 ( #14002, #17402 ),
 ( #15818, #1022 ),
 ( #12512, #15501 ),
 ( #5807, #20679 ),
 ( #18793, #18680 ),
 ( #12313, #2520 ) ),
 .UNSPECIFIED., .F., .F., .F.,
 ( 4, 1, 1, 1, 1, 1, 1, 1, 4 ),
 ( 2, 2 ),
 ( 0.000000000000000000, 0.2096989846417539882, 0.3830033715279665407, 0.5180517223345033617, 0.6192761841629320640, 0.7029005363942016915, 0.7892332632667665715, 0.8867012962659018838, 1.000000000000000000 ),
 ( 0.000000000000000000, 1.000000000000000000 ),
 .UNSPECIFIED. ) ;
#4589=CARTESIAN_POINT ( 'NONE',  ( 9.353187571392870936, 42.82582100880699016, 77.22643688620827618 ) ) ;
#4591=CARTESIAN_POINT ( 'NONE',  ( 5.037341483232629535, 37.31725042616477594, 78.09625056423675460 ) ) ;
#4593=CARTESIAN_POINT ( 'NONE',  ( 4.942331607238935831, 51.83758864179496584, 75.54250430092201896 ) ) ;
#4594=ORIENTED_EDGE ( 'NONE', *, *, #14448, .F. ) ;
#4595=CARTESIAN_POINT ( 'NONE',  ( -5.391925874121969109, 49.83202182525327117, 78.49957729094111869 ) ) ;
#4596=CARTESIAN_POINT ( 'NONE',  ( 2.484494565094233831, 50.04344131194918788, 78.25433879953088478 ) ) ;
#4597=ORIENTED_EDGE ( 'NONE', *, *, #13910, .T. ) ;
#4598=CARTESIAN_POINT ( 'NONE',  ( 4.490969506678155199, 36.18237959297783135, 75.97723610431854979 ) ) ;
#4599=EDGE_CURVE ( 'NONE', #18313, #6954, #11982, .T. ) ;
#4600=CARTESIAN_POINT ( 'NONE',  ( 5.694198211105373275, 51.28221506855305734, 75.97344461144770378 ) ) ;
#4601=CARTESIAN_POINT ( 'NONE',  ( 5.428124502387796646, 36.85203624147762724, 77.45531005930804724 ) ) ;
#4602=VERTEX_POINT ( 'NONE', #474 ) ;
#4607=CARTESIAN_POINT ( 'NONE',  ( 4.551159079667362661, 51.21251702529338701, 77.70137231118654597 ) ) ;
#4612=CARTESIAN_POINT ( 'NONE',  ( -4.340948238162491535, 40.55733868359232730, 75.45433879953087342 ) ) ;
#4613=CARTESIAN_POINT ( 'NONE',  ( -3.557428649121372022, 36.23518994195449494, 77.32142682847380399 ) ) ;
#4615=CARTESIAN_POINT ( 'NONE',  ( 2.091073016766569648, 52.20170728465966903, 78.67719617274387645 ) ) ;
#4617=EDGE_CURVE ( 'NONE', #16250, #17122, #7057, .T. ) ;
#4618=VERTEX_POINT ( 'NONE', #18146 ) ;
#4619=CARTESIAN_POINT ( 'NONE',  ( -7.774959294756113692, 41.22996117453095621, 78.61536821129558916 ) ) ;
#4620=CARTESIAN_POINT ( 'NONE',  ( -0.9425155279038999190, 52.23031283747450004, 76.97503235252658271 ) ) ;
#4622=CARTESIAN_POINT ( 'NONE',  ( -2.920505538251614297, 51.60450474689833555, 76.49565832826704082 ) ) ;
#4624=CARTESIAN_POINT ( 'NONE',  ( 5.613949991644618720, 51.34149119567325670, 78.06835901908682729 ) ) ;
#4626=CARTESIAN_POINT ( 'NONE',  ( -3.872497565881518611, 36.46791865901509055, 75.57130654555172100 ) ) ;
#4628=CARTESIAN_POINT ( 'NONE',  ( 5.323881593982134675, 50.64173803113060757, 79.54845644658969661 ) ) ;
#4630=CARTESIAN_POINT ( 'NONE',  ( -4.233078557257877073, 37.50902643103172807, 77.20593245741272881 ) ) ;
#4631=CARTESIAN_POINT ( 'NONE',  ( 8.242077797972765296, 41.41581020936537527, 77.48357784852399277 ) ) ;
#4633=CIRCLE ( 'NONE', #6315, 8.199999999999995737 ) ;
#4635=ORIENTED_EDGE ( 'NONE', *, *, #1901, .T. ) ;
#4636=CARTESIAN_POINT ( 'NONE',  ( -7.774959294756113692, 41.22996117453095621, 78.61536821129558916 ) ) ;
#4640=( NAMED_UNIT ( * ) SI_UNIT ( $, .STERADIAN. ) SOLID_ANGLE_UNIT ( ) );
#4641=CARTESIAN_POINT ( 'NONE',  ( -5.782670150369643380, 50.47275727106970322, 76.07566230427023868 ) ) ;
#4643=DIRECTION ( 'NONE',  ( -1.540237394707283727E-16, -1.793354297423763257E-16, 1.000000000000000000 ) ) ;
#4644=CARTESIAN_POINT ( 'NONE',  ( -0.7221989753287875180, 52.21573735104068703, 79.09854784679095019 ) ) ;
#4648=CARTESIAN_POINT ( 'NONE',  ( 8.387651578222229176, 39.93204838481331365, 78.28891658965622469 ) ) ;
#4649=CARTESIAN_POINT ( 'NONE',  ( 1.039473849130955418, 52.94750985498448870, 79.52524494518011977 ) ) ;
#4651=EDGE_LOOP ( 'NONE', ( #16665, #20334, #7065, #9170 ) ) ;
#4653=CARTESIAN_POINT ( 'NONE',  ( 8.244390605783030068, 41.39379493652497644, 75.36077184440998167 ) ) ;
#4654=CARTESIAN_POINT ( 'NONE',  ( -3.798798875594516122, 36.41348040526440144, 79.26586447293075821 ) ) ;
#4657=CARTESIAN_POINT ( 'NONE',  ( 8.941883057029242465, 41.59311528658734147, 77.39218765127517941 ) ) ;
#4659=CARTESIAN_POINT ( 'NONE',  ( 9.292527943876132568, 42.64402025696431764, 77.82525376769920911 ) ) ;
#4662=CARTESIAN_POINT ( 'NONE',  ( -4.952297205838755545, 37.26552315606879517, 79.54733240137164785 ) ) ;
#4663=EDGE_CURVE ( 'NONE', #2198, #16412, #16756, .T. ) ;
#4666=CARTESIAN_POINT ( 'NONE',  ( -3.379507664096216946, 36.94932017462306106, 77.62000880070094411 ) ) ;
#4667=ORIENTED_EDGE ( 'NONE', *, *, #19903, .F. ) ;
#4668=CARTESIAN_POINT ( 'NONE',  ( 0.5934291639749685876, 52.36187159818830850, 75.36022115247205022 ) ) ;
#4669=EDGE_CURVE ( 'NONE', #19301, #2672, #20631, .T. ) ;
#4670=EDGE_CURVE ( 'NONE', #5430, #5246, #17348, .T. ) ;
#4673=CARTESIAN_POINT ( 'NONE',  ( 6.424237833264311526, 38.48359793996362299, 76.18799845131768222 ) ) ;
#4674=CARTESIAN_POINT ( 'NONE',  ( 8.238767346824911186, 41.44068808925890579, 77.95380709400741637 ) ) ;
#4675=CARTESIAN_POINT ( 'NONE',  ( 6.212565296439490403, 37.41256891269643603, 78.35997004935869370 ) ) ;
#4676=PLANE ( 'NONE',  #4820 ) ;
#4677=ORIENTED_EDGE ( 'NONE', *, *, #4678, .T. ) ;
#4678=EDGE_CURVE ( 'NONE', #13937, #5501, #12593, .T. ) ;
#4679=FACE_OUTER_BOUND ( 'NONE', #11386, .T. ) ;
#4681=VERTEX_POINT ( 'NONE', #5961 ) ;
#4683=DIRECTION ( 'NONE',  ( -1.540237394707284467E-16, -1.793354297423764243E-16, 1.000000000000000000 ) ) ;
#4684=CARTESIAN_POINT ( 'NONE',  ( -7.425569853284181399, 47.94249712161214916, 78.80863703060173009 ) ) ;
#4685=B_SPLINE_CURVE_WITH_KNOTS ( 'NONE', 3,
 ( #11089, #7988, #7775, #20634, #16079, #14254, #11189, #12988, #19252, #4666, #1285, #6064 ),
 .UNSPECIFIED., .F., .F.,
 ( 4, 2, 2, 2, 2, 4 ),
 ( 0.000000000000000000, 0.0003362723517171105499, 0.0006725447034342210998, 0.0008406808792927945081, 0.001008817055151368025, 0.001345089406868523949 ),
 .UNSPECIFIED. ) ;
#4687=CARTESIAN_POINT ( 'NONE',  ( -5.955451856753747109, 38.00651308716548726, 76.73301527011911105 ) ) ;
#4689=CARTESIAN_POINT ( 'NONE',  ( 8.240531579721347200, 41.39327284936243245, 76.03295302879951123 ) ) ;
#4692=CARTESIAN_POINT ( 'NONE',  ( -3.364492789658395377, 52.20069827791003547, 76.33204918460485544 ) ) ;
#4695=CARTESIAN_POINT ( 'NONE',  ( -7.868132033238831369, 41.48904945220900942, 77.97272179757899835 ) ) ;
#4697=CARTESIAN_POINT ( 'NONE',  ( 2.046082049342416109, 52.21940049450358856, 77.27552032814631389 ) ) ;
#4699=CARTESIAN_POINT ( 'NONE',  ( -4.227598324046955014, 37.48485322674370224, 78.89954634079194307 ) ) ;
#4700=CARTESIAN_POINT ( 'NONE',  ( -4.188116532274838377, 50.86525147400593738, 78.93463757479271692 ) ) ;
#4703=DIRECTION ( 'NONE',  ( 0.3165065846431827645, 0.9485903129789529098, 0.000000000000000000 ) ) ;
#4705=ORIENTED_EDGE ( 'NONE', *, *, #8850, .T. ) ;
#4706=CARTESIAN_POINT ( 'NONE',  ( 4.510527851286438406, 51.24252967697265149, 77.72408214165703555 ) ) ;
#4709=CARTESIAN_POINT ( 'NONE',  ( 0.7411699536762380580, 52.95947911001109532, 78.88801344401531424 ) ) ;
#4712=DIRECTION ( 'NONE',  ( -0.5941461771851693774, -0.8043570849667760481, -2.357623395011396791E-16 ) ) ;
#4713=VECTOR ( 'NONE', #13908, 1000.000000000000000 ) ;
#4714=CARTESIAN_POINT ( 'NONE',  ( -3.059272215776527304, 36.79205479859442818, 76.91456057462045237 ) ) ;
#4715=ORIENTED_EDGE ( 'NONE', *, *, #11962, .T. ) ;
#4716=CARTESIAN_POINT ( 'NONE',  ( 2.083608154845512317, 52.20176614783930802, 78.73916595950259989 ) ) ;
#4717=AXIS2_PLACEMENT_3D ( 'NONE', #20304, #19212, #4138 ) ;
#4718=ORIENTED_EDGE ( 'NONE', *, *, #18055, .T. ) ;
#4719=CARTESIAN_POINT ( 'NONE',  ( 8.869748494521283888, 41.37692342661967615, 77.52492703482499792 ) ) ;
#4720=CARTESIAN_POINT ( 'NONE',  ( 5.848951923618479931, 37.15274410921379911, 77.37492703482499223 ) ) ;
#4722=CARTESIAN_POINT ( 'NONE',  ( -7.605668267552800010, 43.10965446021727132, 76.06610350541322418 ) ) ;
#4723=ORIENTED_EDGE ( 'NONE', *, *, #7806, .F. ) ;
#4726=ORIENTED_EDGE ( 'NONE', *, *, #15267, .T. ) ;
#4727=CARTESIAN_POINT ( 'NONE',  ( -4.002011967609277576, 36.56358573041304538, 75.49480657079904233 ) ) ;
#4728=DIRECTION ( 'NONE',  ( -0.5941461771851691553, -0.8043570849667760481, -2.357623395011396791E-16 ) ) ;
#4731=CARTESIAN_POINT ( 'NONE',  ( -5.018595066975972685, 37.31449471545010965, 77.33253961758860839 ) ) ;
#4732=CARTESIAN_POINT ( 'NONE',  ( 8.787982635420597433, 41.13186595976554116, 77.18134264024645574 ) ) ;
#4738=FACE_OUTER_BOUND ( 'NONE', #20127, .T. ) ;
#4740=ADVANCED_FACE ( 'NONE', ( #18940 ), #17346, .F. ) ;
#4742=CARTESIAN_POINT ( 'NONE',  ( -5.483735557913453462, 50.68636498614493036, 75.61447646545406087 ) ) ;
#4745=CARTESIAN_POINT ( 'NONE',  ( 8.787982635420597433, 41.13186595976554116, 77.18134264024645574 ) ) ;
#4746=DIRECTION ( 'NONE',  ( 0.01891643426601404346, 0.01351699135163154063, 0.9997296931968457923 ) ) ;
#4749=ORIENTED_EDGE ( 'NONE', *, *, #15853, .F. ) ;
#4750=FACE_OUTER_BOUND ( 'NONE', #4363, .T. ) ;
#4751=CARTESIAN_POINT ( 'NONE',  ( 8.634055581509258559, 43.03495486475600984, 76.16967972087822147 ) ) ;
#4752=CARTESIAN_POINT ( 'NONE',  ( 5.561486116954087677, 51.38024414653337146, 76.36928804473561172 ) ) ;
#4753=CARTESIAN_POINT ( 'NONE',  ( 1.921644402852825451, 52.85035846467894771, 79.11952361228654240 ) ) ;
#4754=ORIENTED_EDGE ( 'NONE', *, *, #2629, .F. ) ;
#4757=CARTESIAN_POINT ( 'NONE',  ( 0.8455950101471346736, 52.35579997042385259, 78.52566232894263010 ) ) ;
#4758=PLANE ( 'NONE',  #11480 ) ;
#4759=CARTESIAN_POINT ( 'NONE',  ( 6.778550821858020825, 50.48124747537763568, 77.88538524077617353 ) ) ;
#4760=EDGE_CURVE ( 'NONE', #1769, #13579, #12984, .T. ) ;
#4761=LINE ( 'NONE', #1491, #7601 ) ;
#4762=B_SPLINE_SURFACE_WITH_KNOTS ( 'NONE', 3, 1, ( 
 ( #7725, #20988 ),
 ( #20887, #14313 ),
 ( #11036, #1233 ),
 ( #6223, #15821 ),
 ( #14206, #19200 ),
 ( #6422, #20682 ),
 ( #6318, #6117 ),
 ( #4615, #17506 ),
 ( #4716, #11137 ),
 ( #9544, #16027 ),
 ( #3148, #16131 ),
 ( #8036, #12931 ),
 ( #19410, #4829 ),
 ( #17817, #3247 ),
 ( #9747, #16230 ),
 ( #1654, #13138 ),
 ( #3345, #19516 ),
 ( #466, #19614 ),
 ( #14735, #11761 ),
 ( #4928, #359 ),
 ( #1963, #8566 ),
 ( #17921, #19823 ),
 ( #156, #8457 ) ),
 .UNSPECIFIED., .F., .F., .F.,
 ( 4, 1, 1, 1, 1, 1, 1, 1, 1, 1, 1, 1, 1, 1, 1, 1, 1, 1, 1, 1, 4 ),
 ( 2, 2 ),
 ( 0.000000000000000000, 0.04297438296114229617, 0.08348499068739016760, 0.1209138123397622833, 0.1552987673628354603, 0.1872381756066306413, 0.2161558137575471383, 0.2423469948807361607, 0.2659345218879605177, 0.3103547245860572290, 0.3557075913687650637, 0.4032107411089864146, 0.4537893912586022926, 0.5075094828293470473, 0.5641094501553882701, 0.6252262897377069972, 0.6910483815401738950, 0.7616865875262860408, 0.8363505414003653549, 0.9158720556281316760, 1.000000000000000000 ),
 ( 0.000000000000000000, 1.000000000000000000 ),
 .UNSPECIFIED. ) ;
#4766=CARTESIAN_POINT ( 'NONE',  ( 5.008975552073978932, 51.78836144432716537, 77.68963291717794561 ) ) ;
#4767=CARTESIAN_POINT ( 'NONE',  ( 6.569564547327074955, 50.63561721789299952, 77.67636243622263237 ) ) ;
#4768=CARTESIAN_POINT ( 'NONE',  ( -3.053082554203017995, 36.78748274492484427, 76.62933879953087057 ) ) ;
#4772=EDGE_CURVE ( 'NONE', #9577, #15919, #9592, .T. ) ;
#4777=CARTESIAN_POINT ( 'NONE',  ( 8.707758170209565662, 40.89142814818289651, 75.40210940951681096 ) ) ;
#4779=CARTESIAN_POINT ( 'NONE',  ( -0.4031263708652977340, 52.21524339649662494, 75.56421855115301867 ) ) ;
#4781=CARTESIAN_POINT ( 'NONE',  ( 6.228842675835584153, 38.34397571433836305, 78.14418354478426920 ) ) ;
#4782=CARTESIAN_POINT ( 'NONE',  ( 0.7627568828200497197, 52.96425867272768784, 76.01945459498423929 ) ) ;
#4786=VECTOR ( 'NONE', #10015, 1000.000000000000000 ) ;
#4787=EDGE_CURVE ( 'NONE', #6827, #16377, #8677, .T. ) ;
#4788=CARTESIAN_POINT ( 'NONE',  ( 8.930560609631596591, 41.55918119345393080, 76.05553801048951357 ) ) ;
#4790=ORIENTED_EDGE ( 'NONE', *, *, #11754, .F. ) ;
#4795=DIRECTION ( 'NONE',  ( -0.5941461771851691553, -0.8043570849667760481, -2.357623395011396791E-16 ) ) ;
#4798=ORIENTED_EDGE ( 'NONE', *, *, #12448, .T. ) ;
#4802=ORIENTED_EDGE ( 'NONE', *, *, #18489, .T. ) ;
#4808=CARTESIAN_POINT ( 'NONE',  ( -5.428519676309859321, 37.61728951159455647, 79.46937556254052026 ) ) ;
#4809=CARTESIAN_POINT ( 'NONE',  ( -4.705149740856864327, 37.08296527939383225, 78.93669174070734584 ) ) ;
#4810=CARTESIAN_POINT ( 'NONE',  ( 5.239803326269729666, 50.86322232383581365, 76.04240903267428564 ) ) ;
#4812=VERTEX_POINT ( 'NONE', #18395 ) ;
#4813=CARTESIAN_POINT ( 'NONE',  ( -4.133436435564208367, 50.90432386914923768, 75.98707017319573254 ) ) ;
#4814=CARTESIAN_POINT ( 'NONE',  ( 8.912633302440582383, 46.81545344901155659, 80.45433879953087342 ) ) ;
#4815=VECTOR ( 'NONE', #14128, 1000.000000000000114 ) ;
#4816=ORIENTED_EDGE ( 'NONE', *, *, #364, .F. ) ;
#4817=CARTESIAN_POINT ( 'NONE',  ( 4.582010541884842247, 52.10374329815417127, 78.30859729819620441 ) ) ;
#4818=EDGE_CURVE ( 'NONE', #2000, #9137, #11808, .T. ) ;
#4819=DIRECTION ( 'NONE',  ( 0.3165065846431827645, 0.9485903129789529098, 0.000000000000000000 ) ) ;
#4820=AXIS2_PLACEMENT_3D ( 'NONE', #7892, #17671, #1297 ) ;
#4821=CARTESIAN_POINT ( 'NONE',  ( -5.706182906969134550, 50.52741225482698439, 75.88700421999355683 ) ) ;
#4824=EDGE_CURVE ( 'NONE', #16863, #5156, #8135, .T. ) ;
#4826=EDGE_CURVE ( 'NONE', #15617, #9093, #2225, .T. ) ;
#4827=CARTESIAN_POINT ( 'NONE',  ( -3.639202304192273640, 36.29559284691160315, 77.48323649892105891 ) ) ;
#4829=CARTESIAN_POINT ( 'NONE',  ( 1.940234681537338801, 52.95557165619788265, 79.09265199143256098 ) ) ;
#4830=DIRECTION ( 'NONE',  ( -0.9534635866061451637, -0.3015081906286224411, -2.009271279954815058E-16 ) ) ;
#4831=ORIENTED_EDGE ( 'NONE', *, *, #2173, .F. ) ;
#4832=VECTOR ( 'NONE', #11745, 1000.000000000000227 ) ;
#4833=CARTESIAN_POINT ( 'NONE',  ( -7.780652970462169193, 41.24611481839983895, 78.48594744126245359 ) ) ;
#4834=VECTOR ( 'NONE', #1170, 1000.000000000000227 ) ;
#4836=CARTESIAN_POINT ( 'NONE',  ( -7.590232248627324374, 43.06084092073458436, 76.13058770837619704 ) ) ;
#4839=CARTESIAN_POINT ( 'NONE',  ( -4.269064254816391291, 37.69685299354377861, 75.36022115247205022 ) ) ;
#4840=ORIENTED_EDGE ( 'NONE', *, *, #5484, .T. ) ;
#4841=CARTESIAN_POINT ( 'NONE',  ( 5.008975552073978932, 51.78836144432716537, 77.68963291717794561 ) ) ;
#4842=LINE ( 'NONE', #6132, #13573 ) ;
#4844=VERTEX_POINT ( 'NONE', #12029 ) ;
#4845=CARTESIAN_POINT ( 'NONE',  ( 0.5221537403065015237, 44.16218137147968292, 75.45433879953087342 ) ) ;
#4846=CARTESIAN_POINT ( 'NONE',  ( -4.759934653634315893, 37.89819380636689061, 77.90166954077812989 ) ) ;
#4849=PLANE ( 'NONE',  #10096 ) ;
#4850=DIRECTION ( 'NONE',  ( 1.540237394707283727E-16, 1.793354297423763257E-16, -1.000000000000000000 ) ) ;
#4852=AXIS2_PLACEMENT_3D ( 'NONE', #4814, #5417, #11337 ) ;
#4855=CARTESIAN_POINT ( 'NONE',  ( -1.440187084481231894, 38.28092143101017797, 78.25433879953088478 ) ) ;
#4856=FACE_OUTER_BOUND ( 'NONE', #17476, .T. ) ;
#4858=VERTEX_POINT ( 'NONE', #3702 ) ;
#4861=CARTESIAN_POINT ( 'NONE',  ( 8.535530527220215546, 40.37525097622586401, 79.30521328845429707 ) ) ;
#4862=CARTESIAN_POINT ( 'NONE',  ( 6.138829900063904610, 50.03976854554820619, 77.70577767651062118 ) ) ;
#4863=ORIENTED_EDGE ( 'NONE', *, *, #16806, .F. ) ;
#4865=ADVANCED_FACE ( 'NONE', ( #10112 ), #4244, .F. ) ;
#4866=DIRECTION ( 'NONE',  ( -1.540237394707284467E-16, -1.793354297423764243E-16, 1.000000000000000000 ) ) ;
#4868=DIRECTION ( 'NONE',  ( -1.540237394707284220E-16, -1.793354297423764243E-16, 1.000000000000000000 ) ) ;
#4870=DIRECTION ( 'NONE',  ( -0.5813877811927011807, 0.8136266022444372803, 5.636455622144619183E-17 ) ) ;
#4871=CARTESIAN_POINT ( 'NONE',  ( 0.3293525775907221176, 52.35991604324109971, 77.67332569164774725 ) ) ;
#4872=CARTESIAN_POINT ( 'NONE',  ( 6.446086404075624721, 49.80199260132323502, 77.33077842133744184 ) ) ;
#4873=DIRECTION ( 'NONE',  ( -0.5813877811927011807, 0.8136266022444372803, 5.636455622144619183E-17 ) ) ;
#4877=CARTESIAN_POINT ( 'NONE',  ( -5.769203958596529347, 48.43638519259696551, 72.45432679953087529 ) ) ;
#4878=VERTEX_POINT ( 'NONE', #19667 ) ;
#4879=CARTESIAN_POINT ( 'NONE',  ( -5.832343694407396306, 50.43726237516484900, 78.41225960292398156 ) ) ;
#4880=EDGE_CURVE ( 'NONE', #1872, #7531, #203, .T. ) ;
#4881=CARTESIAN_POINT ( 'NONE',  ( 6.012275498921958672, 37.26944915646792822, 78.37198585835440667 ) ) ;
#4883=CARTESIAN_POINT ( 'NONE',  ( 8.889236131602293867, 41.43532911122410667, 77.52218233473911368 ) ) ;
#4884=CARTESIAN_POINT ( 'NONE',  ( 9.035997676120972599, 41.87518277052537030, 78.13634973986094678 ) ) ;
#4885=ORIENTED_EDGE ( 'NONE', *, *, #7288, .T. ) ;
#4886=CARTESIAN_POINT ( 'NONE',  ( 0.1862881254137638554, 52.21059564658006025, 75.38460717221940399 ) ) ;
#4887=CARTESIAN_POINT ( 'NONE',  ( 0.2893871155212132673, 52.97020135390489060, 79.53425070713537082 ) ) ;
#4888=CARTESIAN_POINT ( 'NONE',  ( 0.5221537403065005245, 44.16218137147968292, 82.45433879953087342 ) ) ;
#4889=CARTESIAN_POINT ( 'NONE',  ( 4.108651072766817514, 51.53644210273448323, 76.21360399200699476 ) ) ;
#4890=CARTESIAN_POINT ( 'NONE',  ( 0.5221537403065019678, 44.16218137147968292, 72.45433879953087342 ) ) ;
#4891=ORIENTED_EDGE ( 'NONE', *, *, #11997, .F. ) ;
#4893=ADVANCED_FACE ( 'NONE', ( #5723 ), #15320, .T. ) ;
#4894=ORIENTED_EDGE ( 'NONE', *, *, #14802, .F. ) ;
#4896=CARTESIAN_POINT ( 'NONE',  ( -7.813542802050427838, 46.98339118501086631, 79.23467789972187347 ) ) ;
#4898=CARTESIAN_POINT ( 'NONE',  ( -7.324551137483023666, 41.80748339028045280, 78.91811502121268518 ) ) ;
#4899=ADVANCED_FACE ( 'NONE', ( #732 ), #1557, .T. ) ;
#4902=CARTESIAN_POINT ( 'NONE',  ( -4.557243880370988265, 36.97371317826440418, 76.05537227506185616 ) ) ;
#4904=CARTESIAN_POINT ( 'NONE',  ( -7.649386493801853426, 47.42852896470760982, 78.28566691767271379 ) ) ;
#4905=CARTESIAN_POINT ( 'NONE',  ( 5.753005855668248181, 51.23877623043087937, 78.93669174070734584 ) ) ;
#4907=ORIENTED_EDGE ( 'NONE', *, *, #19710, .F. ) ;
#4908=CARTESIAN_POINT ( 'NONE',  ( -5.838300394258943093, 50.43300593553962585, 78.21416447440572028 ) ) ;
#4909=CARTESIAN_POINT ( 'NONE',  ( -4.952297205838751992, 37.26552315606879517, 79.54733240137164785 ) ) ;
#4910=B_SPLINE_CURVE_WITH_KNOTS ( 'NONE', 3,
 ( #10445, #14036, #5946, #18924, #12132, #4648, #2763, #6254, #9468, #15751, #14559, #17752, #3074, #10968, #7969, #19333, #9266, #4861, #15953, #17637, #1263, #15849, #7654, #20826, #2863, #20716, #16163 ),
 .UNSPECIFIED., .F., .F.,
 ( 4, 1, 1, 1, 1, 1, 1, 1, 1, 1, 1, 1, 1, 1, 1, 1, 1, 1, 1, 1, 1, 1, 1, 1, 4 ),
 ( 0.000000000000000000, 0.05993306358482522467, 0.1145105083304139432, 0.1639926324650750333, 0.2083799252409545000, 0.2474206522578790979, 0.2813744068707942358, 0.3102651545178817805, 0.3340707221093189849, 0.3764843156245091249, 0.4195869878574357559, 0.4649490021377667981, 0.5131068515344550107, 0.5381792345077858197, 0.5638273912065150384, 0.5896398555221948889, 0.6163062535856453916, 0.6433841197412238921, 0.6712141767968796691, 0.7000136030487154049, 0.7297781433983795418, 0.7919609919944711196, 0.8575419152218471952, 0.9267698348267595643, 1.000000000000000000 ),
 .UNSPECIFIED. ) ;
#4911=CARTESIAN_POINT ( 'NONE',  ( 5.928804517645879457, 51.10892084043006633, 76.16996516156804375 ) ) ;
#4912=CARTESIAN_POINT ( 'NONE',  ( -4.030277663924256792, 50.97803735047946105, 78.47566305278908771 ) ) ;
#4914=ORIENTED_EDGE ( 'NONE', *, *, #7439, .F. ) ;
#4915=LINE ( 'NONE', #19813, #6441 ) ;
#4917=VERTEX_POINT ( 'NONE', #12343 ) ;
#4919=CARTESIAN_POINT ( 'NONE',  ( -7.419120997399995865, 40.07157761357974124, 78.50801527011910252 ) ) ;
#4920=CARTESIAN_POINT ( 'NONE',  ( -4.699374957658429608, 51.24684035381270064, 75.36124333316173818 ) ) ;
#4924=DIRECTION ( 'NONE',  ( -0.5941461771851691553, -0.8043570849667760481, -2.357623395011396791E-16 ) ) ;
#4925=CARTESIAN_POINT ( 'NONE',  ( 5.619997200715287633, 36.98914144679460492, 77.75986257808632729 ) ) ;
#4926=CARTESIAN_POINT ( 'NONE',  ( 5.504825744318520897, 50.66746093937735651, 76.01152026380901816 ) ) ;
#4928=CARTESIAN_POINT ( 'NONE',  ( 1.023998609437386520, 52.21012155851776981, 79.52671882365912381 ) ) ;
#4929=DIRECTION ( 'NONE',  ( -0.3165065846431775465, -0.9485903129789546862, 0.000000000000000000 ) ) ;
#4931=ORIENTED_EDGE ( 'NONE', *, *, #13920, .T. ) ;
#4932=CARTESIAN_POINT ( 'NONE',  ( -7.831411425717313968, 41.39424600171143709, 78.12842291999400857 ) ) ;
#4933=EDGE_CURVE ( 'NONE', #19814, #14654, #5399, .T. ) ;
#4935=CARTESIAN_POINT ( 'NONE',  ( 9.060635047751631532, 41.94902253626816702, 79.49775514261133935 ) ) ;
#4936=B_SPLINE_SURFACE_WITH_KNOTS ( 'NONE', 3, 1, ( 
 ( #20579, #6005 ),
 ( #2921, #4201 ),
 ( #17288, #14096 ),
 ( #12503, #12305 ),
 ( #15811, #1224 ),
 ( #10726, #13882 ),
 ( #7393, #17187 ),
 ( #15597, #5912 ),
 ( #7713, #12610 ),
 ( #20365, #18787 ),
 ( #20671, #19096 ),
 ( #16436, #2142 ),
 ( #9837, #6622 ),
 ( #3439, #17808 ),
 ( #3022, #13126 ) ),
 .UNSPECIFIED., .F., .F., .F.,
 ( 4, 1, 1, 1, 1, 1, 1, 1, 1, 1, 1, 1, 4 ),
 ( 2, 2 ),
 ( 0.000000000000000000, 0.07572900668544887970, 0.1557212283653267859, 0.2428008865684916084, 0.3367971223029513350, 0.3882775785060046392, 0.4462854066205887982, 0.5120087213739217269, 0.5869354790617866691, 0.6733690469438747828, 0.7707158190319922664, 0.8795326993170452523, 1.000000000000000000 ),
 ( 0.000000000000000000, 1.000000000000000000 ),
 .UNSPECIFIED. ) ;
#4937=EDGE_LOOP ( 'NONE', ( #11043, #3843, #17393, #11659 ) ) ;
#4939=CARTESIAN_POINT ( 'NONE',  ( -5.362906160289790947, 38.50482994647732227, 75.80435357840198662 ) ) ;
#4940=ORIENTED_EDGE ( 'NONE', *, *, #15640, .F. ) ;
#4942=CARTESIAN_POINT ( 'NONE',  ( 0.3326973149608336566, 52.96014171822455552, 77.10139762306027933 ) ) ;
#4943=ADVANCED_FACE ( 'NONE', ( #4548 ), #9570, .F. ) ;
#4946=CARTESIAN_POINT ( 'NONE',  ( -4.765255033702754162, 37.90212375680545875, 77.33633635728615729 ) ) ;
#4949=ADVANCED_FACE ( 'NONE', ( #4856 ), #19327, .T. ) ;
#4950=ORIENTED_EDGE ( 'NONE', *, *, #2854, .F. ) ;
#4951=CARTESIAN_POINT ( 'NONE',  ( -4.795362370604993707, 51.17825126284458293, 76.19771883405211099 ) ) ;
#4953=CARTESIAN_POINT ( 'NONE',  ( 2.119851040271390374, 52.81592988514039178, 76.48963291717792856 ) ) ;
#4956=CARTESIAN_POINT ( 'NONE',  ( -4.435834490810350417, 37.63071868037679479, 75.97716382624557241 ) ) ;
#4957=CYLINDRICAL_SURFACE ( 'NONE', #408, 8.199999999999995737 ) ;
#4958=CARTESIAN_POINT ( 'NONE',  ( 3.961507247562192635, 36.71833509068318335, 76.73963291717792856 ) ) ;
#4959=CARTESIAN_POINT ( 'NONE',  ( 7.684216168072399711, 40.18822588599692125, 78.67376765716130649 ) ) ;
#4960=ORIENTED_EDGE ( 'NONE', *, *, #1259, .T. ) ;
#4961=DIRECTION ( 'NONE',  ( -0.5941461771851691553, -0.8043570849667760481, -2.357623395011396791E-16 ) ) ;
#4962=CARTESIAN_POINT ( 'NONE',  ( 9.353600933836910158, 42.82705988227500882, 76.64232882509132594 ) ) ;
#4964=CARTESIAN_POINT ( 'NONE',  ( 2.063676922390465851, 52.82613311267615330, 78.85822911341185204 ) ) ;
#4965=ORIENTED_EDGE ( 'NONE', *, *, #12611, .T. ) ;
#4967=EDGE_CURVE ( 'NONE', #15461, #2251, #3177, .T. ) ;
#4968=DIRECTION ( 'NONE',  ( -1.540237394707284220E-16, -1.793354297423764243E-16, 1.000000000000000000 ) ) ;
#4970=B_SPLINE_CURVE_WITH_KNOTS ( 'NONE', 3,
 ( #19146, #7868, #1269, #6258, #18930, #20525, #5852, #18832, #13939, #17231 ),
 .UNSPECIFIED., .F., .F.,
 ( 4, 2, 2, 2, 4 ),
 ( 0.000000000000000000, 0.0002697494009883096770, 0.0003371867512354173591, 0.0004046241014825250411, 0.0005394988019767708171 ),
 .UNSPECIFIED. ) ;
#4971=CARTESIAN_POINT ( 'NONE',  ( -2.083470957239372368, 47.45622447009557021, 79.40903933791013003 ) ) ;
#4972=DIRECTION ( 'NONE',  ( -0.9999689119394085113, 0.007885122365275776257, -1.526048693634352652E-16 ) ) ;
#4973=CARTESIAN_POINT ( 'NONE',  ( 8.787829143201872029, 41.13140593384864729, 78.45948585835439815 ) ) ;
#4974=CARTESIAN_POINT ( 'NONE',  ( -5.462576778579502523, 43.73439565840071452, 82.45433879953087342 ) ) ;
#4976=B_SPLINE_CURVE_WITH_KNOTS ( 'NONE', 3,
 ( #17461, #9284, #1501, #14149, #4467, #2884, #9382, #14252, #20736, #12675, #19156, #8516, #14784, #20939, #1, #2018, #14680, #6372, #1605, #3606, #6799, #11506, #4879, #5196, #17977, #6480, #19564 ),
 .UNSPECIFIED., .F., .F.,
 ( 4, 1, 1, 1, 1, 1, 1, 1, 1, 1, 1, 1, 1, 1, 1, 1, 1, 1, 1, 1, 1, 1, 1, 1, 4 ),
 ( 0.000000000000000000, 0.08415130211954198469, 0.1639620550106605512, 0.2403084560778752377, 0.3136616503690570767, 0.3487238096526073527, 0.3821668720153286181, 0.4136737894986983743, 0.4437099131648768457, 0.4722505124987256275, 0.4989577201472497614, 0.5245780966751731889, 0.5489676856186370690, 0.5954867311152326481, 0.6405007172309487018, 0.6844907576478919120, 0.7283883565803446203, 0.7516682776372889396, 0.7779555554382332483, 0.8073737814008299374, 0.8396655338036946858, 0.8751296329422569853, 0.9135058715745314473, 0.9551265033309996877, 1.000000000000000000 ),
 .UNSPECIFIED. ) ;
#4978=CARTESIAN_POINT ( 'NONE',  ( 6.931410089129659724, 50.36833649219094866, 77.12327887040382279 ) ) ;
#4979=CARTESIAN_POINT ( 'NONE',  ( -3.496029822981027380, 36.18983710238020279, 76.51650556680409920 ) ) ;
#4980=LINE ( 'NONE', #7400, #6918 ) ;
#4981=AXIS2_PLACEMENT_3D ( 'NONE', #13972, #2687, #7591 ) ;
#4983=ORIENTED_EDGE ( 'NONE', *, *, #17178, .F. ) ;
#4985=CARTESIAN_POINT ( 'NONE',  ( 8.865792162213244509, 41.36506604770743678, 78.93669174070734584 ) ) ;
#4986=CARTESIAN_POINT ( 'NONE',  ( -4.853223633226585676, 37.19234149890714036, 78.86751516113972116 ) ) ;
#4988=CARTESIAN_POINT ( 'NONE',  ( 9.222679282817953350, 42.43467938865651945, 77.98843304575544266 ) ) ;
#4990=VERTEX_POINT ( 'NONE', #14346 ) ;
#4991=CARTESIAN_POINT ( 'NONE',  ( 6.882613847952937292, 37.89136107556471700, 76.65924029158320252 ) ) ;
#4992=B_SPLINE_CURVE_WITH_KNOTS ( 'NONE', 3,
 ( #11684, #8483, #14967, #386, #9333, #7403, #15401, #20586, #816, #15716, #5693, #12202, #10933, #9119 ),
 .UNSPECIFIED., .F., .F.,
 ( 4, 2, 2, 2, 2, 2, 4 ),
 ( 0.000000000000000000, 9.722885556680744862E-05, 0.0001944577111336148972, 0.0003889154222671841496, 0.0007778308445342767925, 0.001555661689068462078, 0.003111323378136812267 ),
 .UNSPECIFIED. ) ;
#4995=CARTESIAN_POINT ( 'NONE',  ( 5.083341947918205150, 50.97915212978642785, 75.37133819800362744 ) ) ;
#5002=VECTOR ( 'NONE', #4870, 1000.000000000000227 ) ;
#5003=CARTESIAN_POINT ( 'NONE',  ( 1.081950717574418963, 52.20974765063458989, 76.77198585835439815 ) ) ;
#5006=CARTESIAN_POINT ( 'NONE',  ( -1.403474231502331637, 49.90122385011594019, 75.45433879953087342 ) ) ;
#5011=CARTESIAN_POINT ( 'NONE',  ( -7.712688300188555779, 47.26501720182910304, 78.14978456997452838 ) ) ;
#5013=DIRECTION ( 'NONE',  ( 1.540237394707284220E-16, 1.793354297423764243E-16, -1.000000000000000000 ) ) ;
#5015=CARTESIAN_POINT ( 'NONE',  ( 8.253192067227004713, 41.42870919820841635, 77.94607846572662879 ) ) ;
#5016=CARTESIAN_POINT ( 'NONE',  ( -5.086258153195707621, 37.36447471160525424, 79.53654225555244750 ) ) ;
#5018=CARTESIAN_POINT ( 'NONE',  ( 5.904402762709062280, 51.12694543383925350, 76.06909773771320715 ) ) ;
#5019=CARTESIAN_POINT ( 'NONE',  ( -4.030505877904165146, 50.97787427712486164, 78.52322435057745054 ) ) ;
#5020=PLANE ( 'NONE',  #7885 ) ;
#5023=CARTESIAN_POINT ( 'NONE',  ( 5.902048492000326441, 51.12868443877599134, 78.27786821129558348 ) ) ;
#5024=ORIENTED_EDGE ( 'NONE', *, *, #4151, .T. ) ;
#5025=CARTESIAN_POINT ( 'NONE',  ( 4.186600743578833494, 51.48180158285643415, 78.06776350345396054 ) ) ;
#5027=DIRECTION ( 'NONE',  ( -0.3165065846431827645, -0.9485903129789529098, 0.000000000000000000 ) ) ;
#5029=EDGE_CURVE ( 'NONE', #19138, #18543, #17992, .T. ) ;
#5031=CARTESIAN_POINT ( 'NONE',  ( 5.407234661254054942, 37.58402455804959175, 75.99604373986946371 ) ) ;
#5034=CARTESIAN_POINT ( 'NONE',  ( 5.937214047150960461, 51.10270905974117994, 76.26580079864017137 ) ) ;
#5035=VERTEX_POINT ( 'NONE', #9777 ) ;
#5036=CARTESIAN_POINT ( 'NONE',  ( 1.851481395807867747, 48.14626068599128672, 82.45433879953087342 ) ) ;
#5037=LINE ( 'NONE', #19923, #9576 ) ;
#5040=EDGE_CURVE ( 'NONE', #889, #16595, #19438, .T. ) ;
#5042=CARTESIAN_POINT ( 'NONE',  ( 9.150799720292940975, 42.21925177981464117, 79.41516958226422673 ) ) ;
#5045=CARTESIAN_POINT ( 'NONE',  ( -5.933958468462563474, 37.99063678704128222, 76.24300064276494027 ) ) ;
#5046=ORIENTED_EDGE ( 'NONE', *, *, #14969, .T. ) ;
#5047=EDGE_CURVE ( 'NONE', #54, #9854, #10963, .T. ) ;
#5050=FACE_OUTER_BOUND ( 'NONE', #5293, .T. ) ;
#5052=DIRECTION ( 'NONE',  ( 1.540237394707284220E-16, 1.793354297423764243E-16, -1.000000000000000000 ) ) ;
#5056=VERTEX_POINT ( 'NONE', #1477 ) ;
#5058=LINE ( 'NONE', #16358, #16223 ) ;
#5059=CARTESIAN_POINT ( 'NONE',  ( 5.396367158938475406, 37.56735342610807749, 75.36172901897782594 ) ) ;
#5062=EDGE_CURVE ( 'NONE', #18903, #8686, #3054, .T. ) ;
#5065=LINE ( 'NONE', #19541, #8235 ) ;
#5067=CARTESIAN_POINT ( 'NONE',  ( 4.523044550153707988, 37.12507482698154604, 75.49492869865662215 ) ) ;
#5069=VERTEX_POINT ( 'NONE', #11063 ) ;
#5070=CYLINDRICAL_SURFACE ( 'NONE', #16642, 8.799999999999995381 ) ;
#5071=DIRECTION ( 'NONE',  ( 0.007885122365275663500, 0.9999689119394085113, 1.805443505845543142E-16 ) ) ;
#5073=CARTESIAN_POINT ( 'NONE',  ( 2.101630697682613125, 52.81929183848976805, 78.66284909142584070 ) ) ;
#5076=VECTOR ( 'NONE', #18658, 1000.000000000000227 ) ;
#5080=VECTOR ( 'NONE', #3339, 1000.000000000000000 ) ;
#5081=CARTESIAN_POINT ( 'NONE',  ( 6.876224750190004897, 50.40909967906462441, 75.93520998463665705 ) ) ;
#5082=CARTESIAN_POINT ( 'NONE',  ( 9.353743827924017040, 42.82748814491910139, 76.70850639745313515 ) ) ;
#5083=CARTESIAN_POINT ( 'NONE',  ( -0.9074515375185698840, 52.84529689527732899, 76.19569360893534338 ) ) ;
#5085=VECTOR ( 'NONE', #9032, 1000.000000000000000 ) ;
#5088=CARTESIAN_POINT ( 'NONE',  ( 4.575658464751415799, 52.10843532165534953, 76.08931382966170531 ) ) ;
#5089=CARTESIAN_POINT ( 'NONE',  ( 8.617444985878929486, 45.46842246209711647, 78.98986195196137317 ) ) ;
#5090=CARTESIAN_POINT ( 'NONE',  ( 8.385679600361122255, 39.92613824206362949, 77.13595644658970230 ) ) ;
#5091=ADVANCED_FACE ( 'NONE', ( #6347 ), #15995, .T. ) ;
#5095=CARTESIAN_POINT ( 'NONE',  ( 0.4418570709954666720, 52.35535905447424199, 75.99769453967874711 ) ) ;
#5096=LINE ( 'NONE', #11615, #4786 ) ;
#5100=CARTESIAN_POINT ( 'NONE',  ( 9.155505153612395475, 42.23335426198017473, 78.07975471416389723 ) ) ;
#5103=CARTESIAN_POINT ( 'NONE',  ( 0.6392524745555471233, 52.20500180601669626, 79.54845644658969661 ) ) ;
#5104=CARTESIAN_POINT ( 'NONE',  ( 7.696648035528455445, 40.19142276524996760, 78.71587240337095182 ) ) ;
#5105=DIRECTION ( 'NONE',  ( 0.3015081906286226077, -0.9534635866061452747, -1.245503830460468341E-16 ) ) ;
#5107=ORIENTED_EDGE ( 'NONE', *, *, #2468, .F. ) ;
#5108=CARTESIAN_POINT ( 'NONE',  ( 8.375126220672854060, 41.81456477263208882, 76.36070165242202279 ) ) ;
#5109=LINE ( 'NONE', #15338, #7480 ) ;
#5112=CARTESIAN_POINT ( 'NONE',  ( -7.783762692441060338, 41.22945570740913723, 78.68823452940202401 ) ) ;
#5114=CARTESIAN_POINT ( 'NONE',  ( 8.530649028577993676, 48.02340768410154936, 78.56977997600147035 ) ) ;
#5121=LINE ( 'NONE', #14498, #15948 ) ;
#5122=VERTEX_POINT ( 'NONE', #6875 ) ;
#5127=CARTESIAN_POINT ( 'NONE',  ( 0.4713596985539078577, 52.96647961732049481, 78.91893668031715947 ) ) ;
#5128=ORIENTED_EDGE ( 'NONE', *, *, #15102, .T. ) ;
#5129=CARTESIAN_POINT ( 'NONE',  ( -4.392497846706504561, 51.46612350181082007, 76.19049300047602458 ) ) ;
#5130=VERTEX_POINT ( 'NONE', #5270 ) ;
#5132=CARTESIAN_POINT ( 'NONE',  ( -7.508333715179515977, 40.35369624421328183, 77.67144260532384692 ) ) ;
#5133=CARTESIAN_POINT ( 'NONE',  ( -4.792503378000012582, 37.91763016944491227, 77.33669174070733732 ) ) ;
#5137=CARTESIAN_POINT ( 'NONE',  ( 5.824901997307729395, 37.13555891239614226, 76.06531707679772580 ) ) ;
#5138=CIRCLE ( 'NONE', #2108, 6.000000000000002665 ) ;
#5141=DIRECTION ( 'NONE',  ( -1.540237394707284220E-16, -1.793354297423764243E-16, 1.000000000000000000 ) ) ;
#5142=LINE ( 'NONE', #9851, #17713 ) ;
#5143=ORIENTED_EDGE ( 'NONE', *, *, #2750, .T. ) ;
#5144=CARTESIAN_POINT ( 'NONE',  ( -5.838428831739582492, 50.43291415881836315, 76.76022115247205591 ) ) ;
#5145=ADVANCED_FACE ( 'NONE', ( #6970 ), #13474, .T. ) ;
#5149=CARTESIAN_POINT ( 'NONE',  ( -4.501441463659942244, 37.86850067699155886, 75.36972643424059015 ) ) ;
#5151=AXIS2_PLACEMENT_3D ( 'NONE', #8834, #17020, #4343 ) ;
#5153=LINE ( 'NONE', #8581, #2704 ) ;
#5156=VERTEX_POINT ( 'NONE', #4958 ) ;
#5159=LINE ( 'NONE', #16462, #13495 ) ;
#5161=EDGE_CURVE ( 'NONE', #20489, #10457, #4056, .T. ) ;
#5162=CARTESIAN_POINT ( 'NONE',  ( 5.956380690854414794, 50.16371848513034593, 75.46588380158773646 ) ) ;
#5163=CARTESIAN_POINT ( 'NONE',  ( 5.848951923618479931, 37.15274410921379911, 76.58742703482498371 ) ) ;
#5164=VECTOR ( 'NONE', #4209, 1000.000000000000000 ) ;
#5165=CARTESIAN_POINT ( 'NONE',  ( -4.307690844420870135, 37.53294895003197951, 79.54647054202554557 ) ) ;
#5166=CARTESIAN_POINT ( 'NONE',  ( 5.378304226687590450, 36.81643649649897299, 75.37835156746757548 ) ) ;
#5167=VECTOR ( 'NONE', #13291, 1000.000000000000114 ) ;
#5168=EDGE_CURVE ( 'NONE', #18997, #15510, #13790, .T. ) ;
#5169=CARTESIAN_POINT ( 'NONE',  ( 7.678973061664008171, 40.17251196347450559, 78.40165754912887053 ) ) ;
#5171=CARTESIAN_POINT ( 'NONE',  ( -0.9271010316932370987, 52.23309654930653778, 78.54091960784487014 ) ) ;
#5172=CARTESIAN_POINT ( 'NONE',  ( 8.637025618647824032, 43.04385625447593355, 76.23134092453109645 ) ) ;
#5173=DIRECTION ( 'NONE',  ( 0.5670994908670485835, -0.8236492988270761595, -6.036271672687166828E-17 ) ) ;
#5176=ADVANCED_FACE ( 'NONE', ( #9122 ), #12763, .F. ) ;
#5178=EDGE_CURVE ( 'NONE', #6135, #7903, #10631, .T. ) ;
#5179=ORIENTED_EDGE ( 'NONE', *, *, #13683, .F. ) ;
#5180=CARTESIAN_POINT ( 'NONE',  ( 5.542130322670880460, 50.64142601547018785, 78.59183879953087626 ) ) ;
#5182=CARTESIAN_POINT ( 'NONE',  ( 5.522356516757287892, 50.66127187491098027, 76.02767501797669070 ) ) ;
#5183=CARTESIAN_POINT ( 'NONE',  ( 9.162426004170315608, 42.25409649015283975, 75.50722976489458915 ) ) ;
#5184=DIRECTION ( 'NONE',  ( -0.5800177190770277047, -0.8146038580541355989, -2.354238310054624259E-16 ) ) ;
#5185=EDGE_CURVE ( 'NONE', #188, #17910, #6093, .T. ) ;
#5186=DIRECTION ( 'NONE',  ( -1.540237394707284220E-16, -1.793354297423764243E-16, 1.000000000000000000 ) ) ;
#5187=DIRECTION ( 'NONE',  ( 0.007885122365278605591, 0.9999689119394085113, 1.805443505845548073E-16 ) ) ;
#5188=CARTESIAN_POINT ( 'NONE',  ( 0.8460310913591665427, 52.96352569016541878, 77.64755553332491900 ) ) ;
#5189=CARTESIAN_POINT ( 'NONE',  ( 5.901851037876958195, 51.12883029018298231, 78.62249727093715990 ) ) ;
#5190=CARTESIAN_POINT ( 'NONE',  ( 4.732847133705871734, 51.99232638384451377, 75.72008365543779007 ) ) ;
#5193=ORIENTED_EDGE ( 'NONE', *, *, #16267, .T. ) ;
#5196=CARTESIAN_POINT ( 'NONE',  ( -5.835675398032521777, 50.43488166173578691, 78.31711373209397209 ) ) ;
#5197=CARTESIAN_POINT ( 'NONE',  ( -4.519331755718375199, 37.70034496097993326, 78.77850703318271997 ) ) ;
#5198=EDGE_CURVE ( 'NONE', #6491, #13246, #9431, .T. ) ;
#5201=EDGE_CURVE ( 'NONE', #2164, #19006, #4416, .T. ) ;
#5205=CARTESIAN_POINT ( 'NONE',  ( 6.104265285658651230, 38.25495727238729415, 78.24541959536460922 ) ) ;
#5206=CARTESIAN_POINT ( 'NONE',  ( -3.495065479208315562, 36.18912478048144266, 76.62933879953087057 ) ) ;
#5207=ADVANCED_FACE ( 'NONE', ( #2832 ), #4762, .F. ) ;
#5208=CARTESIAN_POINT ( 'NONE',  ( 0.6901636094616421246, 52.96072213236104176, 75.98019638678815113 ) ) ;
#5209=VERTEX_POINT ( 'NONE', #5244 ) ;
#5210=CARTESIAN_POINT ( 'NONE',  ( -4.427139072037590495, 51.44137015048543304, 78.85744209785094938 ) ) ;
#5212=VECTOR ( 'NONE', #8182, 1000.000000000000114 ) ;
#5213=CARTESIAN_POINT ( 'NONE',  ( -4.539440361571185356, 36.96056243609647396, 78.81995494622690046 ) ) ;
#5214=VERTEX_POINT ( 'NONE', #18236 ) ;
#5216=CARTESIAN_POINT ( 'NONE',  ( 2.120143825079129574, 52.94022564282578003, 77.78911287202200242 ) ) ;
#5219=B_SPLINE_CURVE_WITH_KNOTS ( 'NONE', 3,
 ( #13781, #12194, #20481, #15813, #9009, #4203, #17091, #9223, #12308, #9112, #4510, #15599, #2612, #14195, #17189, #7715, #12411, #2514 ),
 .UNSPECIFIED., .F., .F.,
 ( 4, 2, 2, 2, 2, 2, 2, 2, 4 ),
 ( 8.673617379884035472E-19, 0.0003077246462501492027, 0.0006154492925002975380, 0.0009231739387504458733, 0.001230898585000594209, 0.001538623231250742544, 0.001846347877500890879, 0.002154072523751038998, 0.002461797170001187550 ),
 .UNSPECIFIED. ) ;
#5220=CARTESIAN_POINT ( 'NONE',  ( 8.121917471046002035, 44.10225444150351137, 75.45433879953087342 ) ) ;
#5221=EDGE_LOOP ( 'NONE', ( #9651, #13606, #10412, #918 ) ) ;
#5222=CARTESIAN_POINT ( 'NONE',  ( -4.383473025373059606, 51.47257230871590394, 78.45066232894264147 ) ) ;
#5223=VERTEX_POINT ( 'NONE', #16447 ) ;
#5224=LINE ( 'NONE', #13432, #8163 ) ;
#5226=ORIENTED_EDGE ( 'NONE', *, *, #915, .T. ) ;
#5227=B_SPLINE_CURVE_WITH_KNOTS ( 'NONE', 3,
 ( #2606, #15388, #13561, #12405, #3876, #7287, #579, #5471, #5678, #18667, #5797, #10723, #17183, #10503, #7061 ),
 .UNSPECIFIED., .F., .F.,
 ( 4, 1, 1, 1, 1, 1, 1, 1, 1, 1, 1, 1, 4 ),
 ( 0.000000000000000000, 0.1198978896105060005, 0.2272848286615199442, 0.3233685559759303385, 0.4081414772668706115, 0.4819378103613651820, 0.5435227337441967954, 0.5948163272532476231, 0.6357474925148977052, 0.7079723711143988130, 0.7877128652614201476, 0.8832591045952046249, 1.000000000000000000 ),
 .UNSPECIFIED. ) ;
#5228=CARTESIAN_POINT ( 'NONE',  ( -6.613032277150673544, 45.52591812603678534, 75.45433879953087342 ) ) ;
#5229=CARTESIAN_POINT ( 'NONE',  ( 8.707758170209565662, 40.89142814818289651, 75.40210940951681096 ) ) ;
#5230=CARTESIAN_POINT ( 'NONE',  ( -4.689916854477828245, 37.07171335984372718, 78.93589701864812014 ) ) ;
#5231=CARTESIAN_POINT ( 'NONE',  ( 0.3326973149608342673, 52.96014171822455552, 72.45433879953087342 ) ) ;
#5232=EDGE_CURVE ( 'NONE', #502, #19108, #6779, .T. ) ;
#5233=CARTESIAN_POINT ( 'NONE',  ( 0.3328022465261254448, 52.96757219375044201, 78.52223653336807274 ) ) ;
#5236=ORIENTED_EDGE ( 'NONE', *, *, #6503, .F. ) ;
#5237=CARTESIAN_POINT ( 'NONE',  ( -3.304399724198308519, 36.90940894797284955, 77.85413967038655869 ) ) ;
#5238=CARTESIAN_POINT ( 'NONE',  ( -6.731127884703168363, 40.37999424897662948, 78.06261470525505786 ) ) ;
#5239=CARTESIAN_POINT ( 'NONE',  ( -4.646812029368017072, 37.79580252097101578, 77.33278042858304957 ) ) ;
#5242=CARTESIAN_POINT ( 'NONE',  ( 5.846647460608473956, 37.15109742431862827, 76.40678776405631822 ) ) ;
#5243=EDGE_LOOP ( 'NONE', ( #5107, #7114, #16867, #4705 ) ) ;
#5244=CARTESIAN_POINT ( 'NONE',  ( -4.249412910294118717, 50.83092575845958550, 78.93669174070734584 ) ) ;
#5246=VERTEX_POINT ( 'NONE', #9850 ) ;
#5247=LINE ( 'NONE', #5144, #15651 ) ;
#5248=EDGE_CURVE ( 'NONE', #3162, #8103, #16648, .T. ) ;
#5253=CARTESIAN_POINT ( 'NONE',  ( -5.056163503743588805, 37.34224500634140043, 75.38158877174898009 ) ) ;
#5255=FACE_OUTER_BOUND ( 'NONE', #19209, .T. ) ;
#5256=CARTESIAN_POINT ( 'NONE',  ( 0.5311529524219201770, 52.96235922873796653, 76.89393617185528740 ) ) ;
#5257=ORIENTED_EDGE ( 'NONE', *, *, #16533, .T. ) ;
#5258=CARTESIAN_POINT ( 'NONE',  ( -4.753731435370094793, 37.11885062014069092, 77.91594000873737969 ) ) ;
#5261=CARTESIAN_POINT ( 'NONE',  ( 0.8256759245549851745, 52.35658408014969467, 77.54407321495646954 ) ) ;
#5262=CARTESIAN_POINT ( 'NONE',  ( 0.7793394610543057377, 52.95888126071579904, 75.36251995630715328 ) ) ;
#5264=CARTESIAN_POINT ( 'NONE',  ( 5.547294332158212882, 50.64200668057274157, 77.20373336814266452 ) ) ;
#5266=B_SPLINE_CURVE_WITH_KNOTS ( 'NONE', 3,
 ( #1719, #4884, #11303, #14476, #20942, #3202, #5100, #11618, #3515, #4988, #19467, #9, #14581, #10018, #310, #6483, #6376, #11405, #9804, #2807, #4589, #2696, #2910 ),
 .UNSPECIFIED., .F., .F.,
 ( 4, 1, 1, 1, 1, 1, 1, 1, 1, 1, 1, 1, 1, 1, 1, 1, 1, 1, 1, 1, 4 ),
 ( 0.000000000000000000, 0.05038957832574614271, 0.09924218466120336701, 0.1466944942679149211, 0.1933274803506509210, 0.2393051970681265017, 0.2845336341364397836, 0.3290963736026611408, 0.3737734709422849688, 0.4170414937111141529, 0.4581341819676884586, 0.4966705307863439889, 0.5335170563061359950, 0.5686625127317078698, 0.6026561223054673899, 0.6353294289861355360, 0.6676748031221235724, 0.7363421380907280156, 0.8138933404431207830, 0.9017813486866357309, 1.000000000000000000 ),
 .UNSPECIFIED. ) ;
#5267=DIRECTION ( 'NONE',  ( 0.009567942452863074584, -0.9999542261909885044, -1.778535306010356147E-16 ) ) ;
#5270=CARTESIAN_POINT ( 'NONE',  ( -5.838428831739582492, 50.43291415881836315, 76.76022115247205591 ) ) ;
#5271=CARTESIAN_POINT ( 'NONE',  ( 7.748486061697145821, 40.38084683439631561, 79.09910503406773330 ) ) ;
#5273=CARTESIAN_POINT ( 'NONE',  ( -0.9424882101290802394, 52.23031780077558039, 78.01134710528980065 ) ) ;
#5274=DIRECTION ( 'NONE',  ( -0.9534635866061452747, -0.3015081906286225522, -2.009271279954815797E-16 ) ) ;
#5276=ORIENTED_EDGE ( 'NONE', *, *, #16254, .T. ) ;
#5281=VERTEX_POINT ( 'NONE', #16754 ) ;
#5283=CARTESIAN_POINT ( 'NONE',  ( 9.064651367107570579, 41.96105970016846243, 75.41143022427675646 ) ) ;
#5284=DIRECTION ( 'NONE',  ( -0.5941461771851691553, -0.8043570849667760481, -2.357623395011396791E-16 ) ) ;
#5285=CARTESIAN_POINT ( 'NONE',  ( -7.376743071288316855, 41.96049357349896525, 72.45433879953085921 ) ) ;
#5287=B_SPLINE_SURFACE_WITH_KNOTS ( 'NONE', 3, 1, ( 
 ( #20931, #19150 ),
 ( #6263, #17765 ),
 ( #19246, #1706 ),
 ( #14572, #4561 ),
 ( #4978, #11083 ),
 ( #14674, #99 ),
 ( #6367, #4872 ),
 ( #1598, #2973 ),
 ( #19558, #12867 ),
 ( #12765, #19349 ),
 ( #15965, #11182 ),
 ( #9479, #11499 ),
 ( #20837, #8080 ),
 ( #4767, #3192 ),
 ( #16175, #14983 ) ),
 .UNSPECIFIED., .F., .F., .F.,
 ( 4, 1, 1, 1, 1, 1, 1, 1, 1, 1, 1, 1, 4 ),
 ( 2, 2 ),
 ( 0.000000000000000000, 0.1372453196419673171, 0.2656077965333414337, 0.3855481208555507355, 0.4976308828580581767, 0.5516434046647483713, 0.6057582083304485776, 0.6621535423365251249, 0.7211227168729713588, 0.7835375577407022174, 0.8505035567791932039, 0.9228138635028276804, 1.000000000000000000 ),
 ( 0.000000000000000000, 1.000000000000000000 ),
 .UNSPECIFIED. ) ;
#5288=CARTESIAN_POINT ( 'NONE',  ( 8.221537414170169811, 41.35424937605134943, 76.10950202369875228 ) ) ;
#5289=DIRECTION ( 'NONE',  ( -0.5954989751681698529, 0.8033560671169786005, 5.234922652618075161E-17 ) ) ;
#5290=CARTESIAN_POINT ( 'NONE',  ( 4.611425380024144260, 52.08201574212262130, 75.94315254166910734 ) ) ;
#5293=EDGE_LOOP ( 'NONE', ( #10389, #11736, #240, #1910 ) ) ;
#5294=CARTESIAN_POINT ( 'NONE',  ( 0.3284214782166970936, 52.35625353581157526, 76.35041178738960355 ) ) ;
#5296=ORIENTED_EDGE ( 'NONE', *, *, #3595, .F. ) ;
#5299=CARTESIAN_POINT ( 'NONE',  ( -2.083470957239372368, 47.45622447009557021, 79.40903933791013003 ) ) ;
#5302=CARTESIAN_POINT ( 'NONE',  ( 8.312768060858603647, 41.62767341174088642, 77.52218233473911368 ) ) ;
#5303=LINE ( 'NONE', #2134, #3491 ) ;
#5305=CARTESIAN_POINT ( 'NONE',  ( 5.869592478971509486, 51.15265838819242106, 78.02050120841747116 ) ) ;
#5307=CARTESIAN_POINT ( 'NONE',  ( 8.382617512212860333, 42.28137902014101712, 79.47377622490290605 ) ) ;
#5310=ORIENTED_EDGE ( 'NONE', *, *, #8034, .F. ) ;
#5312=LINE ( 'NONE', #10244, #9880 ) ;
#5314=ADVANCED_FACE ( 'NONE', ( #19724 ), #15053, .T. ) ;
#5315=CARTESIAN_POINT ( 'NONE',  ( 1.828298387814866865, 52.94252695135357811, 76.99833242929096855 ) ) ;
#5316=EDGE_CURVE ( 'NONE', #11104, #12307, #18138, .T. ) ;
#5319=DIRECTION ( 'NONE',  ( -0.9485903129789527988, 0.3165065846431829311, -8.934458285744989980E-17 ) ) ;
#5320=ORIENTED_EDGE ( 'NONE', *, *, #12393, .T. ) ;
#5324=ORIENTED_EDGE ( 'NONE', *, *, #11596, .T. ) ;
#5325=VECTOR ( 'NONE', #17943, 1000.000000000000000 ) ;
#5326=DIRECTION ( 'NONE',  ( -0.9539696396349547358, 0.2999031954727300886, -9.315070279690498823E-17 ) ) ;
#5327=B_SPLINE_CURVE_WITH_KNOTS ( 'NONE', 3,
 ( #2968, #14667, #1271, #7765, #12762, #3081, #14243, #15961, #1379, #9581, #17759, #20927, #6362, #14567, #12971 ),
 .UNSPECIFIED., .F., .F.,
 ( 4, 1, 1, 1, 1, 1, 1, 1, 1, 1, 1, 1, 4 ),
 ( 0.000000000000000000, 0.1159675137638946224, 0.2163545172648820292, 0.3041323377849299292, 0.3879046361115746633, 0.4329802283776429395, 0.4868190193916722697, 0.5485431915433492955, 0.6192726642024330985, 0.7001311270025748490, 0.7903233920492748199, 0.8897556754282296421, 1.000000000000000000 ),
 .UNSPECIFIED. ) ;
#5329=EDGE_CURVE ( 'NONE', #7903, #19292, #6417, .T. ) ;
#5333=CARTESIAN_POINT ( 'NONE',  ( 0.5221537403065009686, 44.16218137147968292, 79.40903933791013003 ) ) ;
#5334=FACE_OUTER_BOUND ( 'NONE', #13206, .T. ) ;
#5335=ORIENTED_EDGE ( 'NONE', *, *, #5452, .T. ) ;
#5340=CARTESIAN_POINT ( 'NONE',  ( -6.990385563023369109, 41.19984844700349669, 76.84875211988632770 ) ) ;
#5341=DIRECTION ( 'NONE',  ( 0.5670994908670431434, -0.8236492988270800453, -6.036271672687318437E-17 ) ) ;
#5342=CARTESIAN_POINT ( 'NONE',  ( 7.864691922653266332, 47.81281597943210215, 78.56977997600147035 ) ) ;
#5344=VECTOR ( 'NONE', #5443, 1000.000000000000000 ) ;
#5346=CARTESIAN_POINT ( 'NONE',  ( 8.207311740369052089, 47.02196222218739763, 75.43669174070734584 ) ) ;
#5347=ORIENTED_EDGE ( 'NONE', *, *, #3144, .T. ) ;
#5348=EDGE_CURVE ( 'NONE', #19575, #17248, #18539, .T. ) ;
#5352=ORIENTED_EDGE ( 'NONE', *, *, #534, .T. ) ;
#5353=CARTESIAN_POINT ( 'NONE',  ( -1.293305036878872993, 38.38734275159215059, 75.45433879953087342 ) ) ;
#5356=ORIENTED_EDGE ( 'NONE', *, *, #5624, .T. ) ;
#5358=CARTESIAN_POINT ( 'NONE',  ( -5.419656513257916863, 37.61074265007806616, 75.48149882193594351 ) ) ;
#5359=ORIENTED_EDGE ( 'NONE', *, *, #7426, .F. ) ;
#5362=ORIENTED_EDGE ( 'NONE', *, *, #12093, .T. ) ;
#5363=CARTESIAN_POINT ( 'NONE',  ( -4.917446439638612610, 37.23978029895120301, 77.90454030471208569 ) ) ;
#5366=CARTESIAN_POINT ( 'NONE',  ( -4.346214470222207638, 50.75228047588369407, 75.98997946140892168 ) ) ;
#5372=CARTESIAN_POINT ( 'NONE',  ( -1.293305036878872549, 38.38734275159215059, 72.45432679953087529 ) ) ;
#5373=ORIENTED_EDGE ( 'NONE', *, *, #8944, .F. ) ;
#5374=ORIENTED_EDGE ( 'NONE', *, *, #19385, .T. ) ;
#5375=CARTESIAN_POINT ( 'NONE',  ( 5.201216021426783520, 36.68989574863261538, 75.41205140984322952 ) ) ;
#5378=CARTESIAN_POINT ( 'NONE',  ( 0.5264430316339508975, 52.35469197387742923, 77.38663191694250543 ) ) ;
#5380=EDGE_LOOP ( 'NONE', ( #16768, #16972, #15957, #14788 ) ) ;
#5382=CARTESIAN_POINT ( 'NONE',  ( -3.944959226007136888, 38.51060946023304865, 76.38448585835440952 ) ) ;
#5386=CARTESIAN_POINT ( 'NONE',  ( 0.0004206109058209459473, 52.21206128023939641, 75.41772606587693417 ) ) ;
#5387=CARTESIAN_POINT ( 'NONE',  ( 8.596205818237969254, 40.55709867257476731, 75.50010622114506020 ) ) ;
#5389=LINE ( 'NONE', #16691, #12155 ) ;
#5390=CARTESIAN_POINT ( 'NONE',  ( -0.3407952795220794417, 52.92038597201553074, 75.53001665154320676 ) ) ;
#5392=CARTESIAN_POINT ( 'NONE',  ( -4.361665858399769391, 37.57520132541210245, 75.97198585835440099 ) ) ;
#5394=CARTESIAN_POINT ( 'NONE',  ( 0.5221537403065015237, 44.16218137147968292, 75.45433879953088763 ) ) ;
#5398=CARTESIAN_POINT ( 'NONE',  ( 0.3332418091178914743, 52.96755426434335590, 76.35041178738960355 ) ) ;
#5399=CIRCLE ( 'NONE', #17319, 8.199999999999995737 ) ;
#5403=CARTESIAN_POINT ( 'NONE',  ( -4.529140103682425256, 37.70758999251661692, 78.69750623079058016 ) ) ;
#5407=DIRECTION ( 'NONE',  ( -0.3165065846431827090, -0.9485903129789529098, -2.188653791613874994E-16 ) ) ;
#5408=ADVANCED_FACE ( 'NONE', ( #15580 ), #11251, .T. ) ;
#5410=VERTEX_POINT ( 'NONE', #20238 ) ;
#5411=EDGE_LOOP ( 'NONE', ( #7846, #16578, #2226, #1934 ) ) ;
#5413=CARTESIAN_POINT ( 'NONE',  ( 9.122633311574107395, 42.13483526604063201, 79.44701590970058191 ) ) ;
#5415=CARTESIAN_POINT ( 'NONE',  ( -4.197504116382902772, 37.45658124447859905, 78.86215563453255584 ) ) ;
#5416=VERTEX_POINT ( 'NONE', #5670 ) ;
#5417=DIRECTION ( 'NONE',  ( 0.9534635866061452747, 0.3015081906286223301, 5.201162577080931668E-16 ) ) ;
#5418=CARTESIAN_POINT ( 'NONE',  ( 9.353817388681445522, 42.82770861117572281, 78.41904468188381827 ) ) ;
#5422=B_SPLINE_CURVE_WITH_KNOTS ( 'NONE', 3,
 ( #9163, #12044, #2346, #4243, #20528, #5954, #15655, #12251, #7340, #13943, #10562, #2459, #1071, #5741, #10770 ),
 .UNSPECIFIED., .F., .F.,
 ( 4, 1, 1, 1, 1, 1, 1, 1, 1, 1, 1, 1, 4 ),
 ( 0.000000000000000000, 0.1112587825215290704, 0.2075697215801151074, 0.2973595701983123840, 0.3838682041569268510, 0.4304545292676484891, 0.4853887544929457731, 0.5479167518276804039, 0.6204346596782769341, 0.7008860551074163059, 0.7907659637769564043, 0.8904818903857688595, 1.000000000000000000 ),
 .UNSPECIFIED. ) ;
#5423=CARTESIAN_POINT ( 'NONE',  ( -7.232524501155468855, 41.51784650842750324, 78.89406302991613984 ) ) ;
#5424=CARTESIAN_POINT ( 'NONE',  ( -3.131747484992676078, 36.83477141872401006, 78.11242031084098869 ) ) ;
#5425=EDGE_CURVE ( 'NONE', #10288, #18561, #18873, .T. ) ;
#5428=VECTOR ( 'NONE', #14496, 1000.000000000000227 ) ;
#5429=CARTESIAN_POINT ( 'NONE',  ( -8.146098697889676998, 42.64342655637305768, 79.20824032290880723 ) ) ;
#5430=VERTEX_POINT ( 'NONE', #20178 ) ;
#5439=LINE ( 'NONE', #11954, #2829 ) ;
#5440=ADVANCED_FACE ( 'NONE', ( #10425 ), #1150, .T. ) ;
#5442=CARTESIAN_POINT ( 'NONE',  ( -3.553498346352079285, 52.06564182703182553, 79.13154374754441278 ) ) ;
#5443=DIRECTION ( 'NONE',  ( 1.540237394707284220E-16, 1.793354297423764243E-16, -1.000000000000000000 ) ) ;
#5444=CARTESIAN_POINT ( 'NONE',  ( -0.9388773962491537839, 52.84004908296358138, 77.77566232894263010 ) ) ;
#5445=CARTESIAN_POINT ( 'NONE',  ( 0.5623910665089989491, 52.35440851336043977, 78.93584868477675798 ) ) ;
#5446=ORIENTED_EDGE ( 'NONE', *, *, #7159, .T. ) ;
#5448=CARTESIAN_POINT ( 'NONE',  ( 5.748274343403733333, 51.24227120794373747, 77.94845644658968808 ) ) ;
#5449=ORIENTED_EDGE ( 'NONE', *, *, #11800, .F. ) ;
#5450=CARTESIAN_POINT ( 'NONE',  ( 2.035123479059381957, 36.10296785094195826, 76.16022115247204738 ) ) ;
#5452=EDGE_CURVE ( 'NONE', #7102, #18032, #8480, .T. ) ;
#5453=CARTESIAN_POINT ( 'NONE',  ( 0.5221537403065013017, 44.16218137147968292, 77.05433879953086773 ) ) ;
#5454=CARTESIAN_POINT ( 'NONE',  ( -7.292942379224079730, 40.11689118711894508, 78.38760373728354125 ) ) ;
#5455=FACE_OUTER_BOUND ( 'NONE', #1002, .T. ) ;
#5457=CARTESIAN_POINT ( 'NONE',  ( 5.489796880388170486, 37.64302049704706121, 76.21413800766271152 ) ) ;
#5458=CARTESIAN_POINT ( 'NONE',  ( -4.561334846378493069, 51.34547876336230843, 75.36123162944792853 ) ) ;
#5459=ORIENTED_EDGE ( 'NONE', *, *, #5040, .F. ) ;
#5460=CARTESIAN_POINT ( 'NONE',  ( 8.792941515635112282, 41.14672803835393466, 78.80099766627323277 ) ) ;
#5461=PRODUCT_DEFINITION_FORMATION_WITH_SPECIFIED_SOURCE ( 'ANY', '', #18386, .NOT_KNOWN. ) ;
#5463=DIRECTION ( 'NONE',  ( 0.8043570849675437673, -0.5941461771841298756, 1.733862608136950550E-17 ) ) ;
#5469=DIRECTION ( 'NONE',  ( -1.540237394707284220E-16, -1.793354297423764243E-16, 1.000000000000000000 ) ) ;
#5471=CARTESIAN_POINT ( 'NONE',  ( -4.785381074711875016, 51.18538353145122954, 78.79723525346945223 ) ) ;
#5472=EDGE_CURVE ( 'NONE', #867, #6210, #1043, .T. ) ;
#5475=CARTESIAN_POINT ( 'NONE',  ( 2.103244830950438349, 52.20830968050383802, 78.56392946132328348 ) ) ;
#5477=AXIS2_PLACEMENT_3D ( 'NONE', #3585, #19752, #17853 ) ;
#5478=VERTEX_POINT ( 'NONE', #17208 ) ;
#5479=CARTESIAN_POINT ( 'NONE',  ( -4.592862224480082745, 51.32295045326189609, 75.97198585835440099 ) ) ;
#5481=ADVANCED_FACE ( 'NONE', ( #5932 ), #18491, .T. ) ;
#5484=EDGE_CURVE ( 'NONE', #8638, #16327, #12112, .T. ) ;
#5486=CARTESIAN_POINT ( 'NONE',  ( -4.534948301111437985, 37.71188027398896736, 76.38448585835440952 ) ) ;
#5488=CARTESIAN_POINT ( 'NONE',  ( -3.100601612254845207, 36.80584749508156506, 78.55896582016906393 ) ) ;
#5489=B_SPLINE_CURVE_WITH_KNOTS ( 'NONE', 3,
 ( #7573, #2783, #760, #18633, #2470, #5964, #15774, #12462, #7245, #5189, #19966 ),
 .UNSPECIFIED., .F., .F.,
 ( 4, 1, 1, 1, 1, 1, 1, 1, 4 ),
 ( 0.000000000000000000, 0.1116983415361904319, 0.2084596166200352318, 0.2965296202300037876, 0.3842340601578678183, 0.4893760538913073388, 0.6260801343201788383, 0.7954079187270842732, 1.000000000000000000 ),
 .UNSPECIFIED. ) ;
#5490=ORIENTED_EDGE ( 'NONE', *, *, #2497, .F. ) ;
#5492=DIRECTION ( 'NONE',  ( 1.540237394707284220E-16, 1.793354297423764243E-16, -1.000000000000000000 ) ) ;
#5493=EDGE_LOOP ( 'NONE', ( #18846, #18145, #8443, #1222, #4319, #18397 ) ) ;
#5496=CARTESIAN_POINT ( 'NONE',  ( -5.086207797142201947, 38.17983230318012744, 75.51021574373382350 ) ) ;
#5499=VECTOR ( 'NONE', #18826, 1000.000000000000000 ) ;
#5501=VERTEX_POINT ( 'NONE', #15305 ) ;
#5502=LINE ( 'NONE', #16889, #9986 ) ;
#5503=ORIENTED_EDGE ( 'NONE', *, *, #11326, .F. ) ;
#5504=CARTESIAN_POINT ( 'NONE',  ( -3.798187483714128287, 36.41302879471073339, 77.61986069475027250 ) ) ;
#5507=CARTESIAN_POINT ( 'NONE',  ( 4.187809154542623702, 51.47009103659679852, 77.37197156638603701 ) ) ;
#5510=DIRECTION ( 'NONE',  ( -0.5941461771851691553, -0.8043570849667760481, -2.357623395011396791E-16 ) ) ;
#5511=CARTESIAN_POINT ( 'NONE',  ( 0.8455664304067509462, 52.35217556859831944, 77.76169174070734869 ) ) ;
#5512=VECTOR ( 'NONE', #9718, 1000.000000000000000 ) ;
#5514=FACE_OUTER_BOUND ( 'NONE', #19168, .T. ) ;
#5517=CARTESIAN_POINT ( 'NONE',  ( -5.769203958596529347, 48.43638519259695840, 75.45433879953087342 ) ) ;
#5519=CARTESIAN_POINT ( 'NONE',  ( 0.3281079151674232142, 52.35625600837144589, 76.41414202728766725 ) ) ;
#5521=LINE ( 'NONE', #3919, #313 ) ;
#5523=CARTESIAN_POINT ( 'NONE',  ( -3.653812822066824673, 51.99396077543343608, 79.24282704039583791 ) ) ;
#5526=CARTESIAN_POINT ( 'NONE',  ( -4.887610060180215932, 37.21774136732800997, 76.16751655709613544 ) ) ;
#5529=EDGE_CURVE ( 'NONE', #10926, #19585, #2633, .T. ) ;
#5530=CIRCLE ( 'NONE', #1807, 8.199999999999995737 ) ;
#5531=CARTESIAN_POINT ( 'NONE',  ( 3.983393151002396326, 36.72848634532711287, 75.45433879953088763 ) ) ;
#5533=CARTESIAN_POINT ( 'NONE',  ( 9.223886884231923489, 42.43829864670298946, 79.29919401074631935 ) ) ;
#5535=CARTESIAN_POINT ( 'NONE',  ( -4.159936764691080313, 37.43031352553058611, 78.66301351013966325 ) ) ;
#5538=CARTESIAN_POINT ( 'NONE',  ( 5.739698376139652503, 51.24860592950068394, 77.28905211432859801 ) ) ;
#5539=CARTESIAN_POINT ( 'NONE',  ( -8.191524702974342986, 42.93261893028977738, 75.65823721589713102 ) ) ;
#5541=CARTESIAN_POINT ( 'NONE',  ( -7.285980590069234708, 41.68689144931414603, 78.93669174070734584 ) ) ;
#5543=CARTESIAN_POINT ( 'NONE',  ( -7.088924111666181638, 47.02415304900689108, 77.58227997600145898 ) ) ;
#5546=CARTESIAN_POINT ( 'NONE',  ( -8.192078482032012943, 42.93655631659661509, 78.28007409364852265 ) ) ;
#5548=CARTESIAN_POINT ( 'NONE',  ( 1.720761564499668772, 52.27449377805036335, 75.61803672508528962 ) ) ;
#5555=DIRECTION ( 'NONE',  ( -0.3165065846431824870, -0.9485903129789529098, 0.000000000000000000 ) ) ;
#5558=CARTESIAN_POINT ( 'NONE',  ( 0.8487652345708711632, 52.95611971486915337, 77.67431885501342492 ) ) ;
#5559=CARTESIAN_POINT ( 'NONE',  ( 5.583914945631950566, 51.36367687427735973, 77.16202479023476712 ) ) ;
#5560=CARTESIAN_POINT ( 'NONE',  ( 0.4665392529312449854, 52.35516434013662490, 78.91893668031715947 ) ) ;
#5562=CARTESIAN_POINT ( 'NONE',  ( 8.215015453637320775, 41.32318875976580586, 77.19119496967930161 ) ) ;
#5564=CARTESIAN_POINT ( 'NONE',  ( 5.665287683258889651, 37.02150436742986273, 75.36022115247205022 ) ) ;
#5566=CARTESIAN_POINT ( 'NONE',  ( 6.888069329080921399, 50.40035056576664374, 77.33077842133744184 ) ) ;
#5567=CARTESIAN_POINT ( 'NONE',  ( 5.490991456512046121, 37.63909523311460248, 76.17446293557725312 ) ) ;
#5569=CARTESIAN_POINT ( 'NONE',  ( -5.888951387225212386, 37.95739186912707908, 75.98496980016291502 ) ) ;
#5571=CARTESIAN_POINT ( 'NONE',  ( 8.212727718596601889, 41.32804861490897252, 78.71078388337100762 ) ) ;
#5572=EDGE_LOOP ( 'NONE', ( #11049, #8969, #3880, #16459 ) ) ;
#5573=CARTESIAN_POINT ( 'NONE',  ( -3.795408181706389605, 50.97300633329361830, 75.39163409230444302 ) ) ;
#5576=ORIENTED_EDGE ( 'NONE', *, *, #1069, .T. ) ;
#5580=DIRECTION ( 'NONE',  ( -0.5670994908670485835, 0.8236492988270761595, 6.036271672687166828E-17 ) ) ;
#5581=LINE ( 'NONE', #15490, #2374 ) ;
#5583=LINE ( 'NONE', #16970, #20713 ) ;
#5585=ORIENTED_EDGE ( 'NONE', *, *, #16049, .F. ) ;
#5587=CARTESIAN_POINT ( 'NONE',  ( 5.162414546052650266, 37.40137004776163820, 76.01747768713747178 ) ) ;
#5591=CARTESIAN_POINT ( 'NONE',  ( 0.3792072784172939581, 52.96103218509968968, 78.83587726364804382 ) ) ;
#5594=ORIENTED_EDGE ( 'NONE', *, *, #755, .F. ) ;
#5595=ADVANCED_FACE ( 'NONE', ( #9245 ), #13590, .F. ) ;
#5597=CARTESIAN_POINT ( 'NONE',  ( 1.080293470566400904, 52.20967668552454910, 75.39315892328370694 ) ) ;
#5599=CARTESIAN_POINT ( 'NONE',  ( -0.1859286156583806748, 52.33238584150070238, 79.44675239646682030 ) ) ;
#5600=ADVANCED_FACE ( 'NONE', ( #18593 ), #18809, .F. ) ;
#5601=CARTESIAN_POINT ( 'NONE',  ( 0.3294087859111602401, 52.35624566131623681, 77.66452874556115660 ) ) ;
#5604=ORIENTED_EDGE ( 'NONE', *, *, #5624, .F. ) ;
#5605=CARTESIAN_POINT ( 'NONE',  ( 6.701747691083868474, 50.53797885426168079, 79.21482656134288902 ) ) ;
#5607=CARTESIAN_POINT ( 'NONE',  ( -3.847049756032938639, 36.44912138698024506, 77.64672866243046201 ) ) ;
#5609=CARTESIAN_POINT ( 'NONE',  ( 7.814414200452987735, 40.59520435765989532, 75.60774188071792423 ) ) ;
#5611=CARTESIAN_POINT ( 'NONE',  ( 4.584522445964598347, 52.10188785579612158, 77.22170381446332499 ) ) ;
#5614=CARTESIAN_POINT ( 'NONE',  ( 0.8412106418144055242, 52.35220991559214809, 77.64755553332491900 ) ) ;
#5615=LINE ( 'NONE', #10106, #1359 ) ;
#5618=CARTESIAN_POINT ( 'NONE',  ( 2.246318977524931704, 38.35943151540528362, 75.45433879953087342 ) ) ;
#5619=CARTESIAN_POINT ( 'NONE',  ( 8.373444093038859393, 41.80954323823455354, 78.74360054667872078 ) ) ;
#5624=EDGE_CURVE ( 'NONE', #10630, #8638, #4407, .T. ) ;
#5625=DIRECTION ( 'NONE',  ( 0.6080936526121348829, 0.7938652969193402686, 2.360290325043241787E-16 ) ) ;
#5628=CARTESIAN_POINT ( 'NONE',  ( -7.520603205048787210, 47.87625257981667914, 78.82648837639791850 ) ) ;
#5629=DIRECTION ( 'NONE',  ( 0.3165065846431827645, 0.9485903129789529098, 0.000000000000000000 ) ) ;
#5630=CARTESIAN_POINT ( 'NONE',  ( 5.542130322670884013, 50.64142601547019495, 78.27786821129558348 ) ) ;
#5632=ORIENTED_EDGE ( 'NONE', *, *, #17554, .T. ) ;
#5633=CARTESIAN_POINT ( 'NONE',  ( 6.377548835851594156, 49.90291338712703606, 77.49502509244548776 ) ) ;
#5639=CARTESIAN_POINT ( 'NONE',  ( -0.1811115068269047168, 52.93481103811284783, 79.44677385717197637 ) ) ;
#5640=CARTESIAN_POINT ( 'NONE',  ( -7.727133660016102468, 47.23791965223615819, 77.68791732120209304 ) ) ;
#5642=B_SPLINE_SURFACE_WITH_KNOTS ( 'NONE', 3, 1, ( 
 ( #11383, #14658 ),
 ( #6566, #3792 ),
 ( #5378, #14010 ),
 ( #13696, #12106 ),
 ( #8703, #12010 ),
 ( #10739, #18481 ),
 ( #2307, #20269 ),
 ( #11897, #20062 ),
 ( #5601, #5815 ),
 ( #7194, #13581 ),
 ( #9022, #18374 ) ),
 .UNSPECIFIED., .F., .F., .F.,
 ( 4, 1, 1, 1, 1, 1, 1, 1, 4 ),
 ( 2, 2 ),
 ( 0.000000000000000000, 0.1183643824554993229, 0.2230508441810244713, 0.3193022156518771082, 0.4115690293017447154, 0.5153686147994278599, 0.6444437064119312719, 0.8055807690274368049, 1.000000000000000000 ),
 ( 0.000000000000000000, 1.000000000000000000 ),
 .UNSPECIFIED. ) ;
#5643=DIRECTION ( 'NONE',  ( 1.540237394707284220E-16, 1.793354297423764243E-16, -1.000000000000000000 ) ) ;
#5644=VERTEX_POINT ( 'NONE', #2944 ) ;
#5645=CARTESIAN_POINT ( 'NONE',  ( 5.939900590116411472, 51.10072461867315496, 76.90580938776616904 ) ) ;
#5646=ORIENTED_EDGE ( 'NONE', *, *, #20564, .T. ) ;
#5647=CARTESIAN_POINT ( 'NONE',  ( -4.799400614414246036, 51.17536568166803335, 78.65631888207801126 ) ) ;
#5649=VERTEX_POINT ( 'NONE', #10949 ) ;
#5651=B_SPLINE_CURVE_WITH_KNOTS ( 'NONE', 3,
 ( #20129, #7154, #15256, #18549, #672, #10596, #5566, #18764, #883, #13758, #13543, #20229, #16850, #11965, #9087 ),
 .UNSPECIFIED., .F., .F.,
 ( 4, 1, 1, 1, 1, 1, 1, 1, 1, 1, 1, 1, 4 ),
 ( 0.000000000000000000, 0.1372453196419673171, 0.2656077965333414337, 0.3855481208555507355, 0.4976308828580581767, 0.5516434046647483713, 0.6057582083304485776, 0.6621535423365251249, 0.7211227168729713588, 0.7835375577407022174, 0.8505035567791932039, 0.9228138635028276804, 1.000000000000000000 ),
 .UNSPECIFIED. ) ;
#5652=CARTESIAN_POINT ( 'NONE',  ( 4.100190290135135029, 51.54036911970691648, 72.45433879953087342 ) ) ;
#5654=CARTESIAN_POINT ( 'NONE',  ( -3.405315259844419185, 52.17152803532113126, 78.78030711080756987 ) ) ;
#5655=CARTESIAN_POINT ( 'NONE',  ( 0.8503282811412333775, 52.95606000782370870, 77.76169174070734869 ) ) ;
#5656=CARTESIAN_POINT ( 'NONE',  ( 5.200734800563608928, 50.89208066999871249, 76.90580938776616904 ) ) ;
#5657=CARTESIAN_POINT ( 'NONE',  ( -3.198686620050343876, 36.88421666131827692, 79.01720576857120193 ) ) ;
#5659=CARTESIAN_POINT ( 'NONE',  ( 4.019338295582739029, 36.74531179668952774, 78.10496264922831244 ) ) ;
#5662=CARTESIAN_POINT ( 'NONE',  ( -4.205066710492285864, 37.45915809019812315, 75.36189689747067177 ) ) ;
#5663=CARTESIAN_POINT ( 'NONE',  ( 0.5221537403065005245, 44.16218137147968292, 82.45433879953087342 ) ) ;
#5664=CARTESIAN_POINT ( 'NONE',  ( 5.898472913175941024, 51.13132557482045826, 79.54598470662274678 ) ) ;
#5665=CARTESIAN_POINT ( 'NONE',  ( -4.517072128342571880, 36.94403992325788977, 78.34992703482498655 ) ) ;
#5667=CARTESIAN_POINT ( 'NONE',  ( 5.541475489004265675, 50.64875218668856860, 79.54599097325484536 ) ) ;
#5668=AXIS2_PLACEMENT_3D ( 'NONE', #20339, #11181, #15571 ) ;
#5670=CARTESIAN_POINT ( 'NONE',  ( 5.631785411401764918, 36.99756487055721976, 77.76022115247205591 ) ) ;
#5672=DIRECTION ( 'NONE',  ( -0.9485903129789527988, 0.3165065846431829311, -8.934458285744989980E-17 ) ) ;
#5674=VERTEX_POINT ( 'NONE', #6236 ) ;
#5678=CARTESIAN_POINT ( 'NONE',  ( -4.777409764772176715, 51.19107953768585872, 78.82882669246485818 ) ) ;
#5680=ORIENTED_EDGE ( 'NONE', *, *, #3505, .F. ) ;
#5681=CARTESIAN_POINT ( 'NONE',  ( 0.8388999841772379895, 52.35664863430569937, 79.54465842518074226 ) ) ;
#5684=ADVANCED_FACE ( 'NONE', ( #8052 ), #680, .F. ) ;
#5686=DIRECTION ( 'NONE',  ( 0.007885122365275720746, 0.9999689119394086223, 1.805443505845543882E-16 ) ) ;
#5687=DIRECTION ( 'NONE',  ( 1.540237394707284220E-16, 1.793354297423764243E-16, -1.000000000000000000 ) ) ;
#5688=LINE ( 'NONE', #12196, #3848 ) ;
#5690=CARTESIAN_POINT ( 'NONE',  ( -4.534424312541050384, 37.71149322473957000, 76.32271929704664615 ) ) ;
#5692=VECTOR ( 'NONE', #2971, 1000.000000000000000 ) ;
#5693=CARTESIAN_POINT ( 'NONE',  ( -7.390568127015174404, 42.00488250642126786, 77.49325708768887466 ) ) ;
#5694=EDGE_CURVE ( 'NONE', #11086, #20176, #1548, .T. ) ;
#5696=CARTESIAN_POINT ( 'NONE',  ( 2.038089102302941047, 52.95496222620524662, 76.00457246026148539 ) ) ;
#5698=EDGE_LOOP ( 'NONE', ( #3918, #13267, #20700, #13360 ) ) ;
#5699=CARTESIAN_POINT ( 'NONE',  ( 6.960985561621730433, 50.34649028203376275, 76.51259071708746262 ) ) ;
#5703=ADVANCED_FACE ( 'NONE', ( #20904 ), #12253, .T. ) ;
#5704=CARTESIAN_POINT ( 'NONE',  ( 5.934911976351838092, 50.19039450147929671, 79.44748646226150868 ) ) ;
#5705=ORIENTED_EDGE ( 'NONE', *, *, #2105, .F. ) ;
#5707=ADVANCED_FACE ( 'NONE', ( #1356 ), #12937, .F. ) ;
#5708=CARTESIAN_POINT ( 'NONE',  ( 2.246318977524932148, 38.35943151540528362, 72.45432679953087529 ) ) ;
#5712=CARTESIAN_POINT ( 'NONE',  ( 5.394152393224890041, 50.75790946820724514, 75.36022115247205022 ) ) ;
#5713=CARTESIAN_POINT ( 'NONE',  ( -5.917125461193805336, 40.64525615903904310, 75.45433879953087342 ) ) ;
#5715=CARTESIAN_POINT ( 'NONE',  ( -7.435644857393074680, 42.18194711778849637, 79.51259448158572241 ) ) ;
#5716=DIRECTION ( 'NONE',  ( 1.540237394707284220E-16, 1.793354297423764243E-16, -1.000000000000000000 ) ) ;
#5717=CARTESIAN_POINT ( 'NONE',  ( 0.5221537403065008576, 44.16218137147968292, 80.45433879953087342 ) ) ;
#5718=CARTESIAN_POINT ( 'NONE',  ( -5.754662135367683895, 50.49277077315122142, 75.98690818113186651 ) ) ;
#5719=CARTESIAN_POINT ( 'NONE',  ( 4.801502123416836021, 51.01678076155011610, 75.41617184184443090 ) ) ;
#5722=CARTESIAN_POINT ( 'NONE',  ( -7.956811444893308938, 41.77663113577187204, 78.52713215918005574 ) ) ;
#5723=FACE_OUTER_BOUND ( 'NONE', #3371, .T. ) ;
#5724=AXIS2_PLACEMENT_3D ( 'NONE', #12271, #20218, #16631 ) ;
#5725=VERTEX_POINT ( 'NONE', #8585 ) ;
#5727=DIRECTION ( 'NONE',  ( -0.3014917755252044529, 0.9534116768940187336, -0.01043473300065710097 ) ) ;
#5731=CARTESIAN_POINT ( 'NONE',  ( -7.607017829814316734, 43.12095717434316100, 78.33204358585338412 ) ) ;
#5732=CARTESIAN_POINT ( 'NONE',  ( 8.443422548343662015, 42.04239353520513589, 78.13669174070733447 ) ) ;
#5733=PLANE ( 'NONE',  #15287 ) ;
#5734=ORIENTED_EDGE ( 'NONE', *, *, #18091, .F. ) ;
#5737=CARTESIAN_POINT ( 'NONE',  ( 9.318068138769051600, 42.72056584129816059, 78.97126489842982267 ) ) ;
#5738=CARTESIAN_POINT ( 'NONE',  ( -3.872497565881518611, 36.46791865901509766, 75.57130654555172100 ) ) ;
#5741=CARTESIAN_POINT ( 'NONE',  ( 5.939883047636084434, 51.10073757659671401, 76.92469047792664583 ) ) ;
#5744=CARTESIAN_POINT ( 'NONE',  ( 8.491425378215518904, 42.60748309719328830, 78.02362291919803283 ) ) ;
#5746=EDGE_CURVE ( 'NONE', #20489, #3856, #1670, .T. ) ;
#5748=( BOUNDED_CURVE ( )  B_SPLINE_CURVE ( 3, ( #460, #15469, #6941, #5342 ),
 .UNSPECIFIED., .F., .F. ) 
 B_SPLINE_CURVE_WITH_KNOTS ( ( 4, 4 ),
 ( 1.414584307249941553, 1.415673517910795987 ),
 .UNSPECIFIED. ) 
 CURVE ( )  GEOMETRIC_REPRESENTATION_ITEM ( )  RATIONAL_B_SPLINE_CURVE ( ( 1.000000000000000000, 0.9999999011350138023, 0.9999999011350138023, 1.000000000000000000 ) ) 
 REPRESENTATION_ITEM ( '' )  );
#5749=CARTESIAN_POINT ( 'NONE',  ( -4.385532207686900996, 51.47110089242590902, 76.31459635612003467 ) ) ;
#5753=VECTOR ( 'NONE', #4728, 1000.000000000000227 ) ;
#5754=CARTESIAN_POINT ( 'NONE',  ( 6.490738213730996797, 37.61134109483241872, 75.55565825109377442 ) ) ;
#5756=EDGE_CURVE ( 'NONE', #20991, #13992, #1980, .T. ) ;
#5757=DIRECTION ( 'NONE',  ( 1.540237394707284220E-16, 1.793354297423764243E-16, -1.000000000000000000 ) ) ;
#5760=CARTESIAN_POINT ( 'NONE',  ( -4.432065751971962619, 50.69093429316135513, 78.79723525346945223 ) ) ;
#5764=PLANE ( 'NONE',  #5724 ) ;
#5765=VECTOR ( 'NONE', #12429, 1000.000000000000000 ) ;
#5766=AXIS2_PLACEMENT_3D ( 'NONE', #8507, #14992, #5289 ) ;
#5767=CARTESIAN_POINT ( 'NONE',  ( -3.363202728395832342, 52.20162010845611178, 78.48078762820125576 ) ) ;
#5769=CARTESIAN_POINT ( 'NONE',  ( 5.561379608955574483, 51.38032281970146897, 76.90580938776616904 ) ) ;
#5772=CYLINDRICAL_SURFACE ( 'NONE', #3070, 8.799999999999995381 ) ;
#5777=LINE ( 'NONE', #12386, #2654 ) ;
#5778=AXIS2_PLACEMENT_3D ( 'NONE', #20049, #7294, #18674 ) ;
#5781=CARTESIAN_POINT ( 'NONE',  ( -7.332874749269493009, 40.19484192575331605, 78.03982737165262051 ) ) ;
#5782=CARTESIAN_POINT ( 'NONE',  ( 3.099655065065782367, 37.00631057046153671, 72.45433879953085921 ) ) ;
#5783=CARTESIAN_POINT ( 'NONE',  ( -4.202939935851639497, 37.46040681653102666, 78.03811350732550522 ) ) ;
#5784=CARTESIAN_POINT ( 'NONE',  ( 6.443166240752919549, 49.83520380470869071, 78.90732027998019760 ) ) ;
#5785=B_SPLINE_SURFACE_WITH_KNOTS ( 'NONE', 3, 1, ( 
 ( #19501, #3546 ),
 ( #6834, #16530 ),
 ( #42, #1641 ),
 ( #18225, #346 ),
 ( #3643, #10156 ),
 ( #5129, #9950 ),
 ( #19709, #11750 ),
 ( #8233, #14721 ),
 ( #11648, #13232 ),
 ( #14921, #6728 ),
 ( #11436, #16324 ),
 ( #1950, #4813 ),
 ( #6621, #8441 ),
 ( #141, #18127 ),
 ( #16636, #13340 ) ),
 .UNSPECIFIED., .F., .F., .F.,
 ( 4, 1, 1, 1, 1, 1, 1, 1, 1, 1, 1, 1, 4 ),
 ( 2, 2 ),
 ( 0.000000000000000000, 0.1267531625455885769, 0.2402085644777646467, 0.3404273024139109483, 0.4286057740769950719, 0.5026654758471001960, 0.5652545264784208934, 0.6141369997546152204, 0.6524264903941315863, 0.7200380101346053330, 0.7961149349448265466, 0.8886173437222998350, 0.9999999999999998890 ),
 ( 0.000000000000000000, 1.000000000000000000 ),
 .UNSPECIFIED. ) ;
#5795=FACE_BOUND ( 'NONE', #4053, .T. ) ;
#5796=LINE ( 'NONE', #7060, #17622 ) ;
#5797=CARTESIAN_POINT ( 'NONE',  ( -4.744888236371026302, 51.21431823119217341, 78.89490084226201816 ) ) ;
#5798=VERTEX_POINT ( 'NONE', #19737 ) ;
#5799=CARTESIAN_POINT ( 'NONE',  ( 0.5221537403065019678, 44.16218137147968292, 72.45433879953087342 ) ) ;
#5802=ORIENTED_EDGE ( 'NONE', *, *, #5425, .F. ) ;
#5804=CARTESIAN_POINT ( 'NONE',  ( 5.077393176519246154, 37.34383885640306033, 76.55500641741416246 ) ) ;
#5806=CARTESIAN_POINT ( 'NONE',  ( 5.449567083428624947, 36.86735832482640518, 76.18683980367092090 ) ) ;
#5807=CARTESIAN_POINT ( 'NONE',  ( 5.713366999337934793, 51.26805585685155364, 78.93442753446957738 ) ) ;
#5811=DIRECTION ( 'NONE',  ( 0.007885122365275663500, 0.9999689119394085113, 1.805443505845543142E-16 ) ) ;
#5814=CARTESIAN_POINT ( 'NONE',  ( -0.2981274494836149147, 52.32174374914394122, 79.40375978592670947 ) ) ;
#5815=CARTESIAN_POINT ( 'NONE',  ( 0.3342292354559211476, 52.96756143588948618, 77.66452874556115660 ) ) ;
#5818=ORIENTED_EDGE ( 'NONE', *, *, #13819, .T. ) ;
#5820=VECTOR ( 'NONE', #5643, 1000.000000000000000 ) ;
#5823=CARTESIAN_POINT ( 'NONE',  ( 5.427780505986065762, 36.85179043424346190, 76.96022115247204454 ) ) ;
#5824=CARTESIAN_POINT ( 'NONE',  ( 7.670935877285506521, 40.16519072103186261, 76.98031643592585738 ) ) ;
#5825=ADVANCED_FACE ( 'NONE', ( #18153 ), #16666, .F. ) ;
#5826=CARTESIAN_POINT ( 'NONE',  ( 5.320112028679005789, 37.51224306767437611, 77.75838138190746918 ) ) ;
#5827=CARTESIAN_POINT ( 'NONE',  ( -6.930444918848789548, 41.01030821858960707, 79.43600262374511090 ) ) ;
#5830=CARTESIAN_POINT ( 'NONE',  ( -3.944959226007137776, 38.51060946023304865, 78.53742703482498655 ) ) ;
#5831=CARTESIAN_POINT ( 'NONE',  ( 0.6120586831527303762, 52.96175337023965568, 78.93565972088759963 ) ) ;
#5832=CARTESIAN_POINT ( 'NONE',  ( 4.881482038019723468, 51.88253576740703465, 75.58280986828056314 ) ) ;
#5836=CARTESIAN_POINT ( 'NONE',  ( -7.319506999482564780, 40.16856015084685083, 78.85321517283955473 ) ) ;
#5839=EDGE_CURVE ( 'NONE', #6821, #5209, #13563, .T. ) ;
#5841=PLANE ( 'NONE',  #12227 ) ;
#5843=CARTESIAN_POINT ( 'NONE',  ( -4.452164423840478946, 50.68111428912082772, 78.66650520056290929 ) ) ;
#5845=CARTESIAN_POINT ( 'NONE',  ( -4.806942593991912815, 37.15815555953845717, 77.31392376534303423 ) ) ;
#5846=CARTESIAN_POINT ( 'NONE',  ( -8.203676112595456260, 42.55548883657580461, 79.26478910100486530 ) ) ;
#5847=CARTESIAN_POINT ( 'NONE',  ( 8.513836386385465360, 42.32043698847956392, 78.11831813120640788 ) ) ;
#5848=EDGE_CURVE ( 'NONE', #6944, #8267, #10725, .T. ) ;
#5849=VERTEX_POINT ( 'NONE', #2289 ) ;
#5851=VECTOR ( 'NONE', #15106, 1000.000000000000000 ) ;
#5852=CARTESIAN_POINT ( 'NONE',  ( -4.469629189018287541, 37.65660658733380473, 78.89921164031883904 ) ) ;
#5853=CARTESIAN_POINT ( 'NONE',  ( -3.568428810981484567, 36.24331531840702070, 78.81697279211699936 ) ) ;
#5854=DIRECTION ( 'NONE',  ( 0.007885122365275663500, 0.9999689119394085113, 1.805443505845543142E-16 ) ) ;
#5857=CARTESIAN_POINT ( 'NONE',  ( 8.889236131602293867, 41.43532911122410667, 77.52218233473911368 ) ) ;
#5858=FACE_OUTER_BOUND ( 'NONE', #16092, .T. ) ;
#5861=CARTESIAN_POINT ( 'NONE',  ( -0.9388773962491537839, 52.84004908296358138, 77.77566232894263010 ) ) ;
#5866=CARTESIAN_POINT ( 'NONE',  ( 0.5838706545074757726, 52.36194911346490954, 78.93669174070734584 ) ) ;
#5870=CARTESIAN_POINT ( 'NONE',  ( 2.049637653786152036, 52.21875004887607474, 76.04051628124992135 ) ) ;
#5871=ORIENTED_EDGE ( 'NONE', *, *, #8972, .F. ) ;
#5872=CARTESIAN_POINT ( 'NONE',  ( -4.804534436424639843, 51.17169724042062739, 78.47639829077699858 ) ) ;
#5873=EDGE_CURVE ( 'NONE', #1868, #8638, #10401, .T. ) ;
#5876=ORIENTED_EDGE ( 'NONE', *, *, #20426, .T. ) ;
#5879=CARTESIAN_POINT ( 'NONE',  ( -0.9437706019779806832, 52.21950657494897285, 77.21536821129558348 ) ) ;
#5880=CARTESIAN_POINT ( 'NONE',  ( 8.359840211550212175, 41.80355114555996465, 78.11862058389174024 ) ) ;
#5882=CARTESIAN_POINT ( 'NONE',  ( 5.210721989228209949, 50.88470353604066787, 77.09285305542944400 ) ) ;
#5883=CARTESIAN_POINT ( 'NONE',  ( -4.374795797692404342, 37.75296113427494049, 79.54845644658969661 ) ) ;
#5884=ORIENTED_EDGE ( 'NONE', *, *, #3217, .F. ) ;
#5885=CARTESIAN_POINT ( 'NONE',  ( 5.649998448837412646, 37.01057924028687296, 77.75931883872233641 ) ) ;
#5887=ORIENTED_EDGE ( 'NONE', *, *, #3709, .F. ) ;
#5888=CARTESIAN_POINT ( 'NONE',  ( -4.359893715479207899, 37.57388776543446340, 75.36022115247205022 ) ) ;
#5891=DIRECTION ( 'NONE',  ( -0.8136266022444372803, -0.5813877811927011807, -2.295812393977109100E-16 ) ) ;
#5892=CARTESIAN_POINT ( 'NONE',  ( -4.159044950571627375, 37.42969452488605953, 78.30435701636687895 ) ) ;
#5893=CARTESIAN_POINT ( 'NONE',  ( 5.225516393853212982, 37.44489119831073509, 78.25751643855714690 ) ) ;
#5894=B_SPLINE_CURVE_WITH_KNOTS ( 'NONE', 3,
 ( #3106, #16090, #1513, #1099, #14269, #19073, #11003, #7788, #20451, #5885, #17474 ),
 .UNSPECIFIED., .F., .F.,
 ( 4, 1, 1, 1, 1, 1, 1, 1, 4 ),
 ( 0.000000000000000000, 0.1895954080786773355, 0.3480750146108056442, 0.4761617831461403827, 0.5797469728315796100, 0.6725800605763750939, 0.7701180849273350226, 0.8764776678571430946, 1.000000000000000000 ),
 .UNSPECIFIED. ) ;
#5898=VECTOR ( 'NONE', #4683, 1000.000000000000000 ) ;
#5900=EDGE_CURVE ( 'NONE', #889, #4602, #1073, .T. ) ;
#5902=CARTESIAN_POINT ( 'NONE',  ( -7.813433995296899859, 41.31607707846453792, 78.28419725522122974 ) ) ;
#5903=ORIENTED_EDGE ( 'NONE', *, *, #6533, .F. ) ;
#5907=VERTEX_POINT ( 'NONE', #13679 ) ;
#5908=CARTESIAN_POINT ( 'NONE',  ( 6.799065290779627624, 37.83166033551658103, 77.90902863000688683 ) ) ;
#5910=EDGE_LOOP ( 'NONE', ( #14645, #9514, #17185, #18195 ) ) ;
#5911=FACE_BOUND ( 'NONE', #2942, .T. ) ;
#5912=CARTESIAN_POINT ( 'NONE',  ( 0.8019475441090054835, 52.96387723590659391, 78.82560697059345500 ) ) ;
#5913=ORIENTED_EDGE ( 'NONE', *, *, #4035, .F. ) ;
#5917=AXIS2_PLACEMENT_3D ( 'NONE', #4380, #2803, #15888 ) ;
#5918=CARTESIAN_POINT ( 'NONE',  ( 5.429213800673928780, 36.85281461415114279, 76.52220546472133833 ) ) ;
#5919=CARTESIAN_POINT ( 'NONE',  ( 5.549530740019891439, 36.93878869392346331, 75.99415254657458263 ) ) ;
#5922=CARTESIAN_POINT ( 'NONE',  ( 0.8476006048031659024, 52.21151155428714219, 75.36710396340995999 ) ) ;
#5923=ORIENTED_EDGE ( 'NONE', *, *, #19042, .F. ) ;
#5925=CARTESIAN_POINT ( 'NONE',  ( -0.9436870690626151248, 52.23009998296728895, 77.21536821129558348 ) ) ;
#5928=CARTESIAN_POINT ( 'NONE',  ( -7.261062830191108652, 41.57632160563495205, 76.33871209835143645 ) ) ;
#5929=B_SPLINE_CURVE_WITH_KNOTS ( 'NONE', 3,
 ( #17520, #5928, #6233, #6025, #17617, #4432, #17417, #3049, #2843, #15831, #1242, #7736, #11259, #3570, #16040, #6652 ),
 .UNSPECIFIED., .F., .F.,
 ( 4, 2, 2, 2, 2, 2, 2, 4 ),
 ( 0.000000000000000000, 0.0007160198473685760534, 0.001432039694737152107, 0.001790049618421429671, 0.002148059542105707018, 0.002506069465789984366, 0.002685074427632146241, 0.002864079389474307250 ),
 .UNSPECIFIED. ) ;
#5930=ORIENTED_EDGE ( 'NONE', *, *, #5944, .F. ) ;
#5931=CARTESIAN_POINT ( 'NONE',  ( 5.086801335794131518, 51.73087467290688579, 79.44143248960128290 ) ) ;
#5932=FACE_OUTER_BOUND ( 'NONE', #5698, .T. ) ;
#5933=CARTESIAN_POINT ( 'NONE',  ( 7.720651971079942832, 40.31419300806396677, 75.89798363837520867 ) ) ;
#5936=CARTESIAN_POINT ( 'NONE',  ( -7.733416094750764636, 41.06364772483073011, 79.50989352969267543 ) ) ;
#5941=CARTESIAN_POINT ( 'NONE',  ( -1.440187084481237445, 38.28092143101015665, 78.25433879953088478 ) ) ;
#5943=CARTESIAN_POINT ( 'NONE',  ( -5.667418469993653396, 43.80274312437727247, 78.25433879953087057 ) ) ;
#5944=EDGE_CURVE ( 'NONE', #17793, #13982, #5583, .T. ) ;
#5945=LINE ( 'NONE', #18923, #13318 ) ;
#5946=CARTESIAN_POINT ( 'NONE',  ( 8.385938212755766230, 39.92691331981644254, 77.86095545630369941 ) ) ;
#5947=B_SPLINE_CURVE_WITH_KNOTS ( 'NONE', 3,
 ( #16397, #13091, #3607, #6585, #8305, #16812, #19777, #11718, #18189, #421, #16598, #19565, #2019, #6906, #14785, #3820 ),
 .UNSPECIFIED., .F., .F.,
 ( 4, 2, 2, 2, 2, 2, 2, 4 ),
 ( 0.000000000000000000, 0.0005979303682485993549, 0.0008968955523729210417, 0.001195860736497242728, 0.001494825920621564632, 0.001793791104745886102, 0.002092756288870208006, 0.002391721472994529692 ),
 .UNSPECIFIED. ) ;
#5948=CARTESIAN_POINT ( 'NONE',  ( -7.908914151385613600, 41.62335894602711051, 79.54737348031042643 ) ) ;
#5949=CARTESIAN_POINT ( 'NONE',  ( 0.5221537403065019678, 44.16218137147968292, 72.45433879953087342 ) ) ;
#5952=DIRECTION ( 'NONE',  ( -0.02533578529877749536, -0.9996789974703350623, -1.831801750099157041E-16 ) ) ;
#5954=CARTESIAN_POINT ( 'NONE',  ( 5.894741035747108171, 51.13408216234794423, 77.22227766523002401 ) ) ;
#5955=B_SPLINE_SURFACE_WITH_KNOTS ( 'NONE', 3, 1, ( 
 ( #13844, #20440 ),
 ( #5872, #12156 ),
 ( #11950, #20114 ),
 ( #15558, #4050 ),
 ( #5647, #10578 ),
 ( #868, #9069 ),
 ( #4259, #2673 ),
 ( #3844, #5760 ),
 ( #7138, #15452 ),
 ( #2474, #7352 ),
 ( #12267, #10471 ),
 ( #3947, #657 ),
 ( #18747, #13638 ),
 ( #17150, #8753 ),
 ( #17250, #20324 ) ),
 .UNSPECIFIED., .F., .F., .F.,
 ( 4, 1, 1, 1, 1, 1, 1, 1, 1, 1, 1, 1, 4 ),
 ( 2, 2 ),
 ( 0.000000000000000000, 0.1198978896105060005, 0.2272848286615199442, 0.3233685559759303385, 0.4081414772668706115, 0.4819378103613651820, 0.5435227337441967954, 0.5948163272532476231, 0.6357474925148977052, 0.7079723711143988130, 0.7877128652614201476, 0.8832591045952046249, 1.000000000000000000 ),
 ( 0.000000000000000000, 1.000000000000000000 ),
 .UNSPECIFIED. ) ;
#5956=CARTESIAN_POINT ( 'NONE',  ( 8.951667845840693971, 41.62244091939069790, 77.14698585835439815 ) ) ;
#5959=CARTESIAN_POINT ( 'NONE',  ( -0.9051307205072449680, 52.84566602866379981, 78.71653944640904399 ) ) ;
#5960=ORIENTED_EDGE ( 'NONE', *, *, #19907, .T. ) ;
#5961=CARTESIAN_POINT ( 'NONE',  ( 0.5981602388297567741, 52.96185312741366857, 75.36022115247205022 ) ) ;
#5962=ADVANCED_FACE ( 'NONE', ( #8902, #5911, #13881, #15391, #804, #20252 ), #20363, .T. ) ;
#5964=CARTESIAN_POINT ( 'NONE',  ( 5.873814141894775354, 51.14954001584995069, 78.86250487280319987 ) ) ;
#5965=CARTESIAN_POINT ( 'NONE',  ( -4.804644443005473775, 51.17161863374555963, 78.45066232894264147 ) ) ;
#5966=ORIENTED_EDGE ( 'NONE', *, *, #9221, .F. ) ;
#5972=CARTESIAN_POINT ( 'NONE',  ( 8.804199926738755622, 41.18047021065184055, 77.88643322029270166 ) ) ;
#5974=DIRECTION ( 'NONE',  ( 0.5800177190770223756, 0.8146038580541392626, 2.354238310054622780E-16 ) ) ;
#5975=CARTESIAN_POINT ( 'NONE',  ( -4.323846805489822032, 36.80131216085734280, 79.51042285023450518 ) ) ;
#5976=ORIENTED_EDGE ( 'NONE', *, *, #17975, .T. ) ;
#5977=ADVANCED_FACE ( 'NONE', ( #14191 ), #7712, .F. ) ;
#5978=DIRECTION ( 'NONE',  ( 0.5813877811927012917, -0.8136266022444372803, -5.636455622144620416E-17 ) ) ;
#5979=EDGE_CURVE ( 'NONE', #10089, #16685, #4507, .T. ) ;
#5981=CARTESIAN_POINT ( 'NONE',  ( -3.352688059453197589, 36.93499797900584980, 75.66110898724838307 ) ) ;
#5983=DIRECTION ( 'NONE',  ( 1.540237394707284220E-16, 1.793354297423764243E-16, -1.000000000000000000 ) ) ;
#5984=LINE ( 'NONE', #2998, #12699 ) ;
#5985=PLANE ( 'NONE',  #19318 ) ;
#5987=CARTESIAN_POINT ( 'NONE',  ( -5.810228987958474534, 37.89924280392040856, 75.80435357840198662 ) ) ;
#5988=EDGE_CURVE ( 'NONE', #20868, #14733, #9420, .T. ) ;
#5989=EDGE_CURVE ( 'NONE', #12039, #3841, #16115, .T. ) ;
#5991=CARTESIAN_POINT ( 'NONE',  ( 4.597613975033692846, 52.09221767063174013, 78.17666347917207759 ) ) ;
#5997=CARTESIAN_POINT ( 'NONE',  ( -1.117719678584871090, 36.12782917792895176, 76.16022115247204738 ) ) ;
#6000=LINE ( 'NONE', #12801, #12002 ) ;
#6001=CARTESIAN_POINT ( 'NONE',  ( 0.5221537403065010796, 44.16218137147968292, 78.32492703482499508 ) ) ;
#6002=CARTESIAN_POINT ( 'NONE',  ( 5.379940827581942919, 50.75970839669936652, 75.97198585835440099 ) ) ;
#6003=VERTEX_POINT ( 'NONE', #14095 ) ;
#6005=CARTESIAN_POINT ( 'NONE',  ( 0.5886303428198357279, 52.96555932043412440, 78.93669174070734584 ) ) ;
#6006=ORIENTED_EDGE ( 'NONE', *, *, #10629, .F. ) ;
#6007=CARTESIAN_POINT ( 'NONE',  ( -4.537099264183359182, 37.70896829297682729, 78.53742703482498655 ) ) ;
#6013=CARTESIAN_POINT ( 'NONE',  ( 8.849350546267242379, 41.31578948168061061, 75.97436175383765544 ) ) ;
#6014=DIRECTION ( 'NONE',  ( -0.003146157466721092449, 0.009949137952083964009, 0.9999455566915655957 ) ) ;
#6016=CARTESIAN_POINT ( 'NONE',  ( 1.645479938302748302, 52.89041620713354064, 76.88712749246440126 ) ) ;
#6017=VERTEX_POINT ( 'NONE', #20670 ) ;
#6018=CARTESIAN_POINT ( 'NONE',  ( 0.4007422551837632740, 52.36478753559008226, 79.54789450279270113 ) ) ;
#6019=CARTESIAN_POINT ( 'NONE',  ( -0.9120904517194043937, 52.23579355909702571, 76.19475685965670664 ) ) ;
#6021=VERTEX_POINT ( 'NONE', #14406 ) ;
#6022=ORIENTED_EDGE ( 'NONE', *, *, #1689, .F. ) ;
#6023=AXIS2_PLACEMENT_3D ( 'NONE', #8179, #3494, #5184 ) ;
#6024=CARTESIAN_POINT ( 'NONE',  ( -3.138905401831777908, 36.85087662531303465, 75.96390267329995538 ) ) ;
#6025=CARTESIAN_POINT ( 'NONE',  ( -7.100878668512206282, 41.13669111622050423, 76.88078815947486078 ) ) ;
#6027=CARTESIAN_POINT ( 'NONE',  ( 2.029186242314200861, 35.35002428291939225, 76.16022115247204738 ) ) ;
#6029=CARTESIAN_POINT ( 'NONE',  ( 7.670764403146932864, 40.16467680216042169, 77.13595644658970230 ) ) ;
#6030=ORIENTED_EDGE ( 'NONE', *, *, #13251, .T. ) ;
#6031=CARTESIAN_POINT ( 'NONE',  ( -4.517072128342571880, 36.94403992325788977, 78.34992703482498655 ) ) ;
#6032=CARTESIAN_POINT ( 'NONE',  ( -7.419646991370012934, 40.07141128159558008, 78.50801527011910252 ) ) ;
#6033=CARTESIAN_POINT ( 'NONE',  ( -4.811608766808348037, 37.16160227343304712, 79.54845644658969661 ) ) ;
#6035=FACE_OUTER_BOUND ( 'NONE', #8624, .T. ) ;
#6036=CIRCLE ( 'NONE', #2298, 8.199999999999995737 ) ;
#6037=CARTESIAN_POINT ( 'NONE',  ( 6.047224684482838342, 38.10257960454464410, 78.30195251056140648 ) ) ;
#6042=ORIENTED_EDGE ( 'NONE', *, *, #16509, .T. ) ;
#6043=CARTESIAN_POINT ( 'NONE',  ( 8.616653853821931719, 45.47331367307960193, 79.47125056423675460 ) ) ;
#6045=CARTESIAN_POINT ( 'NONE',  ( 5.588830122182042004, 51.36004623135520575, 76.07177712439327877 ) ) ;
#6049=CARTESIAN_POINT ( 'NONE',  ( -7.570386300417477621, 43.00511677435682145, 78.99227765976493743 ) ) ;
#6050=CARTESIAN_POINT ( 'NONE',  ( 5.729336661111230633, 37.06727142202039715, 75.98270377909689444 ) ) ;
#6051=ORIENTED_EDGE ( 'NONE', *, *, #12953, .F. ) ;
#6052=DIRECTION ( 'NONE',  ( 0.007885122365275663500, 0.9999689119394085113, 1.805443505845543142E-16 ) ) ;
#6054=CARTESIAN_POINT ( 'NONE',  ( 8.882424425600639495, 41.41491399621057923, 75.97389479739716478 ) ) ;
#6056=CARTESIAN_POINT ( 'NONE',  ( 5.254031822315176292, 50.85423277236746742, 78.06835901908682729 ) ) ;
#6057=CARTESIAN_POINT ( 'NONE',  ( -4.205412028552263592, 50.86240891746721360, 78.93510015035742811 ) ) ;
#6058=FACE_OUTER_BOUND ( 'NONE', #12392, .T. ) ;
#6061=DIRECTION ( 'NONE',  ( -0.3165065846431827645, -0.9485903129789529098, 0.000000000000000000 ) ) ;
#6063=EDGE_CURVE ( 'NONE', #8766, #12382, #15641, .T. ) ;
#6064=CARTESIAN_POINT ( 'NONE',  ( -3.567022099613818664, 37.05453471803580356, 77.68963291717793140 ) ) ;
#6066=CARTESIAN_POINT ( 'NONE',  ( -0.1994209430448784792, 35.36759766960258844, 76.86610350541323555 ) ) ;
#6068=ORIENTED_EDGE ( 'NONE', *, *, #16493, .F. ) ;
#6070=VECTOR ( 'NONE', #6698, 1000.000000000000114 ) ;
#6071=CARTESIAN_POINT ( 'NONE',  ( -0.9338558694244919467, 52.21942839363907041, 76.50701133828320621 ) ) ;
#6072=CARTESIAN_POINT ( 'NONE',  ( -4.453436368711327198, 50.68011839687689957, 76.44036821129557779 ) ) ;
#6074=CARTESIAN_POINT ( 'NONE',  ( 0.8331116901989662482, 52.96370389921568034, 76.10706146582900544 ) ) ;
#6075=CARTESIAN_POINT ( 'NONE',  ( -3.752375145463847428, 37.29320407110694191, 79.48068319027247242 ) ) ;
#6076=ORIENTED_EDGE ( 'NONE', *, *, #14130, .T. ) ;
#6077=CARTESIAN_POINT ( 'NONE',  ( 3.983393151002396326, 36.72848634532711287, 72.45433879953087342 ) ) ;
#6079=ORIENTED_EDGE ( 'NONE', *, *, #2220, .F. ) ;
#6083=CARTESIAN_POINT ( 'NONE',  ( -4.506141062785093965, 37.68465281199856065, 77.90783589451615399 ) ) ;
#6084=CARTESIAN_POINT ( 'NONE',  ( -3.349688636638950889, 52.21127678364309332, 76.69845644658968808 ) ) ;
#6087=DIRECTION ( 'NONE',  ( 1.540237394707284220E-16, 1.793354297423764243E-16, -1.000000000000000000 ) ) ;
#6088=ADVANCED_FACE ( 'NONE', ( #11336 ), #5785, .T. ) ;
#6089=ADVANCED_FACE ( 'NONE', ( #6519 ), #11539, .T. ) ;
#6091=CARTESIAN_POINT ( 'NONE',  ( -2.981657746618395333, 51.55448260090251722, 76.06019729239972094 ) ) ;
#6093=B_SPLINE_CURVE_WITH_KNOTS ( 'NONE', 3,
 ( #2523, #4211, #15921, #7935, #1341, #2930, #17606, #12723, #1550, #12819, #9433, #9649, #19302, #19107, #14106, #9335 ),
 .UNSPECIFIED., .F., .F.,
 ( 4, 2, 2, 2, 2, 2, 2, 4 ),
 ( 0.000000000000000000, 0.0003384834742446624664, 0.0005077252113669950820, 0.0006769669484893277517, 0.0007615878170504936529, 0.0008462086856116595541, 0.001015450422733994284, 0.001353933896978663960 ),
 .UNSPECIFIED. ) ;
#6095=CARTESIAN_POINT ( 'NONE',  ( 4.539372959821318609, 52.13523796247791608, 76.58963291717793709 ) ) ;
#6098=CARTESIAN_POINT ( 'NONE',  ( -5.381123819449237899, 50.75968757759591909, 79.33884456587460932 ) ) ;
#6100=CARTESIAN_POINT ( 'NONE',  ( 5.566326199328858415, 51.37666897265353327, 76.21945306000542075 ) ) ;
#6101=EDGE_CURVE ( 'NONE', #2938, #10515, #4915, .T. ) ;
#6108=CARTESIAN_POINT ( 'NONE',  ( -2.073200253767597978, 36.38374080505226971, 75.45433879953088763 ) ) ;
#6114=CARTESIAN_POINT ( 'NONE',  ( 5.443310442819001338, 36.86288755851700927, 76.23948081211554495 ) ) ;
#6115=CARTESIAN_POINT ( 'NONE',  ( -3.899663497332589213, 36.48798503826752437, 77.67016408458685817 ) ) ;
#6116=ORIENTED_EDGE ( 'NONE', *, *, #16529, .T. ) ;
#6117=CARTESIAN_POINT ( 'NONE',  ( 2.104760201255253538, 52.95427431201078150, 78.60861935269869605 ) ) ;
#6119=CARTESIAN_POINT ( 'NONE',  ( -3.462746425278574680, 37.07926700246258633, 77.72081520951157074 ) ) ;
#6121=ORIENTED_EDGE ( 'NONE', *, *, #11269, .F. ) ;
#6123=ADVANCED_FACE ( 'NONE', ( #454 ), #15038, .T. ) ;
#6124=CARTESIAN_POINT ( 'NONE',  ( 5.296683126097495808, 37.50502847857675448, 77.75931883872233641 ) ) ;
#6126=B_SPLINE_SURFACE_WITH_KNOTS ( 'NONE', 3, 1, ( 
 ( #20076, #10105 ),
 ( #10534, #18497 ),
 ( #2008, #18181 ),
 ( #8505, #19963 ),
 ( #17004, #16898 ),
 ( #725, #19866 ),
 ( #10327, #3908 ),
 ( #8617, #5288 ),
 ( #11802, #10433 ),
 ( #7206, #18278 ),
 ( #833, #16695 ),
 ( #20184, #7319 ),
 ( #13808, #2118 ),
 ( #508, #6986 ),
 ( #8715, #13491 ) ),
 .UNSPECIFIED., .F., .F., .F.,
 ( 4, 1, 1, 1, 1, 1, 1, 1, 1, 1, 1, 1, 4 ),
 ( 2, 2 ),
 ( 0.000000000000000000, 0.1107947361882193060, 0.2116365373969002206, 0.3025951166517907298, 0.3827141919669941328, 0.4557983700405009997, 0.5187458605491411801, 0.5729830782426720281, 0.6198356358567430613, 0.7053145269299332387, 0.7944869293383459707, 0.8901174066118697770, 1.000000000000000000 ),
 ( 0.000000000000000000, 1.000000000000000000 ),
 .UNSPECIFIED. ) ;
#6127=CARTESIAN_POINT ( 'NONE',  ( -0.8071739151948656987, 40.17810205696807913, 79.40903933791013003 ) ) ;
#6129=VERTEX_POINT ( 'NONE', #17807 ) ;
#6130=VECTOR ( 'NONE', #11504, 1000.000000000000000 ) ;
#6132=CARTESIAN_POINT ( 'NONE',  ( -1.293305036878872549, 38.38734275159215059, 72.45433879953085921 ) ) ;
#6134=CARTESIAN_POINT ( 'NONE',  ( -5.389442353508429484, 49.84491604607124771, 76.26826950560264606 ) ) ;
#6135=VERTEX_POINT ( 'NONE', #1754 ) ;
#6136=CARTESIAN_POINT ( 'NONE',  ( 4.649988366678187823, 51.13951581206499952, 79.44143248960128290 ) ) ;
#6137=CARTESIAN_POINT ( 'NONE',  ( 8.863132018971368709, 41.35709342965520818, 77.52392363563762956 ) ) ;
#6141=CARTESIAN_POINT ( 'NONE',  ( 5.700162184304335966, 50.52331579763416869, 75.37176668953071612 ) ) ;
#6142=CARTESIAN_POINT ( 'NONE',  ( -6.751500244480902246, 40.44442896114340158, 79.01214282451080351 ) ) ;
#6143=CARTESIAN_POINT ( 'NONE',  ( 6.403592332820982946, 38.44823507962264841, 76.00831143408265689 ) ) ;
#6146=CARTESIAN_POINT ( 'NONE',  ( 6.450247442662826458, 38.49669771550791353, 77.26022115247205591 ) ) ;
#6149=CARTESIAN_POINT ( 'NONE',  ( -0.2726345245567728393, 52.97463310108326340, 79.40856224512604911 ) ) ;
#6150=ORIENTED_EDGE ( 'NONE', *, *, #1300, .F. ) ;
#6153=CARTESIAN_POINT ( 'NONE',  ( 5.570264759168902735, 51.37375971715457013, 76.17377400622436312 ) ) ;
#6155=ORIENTED_EDGE ( 'NONE', *, *, #13213, .T. ) ;
#6157=VERTEX_POINT ( 'NONE', #5448 ) ;
#6159=CARTESIAN_POINT ( 'NONE',  ( -5.531051774427890422, 44.10426199826898142, 72.45433879953085921 ) ) ;
#6161=LINE ( 'NONE', #4559, #17121 ) ;
#6162=CARTESIAN_POINT ( 'NONE',  ( 8.876519138579782364, 41.39721547638464472, 77.52397343602532942 ) ) ;
#6163=VECTOR ( 'NONE', #6271, 1000.000000000000114 ) ;
#6164=CARTESIAN_POINT ( 'NONE',  ( 9.353599821682333726, 42.82705654907719151, 77.11956464767864361 ) ) ;
#6165=PLANE ( 'NONE',  #19638 ) ;
#6166=CARTESIAN_POINT ( 'NONE',  ( 5.205086686352852432, 50.89348831148397778, 76.20630380245266622 ) ) ;
#6169=EDGE_CURVE ( 'NONE', #11401, #11113, #10199, .T. ) ;
#6174=LINE ( 'NONE', #17358, #10222 ) ;
#6177=CARTESIAN_POINT ( 'NONE',  ( 5.901490163600553451, 51.12909685347405286, 78.67852979887695142 ) ) ;
#6178=CARTESIAN_POINT ( 'NONE',  ( -0.9427404655910675002, 52.21949845194497897, 76.89011419028814487 ) ) ;
#6179=CARTESIAN_POINT ( 'NONE',  ( 8.425866390803962602, 42.00143579340615929, 78.13577067582016866 ) ) ;
#6180=CARTESIAN_POINT ( 'NONE',  ( -4.453436368711328974, 50.68011839687689957, 78.45066232894264147 ) ) ;
#6181=CARTESIAN_POINT ( 'NONE',  ( 0.5705748789227172990, 52.35433120667131135, 75.97198585835440099 ) ) ;
#6183=EDGE_LOOP ( 'NONE', ( #10909, #3666, #2404, #4188 ) ) ;
#6184=CARTESIAN_POINT ( 'NONE',  ( 8.292349522058055200, 41.56647775562769453, 75.97198585835440099 ) ) ;
#6185=ORIENTED_EDGE ( 'NONE', *, *, #6387, .T. ) ;
#6187=EDGE_CURVE ( 'NONE', #10035, #8755, #4174, .T. ) ;
#6188=CARTESIAN_POINT ( 'NONE',  ( 6.457023732898393042, 39.40536329938229443, 72.45432679953087529 ) ) ;
#6189=CARTESIAN_POINT ( 'NONE',  ( 0.3292270019246527069, 52.35991533748182292, 76.18796821092257687 ) ) ;
#6191=CARTESIAN_POINT ( 'NONE',  ( 5.824901997307729395, 37.13555891239614226, 76.06531707679772580 ) ) ;
#6195=CARTESIAN_POINT ( 'NONE',  ( 4.715683878568929011, 52.00500418903608590, 77.90619853385557292 ) ) ;
#6196=VERTEX_POINT ( 'NONE', #7150 ) ;
#6197=DIRECTION ( 'NONE',  ( -0.5941461771851691553, -0.8043570849667760481, -2.357623395011396791E-16 ) ) ;
#6198=EDGE_CURVE ( 'NONE', #5069, #1854, #15362, .T. ) ;
#6200=CARTESIAN_POINT ( 'NONE',  ( 4.661142417382979630, 52.04529176935007939, 75.82370277575662953 ) ) ;
#6201=ORIENTED_EDGE ( 'NONE', *, *, #15051, .F. ) ;
#6202=CARTESIAN_POINT ( 'NONE',  ( -5.400510509167274265, 49.82588755935344693, 78.31711373209397209 ) ) ;
#6203=DIRECTION ( 'NONE',  ( 1.540237394707284220E-16, 1.793354297423764243E-16, -1.000000000000000000 ) ) ;
#6206=B_SPLINE_CURVE_WITH_KNOTS ( 'NONE', 3,
 ( #2770, #19241, #10978, #17343, #7869, #7764, #14358, #14242, #9161, #15653, #12760, #12355 ),
 .UNSPECIFIED., .F., .F.,
 ( 4, 2, 2, 2, 2, 4 ),
 ( 0.000000000000000000, 0.0001655740708910906161, 0.0003311481417821812321, 0.0004139351772277070516, 0.0004967222126732328711, 0.0006622962835642647777 ),
 .UNSPECIFIED. ) ;
#6207=FACE_OUTER_BOUND ( 'NONE', #11570, .T. ) ;
#6208=CARTESIAN_POINT ( 'NONE',  ( -4.061474658916792713, 50.95574512005268275, 78.82303764823565473 ) ) ;
#6209=FACE_BOUND ( 'NONE', #7670, .T. ) ;
#6210=VERTEX_POINT ( 'NONE', #2581 ) ;
#6214=CARTESIAN_POINT ( 'NONE',  ( 4.140412088821458170, 51.51591928153320765, 78.46169174070733732 ) ) ;
#6216=CARTESIAN_POINT ( 'NONE',  ( 0.8503282811412331554, 52.95606000782370870, 78.52566232894263010 ) ) ;
#6218=CARTESIAN_POINT ( 'NONE',  ( 5.497686461428984650, 36.90174267058258550, 76.03636210503219672 ) ) ;
#6219=CARTESIAN_POINT ( 'NONE',  ( -3.944959226007137776, 38.51060946023304865, 78.18375056423674607 ) ) ;
#6220=VECTOR ( 'NONE', #10925, 1000.000000000000227 ) ;
#6221=CARTESIAN_POINT ( 'NONE',  ( -3.607485548685021914, 36.27216495724724155, 77.44024473021482891 ) ) ;
#6222=ORIENTED_EDGE ( 'NONE', *, *, #13956, .T. ) ;
#6223=CARTESIAN_POINT ( 'NONE',  ( 2.112089635657790954, 52.20154156089598274, 78.36218633565054859 ) ) ;
#6226=LINE ( 'NONE', #12727, #15370 ) ;
#6231=CARTESIAN_POINT ( 'NONE',  ( -4.169456222845758120, 37.61210300367680048, 75.36135576041903050 ) ) ;
#6232=LINE ( 'NONE', #8048, #669 ) ;
#6233=CARTESIAN_POINT ( 'NONE',  ( -7.210177143685434942, 41.42808673320669755, 76.51871785122798997 ) ) ;
#6234=ORIENTED_EDGE ( 'NONE', *, *, #20564, .F. ) ;
#6235=CARTESIAN_POINT ( 'NONE',  ( -4.517625420443600603, 36.94444861784495515, 76.85096240152589075 ) ) ;
#6236=CARTESIAN_POINT ( 'NONE',  ( 5.740585635973905809, 51.24795054640212300, 75.97198585835440099 ) ) ;
#6240=FACE_OUTER_BOUND ( 'NONE', #1314, .T. ) ;
#6241=CARTESIAN_POINT ( 'NONE',  ( 5.748274343403733333, 51.24227120794373747, 77.94845644658968808 ) ) ;
#6242=CARTESIAN_POINT ( 'NONE',  ( 5.925147347628167971, 37.99321178357424600, 75.45609877704765722 ) ) ;
#6245=EDGE_CURVE ( 'NONE', #12496, #12950, #15545, .T. ) ;
#6246=CARTESIAN_POINT ( 'NONE',  ( -4.652687709939232086, 51.28020135170361016, 75.36022115247205022 ) ) ;
#6247=CARTESIAN_POINT ( 'NONE',  ( 0.9516664821082820858, 52.34032181963752350, 76.77464780632124075 ) ) ;
#6248=ADVANCED_FACE ( 'NONE', ( #13755 ), #5772, .T. ) ;
#6250=EDGE_CURVE ( 'NONE', #14881, #12080, #8493, .T. ) ;
#6251=CARTESIAN_POINT ( 'NONE',  ( -0.5458045384150788104, 52.97678714703417313, 79.25925238658010130 ) ) ;
#6254=CARTESIAN_POINT ( 'NONE',  ( 8.390051116449676272, 39.93923995310483832, 78.49952087821802138 ) ) ;
#6255=CARTESIAN_POINT ( 'NONE',  ( 8.787829143201870252, 41.13140593384865440, 76.40801527011910821 ) ) ;
#6258=CARTESIAN_POINT ( 'NONE',  ( -4.511982275096481310, 37.68935279624734846, 78.82711781305037846 ) ) ;
#6262=CARTESIAN_POINT ( 'NONE',  ( 8.933414522996312002, 41.56773455285687646, 77.44430071719698105 ) ) ;
#6263=CARTESIAN_POINT ( 'NONE',  ( 6.961260622506120654, 50.34628710563859499, 76.69700829373513784 ) ) ;
#6265=CARTESIAN_POINT ( 'NONE',  ( 6.960985561621730433, 50.34649028203376275, 76.51259071708746262 ) ) ;
#6268=EDGE_CURVE ( 'NONE', #11304, #17122, #879, .T. ) ;
#6269=CARTESIAN_POINT ( 'NONE',  ( -4.811608766808351589, 37.16160227343304712, 79.54845644658969661 ) ) ;
#6270=DIRECTION ( 'NONE',  ( 0.3165065846431827645, 0.9485903129789529098, 0.000000000000000000 ) ) ;
#6271=DIRECTION ( 'NONE',  ( -0.9485903129789527988, 0.3165065846431829311, -8.934458285744989980E-17 ) ) ;
#6275=ORIENTED_EDGE ( 'NONE', *, *, #19507, .T. ) ;
#6276=CARTESIAN_POINT ( 'NONE',  ( -0.6425283709582511049, 52.97632458963546753, 75.74123345422913189 ) ) ;
#6277=B_SPLINE_CURVE_WITH_KNOTS ( 'NONE', 3,
 ( #14773, #3188, #7977, #9693, #14462, #17967, #9789, #12863, #8394, #8181, #17860, #16171, #19343, #19658, #1594, #14568 ),
 .UNSPECIFIED., .F., .F.,
 ( 4, 2, 2, 2, 2, 2, 2, 4 ),
 ( 8.673617379884035472E-19, 0.0005211411850466844947, 0.0007817117775700237062, 0.001042282370093363135, 0.001302852962616702238, 0.001563423555140041558, 0.001823994147663380878, 0.002084564740186720198 ),
 .UNSPECIFIED. ) ;
#6278=CARTESIAN_POINT ( 'NONE',  ( 8.439922054675561114, 42.04356150970401984, 78.13669174070733447 ) ) ;
#6279=CARTESIAN_POINT ( 'NONE',  ( 6.046986631774924348, 37.29425246114896453, 78.37121987722640881 ) ) ;
#6280=CARTESIAN_POINT ( 'NONE',  ( -5.530828587017968978, 50.65271403173267117, 79.22855648223701053 ) ) ;
#6282=ORIENTED_EDGE ( 'NONE', *, *, #13239, .F. ) ;
#6284=ORIENTED_EDGE ( 'NONE', *, *, #6361, .F. ) ;
#6285=LINE ( 'NONE', #14383, #16255 ) ;
#6287=DIRECTION ( 'NONE',  ( 0.9485903129789527988, -0.3165065846431829311, 8.934458285744989980E-17 ) ) ;
#6289=CARTESIAN_POINT ( 'NONE',  ( -4.209923912819721892, 38.70632820095286775, 77.33669174070733732 ) ) ;
#6290=B_SPLINE_SURFACE_WITH_KNOTS ( 'NONE', 3, 1, ( 
 ( #4768, #3288 ),
 ( #13189, #19559 ),
 ( #11606, #4979 ),
 ( #9907, #19662 ),
 ( #18082, #1907 ),
 ( #8399, #4431 ),
 ( #10944, #7945 ),
 ( #2939, #17311 ),
 ( #6024, #1146 ),
 ( #9445, #12734 ),
 ( #12831, #4317 ),
 ( #4529, #1459 ),
 ( #11046, #15931 ),
 ( #18905, #15728 ),
 ( #20804, #2737 ),
 ( #19311, #4626 ),
 ( #19211, #1351 ),
 ( #11147, #4727 ),
 ( #7633, #14428 ),
 ( #17416, #10843 ),
 ( #7843, #14325 ),
 ( #9345, #2842 ),
 ( #7734, #15830 ),
 ( #1241, #20898 ),
 ( #6231, #9239 ),
 ( #12523, #14114 ),
 ( #17615, #3047 ) ),
 .UNSPECIFIED., .F., .F., .F.,
 ( 4, 1, 1, 1, 1, 1, 1, 1, 1, 1, 1, 1, 1, 1, 1, 1, 1, 1, 1, 1, 1, 1, 1, 1, 4 ),
 ( 2, 2 ),
 ( 0.000000000000000000, 0.04981064803454772483, 0.09714544705284619552, 0.1414600528990057893, 0.1834992459999073566, 0.2227657660311612720, 0.2600403684493295953, 0.2949019026928859644, 0.3281718573768891978, 0.3602550803352915776, 0.3926260793274650163, 0.4253773651182169435, 0.4592860034499685606, 0.4939555262694102500, 0.5299277977440765008, 0.5677681756169172811, 0.6073809588441169138, 0.6486765994917140787, 0.6919144726687150859, 0.7374495574558619371, 0.7851062196494249523, 0.8349986418379958808, 0.8875444209637680659, 0.9425288195084158271, 1.000000000000000000 ),
 ( 0.000000000000000000, 1.000000000000000000 ),
 .UNSPECIFIED. ) ;
#6291=ORIENTED_EDGE ( 'NONE', *, *, #3722, .F. ) ;
#6292=CARTESIAN_POINT ( 'NONE',  ( 4.837856207073459203, 51.91476041137136832, 77.79664654212120922 ) ) ;
#6295=LINE ( 'NONE', #12489, #12568 ) ;
#6297=CARTESIAN_POINT ( 'NONE',  ( -7.826013883771545387, 41.35585863650159411, 78.20300316143082853 ) ) ;
#6298=VERTEX_POINT ( 'NONE', #7364 ) ;
#6299=ADVANCED_FACE ( 'NONE', ( #12166 ), #20224, .T. ) ;
#6300=CARTESIAN_POINT ( 'NONE',  ( -5.761564881245698544, 50.48783832367244884, 78.87652712212219797 ) ) ;
#6302=CARTESIAN_POINT ( 'NONE',  ( -4.539440361571186244, 36.96056243609646685, 78.81995494622690046 ) ) ;
#6303=CARTESIAN_POINT ( 'NONE',  ( 5.259329269783745708, 50.84879929591499348, 76.01203914421944319 ) ) ;
#6307=CARTESIAN_POINT ( 'NONE',  ( 0.7959481941832846630, 52.35792193448483545, 76.79590682236855059 ) ) ;
#6308=ORIENTED_EDGE ( 'NONE', *, *, #10579, .F. ) ;
#6310=DIRECTION ( 'NONE',  ( 0.3165065846431827645, 0.9485903129789529098, 0.000000000000000000 ) ) ;
#6311=CARTESIAN_POINT ( 'NONE',  ( -5.400724308821385655, 49.82590620323193065, 76.54939005541714891 ) ) ;
#6315=AXIS2_PLACEMENT_3D ( 'NONE', #7009, #18517, #15010 ) ;
#6316=CARTESIAN_POINT ( 'NONE',  ( -3.115445724116070902, 36.83354790639791077, 77.32142682847380399 ) ) ;
#6317=ORIENTED_EDGE ( 'NONE', *, *, #3709, .T. ) ;
#6318=CARTESIAN_POINT ( 'NONE',  ( 2.098825451632840178, 52.20164615386168805, 78.60861935269869605 ) ) ;
#6319=CARTESIAN_POINT ( 'NONE',  ( -3.799298760401091268, 51.89000185047994052, 75.54713691134779197 ) ) ;
#6320=ORIENTED_EDGE ( 'NONE', *, *, #13177, .F. ) ;
#6323=CARTESIAN_POINT ( 'NONE',  ( 9.353817388681445522, 42.82770861117572281, 78.41904468188381827 ) ) ;
#6324=CARTESIAN_POINT ( 'NONE',  ( -2.932686190032669948, 51.59885408774670879, 76.34467759591066738 ) ) ;
#6325=ORIENTED_EDGE ( 'NONE', *, *, #3217, .T. ) ;
#6326=FACE_OUTER_BOUND ( 'NONE', #17289, .T. ) ;
#6329=CARTESIAN_POINT ( 'NONE',  ( -7.949137504989498559, 41.77948864320536160, 78.50654468188380974 ) ) ;
#6330=CARTESIAN_POINT ( 'NONE',  ( 8.377992009893507230, 41.81147811158319172, 78.64980314354953350 ) ) ;
#6331=DIRECTION ( 'NONE',  ( -0.5813877811927012917, 0.8136266022444372803, 5.636455622144620416E-17 ) ) ;
#6333=CARTESIAN_POINT ( 'NONE',  ( -4.359867457993620299, 37.60268028463676870, 77.29630340639747033 ) ) ;
#6334=DIRECTION ( 'NONE',  ( -0.3165065846431825980, -0.9485903129789530208, 0.000000000000000000 ) ) ;
#6336=AXIS2_PLACEMENT_3D ( 'NONE', #8341, #16119, #3024 ) ;
#6337=VERTEX_POINT ( 'NONE', #558 ) ;
#6338=CARTESIAN_POINT ( 'NONE',  ( -4.699529792962120034, 51.24672971417357559, 75.98997946140892168 ) ) ;
#6343=EDGE_CURVE ( 'NONE', #5798, #5122, #7040, .T. ) ;
#6344=CARTESIAN_POINT ( 'NONE',  ( 8.230299787179362170, 47.07948288808702841, 79.45405409817819020 ) ) ;
#6346=CARTESIAN_POINT ( 'NONE',  ( 0.3327597288346153537, 52.96805686913342015, 77.10139762306027933 ) ) ;
#6347=FACE_OUTER_BOUND ( 'NONE', #12294, .T. ) ;
#6348=CARTESIAN_POINT ( 'NONE',  ( -0.9437865455955903871, 52.21748465046702137, 77.77566232894263010 ) ) ;
#6350=ORIENTED_EDGE ( 'NONE', *, *, #13739, .T. ) ;
#6351=CARTESIAN_POINT ( 'NONE',  ( -4.158995335318336650, 37.42966003176047707, 76.41545151846887052 ) ) ;
#6354=CARTESIAN_POINT ( 'NONE',  ( 0.8402845321420674418, 52.35600907897080702, 76.16933144905489428 ) ) ;
#6355=CARTESIAN_POINT ( 'NONE',  ( 0.7444978820518556306, 52.95993232485279378, 79.54697877576636245 ) ) ;
#6356=EDGE_CURVE ( 'NONE', #8103, #14909, #12478, .T. ) ;
#6361=EDGE_CURVE ( 'NONE', #15505, #13342, #2900, .T. ) ;
#6362=CARTESIAN_POINT ( 'NONE',  ( -4.895222749246782357, 37.22336455408366618, 78.59503622499421738 ) ) ;
#6364=CARTESIAN_POINT ( 'NONE',  ( 5.239838662427071192, 50.86471668784145805, 78.21422674182478829 ) ) ;
#6365=VECTOR ( 'NONE', #14805, 1000.000000000000114 ) ;
#6367=CARTESIAN_POINT ( 'NONE',  ( 6.888069329080921399, 50.40035056576664374, 77.33077842133744184 ) ) ;
#6370=CARTESIAN_POINT ( 'NONE',  ( 8.788011242024285963, 41.13195169557157271, 78.55826321071354812 ) ) ;
#6372=CARTESIAN_POINT ( 'NONE',  ( -5.787187992231675793, 50.46952898668384790, 78.79017217825926878 ) ) ;
#6376=CARTESIAN_POINT ( 'NONE',  ( 9.324313659942287558, 42.73928406446282224, 77.68070116889359156 ) ) ;
#6377=ORIENTED_EDGE ( 'NONE', *, *, #20787, .F. ) ;
#6378=CARTESIAN_POINT ( 'NONE',  ( 6.286916181961658801, 38.38547291560929153, 75.79056106475293575 ) ) ;
#6380=CARTESIAN_POINT ( 'NONE',  ( 6.539349088566551949, 37.64607664623218142, 78.24541959536460922 ) ) ;
#6385=LINE ( 'NONE', #14795, #8765 ) ;
#6387=EDGE_CURVE ( 'NONE', #14867, #1091, #4373, .T. ) ;
#6388=ORIENTED_EDGE ( 'NONE', *, *, #17314, .T. ) ;
#6391=CARTESIAN_POINT ( 'NONE',  ( -7.719292346789278447, 47.24975066309455229, 79.05982662974776076 ) ) ;
#6392=CARTESIAN_POINT ( 'NONE',  ( 5.394152393224890041, 50.75790946820724514, 75.36022115247205022 ) ) ;
#6394=ADVANCED_FACE ( 'NONE', ( #4679 ), #15679, .T. ) ;
#6396=CARTESIAN_POINT ( 'NONE',  ( 4.947340820402381212, 51.83388853781453776, 77.72408214165703555 ) ) ;
#6397=VECTOR ( 'NONE', #17141, 1000.000000000000000 ) ;
#6398=ORIENTED_EDGE ( 'NONE', *, *, #8821, .F. ) ;
#6399=CARTESIAN_POINT ( 'NONE',  ( -3.569019236227245706, 51.13477558510469834, 75.44813358671753178 ) ) ;
#6403=CARTESIAN_POINT ( 'NONE',  ( -5.838384959142698172, 50.43294550856981573, 78.14282209630749776 ) ) ;
#6404=CARTESIAN_POINT ( 'NONE',  ( -5.747619332630492295, 37.85299557360038136, 79.28390783734228364 ) ) ;
#6405=CARTESIAN_POINT ( 'NONE',  ( -4.300787881984191152, 37.53891540493670931, 78.93441095796421791 ) ) ;
#6406=CARTESIAN_POINT ( 'NONE',  ( 5.588830122182042004, 51.36004623135520575, 76.07177712439327877 ) ) ;
#6407=DIRECTION ( 'NONE',  ( -0.3164954110480847627, -0.9485568250056046757, 0.008402649629174620272 ) ) ;
#6412=CARTESIAN_POINT ( 'NONE',  ( 4.140566530694384184, 51.51580520154297460, 78.43496551412393103 ) ) ;
#6414=CARTESIAN_POINT ( 'NONE',  ( -5.809877882140231264, 50.45331562208507847, 76.21531548689122815 ) ) ;
#6417=( BOUNDED_CURVE ( )  B_SPLINE_CURVE ( 3, ( #2594, #8888, #13980, #17172 ),
 .UNSPECIFIED., .F., .F. ) 
 B_SPLINE_CURVE_WITH_KNOTS ( ( 4, 4 ),
 ( 4.518932018683322838, 4.653621299756558471 ),
 .UNSPECIFIED. ) 
 CURVE ( )  GEOMETRIC_REPRESENTATION_ITEM ( )  RATIONAL_B_SPLINE_CURVE ( ( 1.000000000000000000, 0.9984888044037290022, 0.9984888044037290022, 1.000000000000000000 ) ) 
 REPRESENTATION_ITEM ( '' )  );
#6419=CARTESIAN_POINT ( 'NONE',  ( 5.278470088661852522, 37.49201410884709418, 77.76022115247205591 ) ) ;
#6420=CARTESIAN_POINT ( 'NONE',  ( -3.495065479208319559, 36.18912478048144266, 76.62933879953087057 ) ) ;
#6422=CARTESIAN_POINT ( 'NONE',  ( 2.104109567847143314, 52.20160448666339903, 78.53328619179760040 ) ) ;
#6423=CARTESIAN_POINT ( 'NONE',  ( -3.410233088748519492, 37.04047751613406092, 77.75315568452884918 ) ) ;
#6425=EDGE_LOOP ( 'NONE', ( #12677, #17665, #12469, #8476, #3046, #6076 ) ) ;
#6426=CARTESIAN_POINT ( 'NONE',  ( -7.775446761845334898, 41.23134052849093223, 78.58228875689293602 ) ) ;
#6428=CARTESIAN_POINT ( 'NONE',  ( 8.198902672654092783, 41.73077399133128296, 75.36120592425527320 ) ) ;
#6429=ORIENTED_EDGE ( 'NONE', *, *, #1184, .F. ) ;
#6431=PLANE ( 'NONE',  #2046 ) ;
#6432=CARTESIAN_POINT ( 'NONE',  ( -7.240840862912148346, 41.96299060810435577, 79.54527856538405217 ) ) ;
#6433=ORIENTED_EDGE ( 'NONE', *, *, #10247, .F. ) ;
#6435=LINE ( 'NONE', #18725, #5753 ) ;
#6437=ORIENTED_EDGE ( 'NONE', *, *, #8479, .T. ) ;
#6438=CARTESIAN_POINT ( 'NONE',  ( -4.200477280862170204, 37.48494518141774279, 77.15538146413656762 ) ) ;
#6439=CARTESIAN_POINT ( 'NONE',  ( 8.788263343888127466, 41.13270726085054463, 77.24417474779077963 ) ) ;
#6441=VECTOR ( 'NONE', #8552, 1000.000000000000000 ) ;
#6442=VECTOR ( 'NONE', #3443, 1000.000000000000000 ) ;
#6443=VERTEX_POINT ( 'NONE', #7687 ) ;
#6445=CARTESIAN_POINT ( 'NONE',  ( 5.630409355376515990, 37.74693565085873104, 75.37982132168592386 ) ) ;
#6448=EDGE_CURVE ( 'NONE', #15690, #16873, #4482, .T. ) ;
#6449=CARTESIAN_POINT ( 'NONE',  ( -5.838369852643723767, 50.43295630312090339, 76.72345405564152543 ) ) ;
#6450=VECTOR ( 'NONE', #8646, 1000.000000000000000 ) ;
#6451=CARTESIAN_POINT ( 'NONE',  ( -3.349688636638950889, 52.21127678364309332, 76.69845644658968808 ) ) ;
#6453=CARTESIAN_POINT ( 'NONE',  ( 8.787829143201870252, 41.13140593384865440, 77.14698585835439815 ) ) ;
#6457=CARTESIAN_POINT ( 'NONE',  ( -4.208268149563465066, 37.46415075985294862, 76.03844061143841770 ) ) ;
#6459=CARTESIAN_POINT ( 'NONE',  ( 2.029186242314200861, 35.35002428291939225, 76.16022115247204738 ) ) ;
#6461=EDGE_LOOP ( 'NONE', ( #18844, #17614, #8565, #5871, #16755, #4749, #13968, #10013, #19634, #2667, #9760, #10701 ) ) ;
#6462=ADVANCED_FACE ( 'NONE', ( #17675 ), #14524, .F. ) ;
#6465=CARTESIAN_POINT ( 'NONE',  ( 7.690600091884840062, 40.18054381350538051, 76.29938702471172007 ) ) ;
#6466=PLANE ( 'NONE',  #6023 ) ;
#6467=CARTESIAN_POINT ( 'NONE',  ( 6.923000991621626632, 50.37454795378102546, 78.43783143115764744 ) ) ;
#6470=EDGE_CURVE ( 'NONE', #225, #5416, #5894, .T. ) ;
#6471=B_SPLINE_SURFACE_WITH_KNOTS ( 'NONE', 3, 1, ( 
 ( #11433, #17905 ),
 ( #8230, #18433 ),
 ( #8870, #13849 ),
 ( #15356, #7359 ),
 ( #5767, #13750 ),
 ( #15457, #7254 ),
 ( #2479, #15141 ),
 ( #5654, #10476 ),
 ( #2368, #10694 ),
 ( #13535, #20330 ),
 ( #552, #4169 ),
 ( #10371, #12272 ),
 ( #5442, #16841 ),
 ( #20219, #8974 ),
 ( #17156, #18755 ),
 ( #18323, #18538 ),
 ( #10263, #8758 ),
 ( #15248, #3953 ),
 ( #2260, #12161 ),
 ( #2576, #874 ),
 ( #11846, #17054 ),
 ( #13964, #9077 ),
 ( #772, #18642 ),
 ( #4058, #20119 ),
 ( #663, #20006 ),
 ( #12059, #16737 ),
 ( #7035, #16941 ) ),
 .UNSPECIFIED., .F., .F., .F.,
 ( 4, 1, 1, 1, 1, 1, 1, 1, 1, 1, 1, 1, 1, 1, 1, 1, 1, 1, 1, 1, 1, 1, 1, 1, 4 ),
 ( 2, 2 ),
 ( 0.000000000000000000, 0.05524556061070538121, 0.1069179814647366472, 0.1553727729060086771, 0.2000758033479648479, 0.2417614041178833273, 0.2799066487053696317, 0.3152370222690974444, 0.3476361288249658066, 0.3788200842211088548, 0.4103815830948299714, 0.4425365161269811387, 0.4758329365342930384, 0.5105782220665333604, 0.5468313811506283484, 0.5849849847693828764, 0.6253480228319793222, 0.6671656491570584491, 0.7102157423341657339, 0.7546653220675233475, 0.8003710923354008244, 0.8474641787091774514, 0.8966644363699035614, 0.9474646149202431422, 1.000000000000000000 ),
 ( 0.000000000000000000, 1.000000000000000000 ),
 .UNSPECIFIED. ) ;
#6474=DIRECTION ( 'NONE',  ( -1.540237394707283727E-16, -1.793354297423763257E-16, 1.000000000000000000 ) ) ;
#6475=CARTESIAN_POINT ( 'NONE',  ( 9.324313659942287558, 42.73928406446282224, 77.68070116889359156 ) ) ;
#6479=CARTESIAN_POINT ( 'NONE',  ( -5.850799091716244682, 37.92921030530280291, 79.12851299606570876 ) ) ;
#6480=CARTESIAN_POINT ( 'NONE',  ( -5.838384959142698172, 50.43294550856981573, 78.14282209630749776 ) ) ;
#6482=CARTESIAN_POINT ( 'NONE',  ( 8.365414986285550469, 41.78545958710412833, 77.39218765127517941 ) ) ;
#6483=CARTESIAN_POINT ( 'NONE',  ( 9.315603341877332966, 42.71317868864986877, 77.73063109826868811 ) ) ;
#6485=CARTESIAN_POINT ( 'NONE',  ( 6.851319717782478946, 37.86899943589613571, 76.12774863075016185 ) ) ;
#6486=AXIS2_PLACEMENT_3D ( 'NONE', #1392, #1606, #3 ) ;
#6487=DIRECTION ( 'NONE',  ( 1.540237394707284220E-16, 1.793354297423764243E-16, -1.000000000000000000 ) ) ;
#6489=CARTESIAN_POINT ( 'NONE',  ( -6.709242558049761662, 40.29605830358345031, 78.50801527011910252 ) ) ;
#6491=VERTEX_POINT ( 'NONE', #9398 ) ;
#6492=CARTESIAN_POINT ( 'NONE',  ( -4.383592986664169189, 51.47248658876933547, 78.47566305278908771 ) ) ;
#6495=ADVANCED_FACE ( 'NONE', ( #20751 ), #9719, .T. ) ;
#6496=CARTESIAN_POINT ( 'NONE',  ( 2.813615989083933844, 36.91585811327295374, 72.45433879953085921 ) ) ;
#6498=EDGE_CURVE ( 'NONE', #2056, #6135, #13319, .T. ) ;
#6500=VECTOR ( 'NONE', #59, 1000.000000000000227 ) ;
#6501=DIRECTION ( 'NONE',  ( 0.007885122365285381421, 0.9999689119394085113, 1.805443505845558673E-16 ) ) ;
#6502=ORIENTED_EDGE ( 'NONE', *, *, #20675, .F. ) ;
#6503=EDGE_CURVE ( 'NONE', #9206, #10690, #6703, .T. ) ;
#6504=CARTESIAN_POINT ( 'NONE',  ( -4.522047388140565616, 36.94771494725497973, 76.29203488853940485 ) ) ;
#6505=COLOUR_RGB ( '', 0.08235294, 0.09019608, 0.10196078) ;
#6508=CARTESIAN_POINT ( 'NONE',  ( -7.719684245581981408, 47.24636383256876115, 78.03730287344849614 ) ) ;
#6511=ORIENTED_EDGE ( 'NONE', *, *, #13749, .T. ) ;
#6512=B_SPLINE_CURVE_WITH_KNOTS ( 'NONE', 3,
 ( #4619, #6426, #7834, #4833, #11353, #17511, #17609, #4932, #12823, #11454, #4522, #58, #3039, #11139 ),
 .UNSPECIFIED., .F., .F.,
 ( 4, 2, 2, 2, 2, 2, 4 ),
 ( 0.000000000000000000, 9.720882473674754556E-05, 0.0001944176494734950911, 0.0003888352989470360982, 0.0007776705978941266233, 0.001555341195788341934, 0.003110682391576773641 ),
 .UNSPECIFIED. ) ;
#6513=CARTESIAN_POINT ( 'NONE',  ( -5.721665869871382704, 50.51634869640449210, 78.97495844722888592 ) ) ;
#6514=CARTESIAN_POINT ( 'NONE',  ( -5.955451856753747997, 38.00651308716548726, 78.53742703482498655 ) ) ;
#6515=CARTESIAN_POINT ( 'NONE',  ( 4.393996117251955269, 36.11308595931626542, 76.96022115247204454 ) ) ;
#6516=DIRECTION ( 'NONE',  ( 1.540237394707284220E-16, 1.793354297423764243E-16, -1.000000000000000000 ) ) ;
#6519=FACE_OUTER_BOUND ( 'NONE', #8805, .T. ) ;
#6520=CARTESIAN_POINT ( 'NONE',  ( 0.4414257598867362131, 52.36183294059821947, 76.96012364693363850 ) ) ;
#6522=ORIENTED_EDGE ( 'NONE', *, *, #19210, .T. ) ;
#6523=CARTESIAN_POINT ( 'NONE',  ( 4.172718597472855784, 51.49205576497796244, 78.11943565213420015 ) ) ;
#6524=CARTESIAN_POINT ( 'NONE',  ( -7.596864591047396864, 40.63365867659160102, 77.28168744664917256 ) ) ;
#6526=CARTESIAN_POINT ( 'NONE',  ( -4.454500421143473332, 37.64505674804929924, 79.54845644658969661 ) ) ;
#6530=LINE ( 'NONE', #9846, #9936 ) ;
#6531=CARTESIAN_POINT ( 'NONE',  ( 5.865470552710490892, 51.15570308908012009, 76.01152026380901816 ) ) ;
#6532=ORIENTED_EDGE ( 'NONE', *, *, #16399, .F. ) ;
#6533=EDGE_CURVE ( 'NONE', #1116, #14804, #6385, .T. ) ;
#6535=LINE ( 'NONE', #14418, #3194 ) ;
#6537=AXIS2_PLACEMENT_3D ( 'NONE', #17181, #5469, #18563 ) ;
#6539=VECTOR ( 'NONE', #10340, 1000.000000000000000 ) ;
#6542=ORIENTED_EDGE ( 'NONE', *, *, #16267, .F. ) ;
#6544=CARTESIAN_POINT ( 'NONE',  ( -5.338436749040046614, 37.55074888198199545, 75.45005776384208218 ) ) ;
#6547=CARTESIAN_POINT ( 'NONE',  ( -4.156531397120291516, 37.43235895057341622, 76.50360254650976799 ) ) ;
#6550=CARTESIAN_POINT ( 'NONE',  ( -4.270971958021394066, 37.53701675973645280, 77.24798498253255730 ) ) ;
#6551=CARTESIAN_POINT ( 'NONE',  ( -4.146809383516695036, 37.44530286752341652, 78.34992703482498655 ) ) ;
#6552=B_SPLINE_CURVE_WITH_KNOTS ( 'NONE', 3,
 ( #888, #7374, #18868, #20460, #5784, #4381, #993, #15372, #10709, #12289, #18769, #7486, #5667, #12177 ),
 .UNSPECIFIED., .F., .F.,
 ( 4, 2, 2, 2, 2, 2, 4 ),
 ( 0.000000000000000000, 0.0002546807491738087856, 0.0005093614983476175712, 0.0007640422475214262484, 0.001018722996695235142, 0.001528084495042833632, 0.002037445993390432555 ),
 .UNSPECIFIED. ) ;
#6558=AXIS2_PLACEMENT_3D ( 'NONE', #4573, #11095, #14868 ) ;
#6559=SHAPE_REPRESENTATION_RELATIONSHIP ( 'NONE' , 'NONE' ,  #9739, #13412 ) ;
#6560=CARTESIAN_POINT ( 'NONE',  ( 1.038073682718705371, 52.33964046710553930, 76.77289608131282250 ) ) ;
#6561=CARTESIAN_POINT ( 'NONE',  ( 5.665287683258889651, 37.02150436742986273, 75.36022115247205022 ) ) ;
#6564=CARTESIAN_POINT ( 'NONE',  ( -5.464671512499847061, 38.55876153151410080, 76.02256373304906845 ) ) ;
#6565=CARTESIAN_POINT ( 'NONE',  ( 8.643446883273359305, 43.06310119191608976, 76.54645538997905874 ) ) ;
#6566=CARTESIAN_POINT ( 'NONE',  ( 0.5658429483755761380, 52.35438129105421723, 77.38474949312757190 ) ) ;
#6567=CARTESIAN_POINT ( 'NONE',  ( 6.545534159973747990, 50.65336749702785113, 77.68963291717794561 ) ) ;
#6570=CARTESIAN_POINT ( 'NONE',  ( 5.541932868547512214, 50.64157186687718593, 78.62249727093715990 ) ) ;
#6572=EDGE_CURVE ( 'NONE', #6821, #11879, #11478, .T. ) ;
#6573=DIRECTION ( 'NONE',  ( -1.540237394707284220E-16, -1.793354297423764243E-16, 1.000000000000000000 ) ) ;
#6574=CARTESIAN_POINT ( 'NONE',  ( 5.427780505986065762, 36.85179043424346190, 77.43080938776617472 ) ) ;
#6575=DIRECTION ( 'NONE',  ( -1.540237394707284220E-16, -1.793354297423764243E-16, 1.000000000000000000 ) ) ;
#6578=CARTESIAN_POINT ( 'NONE',  ( 9.304727838458644484, 42.68058411497499804, 77.77798975163413786 ) ) ;
#6579=CARTESIAN_POINT ( 'NONE',  ( 4.621588727139584130, 51.26391586304784198, 77.68963291717793140 ) ) ;
#6580=EDGE_CURVE ( 'NONE', #165, #15505, #16411, .T. ) ;
#6581=VECTOR ( 'NONE', #3036, 1000.000000000000000 ) ;
#6584=CARTESIAN_POINT ( 'NONE',  ( -5.428519676309861985, 37.61728951159455647, 79.46937556254052026 ) ) ;
#6585=CARTESIAN_POINT ( 'NONE',  ( 8.641007280878683972, 43.01131509312123313, 76.04687335640809920 ) ) ;
#6586=CARTESIAN_POINT ( 'NONE',  ( 8.345005557250493311, 41.72429123353602165, 77.48121952543638713 ) ) ;
#6587=CARTESIAN_POINT ( 'NONE',  ( 8.401796425420881675, 39.97444138920005230, 76.12035193564865665 ) ) ;
#6588=ORIENTED_EDGE ( 'NONE', *, *, #11204, .F. ) ;
#6590=CARTESIAN_POINT ( 'NONE',  ( 6.437297979933394032, 38.49293024261085350, 76.32925572521180868 ) ) ;
#6593=CARTESIAN_POINT ( 'NONE',  ( 8.139872831506870909, 41.12499011683758710, 79.51301525321822794 ) ) ;
#6594=CARTESIAN_POINT ( 'NONE',  ( -1.403474231502331637, 49.90122385011594730, 72.45433879953087342 ) ) ;
#6595=CARTESIAN_POINT ( 'NONE',  ( -0.02883801100815608018, 35.36625256049322275, 79.45433879953087342 ) ) ;
#6597=CARTESIAN_POINT ( 'NONE',  ( 5.902048492000326441, 51.12868443877599134, 78.59183879953087626 ) ) ;
#6598=ORIENTED_EDGE ( 'NONE', *, *, #17656, .T. ) ;
#6600=CARTESIAN_POINT ( 'NONE',  ( 0.3282210660296583371, 52.35988776924397570, 76.39696619987448400 ) ) ;
#6604=EDGE_CURVE ( 'NONE', #20173, #13226, #11517, .T. ) ;
#6607=EDGE_LOOP ( 'NONE', ( #18456, #955, #18242, #16770 ) ) ;
#6611=ORIENTED_EDGE ( 'NONE', *, *, #16614, .F. ) ;
#6612=ADVANCED_FACE ( 'NONE', ( #8644 ), #2460, .T. ) ;
#6613=CARTESIAN_POINT ( 'NONE',  ( -5.827090762987216621, 50.44101592763561115, 78.49957729094111869 ) ) ;
#6615=CARTESIAN_POINT ( 'NONE',  ( -5.681413420386576263, 37.80409193316262417, 79.34222993022952153 ) ) ;
#6616=DIRECTION ( 'NONE',  ( -1.540237394707284467E-16, -1.793354297423764243E-16, 1.000000000000000000 ) ) ;
#6619=DIRECTION ( 'NONE',  ( -1.540237394707283727E-16, -1.793354297423763257E-16, 1.000000000000000000 ) ) ;
#6620=VERTEX_POINT ( 'NONE', #18522 ) ;
#6621=CARTESIAN_POINT ( 'NONE',  ( -4.536263512923754959, 51.36339382032895884, 75.97373057797423712 ) ) ;
#6622=CARTESIAN_POINT ( 'NONE',  ( 0.8497199531031915942, 52.96350053290503013, 78.59044740879555491 ) ) ;
#6624=CARTESIAN_POINT ( 'NONE',  ( 4.577225057937400976, 52.10727814237509392, 78.46169174070733732 ) ) ;
#6625=CARTESIAN_POINT ( 'NONE',  ( -7.419840600255425578, 40.07385322379796833, 78.42124021397933120 ) ) ;
#6627=B_SPLINE_CURVE_WITH_KNOTS ( 'NONE', 3,
 ( #4045, #15235, #20320, #969, #7133, #13632, #9065, #20108, #759, #16931, #8962, #2354, #10572, #15345, #7348, #5754, #12262, #4158, #10683, #2566, #7458, #13954, #7987 ),
 .UNSPECIFIED., .F., .F.,
 ( 4, 1, 1, 1, 1, 1, 1, 1, 1, 1, 1, 1, 1, 1, 1, 1, 1, 1, 1, 1, 4 ),
 ( 0.000000000000000000, 0.04338402653469398268, 0.08365674416537959013, 0.1211563976680593846, 0.1555788671761421382, 0.1872558283108043675, 0.2159034631954582228, 0.2418665822845563473, 0.2649561893498845744, 0.3085842690520175235, 0.3528342053628863995, 0.3996013663067077837, 0.4488757727682718413, 0.5007062493018590299, 0.5562201143629579292, 0.6158399466276373024, 0.6805899729784313790, 0.7509145939079137078, 0.8273700343273244773, 0.9100784481637514967, 0.9999999999999998890 ),
 .UNSPECIFIED. ) ;
#6628=EDGE_CURVE ( 'NONE', #12108, #4469, #751, .T. ) ;
#6629=CARTESIAN_POINT ( 'NONE',  ( -5.050952507338172914, 50.99561590888721696, 75.40305853716382956 ) ) ;
#6632=CARTESIAN_POINT ( 'NONE',  ( 8.119551934336415755, 43.80226376792169418, 72.45432679953087529 ) ) ;
#6633=EDGE_CURVE ( 'NONE', #2886, #1872, #16783, .T. ) ;
#6634=LINE ( 'NONE', #6219, #14251 ) ;
#6636=ORIENTED_EDGE ( 'NONE', *, *, #5161, .F. ) ;
#6638=DIRECTION ( 'NONE',  ( -0.9480563259966822143, -0.3181025035073955509, -2.030702297275135124E-16 ) ) ;
#6640=CARTESIAN_POINT ( 'NONE',  ( -5.412716252285423302, 48.91899944357702879, 72.45432679953087529 ) ) ;
#6642=CARTESIAN_POINT ( 'NONE',  ( 0.5886017282102210535, 52.96193049659134999, 78.93669174070734584 ) ) ;
#6643=B_SPLINE_SURFACE_WITH_KNOTS ( 'NONE', 3, 1, ( 
 ( #13109, #11417 ),
 ( #9717, #11522 ),
 ( #13215, #17890 ),
 ( #16197, #19689 ),
 ( #15021, #13736 ),
 ( #7019, #3938 ),
 ( #5424, #7241 ),
 ( #326, #10359 ),
 ( #16829, #14902 ),
 ( #15233, #646 ),
 ( #7128, #15444 ),
 ( #541, #18528 ),
 ( #10466, #11834 ),
 ( #56, #8037 ),
 ( #7832, #16132 ),
 ( #6423, #17508 ),
 ( #6119, #19201 ),
 ( #19411, #14207 ),
 ( #14523, #1551 ) ),
 .UNSPECIFIED., .F., .F., .F.,
 ( 4, 1, 1, 1, 1, 1, 1, 1, 1, 1, 1, 1, 1, 1, 1, 1, 4 ),
 ( 2, 2 ),
 ( 0.000000000000000000, 0.08150191411353231719, 0.1574413810301363015, 0.2279254944343154510, 0.2925593756674912393, 0.3532811523109508078, 0.4087341836578463616, 0.4609809767707315764, 0.5093835833650265377, 0.5574898171909816735, 0.6095021731789963537, 0.6642568233027335012, 0.7231084493840179706, 0.7857192733158503417, 0.8528940375925012640, 0.9238451209387705809, 1.000000000000000000 ),
 ( 0.000000000000000000, 1.000000000000000000 ),
 .UNSPECIFIED. ) ;
#6644=ORIENTED_EDGE ( 'NONE', *, *, #4826, .F. ) ;
#6647=CARTESIAN_POINT ( 'NONE',  ( -5.496597427495279575, 38.60358230014927727, 76.35020017089209432 ) ) ;
#6650=CARTESIAN_POINT ( 'NONE',  ( 5.599231707071657738, 51.35236299959863970, 78.59183879953087626 ) ) ;
#6652=CARTESIAN_POINT ( 'NONE',  ( -6.709242558049761662, 40.29605830358345031, 78.50801527011910252 ) ) ;
#6654=CARTESIAN_POINT ( 'NONE',  ( -4.146809383516695924, 37.44530286752341652, 76.81463291717793140 ) ) ;
#6657=ORIENTED_EDGE ( 'NONE', *, *, #14800, .T. ) ;
#6658=CARTESIAN_POINT ( 'NONE',  ( -4.804644443005473775, 51.17161863374556674, 76.44036821129557779 ) ) ;
#6659=CARTESIAN_POINT ( 'NONE',  ( 2.029186242314200861, 35.35002428291939225, 76.16022115247204738 ) ) ;
#6662=CARTESIAN_POINT ( 'NONE',  ( 6.062166292594780792, 51.01041186941530015, 75.37891144279687694 ) ) ;
#6663=CARTESIAN_POINT ( 'NONE',  ( 0.7199301301226463945, 52.96500388823179861, 76.81551440955847454 ) ) ;
#6664=CARTESIAN_POINT ( 'NONE',  ( 4.521197205061672442, 36.20397919953602184, 75.90366482745062626 ) ) ;
#6665=EDGE_LOOP ( 'NONE', ( #202, #10076, #11963, #4271 ) ) ;
#6666=CARTESIAN_POINT ( 'NONE',  ( -5.307285386973724428, 38.39462082443735369, 75.68768371633831293 ) ) ;
#6667=CARTESIAN_POINT ( 'NONE',  ( 8.630330997359013878, 43.02379204977451366, 76.09591779779900378 ) ) ;
#6669=DIRECTION ( 'NONE',  ( -0.8043570849667760481, 0.5941461771851693774, -1.733862608106482338E-17 ) ) ;
#6671=ORIENTED_EDGE ( 'NONE', *, *, #4303, .F. ) ;
#6674=ORIENTED_EDGE ( 'NONE', *, *, #19646, .F. ) ;
#6675=CARTESIAN_POINT ( 'NONE',  ( 6.522436035574397550, 49.75115376156129798, 72.45433879953087342 ) ) ;
#6676=CARTESIAN_POINT ( 'NONE',  ( 4.566992627068686694, 51.19000347988376376, 77.68963291717794561 ) ) ;
#6680=CARTESIAN_POINT ( 'NONE',  ( 8.865792162213244509, 41.36506604770743678, 78.93669174070734584 ) ) ;
#6686=ORIENTED_EDGE ( 'NONE', *, *, #5989, .T. ) ;
#6687=CARTESIAN_POINT ( 'NONE',  ( 5.755371611800503828, 51.23702874167446453, 77.28963291717792572 ) ) ;
#6688=B_SPLINE_CURVE_WITH_KNOTS ( 'NONE', 3,
 ( #20737, #19465, #11403, #1502, #20940, #9384, #15870, #12876, #19358, #17773, #12676, #9702, #19157, #16181, #17872, #3294, #4568, #205, #1913, #18289, #19977, #10116 ),
 .UNSPECIFIED., .F., .F.,
 ( 4, 3, 3, 3, 3, 3, 3, 4 ),
 ( 0.000000000000000000, 0.0001160541354670015593, 0.0002104287037779740748, 0.0002730688264539837622, 0.0003158076471914563312, 0.0003585748116541222349, 0.0004150858277573699594, 0.0004567865026589477636 ),
 .UNSPECIFIED. ) ;
#6690=CARTESIAN_POINT ( 'NONE',  ( 8.951667845840693971, 41.62244091939069790, 78.41904468188381827 ) ) ;
#6693=CARTESIAN_POINT ( 'NONE',  ( 8.385679600361122255, 39.92613824206362949, 77.13595644658970230 ) ) ;
#6694=ORIENTED_EDGE ( 'NONE', *, *, #16529, .F. ) ;
#6695=EDGE_LOOP ( 'NONE', ( #16981, #17405, #3944, #18804, #2947, #19278 ) ) ;
#6696=CARTESIAN_POINT ( 'NONE',  ( 6.490738213730996797, 37.61134109483241872, 75.55565825109377442 ) ) ;
#6698=DIRECTION ( 'NONE',  ( -0.9485903129789527988, 0.3165065846431829311, -8.934458285744989980E-17 ) ) ;
#6699=CARTESIAN_POINT ( 'NONE',  ( 6.281388312303515242, 38.38152290233981745, 78.07897440853361104 ) ) ;
#6701=DIRECTION ( 'NONE',  ( -1.540237394707283727E-16, -1.793354297423763257E-16, 1.000000000000000000 ) ) ;
#6703=LINE ( 'NONE', #17883, #13856 ) ;
#6704=CARTESIAN_POINT ( 'NONE',  ( -6.427915807670530945, 42.26053564693651055, 78.50654468188380974 ) ) ;
#6705=VERTEX_POINT ( 'NONE', #5418 ) ;
#6708=CARTESIAN_POINT ( 'NONE',  ( 1.959996514334737094, 52.20282393683998379, 77.13040333250513925 ) ) ;
#6710=EDGE_CURVE ( 'NONE', #15999, #4990, #2347, .T. ) ;
#6711=AXIS2_PLACEMENT_3D ( 'NONE', #13392, #2208, #3901 ) ;
#6712=DIRECTION ( 'NONE',  ( 0.8136266022444372803, 0.5813877811927012917, 2.295812393977109100E-16 ) ) ;
#6716=CARTESIAN_POINT ( 'NONE',  ( -7.585658068012925526, 47.58366583380566794, 78.31170846932076302 ) ) ;
#6719=ORIENTED_EDGE ( 'NONE', *, *, #10339, .T. ) ;
#6721=CARTESIAN_POINT ( 'NONE',  ( 8.874399228141724549, 41.39086197031718228, 75.36031793586835192 ) ) ;
#6722=VECTOR ( 'NONE', #1496, 1000.000000000000114 ) ;
#6723=CARTESIAN_POINT ( 'NONE',  ( 5.865470552710490892, 51.15570308908012009, 76.01152026380901816 ) ) ;
#6725=CARTESIAN_POINT ( 'NONE',  ( -4.804644443005472887, 51.17161863374555963, 76.44036821129557779 ) ) ;
#6728=CARTESIAN_POINT ( 'NONE',  ( -4.070368663726195990, 50.94938978984617961, 76.03815620566271605 ) ) ;
#6731=CARTESIAN_POINT ( 'NONE',  ( -6.708915498156351020, 40.30975170697517029, 78.33343394419354411 ) ) ;
#6732=EDGE_CURVE ( 'NONE', #16948, #3254, #17532, .T. ) ;
#6736=CARTESIAN_POINT ( 'NONE',  ( -7.032228721109727410, 47.19407273119308144, 78.27541057140679470 ) ) ;
#6739=AXIS2_PLACEMENT_3D ( 'NONE', #20004, #13646, #5555 ) ;
#6740=CARTESIAN_POINT ( 'NONE',  ( -4.307156007511903084, 51.52710565553512367, 75.38014013087713749 ) ) ;
#6744=ORIENTED_EDGE ( 'NONE', *, *, #17191, .F. ) ;
#6746=EDGE_CURVE ( 'NONE', #10457, #18032, #18836, .T. ) ;
#6749=CARTESIAN_POINT ( 'NONE',  ( -8.220401128834293303, 42.60303496164632264, 76.44005692701139765 ) ) ;
#6750=ORIENTED_EDGE ( 'NONE', *, *, #5232, .F. ) ;
#6752=CARTESIAN_POINT ( 'NONE',  ( -4.834768248550904701, 37.17870924967544255, 75.36094808373545106 ) ) ;
#6757=ORIENTED_EDGE ( 'NONE', *, *, #3797, .T. ) ;
#6758=CARTESIAN_POINT ( 'NONE',  ( -4.158578283022523081, 37.42937009194851328, 72.45433879953085921 ) ) ;
#6759=VECTOR ( 'NONE', #12901, 1000.000000000000114 ) ;
#6760=ORIENTED_EDGE ( 'NONE', *, *, #17215, .F. ) ;
#6763=EDGE_CURVE ( 'NONE', #17146, #2386, #4245, .T. ) ;
#6764=CARTESIAN_POINT ( 'NONE',  ( -3.296320189938882983, 36.90521795357528845, 79.15353786348812548 ) ) ;
#6766=CARTESIAN_POINT ( 'NONE',  ( 4.086113402153771723, 36.81285982569113457, 75.90366482745062626 ) ) ;
#6767=CIRCLE ( 'NONE', #16307, 6.200000000000000178 ) ;
#6768=CARTESIAN_POINT ( 'NONE',  ( -1.123656915330052408, 35.37488560990637865, 76.16022115247204738 ) ) ;
#6769=EDGE_LOOP ( 'NONE', ( #6997, #11559, #670, #5594, #10883, #9873 ) ) ;
#6771=CARTESIAN_POINT ( 'NONE',  ( 8.622345110544836544, 42.99985784037721004, 76.00948821603452643 ) ) ;
#6774=CARTESIAN_POINT ( 'NONE',  ( 9.176231272041631470, 45.98187388689780164, 75.44992703482499508 ) ) ;
#6775=EDGE_LOOP ( 'NONE', ( #1225, #17691, #3156, #20420 ) ) ;
#6779=CIRCLE ( 'NONE', #8825, 8.199999999999995737 ) ;
#6781=ORIENTED_EDGE ( 'NONE', *, *, #12361, .T. ) ;
#6782=CARTESIAN_POINT ( 'NONE',  ( -3.639202304192269644, 36.29559284691161025, 77.48323649892105891 ) ) ;
#6783=B_SPLINE_CURVE_WITH_KNOTS ( 'NONE', 3,
 ( #1522, #9205, #1111, #19083, #20863, #1210, #19277, #4689, #10910, #7698, #17379, #19175 ),
 .UNSPECIFIED., .F., .F.,
 ( 4, 2, 2, 2, 2, 4 ),
 ( 0.000000000000000000, 0.0001460610222087938687, 0.0002921220444175877374, 0.0003651525555219875584, 0.0004381830666263874879, 0.0005842440888351871841 ),
 .UNSPECIFIED. ) ;
#6784=CARTESIAN_POINT ( 'NONE',  ( 6.898851416363126710, 50.39238627222024292, 76.00796742194241062 ) ) ;
#6785=CARTESIAN_POINT ( 'NONE',  ( 9.343936824499609273, 42.79809593351145480, 76.16967972087822147 ) ) ;
#6786=CARTESIAN_POINT ( 'NONE',  ( 4.809763630234642484, 51.93551126624419112, 77.58315289018165117 ) ) ;
#6790=VECTOR ( 'NONE', #3867, 1000.000000000000114 ) ;
#6791=CARTESIAN_POINT ( 'NONE',  ( 4.219159492377686504, 51.44693380490667778, 75.82370277575662953 ) ) ;
#6793=VECTOR ( 'NONE', #13687, 1000.000000000000000 ) ;
#6794=VECTOR ( 'NONE', #9635, 1000.000000000000114 ) ;
#6797=ORIENTED_EDGE ( 'NONE', *, *, #8209, .T. ) ;
#6798=CARTESIAN_POINT ( 'NONE',  ( 4.732789623540107016, 37.12512171921697046, 75.44058029572614998 ) ) ;
#6799=CARTESIAN_POINT ( 'NONE',  ( -5.819820656548302829, 50.44621087952127425, 78.57924047249254329 ) ) ;
#6801=CARTESIAN_POINT ( 'NONE',  ( -4.753421688333181017, 37.11862182248194841, 78.93508260432024315 ) ) ;
#6802=DIRECTION ( 'NONE',  ( 1.540237394707284220E-16, 1.793354297423764243E-16, -1.000000000000000000 ) ) ;
#6806=ORIENTED_EDGE ( 'NONE', *, *, #2434, .T. ) ;
#6808=DIRECTION ( 'NONE',  ( -0.9585804129707226062, -0.2848220354341972071, -1.987228219138359305E-16 ) ) ;
#6809=CARTESIAN_POINT ( 'NONE',  ( -6.782631326057146026, 43.38225751353197523, 78.13669174070733447 ) ) ;
#6810=CARTESIAN_POINT ( 'NONE',  ( 0.7910648968800085834, 52.95821647980518065, 76.03473320275389824 ) ) ;
#6812=CARTESIAN_POINT ( 'NONE',  ( 8.951594291416542504, 41.62222047211530906, 76.36070165242202279 ) ) ;
#6814=ORIENTED_EDGE ( 'NONE', *, *, #3400, .F. ) ;
#6816=CARTESIAN_POINT ( 'NONE',  ( -7.210499118439378741, 41.44819533126688071, 78.81104446281315745 ) ) ;
#6817=ADVANCED_FACE ( 'NONE', ( #19245 ), #10563, .T. ) ;
#6819=B_SPLINE_SURFACE_WITH_KNOTS ( 'NONE', 3, 1, ( 
 ( #12135, #628 ),
 ( #7110, #13613 ),
 ( #8833, #5628 ),
 ( #18613, #4027 ),
 ( #10552, #7759 ),
 ( #2656, #12350 ),
 ( #18722, #11358 ),
 ( #14136, #14039 ),
 ( #12239, #8942 ),
 ( #17338, #17128 ),
 ( #18927, #17228 ) ),
 .UNSPECIFIED., .F., .F., .F.,
 ( 4, 1, 1, 1, 1, 1, 1, 1, 4 ),
 ( 2, 2 ),
 ( 0.000000000000000000, 0.1449716284489762919, 0.2824273770673361716, 0.4139378473324432095, 0.5393048879599185996, 0.6599329406584737434, 0.7760554297062330908, 0.8894112907033583371, 1.000000000000000000 ),
 ( 0.000000000000000000, 1.000000000000000000 ),
 .UNSPECIFIED. ) ;
#6820=CARTESIAN_POINT ( 'NONE',  ( 8.303614452336031349, 41.57589654819728509, 79.54845644658969661 ) ) ;
#6821=VERTEX_POINT ( 'NONE', #12865 ) ;
#6825=VECTOR ( 'NONE', #16418, 1000.000000000000114 ) ;
#6827=VERTEX_POINT ( 'NONE', #6680 ) ;
#6828=DIRECTION ( 'NONE',  ( 0.5813877811927011807, -0.8136266022444372803, -5.636455622144619183E-17 ) ) ;
#6831=CARTESIAN_POINT ( 'NONE',  ( 2.108290839596759003, 51.34989793853182505, 78.16610350541323271 ) ) ;
#6833=ORIENTED_EDGE ( 'NONE', *, *, #4818, .F. ) ;
#6834=CARTESIAN_POINT ( 'NONE',  ( -4.383574773872678243, 51.47249960296332461, 76.44257241107362688 ) ) ;
#6835=EDGE_CURVE ( 'NONE', #15434, #17850, #12975, .T. ) ;
#6838=CARTESIAN_POINT ( 'NONE',  ( -7.949137504989498559, 41.77948864320536160, 78.50654468188380974 ) ) ;
#6839=CARTESIAN_POINT ( 'NONE',  ( -4.652687709939232086, 51.28020135170361016, 75.36022115247205022 ) ) ;
#6843=CARTESIAN_POINT ( 'NONE',  ( 5.841953631609400510, 37.14774338596793513, 76.17246542145134924 ) ) ;
#6847=ORIENTED_EDGE ( 'NONE', *, *, #3280, .T. ) ;
#6848=DIRECTION ( 'NONE',  ( -0.9534635866061470511, -0.3015081906286169455, -2.009271279954808648E-16 ) ) ;
#6850=ORIENTED_EDGE ( 'NONE', *, *, #16914, .T. ) ;
#6851=PLANE ( 'NONE',  #19027 ) ;
#6854=ORIENTED_EDGE ( 'NONE', *, *, #5201, .T. ) ;
#6855=EDGE_LOOP ( 'NONE', ( #5903, #15697, #6861, #18 ) ) ;
#6856=VECTOR ( 'NONE', #20263, 1000.000000000000000 ) ;
#6857=DIRECTION ( 'NONE',  ( -0.5813877811927011807, 0.8136266022444372803, 5.636455622144619183E-17 ) ) ;
#6858=CARTESIAN_POINT ( 'NONE',  ( 0.5753667321910650445, 52.96202048236657589, 75.97198585835440099 ) ) ;
#6861=ORIENTED_EDGE ( 'NONE', *, *, #14592, .T. ) ;
#6865=ORIENTED_EDGE ( 'NONE', *, *, #15246, .T. ) ;
#6866=CARTESIAN_POINT ( 'NONE',  ( -4.435470484126775581, 50.68850139621873296, 76.15325518536063498 ) ) ;
#6867=DIRECTION ( 'NONE',  ( -0.3165065846431826535, -0.9485903129789529098, -2.188653791613874008E-16 ) ) ;
#6868=CARTESIAN_POINT ( 'NONE',  ( 6.406920570599026199, 49.83092282481639756, 75.87133531663224062 ) ) ;
#6871=LINE ( 'NONE', #2412, #12662 ) ;
#6872=EDGE_CURVE ( 'NONE', #2184, #7903, #3083, .T. ) ;
#6874=ORIENTED_EDGE ( 'NONE', *, *, #2607, .T. ) ;
#6875=CARTESIAN_POINT ( 'NONE',  ( 8.318328750355229673, 41.62059619433301094, 75.36022115247205022 ) ) ;
#6877=CARTESIAN_POINT ( 'NONE',  ( 8.388854304654358884, 39.93565303222995055, 78.40165754912887053 ) ) ;
#6880=DIRECTION ( 'NONE',  ( -0.5941461771851693774, -0.8043570849667760481, -2.357623395011396791E-16 ) ) ;
#6882=ORIENTED_EDGE ( 'NONE', *, *, #2589, .F. ) ;
#6884=CARTESIAN_POINT ( 'NONE',  ( 6.371724945467780898, 50.78175336232117587, 79.44748646226150868 ) ) ;
#6886=CARTESIAN_POINT ( 'NONE',  ( 0.4055551487203246652, 52.96467269406713285, 79.54789469633020360 ) ) ;
#6890=CARTESIAN_POINT ( 'NONE',  ( -7.309558426186682389, 41.73179521895028188, 78.93495393200015542 ) ) ;
#6891=ADVANCED_FACE ( 'NONE', ( #1704 ), #16173, .F. ) ;
#6892=CARTESIAN_POINT ( 'NONE',  ( -0.7955991294133907266, 52.86330977561153333, 75.91305193028594545 ) ) ;
#6894=CARTESIAN_POINT ( 'NONE',  ( 0.8038488827458696306, 52.96385831238255548, 77.48826545068648386 ) ) ;
#6901=CARTESIAN_POINT ( 'NONE',  ( 4.481935269463292570, 36.98100317819196192, 75.54009867650407273 ) ) ;
#6903=ORIENTED_EDGE ( 'NONE', *, *, #2780, .F. ) ;
#6904=CARTESIAN_POINT ( 'NONE',  ( 1.075234721012297667, 51.35804396568124730, 76.77198585835439815 ) ) ;
#6905=DIRECTION ( 'NONE',  ( -0.9534635866061452747, -0.3015081906286225522, -2.009271279954815797E-16 ) ) ;
#6906=CARTESIAN_POINT ( 'NONE',  ( 8.378166699482557433, 41.80998537114106028, 75.36398404145046470 ) ) ;
#6908=CARTESIAN_POINT ( 'NONE',  ( 8.371160148690725222, 41.80267820329873274, 77.32525259820312158 ) ) ;
#6910=FACE_OUTER_BOUND ( 'NONE', #16193, .T. ) ;
#6912=ORIENTED_EDGE ( 'NONE', *, *, #8373, .F. ) ;
#6913=CARTESIAN_POINT ( 'NONE',  ( 9.150799720292940975, 42.21925177981464117, 79.41516958226422673 ) ) ;
#6915=CARTESIAN_POINT ( 'NONE',  ( -4.158578283022523969, 37.42937009194850617, 78.58080938776616620 ) ) ;
#6918=VECTOR ( 'NONE', #2518, 1000.000000000000227 ) ;
#6919=CARTESIAN_POINT ( 'NONE',  ( -4.517072128342571880, 36.94403992325788977, 78.58080938776616620 ) ) ;
#6922=CARTESIAN_POINT ( 'NONE',  ( 2.076668872117770182, 52.20190393242106808, 77.39871602076138402 ) ) ;
#6924=CARTESIAN_POINT ( 'NONE',  ( 8.585425733894268774, 42.66887103129917591, 79.29104084200847069 ) ) ;
#6925=VERTEX_POINT ( 'NONE', #11497 ) ;
#6927=ORIENTED_EDGE ( 'NONE', *, *, #17423, .F. ) ;
#6930=ORIENTED_EDGE ( 'NONE', *, *, #9785, .F. ) ;
#6933=CARTESIAN_POINT ( 'NONE',  ( 0.5221537403065015237, 44.16218137147968292, 75.45433879953088763 ) ) ;
#6936=CARTESIAN_POINT ( 'NONE',  ( -1.403474231502331193, 49.90122385011594730, 72.45432679953087529 ) ) ;
#6937=ORIENTED_EDGE ( 'NONE', *, *, #15127, .F. ) ;
#6938=PLANE ( 'NONE',  #19587 ) ;
#6939=CARTESIAN_POINT ( 'NONE',  ( -6.860950806665904622, 40.79053509876318628, 77.37311125041073012 ) ) ;
#6940=DIRECTION ( 'NONE',  ( -0.3165065846431829311, -0.9485903129789527988, -2.188653791613874255E-16 ) ) ;
#6941=CARTESIAN_POINT ( 'NONE',  ( 7.863366485876452039, 47.81548183651919004, 78.86171667562430798 ) ) ;
#6943=CARTESIAN_POINT ( 'NONE',  ( 5.495247707634323575, 37.64691545862963551, 76.55482881315118959 ) ) ;
#6944=VERTEX_POINT ( 'NONE', #17969 ) ;
#6945=DIRECTION ( 'NONE',  ( 0.009567942452870513079, -0.9999542261909885044, -1.778535306010344808E-16 ) ) ;
#6953=CARTESIAN_POINT ( 'NONE',  ( -5.507653477476715409, 38.61174895890570724, 76.59693911441793546 ) ) ;
#6954=VERTEX_POINT ( 'NONE', #19766 ) ;
#6956=CARTESIAN_POINT ( 'NONE',  ( 0.3339603559181820169, 52.96017240013473071, 76.18796968951495785 ) ) ;
#6961=EDGE_LOOP ( 'NONE', ( #9416, #4110, #9942, #6927 ) ) ;
#6962=CARTESIAN_POINT ( 'NONE',  ( 0.5868117437017631444, 52.36192644938283536, 77.38375056423674891 ) ) ;
#6966=DIRECTION ( 'NONE',  ( 0.007885122365275663500, 0.9999689119394085113, 1.805443505845543142E-16 ) ) ;
#6968=ORIENTED_EDGE ( 'NONE', *, *, #1588, .F. ) ;
#6969=ADVANCED_FACE ( 'NONE', ( #14991 ), #4075, .F. ) ;
#6970=FACE_OUTER_BOUND ( 'NONE', #9746, .T. ) ;
#6971=ADVANCED_FACE ( 'NONE', ( #10217 ), #6126, .T. ) ;
#6972=ORIENTED_EDGE ( 'NONE', *, *, #6580, .F. ) ;
#6973=CARTESIAN_POINT ( 'NONE',  ( 0.5221537403065019678, 44.16218137147968292, 72.45433879953087342 ) ) ;
#6974=FACE_OUTER_BOUND ( 'NONE', #10315, .T. ) ;
#6977=VERTEX_POINT ( 'NONE', #5392 ) ;
#6979=ORIENTED_EDGE ( 'NONE', *, *, #5178, .F. ) ;
#6981=EDGE_CURVE ( 'NONE', #15226, #19138, #15199, .T. ) ;
#6982=CARTESIAN_POINT ( 'NONE',  ( -3.890009847151996603, 51.07470118294932604, 79.52219083255405963 ) ) ;
#6983=CARTESIAN_POINT ( 'NONE',  ( 8.300594306733913186, 41.56682737740558764, 77.52492703482499792 ) ) ;
#6985=B_SPLINE_SURFACE_WITH_KNOTS ( 'NONE', 3, 1, ( 
 ( #4720, #17512 ),
 ( #2934, #1140 ),
 ( #20798, #10938 ),
 ( #20686, #9549 ),
 ( #18901, #16031 ),
 ( #4313, #12824 ),
 ( #9339, #2731 ),
 ( #7835, #1236 ),
 ( #14318, #9234 ),
 ( #14210, #6124 ),
 ( #12627, #19003 ) ),
 .UNSPECIFIED., .F., .F., .F.,
 ( 4, 1, 1, 1, 1, 1, 1, 1, 4 ),
 ( 2, 2 ),
 ( 0.000000000000000000, 0.1895954080786773355, 0.3480750146108056442, 0.4761617831461403827, 0.5797469728315796100, 0.6725800605763750939, 0.7701180849273350226, 0.8764776678571430946, 1.000000000000000000 ),
 ( 0.000000000000000000, 1.000000000000000000 ),
 .UNSPECIFIED. ) ;
#6986=CARTESIAN_POINT ( 'NONE',  ( 8.285567280566995763, 41.54615094762161931, 75.97281361087948426 ) ) ;
#6988=CARTESIAN_POINT ( 'NONE',  ( 4.661142417382979630, 52.04529176935007939, 75.82370277575662953 ) ) ;
#6990=CARTESIAN_POINT ( 'NONE',  ( -7.956575413799908070, 41.77588473132961155, 78.56636689789523587 ) ) ;
#6991=VERTEX_POINT ( 'NONE', #8026 ) ;
#6992=EDGE_CURVE ( 'NONE', #16499, #8766, #2641, .T. ) ;
#6993=CARTESIAN_POINT ( 'NONE',  ( 4.401732967732903568, 36.93750505876209189, 75.58501954835062975 ) ) ;
#6994=ADVANCED_FACE ( 'NONE', ( #10857 ), #9142, .F. ) ;
#6995=EDGE_CURVE ( 'NONE', #18032, #7102, #10482, .T. ) ;
#6997=ORIENTED_EDGE ( 'NONE', *, *, #6732, .F. ) ;
#6998=CARTESIAN_POINT ( 'NONE',  ( 5.204008869086888645, 50.89421323063470481, 76.99291999501369332 ) ) ;
#7000=CARTESIAN_POINT ( 'NONE',  ( -4.435668263947954770, 37.63854610978014392, 78.92026643871187730 ) ) ;
#7002=CARTESIAN_POINT ( 'NONE',  ( -5.160557796315992540, 37.41935686500602287, 77.33669174070733732 ) ) ;
#7008=ORIENTED_EDGE ( 'NONE', *, *, #15634, .T. ) ;
#7009=CARTESIAN_POINT ( 'NONE',  ( 0.5221537403065010796, 44.16218137147968292, 78.18375056423674607 ) ) ;
#7011=DIRECTION ( 'NONE',  ( -1.540237394707284467E-16, -1.793354297423764243E-16, 1.000000000000000000 ) ) ;
#7012=ORIENTED_EDGE ( 'NONE', *, *, #9722, .F. ) ;
#7013=CARTESIAN_POINT ( 'NONE',  ( 0.3279640439667346752, 52.35988168082470651, 77.10139762306027933 ) ) ;
#7018=CARTESIAN_POINT ( 'NONE',  ( 1.561445875196035615, 52.20596665509935974, 76.85511030890285156 ) ) ;
#7019=CARTESIAN_POINT ( 'NONE',  ( -3.118155632002933331, 36.82473166443372037, 78.17158301229430606 ) ) ;
#7022=CARTESIAN_POINT ( 'NONE',  ( -8.188298522726004336, 42.90970694978335587, 78.73977153168188181 ) ) ;
#7023=ORIENTED_EDGE ( 'NONE', *, *, #17554, .F. ) ;
#7025=LINE ( 'NONE', #3630, #6365 ) ;
#7028=FACE_OUTER_BOUND ( 'NONE', #19945, .T. ) ;
#7029=EDGE_CURVE ( 'NONE', #15850, #13342, #4443, .T. ) ;
#7032=LINE ( 'NONE', #19906, #18794 ) ;
#7034=DIRECTION ( 'NONE',  ( 1.540237394707284220E-16, 1.793354297423764243E-16, -1.000000000000000000 ) ) ;
#7035=CARTESIAN_POINT ( 'NONE',  ( -4.574316323987747346, 51.33620267474496757, 79.54845644658969661 ) ) ;
#7036=CARTESIAN_POINT ( 'NONE',  ( 0.6775615626972071315, 52.96083427075867434, 77.39742084373497732 ) ) ;
#7037=CARTESIAN_POINT ( 'NONE',  ( 5.605180980092264953, 51.34796851126965578, 77.21343514867072599 ) ) ;
#7039=ORIENTED_EDGE ( 'NONE', *, *, #15179, .F. ) ;
#7040=LINE ( 'NONE', #1202, #16646 ) ;
#7043=FACE_OUTER_BOUND ( 'NONE', #9193, .T. ) ;
#7044=CARTESIAN_POINT ( 'NONE',  ( -7.871639067970514603, 41.50258186480986922, 76.21059579996631328 ) ) ;
#7045=CARTESIAN_POINT ( 'NONE',  ( 6.371724945467780898, 50.78175336232117587, 79.44748646226150868 ) ) ;
#7048=CARTESIAN_POINT ( 'NONE',  ( 5.494513770740271141, 37.64639101419628986, 76.49330797698027595 ) ) ;
#7050=CARTESIAN_POINT ( 'NONE',  ( 8.289263307265827052, 41.55743062947783528, 78.93669174070734584 ) ) ;
#7053=FACE_BOUND ( 'NONE', #7761, .T. ) ;
#7057=LINE ( 'NONE', #8782, #11918 ) ;
#7060=CARTESIAN_POINT ( 'NONE',  ( -4.463792963332829267, 40.72925446781975722, 72.45433879953085921 ) ) ;
#7061=CARTESIAN_POINT ( 'NONE',  ( -4.598246518171406727, 51.31910303412164609, 78.93669174070734584 ) ) ;
#7063=DIRECTION ( 'NONE',  ( 0.5941461771851692664, 0.8043570849667761591, 2.357623395011396791E-16 ) ) ;
#7065=ORIENTED_EDGE ( 'NONE', *, *, #14174, .F. ) ;
#7071=CARTESIAN_POINT ( 'NONE',  ( -3.625666805699581108, 36.28559471941820647, 77.96849812480175501 ) ) ;
#7073=LINE ( 'NONE', #490, #10289 ) ;
#7076=EDGE_LOOP ( 'NONE', ( #13473, #15820, #2932, #20763 ) ) ;
#7077=DIRECTION ( 'NONE',  ( -1.540237394707284467E-16, -1.793354297423764243E-16, 1.000000000000000000 ) ) ;
#7079=CARTESIAN_POINT ( 'NONE',  ( -4.682451852912701717, 37.82245906599816010, 75.37232954241834193 ) ) ;
#7080=PLANE ( 'NONE',  #19449 ) ;
#7083=CIRCLE ( 'NONE', #12211, 6.200000000000000178 ) ;
#7087=CARTESIAN_POINT ( 'NONE',  ( 6.447293898846322868, 38.50007296029209414, 76.59354538285809610 ) ) ;
#7088=B_SPLINE_CURVE_WITH_KNOTS ( 'NONE', 3,
 ( #521, #2231, #12134, #18612, #20301, #5526, #12238, #15430, #12036, #13932, #2551, #18291, #10232, #18510, #845 ),
 .UNSPECIFIED., .F., .F.,
 ( 4, 1, 1, 1, 1, 1, 1, 1, 1, 1, 1, 1, 4 ),
 ( 0.000000000000000000, 0.1167597168375007488, 0.2214683318549902913, 0.3169846747733736647, 0.4005759510517727939, 0.4723184013547362947, 0.5354911787873812834, 0.5872921887835030885, 0.6299408870648134373, 0.7051993628396346914, 0.7869278594151544182, 0.8829706743529757151, 1.000000000000000000 ),
 .UNSPECIFIED. ) ;
#7090=CARTESIAN_POINT ( 'NONE',  ( 4.163798982342816757, 51.48782638361205954, 77.30394856433355244 ) ) ;
#7092=CARTESIAN_POINT ( 'NONE',  ( -5.004817973257477348, 39.29348442311233214, 76.73301527011911105 ) ) ;
#7093=CARTESIAN_POINT ( 'NONE',  ( 0.8396437586116388685, 52.96357605663151702, 77.59858114993788547 ) ) ;
#7098=CARTESIAN_POINT ( 'NONE',  ( 8.378029088801538293, 41.81159710496287119, 76.29056865213834726 ) ) ;
#7099=CARTESIAN_POINT ( 'NONE',  ( 0.3839191465529612213, 52.96715465491344332, 76.04467822456393833 ) ) ;
#7100=( BOUNDED_CURVE ( )  B_SPLINE_CURVE ( 3, ( #12842, #9982, #11155, #17624 ),
 .UNSPECIFIED., .F., .F. ) 
 B_SPLINE_CURVE_WITH_KNOTS ( ( 4, 4 ),
 ( 4.703063163714124251, 4.858985947692485041 ),
 .UNSPECIFIED. ) 
 CURVE ( )  GEOMETRIC_REPRESENTATION_ITEM ( )  RATIONAL_B_SPLINE_CURVE ( ( 1.000000000000000000, 0.9979750330736136821, 0.9979750330736136821, 1.000000000000000000 ) ) 
 REPRESENTATION_ITEM ( '' )  );
#7102=VERTEX_POINT ( 'NONE', #20508 ) ;
#7103=CARTESIAN_POINT ( 'NONE',  ( -4.383473025373058718, 51.47257230871590394, 76.47051527011910821 ) ) ;
#7106=CARTESIAN_POINT ( 'NONE',  ( -3.425442721482995445, 52.15714568814760810, 78.86270620133520026 ) ) ;
#7109=CARTESIAN_POINT ( 'NONE',  ( -4.545392591669648930, 36.96495910869975887, 77.09144163344554102 ) ) ;
#7110=CARTESIAN_POINT ( 'NONE',  ( -6.812698123362908476, 47.79501813703141266, 78.79824701870994375 ) ) ;
#7112=DIRECTION ( 'NONE',  ( -0.3165065846431829311, -0.9485903129789527988, -2.188653791613874255E-16 ) ) ;
#7114=ORIENTED_EDGE ( 'NONE', *, *, #18489, .F. ) ;
#7117=CARTESIAN_POINT ( 'NONE',  ( 8.316824854331539285, 42.08419425066229991, 79.51559944055343010 ) ) ;
#7118=DIRECTION ( 'NONE',  ( -1.540237394707284220E-16, -1.793354297423764243E-16, 1.000000000000000000 ) ) ;
#7123=VECTOR ( 'NONE', #18887, 1000.000000000000227 ) ;
#7127=CARTESIAN_POINT ( 'NONE',  ( -7.266087475274113139, 41.62398317295264860, 78.93401657524854897 ) ) ;
#7128=CARTESIAN_POINT ( 'NONE',  ( -3.215335549418882444, 36.89651455478302466, 77.93013364623398331 ) ) ;
#7129=CARTESIAN_POINT ( 'NONE',  ( -7.082284374571017338, 47.04405276229815769, 78.10358362899698648 ) ) ;
#7131=AXIS2_PLACEMENT_3D ( 'NONE', #8372, #16562, #14754 ) ;
#7132=AXIS2_PLACEMENT_3D ( 'NONE', #18427, #2571, #13528 ) ;
#7133=CARTESIAN_POINT ( 'NONE',  ( 6.877103025211564358, 37.88742324339783352, 76.41040896618429201 ) ) ;
#7134=ORIENTED_EDGE ( 'NONE', *, *, #1943, .T. ) ;
#7138=CARTESIAN_POINT ( 'NONE',  ( -4.777409764772176715, 51.19107953768585872, 78.82882669246485818 ) ) ;
#7141=LINE ( 'NONE', #8657, #12348 ) ;
#7143=LINE ( 'NONE', #15563, #10875 ) ;
#7145=CARTESIAN_POINT ( 'NONE',  ( 0.8488783891544954274, 52.96357957300006092, 76.31365475201417325 ) ) ;
#7147=ORIENTED_EDGE ( 'NONE', *, *, #19042, .T. ) ;
#7149=ADVANCED_FACE ( 'NONE', ( #6035 ), #4329, .T. ) ;
#7150=CARTESIAN_POINT ( 'NONE',  ( 0.3869120917952209582, 35.96329670974013482, 78.57639762306027365 ) ) ;
#7151=ORIENTED_EDGE ( 'NONE', *, *, #12651, .T. ) ;
#7154=CARTESIAN_POINT ( 'NONE',  ( 6.961260622506120654, 50.34628710563859499, 76.69700829373513784 ) ) ;
#7156=CARTESIAN_POINT ( 'NONE',  ( 0.5221537403065015237, 44.16218137147968292, 75.45433879953088763 ) ) ;
#7158=CARTESIAN_POINT ( 'NONE',  ( -5.772695632942803634, 37.87151842650609268, 75.75097338717934292 ) ) ;
#7159=EDGE_CURVE ( 'NONE', #445, #8755, #6036, .T. ) ;
#7160=CARTESIAN_POINT ( 'NONE',  ( -4.230491984614289436, 51.58188695944873103, 75.39163409230444302 ) ) ;
#7161=CARTESIAN_POINT ( 'NONE',  ( 5.146921702088428141, 37.39801444809555875, 77.71779572520892998 ) ) ;
#7162=ORIENTED_EDGE ( 'NONE', *, *, #15267, .F. ) ;
#7163=CARTESIAN_POINT ( 'NONE',  ( 8.790412360755956556, 41.13914800073450095, 78.76104738055306598 ) ) ;
#7166=CARTESIAN_POINT ( 'NONE',  ( -4.307156007511903084, 51.52710565553512367, 75.38014013087713749 ) ) ;
#7170=EDGE_LOOP ( 'NONE', ( #20841, #14542, #10169, #16391 ) ) ;
#7172=CARTESIAN_POINT ( 'NONE',  ( 0.3333674555516544236, 52.96015614911942748, 77.71750738947619652 ) ) ;
#7174=CARTESIAN_POINT ( 'NONE',  ( 5.378304226687590450, 36.81643649649897299, 75.37835156746757548 ) ) ;
#7175=CARTESIAN_POINT ( 'NONE',  ( -6.341010505665811259, 41.98571378962061829, 78.93669174070734584 ) ) ;
#7176=ORIENTED_EDGE ( 'NONE', *, *, #19619, .T. ) ;
#7177=CARTESIAN_POINT ( 'NONE',  ( 2.113956822022224014, 52.20619733064047807, 78.36540345550628217 ) ) ;
#7178=AXIS2_PLACEMENT_3D ( 'NONE', #8606, #15084, #498 ) ;
#7180=CARTESIAN_POINT ( 'NONE',  ( -4.421065211396600247, 50.69879487670102236, 76.08363728426196815 ) ) ;
#7185=CARTESIAN_POINT ( 'NONE',  ( -4.877877647307895970, 37.21055242598473001, 76.09452555557021469 ) ) ;
#7186=ADVANCED_FACE ( 'NONE', ( #2538 ), #9738, .T. ) ;
#7187=CARTESIAN_POINT ( 'NONE',  ( 0.3821786226492928651, 35.36301154328572949, 75.45433879953087342 ) ) ;
#7190=CARTESIAN_POINT ( 'NONE',  ( 2.106328753683349042, 52.20158602024299910, 76.31288873172051979 ) ) ;
#7191=EDGE_LOOP ( 'NONE', ( #8838, #387, #18907, #14194 ) ) ;
#7192=CIRCLE ( 'NONE', #8916, 8.199999999999995737 ) ;
#7193=CARTESIAN_POINT ( 'NONE',  ( 6.898851416363126710, 50.39238627222024292, 76.00796742194241062 ) ) ;
#7194=CARTESIAN_POINT ( 'NONE',  ( 0.3284562911652677553, 52.35625317208734941, 77.72734411258261389 ) ) ;
#7196=VECTOR ( 'NONE', #15644, 1000.000000000000000 ) ;
#7197=VERTEX_POINT ( 'NONE', #8127 ) ;
#7198=CARTESIAN_POINT ( 'NONE',  ( 6.487242172018640396, 49.78241043515765085, 78.48669174070734300 ) ) ;
#7200=LINE ( 'NONE', #20177, #2304 ) ;
#7201=CARTESIAN_POINT ( 'NONE',  ( 5.599231707071657738, 51.35236299959863970, 78.30875056423674607 ) ) ;
#7203=DIRECTION ( 'NONE',  ( -0.5941461771851691553, -0.8043570849667760481, -2.357623395011396791E-16 ) ) ;
#7204=DIRECTION ( 'NONE',  ( -0.3165065846431824870, -0.9485903129789529098, 0.000000000000000000 ) ) ;
#7205=DIRECTION ( 'NONE',  ( -0.5941461771851692664, -0.8043570849667761591, -2.357623395011396791E-16 ) ) ;
#7206=CARTESIAN_POINT ( 'NONE',  ( 8.807466118993687587, 41.19025919604325026, 76.04813117819971069 ) ) ;
#7209=CARTESIAN_POINT ( 'NONE',  ( -6.779084170873278303, 43.37104029486602030, 76.06610350541322418 ) ) ;
#7210=CARTESIAN_POINT ( 'NONE',  ( 5.270799808619019089, 50.67012946595514933, 75.36064185147203887 ) ) ;
#7215=DIRECTION ( 'NONE',  ( -0.8136266022445296509, -0.5813877811925719508, -2.295812393977019367E-16 ) ) ;
#7216=ORIENTED_EDGE ( 'NONE', *, *, #16509, .F. ) ;
#7217=CARTESIAN_POINT ( 'NONE',  ( -4.664487479516252755, 37.05292970491732518, 75.97486526700035370 ) ) ;
#7218=CARTESIAN_POINT ( 'NONE',  ( -3.767527516087995743, 38.37954780350102624, 75.97198585835440099 ) ) ;
#7219=CARTESIAN_POINT ( 'NONE',  ( -4.181418169567056253, 51.61695331097443784, 79.50772166908967620 ) ) ;
#7222=VECTOR ( 'NONE', #13875, 1000.000000000000114 ) ;
#7223=CARTESIAN_POINT ( 'NONE',  ( -4.956093006374735488, 37.26832696102056275, 77.32892190166411694 ) ) ;
#7225=CARTESIAN_POINT ( 'NONE',  ( 0.3326973149608338787, 52.96014171822455552, 78.50066232894263862 ) ) ;
#7226=VECTOR ( 'NONE', #5173, 1000.000000000000114 ) ;
#7230=CARTESIAN_POINT ( 'NONE',  ( 9.294532183588495755, 42.65002709052886587, 79.09515810002898206 ) ) ;
#7231=CARTESIAN_POINT ( 'NONE',  ( -3.934466035114215554, 36.51369227099507242, 75.53057231289058393 ) ) ;
#7232=LINE ( 'NONE', #1177, #9599 ) ;
#7241=CARTESIAN_POINT ( 'NONE',  ( -3.568560454108622881, 36.24341255788211669, 78.11242031084098869 ) ) ;
#7242=CARTESIAN_POINT ( 'NONE',  ( -6.846424213726333363, 47.75094062703928444, 78.32492703482499508 ) ) ;
#7244=CARTESIAN_POINT ( 'NONE',  ( -8.008709175654551871, 42.00064040251377406, 79.51261075138046408 ) ) ;
#7245=CARTESIAN_POINT ( 'NONE',  ( 5.901490163600553451, 51.12909685347405286, 78.67852979887695142 ) ) ;
#7246=CARTESIAN_POINT ( 'NONE',  ( 5.576345338833139209, 50.61463229589440260, 77.01219674908871582 ) ) ;
#7247=VERTEX_POINT ( 'NONE', #6838 ) ;
#7254=CARTESIAN_POINT ( 'NONE',  ( -2.938659133435201465, 51.58520783560351930, 78.58955347608575437 ) ) ;
#7256=CARTESIAN_POINT ( 'NONE',  ( 5.668901936282467524, 51.30090040776863702, 77.27261723006257910 ) ) ;
#7257=CARTESIAN_POINT ( 'NONE',  ( -3.964734524320792541, 36.53605038468284505, 79.39152984579853012 ) ) ;
#7258=ORIENTED_EDGE ( 'NONE', *, *, #9501, .F. ) ;
#7259=CARTESIAN_POINT ( 'NONE',  ( 5.275862854764398868, 50.84374355665323719, 78.00102387806451532 ) ) ;
#7264=CARTESIAN_POINT ( 'NONE',  ( -7.157526761188767850, 41.72840140584739288, 76.21059579996631328 ) ) ;
#7265=CARTESIAN_POINT ( 'NONE',  ( 5.760694563098077481, 51.23309689197249384, 79.54845644658969661 ) ) ;
#7266=ADVANCED_FACE ( 'NONE', ( #16439 ), #2908, .F. ) ;
#7270=ORIENTED_EDGE ( 'NONE', *, *, #10429, .T. ) ;
#7271=CARTESIAN_POINT ( 'NONE',  ( 8.221417502521635612, 41.35409244860189659, 78.83414475571305502 ) ) ;
#7272=EDGE_CURVE ( 'NONE', #16704, #9302, #5651, .T. ) ;
#7277=ADVANCED_FACE ( 'NONE', ( #20340 ), #989, .T. ) ;
#7279=CARTESIAN_POINT ( 'NONE',  ( -7.895868156129457027, 41.57675978324414245, 77.84082762752957763 ) ) ;
#7280=ORIENTED_EDGE ( 'NONE', *, *, #106, .F. ) ;
#7283=DIRECTION ( 'NONE',  ( 0.8043570849667760481, -0.5941461771851693774, 1.733862608106482338E-17 ) ) ;
#7284=ORIENTED_EDGE ( 'NONE', *, *, #20291, .T. ) ;
#7285=B_SPLINE_CURVE_WITH_KNOTS ( 'NONE', 3,
 ( #5861, #12364, #10775, #1079, #7567, #5959, #18938, #8851, #3937, #10463, #16928, #2351, #5639, #12148, #6886, #8611 ),
 .UNSPECIFIED., .F., .F.,
 ( 4, 2, 2, 2, 2, 2, 2, 4 ),
 ( 0.000000000000000000, 0.0007059943671309979558, 0.0008824929589137576634, 0.001058991550696517263, 0.001411988734262035810, 0.001764985917827553924, 0.002117983101393071822, 0.002823977468524106749 ),
 .UNSPECIFIED. ) ;
#7287=CARTESIAN_POINT ( 'NONE',  ( -4.796459876899764829, 51.17746702502860501, 78.71090438869831019 ) ) ;
#7288=EDGE_CURVE ( 'NONE', #19085, #14373, #1636, .T. ) ;
#7294=DIRECTION ( 'NONE',  ( 0.7938652969193402686, -0.6080936526121349939, 1.322136515274840486E-17 ) ) ;
#7296=CARTESIAN_POINT ( 'NONE',  ( -4.895593109503407980, 37.22363812428620378, 76.38448585835440952 ) ) ;
#7298=CARTESIAN_POINT ( 'NONE',  ( 9.271561067608034890, 45.68041113525027441, 79.47125056423675460 ) ) ;
#7299=ORIENTED_EDGE ( 'NONE', *, *, #13409, .T. ) ;
#7301=CARTESIAN_POINT ( 'NONE',  ( 2.094612936638713840, 52.20167840376603152, 76.22990676838142576 ) ) ;
#7302=ORIENTED_EDGE ( 'NONE', *, *, #10844, .F. ) ;
#7303=CARTESIAN_POINT ( 'NONE',  ( -0.6075024185379280794, 52.28440471269894374, 79.22274745980693922 ) ) ;
#7304=ADVANCED_FACE ( 'NONE', ( #3962 ), #10486, .T. ) ;
#7305=DIRECTION ( 'NONE',  ( -0.9999689119394086223, 0.007885122365275665235, -1.526048693634353392E-16 ) ) ;
#7307=B_SPLINE_SURFACE_WITH_KNOTS ( 'NONE', 3, 1, ( 
 ( #9642, #12336 ),
 ( #7924, #16019 ),
 ( #14411, #15522 ),
 ( #19295, #6311 ),
 ( #12812, #8027 ),
 ( #20400, #9036 ),
 ( #20980, #10651 ),
 ( #6414, #19402 ),
 ( #18707, #4120 ),
 ( #11343, #9143 ),
 ( #5718, #20782 ),
 ( #4821, #937 ),
 ( #9740, #7424 ),
 ( #15632, #13918 ),
 ( #17812, #18818 ),
 ( #16221, #7320 ),
 ( #13809, #2539 ),
 ( #147, #8129 ),
 ( #6629, #350 ),
 ( #8557, #17913 ),
 ( #13032, #11441 ),
 ( #4920, #14621 ),
 ( #6839, #13130 ) ),
 .UNSPECIFIED., .F., .F., .F.,
 ( 4, 1, 1, 1, 1, 1, 1, 1, 1, 1, 1, 1, 1, 1, 1, 1, 1, 1, 1, 1, 4 ),
 ( 2, 2 ),
 ( 0.000000000000000000, 0.04683093660151300269, 0.09055667580802433114, 0.1312013806050136844, 0.1681729499244319359, 0.2024082766003676426, 0.2330515569695218725, 0.2607881417524846590, 0.2857054801288026469, 0.3326652789510584074, 0.3814982805224741425, 0.4333318279156733732, 0.4889629060548432160, 0.5467408684218817427, 0.6046224851005120859, 0.6645427963802341687, 0.7261481924644412889, 0.7902890061914499276, 0.8570127982043956871, 0.9269126820953633716, 1.000000000000000000 ),
 ( 0.000000000000000000, 1.000000000000000000 ),
 .UNSPECIFIED. ) ;
#7308=ORIENTED_EDGE ( 'NONE', *, *, #17478, .F. ) ;
#7309=ADVANCED_FACE ( 'NONE', ( #8880 ), #15367, .F. ) ;
#7312=DIRECTION ( 'NONE',  ( -0.5813877811927012917, 0.8136266022444372803, 5.636455622144620416E-17 ) ) ;
#7313=DIRECTION ( 'NONE',  ( 0.8136266022444427204, 0.5813877811926937422, 2.295812393977104662E-16 ) ) ;
#7314=CARTESIAN_POINT ( 'NONE',  ( 7.677801029594266247, 40.18576601801834869, 76.30598982719874357 ) ) ;
#7316=CARTESIAN_POINT ( 'NONE',  ( -3.805620430632945528, 51.12781903265568673, 79.50514382629147292 ) ) ;
#7317=CARTESIAN_POINT ( 'NONE',  ( -0.9388773962491546721, 52.84004908296358138, 77.21536821129558348 ) ) ;
#7319=CARTESIAN_POINT ( 'NONE',  ( 8.255193350648697859, 41.45511835277029178, 75.98994273744924044 ) ) ;
#7320=CARTESIAN_POINT ( 'NONE',  ( -4.952713483362852109, 50.14603833638137331, 75.54244301425877950 ) ) ;
#7324=VERTEX_POINT ( 'NONE', #13973 ) ;
#7325=CARTESIAN_POINT ( 'NONE',  ( 8.949064546045571333, 41.61463866475444462, 78.77153038569251464 ) ) ;
#7332=CARTESIAN_POINT ( 'NONE',  ( -8.312169971356507148, 42.89858049018356212, 78.28007409364852265 ) ) ;
#7333=CARTESIAN_POINT ( 'NONE',  ( -0.1994209430448784792, 35.36759766960258844, 76.86610350541323555 ) ) ;
#7334=DIRECTION ( 'NONE',  ( 0.007885122365275663500, 0.9999689119394085113, 1.805443505845543142E-16 ) ) ;
#7335=ORIENTED_EDGE ( 'NONE', *, *, #10629, .T. ) ;
#7337=CARTESIAN_POINT ( 'NONE',  ( 9.307108147255313213, 42.68771805144258735, 79.03485483908291087 ) ) ;
#7338=CARTESIAN_POINT ( 'NONE',  ( 5.665287683258889651, 37.02150436742986273, 75.36022115247205022 ) ) ;
#7340=CARTESIAN_POINT ( 'NONE',  ( 5.924340528221679669, 51.11221820959726614, 77.13671500005938242 ) ) ;
#7342=CARTESIAN_POINT ( 'NONE',  ( 8.445623910622046537, 42.47021319322472976, 78.07975471416389723 ) ) ;
#7344=CARTESIAN_POINT ( 'NONE',  ( -4.383574773872678243, 51.47249960296332461, 76.44257241107362688 ) ) ;
#7345=CARTESIAN_POINT ( 'NONE',  ( -7.727380346712589443, 47.23718031655728566, 77.58227997600145898 ) ) ;
#7348=CARTESIAN_POINT ( 'NONE',  ( 6.582016959483238949, 37.67656554461878926, 75.62429547252081363 ) ) ;
#7349=ORIENTED_EDGE ( 'NONE', *, *, #17420, .T. ) ;
#7350=CARTESIAN_POINT ( 'NONE',  ( 5.916041096196198446, 51.11834866571297908, 77.16780247135808679 ) ) ;
#7351=ORIENTED_EDGE ( 'NONE', *, *, #13418, .F. ) ;
#7352=CARTESIAN_POINT ( 'NONE',  ( -4.413575733319255789, 50.70414658352780179, 78.86176377286571437 ) ) ;
#7355=ORIENTED_EDGE ( 'NONE', *, *, #14780, .T. ) ;
#7359=CARTESIAN_POINT ( 'NONE',  ( -2.920516602815223184, 51.59817182374411715, 78.36353918055804968 ) ) ;
#7360=LINE ( 'NONE', #17157, #8078 ) ;
#7361=CARTESIAN_POINT ( 'NONE',  ( 5.571366797620176392, 51.37294568574342435, 77.09285305542944400 ) ) ;
#7363=ORIENTED_EDGE ( 'NONE', *, *, #8965, .T. ) ;
#7364=CARTESIAN_POINT ( 'NONE',  ( 6.457023732898393042, 39.40536329938229443, 75.45433879953087342 ) ) ;
#7365=VERTEX_POINT ( 'NONE', #8984 ) ;
#7367=DIRECTION ( 'NONE',  ( -0.5813877811927011807, 0.8136266022444372803, 5.636455622144619183E-17 ) ) ;
#7370=B_SPLINE_CURVE_WITH_KNOTS ( 'NONE', 3,
 ( #17742, #13166, #4956, #3174, #8275, #19435, #179, #11581, #11375, #17846, #3269, #19639 ),
 .UNSPECIFIED., .F., .F.,
 ( 4, 2, 2, 2, 2, 4 ),
 ( 0.000000000000000000, 0.0001366260637585213467, 0.0002049390956377732380, 0.0002732521275170251293, 0.0004098781912754880376, 0.0005465042550339509458 ),
 .UNSPECIFIED. ) ;
#7371=CARTESIAN_POINT ( 'NONE',  ( -7.308728793983235938, 40.14750922464471472, 78.21036603407506504 ) ) ;
#7374=CARTESIAN_POINT ( 'NONE',  ( 6.488325228803680567, 49.78755270998220084, 78.57237519692213823 ) ) ;
#7376=VERTEX_POINT ( 'NONE', #15467 ) ;
#7377=CARTESIAN_POINT ( 'NONE',  ( 4.574454570626803829, 51.29112378112938586, 77.67115886575356853 ) ) ;
#7378=ORIENTED_EDGE ( 'NONE', *, *, #19135, .F. ) ;
#7380=EDGE_CURVE ( 'NONE', #5156, #13025, #5777, .T. ) ;
#7382=CARTESIAN_POINT ( 'NONE',  ( -8.036666733872158019, 42.02200910348221186, 77.21863129581211638 ) ) ;
#7383=EDGE_LOOP ( 'NONE', ( #16554, #19330, #15299, #17876 ) ) ;
#7386=CARTESIAN_POINT ( 'NONE',  ( 0.3442881027912784719, 52.96038515679411773, 77.58553688243358692 ) ) ;
#7387=AXIS2_PLACEMENT_3D ( 'NONE', #5830, #15739, #12334 ) ;
#7393=CARTESIAN_POINT ( 'NONE',  ( 0.7788067644200915574, 52.35270196965525002, 78.85266037376247539 ) ) ;
#7398=EDGE_CURVE ( 'NONE', #9413, #15226, #10799, .T. ) ;
#7400=CARTESIAN_POINT ( 'NONE',  ( -4.804644443005473775, 51.17161863374555963, 78.45066232894264147 ) ) ;
#7401=CARTESIAN_POINT ( 'NONE',  ( 5.431844598077052666, 36.85469448565577011, 76.44059830477070250 ) ) ;
#7403=CARTESIAN_POINT ( 'NONE',  ( -7.221822550567737586, 41.46565244290277263, 78.36256670375607314 ) ) ;
#7404=ORIENTED_EDGE ( 'NONE', *, *, #3244, .F. ) ;
#7406=CARTESIAN_POINT ( 'NONE',  ( 1.561428751595478115, 52.95872086824613945, 75.52862058684291924 ) ) ;
#7407=ORIENTED_EDGE ( 'NONE', *, *, #4434, .F. ) ;
#7409=DIRECTION ( 'NONE',  ( 1.540237394707284467E-16, 1.793354297423764243E-16, -1.000000000000000000 ) ) ;
#7416=CARTESIAN_POINT ( 'NONE',  ( 7.672101664393531806, 40.16868465895075957, 76.70090004521539129 ) ) ;
#7417=VECTOR ( 'NONE', #16456, 1000.000000000000227 ) ;
#7419=CARTESIAN_POINT ( 'NONE',  ( -7.486598725001505805, 40.28313368935070571, 79.09912640779528203 ) ) ;
#7422=DIRECTION ( 'NONE',  ( 0.3165065846431826535, 0.9485903129789529098, 2.188653791613874008E-16 ) ) ;
#7424=CARTESIAN_POINT ( 'NONE',  ( -5.209532200270762914, 49.96252508401233428, 75.79002994479621691 ) ) ;
#7425=CARTESIAN_POINT ( 'NONE',  ( 5.159368991072407873, 51.67727186915629289, 75.44114465464750197 ) ) ;
#7426=EDGE_CURVE ( 'NONE', #5649, #18616, #12786, .T. ) ;
#7428=CARTESIAN_POINT ( 'NONE',  ( -3.539401246598059991, 43.09270903039240608, 79.40903933791013003 ) ) ;
#7429=EDGE_LOOP ( 'NONE', ( #5024, #14521, #10473, #1431 ) ) ;
#7431=CARTESIAN_POINT ( 'NONE',  ( 8.898741081898894123, 41.46381605024582484, 78.92561463894257656 ) ) ;
#7433=EDGE_CURVE ( 'NONE', #13846, #12245, #17678, .T. ) ;
#7435=DIRECTION ( 'NONE',  ( 0.8136266022444372803, 0.5813877811927012917, 2.295812393977109100E-16 ) ) ;
#7438=( NAMED_UNIT ( * ) SI_UNIT ( $, .STERADIAN. ) SOLID_ANGLE_UNIT ( ) );
#7439=EDGE_CURVE ( 'NONE', #9222, #8755, #6285, .T. ) ;
#7440=CARTESIAN_POINT ( 'NONE',  ( -4.770044440429786370, 37.13090037985040226, 77.30667006270941499 ) ) ;
#7441=CARTESIAN_POINT ( 'NONE',  ( -8.133968313267025962, 42.33505088355195056, 79.40422342893963048 ) ) ;
#7442=FACE_OUTER_BOUND ( 'NONE', #18504, .T. ) ;
#7444=CARTESIAN_POINT ( 'NONE',  ( 0.5759855363013707263, 51.36198072897979472, 78.93669174070734584 ) ) ;
#7448=CARTESIAN_POINT ( 'NONE',  ( 8.951509595531131680, 41.62196663317372725, 77.18036020728871449 ) ) ;
#7450=CARTESIAN_POINT ( 'NONE',  ( 9.026838159693452823, 41.84773111872319618, 78.13669174070733447 ) ) ;
#7453=VECTOR ( 'NONE', #5492, 1000.000000000000000 ) ;
#7454=FACE_OUTER_BOUND ( 'NONE', #15779, .T. ) ;
#7458=CARTESIAN_POINT ( 'NONE',  ( 5.833066520072705430, 37.14139298144173296, 75.36337631951366234 ) ) ;
#7459=ORIENTED_EDGE ( 'NONE', *, *, #18091, .T. ) ;
#7465=ORIENTED_EDGE ( 'NONE', *, *, #20418, .T. ) ;
#7467=CARTESIAN_POINT ( 'NONE',  ( -0.5342115424629445553, 52.21627705124925711, 75.64626500862765113 ) ) ;
#7468=VECTOR ( 'NONE', #20553, 1000.000000000000000 ) ;
#7471=CARTESIAN_POINT ( 'NONE',  ( 0.7902174608934043887, 52.95811370980002408, 77.46569632448046150 ) ) ;
#7475=CARTESIAN_POINT ( 'NONE',  ( 4.033749877938553219, 36.75212424151919777, 78.77947436490163113 ) ) ;
#7478=CARTESIAN_POINT ( 'NONE',  ( -3.729174670837895889, 37.14778277730540168, 75.44287404548305176 ) ) ;
#7479=DIRECTION ( 'NONE',  ( 1.540237394707284220E-16, 1.793354297423764243E-16, -1.000000000000000000 ) ) ;
#7480=VECTOR ( 'NONE', #16925, 1000.000000000000227 ) ;
#7485=CARTESIAN_POINT ( 'NONE',  ( 5.670718203856349504, 37.02538481862475805, 75.97247164366282846 ) ) ;
#7486=CARTESIAN_POINT ( 'NONE',  ( 5.674841441279768084, 50.54324618507919809, 79.53726082601099279 ) ) ;
#7487=B_SPLINE_SURFACE_WITH_KNOTS ( 'NONE', 3, 1, ( 
 ( #9900, #6676 ),
 ( #16379, #13182 ),
 ( #19656, #11599 ),
 ( #6786, #18177 ),
 ( #18074, #3593 ),
 ( #10102, #16585 ),
 ( #2005, #5507 ),
 ( #610, #7090 ),
 ( #5611, #20281 ),
 ( #10645, #10531 ),
 ( #12020, #18275 ),
 ( #8614, #17000 ),
 ( #10324, #16796 ),
 ( #17113, #2213 ),
 ( #15196, #404 ) ),
 .UNSPECIFIED., .F., .F., .F.,
 ( 4, 1, 1, 1, 1, 1, 1, 1, 1, 1, 1, 1, 4 ),
 ( 2, 2 ),
 ( 0.000000000000000000, 0.1027118292588455328, 0.1981555131143932502, 0.2874887429483043433, 0.3729525961046017413, 0.4183424594053214429, 0.4719402630404010424, 0.5343443080544488799, 0.6066182697135418245, 0.6887512500569755725, 0.7816623524051020677, 0.8855466611608181493, 1.000000000000000000 ),
 ( 0.000000000000000000, 1.000000000000000000 ),
 .UNSPECIFIED. ) ;
#7489=AXIS2_PLACEMENT_3D ( 'NONE', #8045, #20997, #12732 ) ;
#7491=CARTESIAN_POINT ( 'NONE',  ( 8.851169967151880869, 41.32124240149376249, 78.93505401271374922 ) ) ;
#7500=FACE_OUTER_BOUND ( 'NONE', #8320, .T. ) ;
#7501=FACE_OUTER_BOUND ( 'NONE', #9131, .T. ) ;
#7502=CARTESIAN_POINT ( 'NONE',  ( 6.012275498921958672, 37.26944915646792822, 78.37198585835440667 ) ) ;
#7515=CARTESIAN_POINT ( 'NONE',  ( 5.427951760950261217, 36.85191280677083370, 76.67247627436783830 ) ) ;
#7516=CARTESIAN_POINT ( 'NONE',  ( 0.5221537403065005245, 44.16218137147968292, 82.45433879953087342 ) ) ;
#7518=CARTESIAN_POINT ( 'NONE',  ( 1.826366013274308475, 52.20379362933912404, 75.70482343270806780 ) ) ;
#7523=ORIENTED_EDGE ( 'NONE', *, *, #6448, .F. ) ;
#7525=CARTESIAN_POINT ( 'NONE',  ( -4.616093716651582746, 50.55342697692977083, 75.38579245895105885 ) ) ;
#7526=VECTOR ( 'NONE', #18632, 1000.000000000000000 ) ;
#7528=CARTESIAN_POINT ( 'NONE',  ( 4.239508620224502700, 51.44272066563755175, 79.02133806855546538 ) ) ;
#7530=CARTESIAN_POINT ( 'NONE',  ( 7.670823270696295104, 40.16485323194035573, 77.08252479744105301 ) ) ;
#7531=VERTEX_POINT ( 'NONE', #12558 ) ;
#7532=CARTESIAN_POINT ( 'NONE',  ( 6.436008563395697379, 49.84285157267152755, 75.88622433235630638 ) ) ;
#7533=CARTESIAN_POINT ( 'NONE',  ( -7.782852850910068732, 41.21998227328707287, 79.53187240040659844 ) ) ;
#7537=LINE ( 'NONE', #5941, #20 ) ;
#7540=VECTOR ( 'NONE', #11765, 1000.000000000000000 ) ;
#7544=FACE_OUTER_BOUND ( 'NONE', #8188, .T. ) ;
#7546=CARTESIAN_POINT ( 'NONE',  ( -4.452986336060421380, 50.68046193778529585, 78.55837781537462661 ) ) ;
#7547=PRESENTATION_STYLE_ASSIGNMENT (( #949 ) ) ;
#7549=CARTESIAN_POINT ( 'NONE',  ( -8.311994772346579907, 42.89802645589339392, 78.33204358585338412 ) ) ;
#7550=CARTESIAN_POINT ( 'NONE',  ( 8.647112560730464637, 43.05498688647372774, 77.35098120998416960 ) ) ;
#7552=EDGE_LOOP ( 'NONE', ( #6433, #11676, #5347, #2602 ) ) ;
#7553=VECTOR ( 'NONE', #8797, 1000.000000000000227 ) ;
#7554=PLANE ( 'NONE',  #18574 ) ;
#7555=CARTESIAN_POINT ( 'NONE',  ( 6.573693162767834330, 44.00881163587200717, 72.45432679953087529 ) ) ;
#7557=LINE ( 'NONE', #12142, #4491 ) ;
#7561=( BOUNDED_CURVE ( )  B_SPLINE_CURVE ( 3, ( #2349, #8848, #5539, #10356 ),
 .UNSPECIFIED., .F., .F. ) 
 B_SPLINE_CURVE_WITH_KNOTS ( ( 4, 4 ),
 ( 1.735985064777024300, 1.737340566640508621 ),
 .UNSPECIFIED. ) 
 CURVE ( )  GEOMETRIC_REPRESENTATION_ITEM ( )  RATIONAL_B_SPLINE_CURVE ( ( 1.000000000000000000, 0.9999998468845641142, 0.9999998468845641142, 1.000000000000000000 ) ) 
 REPRESENTATION_ITEM ( '' )  );
#7562=CARTESIAN_POINT ( 'NONE',  ( 5.675263920727823042, 51.29620106613522523, 77.96371040190514634 ) ) ;
#7564=FACE_OUTER_BOUND ( 'NONE', #7675, .T. ) ;
#7567=CARTESIAN_POINT ( 'NONE',  ( -0.9186189192224099020, 52.84343824287718405, 78.59945191334355741 ) ) ;
#7568=ORIENTED_EDGE ( 'NONE', *, *, #16650, .F. ) ;
#7570=AXIS2_PLACEMENT_3D ( 'NONE', #2507, #7283, #18350 ) ;
#7573=CARTESIAN_POINT ( 'NONE',  ( 5.753005855668248181, 51.23877623043087937, 78.93669174070734584 ) ) ;
#7574=CARTESIAN_POINT ( 'NONE',  ( 5.555396287804228450, 50.63010651601021550, 77.16780247135808679 ) ) ;
#7576=DIRECTION ( 'NONE',  ( -1.540237394707284467E-16, -1.793354297423764243E-16, 1.000000000000000000 ) ) ;
#7578=ORIENTED_EDGE ( 'NONE', *, *, #354, .F. ) ;
#7580=DIRECTION ( 'NONE',  ( 1.540237394707284220E-16, 1.793354297423764243E-16, -1.000000000000000000 ) ) ;
#7581=DIRECTION ( 'NONE',  ( 0.5813877811927011807, -0.8136266022444372803, -5.636455622144619183E-17 ) ) ;
#7585=CARTESIAN_POINT ( 'NONE',  ( -3.131615841865540428, 36.83467417924890697, 78.81697279211699936 ) ) ;
#7586=ORIENTED_EDGE ( 'NONE', *, *, #9125, .F. ) ;
#7588=VECTOR ( 'NONE', #8756, 1000.000000000000000 ) ;
#7591=DIRECTION ( 'NONE',  ( -0.3165065846431826535, -0.9485903129789529098, -2.188653791613874008E-16 ) ) ;
#7598=ORIENTED_EDGE ( 'NONE', *, *, #8884, .F. ) ;
#7599=FACE_OUTER_BOUND ( 'NONE', #16701, .T. ) ;
#7601=VECTOR ( 'NONE', #15764, 1000.000000000000227 ) ;
#7602=LINE ( 'NONE', #20465, #6790 ) ;
#7604=CARTESIAN_POINT ( 'NONE',  ( 5.712782733624313103, 51.26848743039855094, 75.36064185147203887 ) ) ;
#7605=ORIENTED_EDGE ( 'NONE', *, *, #10821, .T. ) ;
#7607=CARTESIAN_POINT ( 'NONE',  ( 8.787829143201870252, 41.13140593384865440, 78.45948585835439815 ) ) ;
#7609=CARTESIAN_POINT ( 'NONE',  ( 4.394267649348433835, 36.11327998621098345, 76.69403369658814995 ) ) ;
#7611=ORIENTED_EDGE ( 'NONE', *, *, #17284, .T. ) ;
#7615=B_SPLINE_CURVE_WITH_KNOTS ( 'NONE', 3,
 ( #18914, #10855, #20605, #16048, #2950, #1572, #17427, #3169, #12844, #11056, #9566, #11372, #1157, #9455 ),
 .UNSPECIFIED., .F., .F.,
 ( 4, 2, 2, 2, 2, 2, 4 ),
 ( 0.000000000000000000, 0.0005039684972345963082, 0.001007936994469192616, 0.001259921243086484103, 0.001511905491703775806, 0.001763889740321067509, 0.002015873988938359212 ),
 .UNSPECIFIED. ) ;
#7616=CARTESIAN_POINT ( 'NONE',  ( 0.4527646634920744484, 35.36245494641288190, 80.45433879953087342 ) ) ;
#7617=CARTESIAN_POINT ( 'NONE',  ( 4.393996117251955269, 36.11308595931626542, 76.96022115247204454 ) ) ;
#7620=CARTESIAN_POINT ( 'NONE',  ( 5.443310442819001338, 36.86288755851700927, 76.23948081211554495 ) ) ;
#7621=CARTESIAN_POINT ( 'NONE',  ( 8.794665453373390562, 41.15189478912013499, 76.14505377247542128 ) ) ;
#7624=ORIENTED_EDGE ( 'NONE', *, *, #9893, .F. ) ;
#7625=CARTESIAN_POINT ( 'NONE',  ( 2.115006173568111159, 52.20151759559819737, 76.48963291717792856 ) ) ;
#7627=CARTESIAN_POINT ( 'NONE',  ( 6.740887235739653427, 50.50906804926147942, 75.70960632971019777 ) ) ;
#7630=CARTESIAN_POINT ( 'NONE',  ( -3.463632283681914892, 51.32894902012767346, 75.51931251450895388 ) ) ;
#7633=CARTESIAN_POINT ( 'NONE',  ( -3.632453822589317038, 37.21544096238353205, 75.46341390175899733 ) ) ;
#7635=ORIENTED_EDGE ( 'NONE', *, *, #12787, .T. ) ;
#7636=LINE ( 'NONE', #15731, #12504 ) ;
#7637=CARTESIAN_POINT ( 'NONE',  ( -6.803379318247109175, 40.47719848869107295, 79.07692288227858057 ) ) ;
#7638=CARTESIAN_POINT ( 'NONE',  ( 7.776991732576825633, 40.48304684739793657, 75.69429397690826988 ) ) ;
#7639=ORIENTED_EDGE ( 'NONE', *, *, #19619, .F. ) ;
#7640=CARTESIAN_POINT ( 'NONE',  ( -4.799158982053665312, 37.15240611894267886, 77.91201545794896788 ) ) ;
#7641=CARTESIAN_POINT ( 'NONE',  ( -7.157701799267968568, 41.72896584388870167, 79.54775079867083321 ) ) ;
#7642=LINE ( 'NONE', #14123, #8837 ) ;
#7644=CARTESIAN_POINT ( 'NONE',  ( -7.507604988220665909, 45.82440120099734315, 72.45433879953085921 ) ) ;
#7645=CARTESIAN_POINT ( 'NONE',  ( 5.385255718775495026, 47.76702405936703855, 72.45432679953087529 ) ) ;
#7648=B_SPLINE_CURVE_WITH_KNOTS ( 'NONE', 3,
 ( #16978, #1988, #14965, #18256, #19844, #5264, #11781, #10192, #16675, #2094, #8595, #489 ),
 .UNSPECIFIED., .F., .F.,
 ( 4, 2, 2, 2, 2, 4 ),
 ( 8.673617379884034509E-19, 0.0001269736000813090034, 0.0001904604001219685602, 0.0002539472001626280899, 0.0003809208002439511066, 0.0005078944003252741776 ),
 .UNSPECIFIED. ) ;
#7649=LINE ( 'NONE', #1163, #4815 ) ;
#7650=CARTESIAN_POINT ( 'NONE',  ( 8.365446634792766289, 41.78557434852172747, 78.83412695248559032 ) ) ;
#7654=CARTESIAN_POINT ( 'NONE',  ( 8.685073573159321825, 40.82344097173932340, 79.49103220525971381 ) ) ;
#7656=CARTESIAN_POINT ( 'NONE',  ( -7.551054721414131699, 42.94398425051771540, 79.08626245367327101 ) ) ;
#7659=EDGE_LOOP ( 'NONE', ( #11228, #19643, #13170, #7008 ) ) ;
#7660=CARTESIAN_POINT ( 'NONE',  ( 8.221673622452696506, 41.34128174147134871, 78.82488780898647462 ) ) ;
#7661=CARTESIAN_POINT ( 'NONE',  ( -7.617292153972126556, 43.16748516956134551, 72.45433879953085921 ) ) ;
#7662=DIRECTION ( 'NONE',  ( -0.5813877811927011807, 0.8136266022444372803, 5.636455622144619183E-17 ) ) ;
#7667=EDGE_CURVE ( 'NONE', #867, #12950, #10983, .T. ) ;
#7668=ADVANCED_FACE ( 'NONE', ( #6058 ), #6165, .T. ) ;
#7670=EDGE_LOOP ( 'NONE', ( #9084, #2388 ) ) ;
#7672=CARTESIAN_POINT ( 'NONE',  ( 0.6746983353010208573, 52.36079151674319831, 78.91894492505406333 ) ) ;
#7673=EDGE_CURVE ( 'NONE', #8340, #11453, #11084, .T. ) ;
#7674=CARTESIAN_POINT ( 'NONE',  ( 5.770850603891227060, 51.22559503374887413, 77.28904345712264501 ) ) ;
#7675=EDGE_LOOP ( 'NONE', ( #19789, #12530, #18162, #8122 ) ) ;
#7676=LINE ( 'NONE', #2984, #20721 ) ;
#7679=ORIENTED_EDGE ( 'NONE', *, *, #14442, .T. ) ;
#7681=CARTESIAN_POINT ( 'NONE',  ( -0.9315166138311854471, 52.97860336813545246, 76.61976384666378692 ) ) ;
#7682=CARTESIAN_POINT ( 'NONE',  ( -4.402123124950023225, 50.71898518566671044, 76.03313496065364063 ) ) ;
#7683=DIRECTION ( 'NONE',  ( -0.3165065846431827090, -0.9485903129789527988, 0.000000000000000000 ) ) ;
#7685=CARTESIAN_POINT ( 'NONE',  ( -3.299506883664278245, 36.95868852876193955, 79.18890841331918296 ) ) ;
#7686=ORIENTED_EDGE ( 'NONE', *, *, #8034, .T. ) ;
#7687=CARTESIAN_POINT ( 'NONE',  ( 6.813511439209503529, 39.88797755036236481, 72.45433879953087342 ) ) ;
#7693=CARTESIAN_POINT ( 'NONE',  ( -4.225674986753855222, 37.47641307392585475, 77.99882451231113123 ) ) ;
#7695=PLANE ( 'NONE',  #8930 ) ;
#7697=ADVANCED_FACE ( 'NONE', ( #7564 ), #1815, .T. ) ;
#7698=CARTESIAN_POINT ( 'NONE',  ( 8.267857704931044438, 41.47037322861213937, 75.97962990480824885 ) ) ;
#7700=EDGE_LOOP ( 'NONE', ( #11150, #4063, #10581, #18113 ) ) ;
#7702=CARTESIAN_POINT ( 'NONE',  ( -3.188252658875160961, 51.40685744052633055, 75.70044805065693083 ) ) ;
#7704=CARTESIAN_POINT ( 'NONE',  ( -7.121523164365337166, 41.57863559946763132, 78.20300316143082853 ) ) ;
#7709=CARTESIAN_POINT ( 'NONE',  ( 6.303853310235981056, 37.47779998508790555, 78.34126521887253602 ) ) ;
#7710=CARTESIAN_POINT ( 'NONE',  ( 5.561690527597086486, 51.38009315662554854, 76.32883089164610624 ) ) ;
#7711=ORIENTED_EDGE ( 'NONE', *, *, #10714, .F. ) ;
#7712=PLANE ( 'NONE',  #335 ) ;
#7713=CARTESIAN_POINT ( 'NONE',  ( 0.8124031970253874357, 52.35243704943727039, 78.79200666326234170 ) ) ;
#7715=CARTESIAN_POINT ( 'NONE',  ( -5.404516697003497683, 49.82915726805031653, 78.31219776780484665 ) ) ;
#7718=AXIS2_PLACEMENT_3D ( 'NONE', #1096, #14068, #5974 ) ;
#7720=CARTESIAN_POINT ( 'NONE',  ( 5.478721299898049679, 36.88819086051147167, 76.06572720930677178 ) ) ;
#7721=CARTESIAN_POINT ( 'NONE',  ( 8.868817592801743643, 41.37413345511091478, 75.97198585835440099 ) ) ;
#7722=CARTESIAN_POINT ( 'NONE',  ( -3.494425977668756289, 37.11348535344146171, 77.68304435440727218 ) ) ;
#7723=ORIENTED_EDGE ( 'NONE', *, *, #206, .T. ) ;
#7724=EDGE_CURVE ( 'NONE', #10690, #19575, #1864, .T. ) ;
#7725=CARTESIAN_POINT ( 'NONE',  ( 2.115006181195345558, 52.20151856286257441, 78.16610350541323271 ) ) ;
#7730=CARTESIAN_POINT ( 'NONE',  ( 8.872773925109784798, 41.38599083402314704, 79.54845644658969661 ) ) ;
#7734=CARTESIAN_POINT ( 'NONE',  ( -3.970777706820451058, 37.46534718714770662, 75.37821288891845484 ) ) ;
#7736=CARTESIAN_POINT ( 'NONE',  ( -6.727933487834448556, 40.33118276386390022, 78.21032190485932745 ) ) ;
#7737=ORIENTED_EDGE ( 'NONE', *, *, #11523, .F. ) ;
#7738=CARTESIAN_POINT ( 'NONE',  ( 4.591414450663933167, 52.09679700955160797, 78.70655549710109256 ) ) ;
#7739=CARTESIAN_POINT ( 'NONE',  ( 8.215380408549069813, 41.33579643961174810, 77.32915800260404637 ) ) ;
#7740=CARTESIAN_POINT ( 'NONE',  ( 8.386307069575464013, 39.92801880710491957, 76.83374382764255017 ) ) ;
#7742=CARTESIAN_POINT ( 'NONE',  ( 6.522560395309022319, 49.75102024682771429, 76.63889762306028786 ) ) ;
#7743=LINE ( 'NONE', #19432, #5325 ) ;
#7744=CARTESIAN_POINT ( 'NONE',  ( 6.434733849016518903, 38.48046520452516717, 76.20198684891533958 ) ) ;
#7748=EDGE_CURVE ( 'NONE', #2200, #2739, #10689, .T. ) ;
#7749=CARTESIAN_POINT ( 'NONE',  ( 6.408921161899227670, 38.45374572596151097, 77.78408325655041722 ) ) ;
#7750=VECTOR ( 'NONE', #5052, 1000.000000000000000 ) ;
#7752=CARTESIAN_POINT ( 'NONE',  ( 5.197291232937072181, 37.60686682075191811, 75.36061873398452349 ) ) ;
#7753=CARTESIAN_POINT ( 'NONE',  ( -0.9377747940352504363, 52.97987797655117959, 77.77566232894263010 ) ) ;
#7756=CARTESIAN_POINT ( 'NONE',  ( 5.600448134661695221, 51.35146447353857013, 76.04240903267428564 ) ) ;
#7759=CARTESIAN_POINT ( 'NONE',  ( -7.650389079877051302, 47.48727607949400209, 78.95058778273427436 ) ) ;
#7760=CARTESIAN_POINT ( 'NONE',  ( 5.670718203856349504, 37.02538481862475805, 75.97247164366282846 ) ) ;
#7761=EDGE_LOOP ( 'NONE', ( #5310, #20906, #2355, #1971, #13233, #18325 ) ) ;
#7763=DIRECTION ( 'NONE',  ( 0.3181025035073955509, -0.9480563259966822143, -1.210247515173838859E-16 ) ) ;
#7764=CARTESIAN_POINT ( 'NONE',  ( -4.051275123961953106, 50.96833819619023842, 76.11298501741460143 ) ) ;
#7765=CARTESIAN_POINT ( 'NONE',  ( -4.796313072339923878, 37.15030396007738744, 78.92026643871187730 ) ) ;
#7766=CARTESIAN_POINT ( 'NONE',  ( -4.283496025856504019, 47.84326572019833179, 72.45432679953087529 ) ) ;
#7768=CARTESIAN_POINT ( 'NONE',  ( 9.348820989215322896, 42.81273408501008504, 77.37738884012668450 ) ) ;
#7772=EDGE_CURVE ( 'NONE', #11143, #16863, #300, .T. ) ;
#7773=CARTESIAN_POINT ( 'NONE',  ( 8.789256573544017570, 41.13568403313856692, 78.71078388337100762 ) ) ;
#7775=CARTESIAN_POINT ( 'NONE',  ( -3.058525104374893111, 36.78526957849948786, 76.85386088035156149 ) ) ;
#7780=CARTESIAN_POINT ( 'NONE',  ( 5.431796663225051169, 50.72292504519191425, 78.93490712750880789 ) ) ;
#7781=CIRCLE ( 'NONE', #12882, 6.200000000000000178 ) ;
#7782=DIRECTION ( 'NONE',  ( -1.540237394707284220E-16, -1.793354297423764243E-16, 1.000000000000000000 ) ) ;
#7783=CARTESIAN_POINT ( 'NONE',  ( 8.217283821720865689, 41.37630060163266421, 77.88643322029270166 ) ) ;
#7785=CARTESIAN_POINT ( 'NONE',  ( 0.8361026161131213108, 52.35223742288051341, 76.13704228601427815 ) ) ;
#7786=CARTESIAN_POINT ( 'NONE',  ( 8.378637954445377289, 41.81363803720061867, 78.41904468188381827 ) ) ;
#7788=CARTESIAN_POINT ( 'NONE',  ( 5.731194756759665054, 37.06859914914154075, 77.74321050730907245 ) ) ;
#7789=ORIENTED_EDGE ( 'NONE', *, *, #16125, .T. ) ;
#7791=CARTESIAN_POINT ( 'NONE',  ( -7.306900047088299210, 46.60106584047063194, 79.40728616877404988 ) ) ;
#7792=CARTESIAN_POINT ( 'NONE',  ( 6.813511439209503529, 39.88797755036236481, 75.45433879953087342 ) ) ;
#7793=CARTESIAN_POINT ( 'NONE',  ( 5.729336661111230633, 37.06727142202039715, 75.98270377909689444 ) ) ;
#7794=FACE_OUTER_BOUND ( 'NONE', #20443, .T. ) ;
#7796=EDGE_LOOP ( 'NONE', ( #19856, #15897, #9925, #15276 ) ) ;
#7797=CARTESIAN_POINT ( 'NONE',  ( 4.640492351041169528, 52.06054514152135937, 78.02172882224894579 ) ) ;
#7799=ORIENTED_EDGE ( 'NONE', *, *, #20025, .T. ) ;
#7800=AXIS2_PLACEMENT_3D ( 'NONE', #5708, #4007, #20500 ) ;
#7801=CARTESIAN_POINT ( 'NONE',  ( -2.929408986750495103, 51.59181765175492274, 76.33204918460485544 ) ) ;
#7804=CARTESIAN_POINT ( 'NONE',  ( -7.136096162509048213, 41.62471999620901641, 78.11653805097020609 ) ) ;
#7806=EDGE_CURVE ( 'NONE', #4618, #14094, #19458, .T. ) ;
#7807=CARTESIAN_POINT ( 'NONE',  ( -5.367147075874662221, 49.84972784727108319, 78.71528818263502103 ) ) ;
#7809=ORIENTED_EDGE ( 'NONE', *, *, #5694, .T. ) ;
#7810=CARTESIAN_POINT ( 'NONE',  ( 5.333553402713407721, 50.79397291885030086, 75.97344461144770378 ) ) ;
#7812=ORIENTED_EDGE ( 'NONE', *, *, #19670, .T. ) ;
#7814=DIRECTION ( 'NONE',  ( 1.540237394707284220E-16, 1.793354297423764243E-16, -1.000000000000000000 ) ) ;
#7817=B_SPLINE_CURVE_WITH_KNOTS ( 'NONE', 3,
 ( #7502, #4395, #9215, #14402, #7709, #15905, #20474, #11120, #20871, #1324, #14188, #11022, #5908, #20771, #4292, #19185, #17390, #20574, #2709 ),
 .UNSPECIFIED., .F., .F.,
 ( 4, 1, 1, 1, 1, 1, 1, 1, 1, 1, 1, 1, 1, 1, 1, 1, 4 ),
 ( 0.000000000000000000, 0.07116601901339190961, 0.1384582187113551910, 0.2014355002094309066, 0.2607329607935783833, 0.3172301401005571675, 0.3704881719161017273, 0.4221645193212664182, 0.4717967126376631515, 0.5218096718684601676, 0.5745631757277218643, 0.6310618342314253670, 0.6925022631777019155, 0.7595319055140381526, 0.8328598856178031085, 0.9128843800434378597, 0.9999999999999998890 ),
 .UNSPECIFIED. ) ;
#7821=ADVANCED_FACE ( 'NONE', ( #16387 ), #6290, .F. ) ;
#7822=CARTESIAN_POINT ( 'NONE',  ( 0.8481543884537371403, 52.95614222172972063, 78.61836828546933020 ) ) ;
#7825=CARTESIAN_POINT ( 'NONE',  ( -3.682072889308528385, 36.32725962120449736, 77.89282216559597316 ) ) ;
#7827=DIRECTION ( 'NONE',  ( -0.3165065846431826535, -0.9485903129789527988, 0.000000000000000000 ) ) ;
#7828=CARTESIAN_POINT ( 'NONE',  ( -3.537323694296536036, 36.22033922170236053, 77.24173421363296654 ) ) ;
#7830=CARTESIAN_POINT ( 'NONE',  ( 1.232152210925365976, 52.93468634029516551, 76.77372409715140122 ) ) ;
#7831=VECTOR ( 'NONE', #13733, 1000.000000000000000 ) ;
#7832=CARTESIAN_POINT ( 'NONE',  ( -3.362469148716389800, 37.00519621768119549, 77.78682928037112276 ) ) ;
#7834=CARTESIAN_POINT ( 'NONE',  ( -7.776276679187434482, 41.23368414744241761, 78.54947220199125013 ) ) ;
#7835=CARTESIAN_POINT ( 'NONE',  ( 5.731194756759665054, 37.06859914914154075, 77.74321050730907245 ) ) ;
#7837=B_SPLINE_SURFACE_WITH_KNOTS ( 'NONE', 3, 1, ( 
 ( #17978, #3402 ),
 ( #8632, #19879 ),
 ( #10229, #6801 ),
 ( #7000, #18088 ),
 ( #16707, #19671 ),
 ( #14885, #4986 ),
 ( #15112, #14681 ),
 ( #518, #307 ),
 ( #5197, #9913 ),
 ( #13306, #3512 ),
 ( #5403, #13501 ),
 ( #13197, #11616 ),
 ( #8193, #15002 ),
 ( #2130, #11924 ),
 ( #16495, #108 ) ),
 .UNSPECIFIED., .F., .F., .F.,
 ( 4, 1, 1, 1, 1, 1, 1, 1, 1, 1, 1, 1, 4 ),
 ( 2, 2 ),
 ( 0.000000000000000000, 0.1159675137638946224, 0.2163545172648820292, 0.3041323377849299292, 0.3879046361115746633, 0.4329802283776429395, 0.4868190193916722697, 0.5485431915433492955, 0.6192726642024330985, 0.7001311270025748490, 0.7903233920492748199, 0.8897556754282296421, 1.000000000000000000 ),
 ( 0.000000000000000000, 1.000000000000000000 ),
 .UNSPECIFIED. ) ;
#7838=CARTESIAN_POINT ( 'NONE',  ( 8.807144941123576487, 41.18929660559136607, 79.54516904849367620 ) ) ;
#7840=FACE_OUTER_BOUND ( 'NONE', #19090, .T. ) ;
#7841=ORIENTED_EDGE ( 'NONE', *, *, #19447, .F. ) ;
#7842=VECTOR ( 'NONE', #18457, 1000.000000000000227 ) ;
#7843=CARTESIAN_POINT ( 'NONE',  ( -3.791754179604009067, 37.33310971910048437, 75.41196988111011024 ) ) ;
#7844=CARTESIAN_POINT ( 'NONE',  ( -4.579686653871015700, 36.99029075099881680, 76.02016401025396419 ) ) ;
#7845=CARTESIAN_POINT ( 'NONE',  ( -5.404861408967762237, 49.82879706497137562, 76.56315823047148683 ) ) ;
#7846=ORIENTED_EDGE ( 'NONE', *, *, #14708, .T. ) ;
#7848=CARTESIAN_POINT ( 'NONE',  ( -5.160557796316017409, 37.41935686500600156, 77.90139762306027649 ) ) ;
#7851=CARTESIAN_POINT ( 'NONE',  ( 5.496601215626250259, 37.64336993767980744, 77.46538603227857323 ) ) ;
#7852=CARTESIAN_POINT ( 'NONE',  ( -7.606224546186219015, 40.66142810410499919, 79.38495514127318131 ) ) ;
#7854=EDGE_CURVE ( 'NONE', #7247, #4065, #15321, .T. ) ;
#7856=CARTESIAN_POINT ( 'NONE',  ( 5.345530521434427307, 50.61492889873513690, 75.36061482756318242 ) ) ;
#7857=CARTESIAN_POINT ( 'NONE',  ( -7.885657102084565828, 41.56435211639550431, 79.54845644658969661 ) ) ;
#7858=DIRECTION ( 'NONE',  ( -0.3165065846431827645, -0.9485903129789529098, 0.000000000000000000 ) ) ;
#7859=CARTESIAN_POINT ( 'NONE',  ( -0.5518162899754186501, 52.21439382095001491, 79.25925238658010130 ) ) ;
#7860=VERTEX_POINT ( 'NONE', #9660 ) ;
#7861=CARTESIAN_POINT ( 'NONE',  ( -4.337980680445880921, 37.55764029813086324, 75.97325816659191844 ) ) ;
#7862=LINE ( 'NONE', #1262, #5499 ) ;
#7865=VECTOR ( 'NONE', #5319, 1000.000000000000114 ) ;
#7868=CARTESIAN_POINT ( 'NONE',  ( -4.536533255567898770, 37.70852454801545406, 78.62737644262512049 ) ) ;
#7869=CARTESIAN_POINT ( 'NONE',  ( -4.039512053894965149, 50.97623261712813303, 76.19470787560661051 ) ) ;
#7870=CARTESIAN_POINT ( 'NONE',  ( 6.575642869179847416, 50.63112740639009246, 77.70577767651062118 ) ) ;
#7872=CARTESIAN_POINT ( 'NONE',  ( -5.486992102393413617, 39.49954625374182626, 72.45432679953087529 ) ) ;
#7873=CIRCLE ( 'NONE', #13995, 8.199999999999995737 ) ;
#7874=CARTESIAN_POINT ( 'NONE',  ( 8.638939746224972183, 43.04959301625464008, 77.37738884012668450 ) ) ;
#7875=DIRECTION ( 'NONE',  ( 0.9429220365244121993, -0.3330135628418984250, 8.551124769255302663E-17 ) ) ;
#7876=CARTESIAN_POINT ( 'NONE',  ( 6.955656837306707807, 50.35042639603116044, 76.39262467917644983 ) ) ;
#7877=STYLED_ITEM ( 'NONE', ( #7547 ), #18516 ) ;
#7882=ORIENTED_EDGE ( 'NONE', *, *, #15601, .T. ) ;
#7883=VECTOR ( 'NONE', #8108, 1000.000000000000000 ) ;
#7884=DIRECTION ( 'NONE',  ( -1.540237394707284467E-16, -1.793354297423764243E-16, 1.000000000000000000 ) ) ;
#7885=AXIS2_PLACEMENT_3D ( 'NONE', #9948, #9525, #6407 ) ;
#7888=CARTESIAN_POINT ( 'NONE',  ( -0.6485145178734266214, 52.21717837221741121, 75.74123345422913189 ) ) ;
#7889=CARTESIAN_POINT ( 'NONE',  ( 8.793292705229012185, 41.14778057584590698, 77.83369646723784285 ) ) ;
#7890=CARTESIAN_POINT ( 'NONE',  ( 6.012275498921958672, 37.26944915646792822, 78.37198585835440667 ) ) ;
#7892=CARTESIAN_POINT ( 'NONE',  ( -0.9504375969237850441, 51.37401713635502887, 77.77566232894263010 ) ) ;
#7895=ORIENTED_EDGE ( 'NONE', *, *, #12906, .F. ) ;
#7896=CARTESIAN_POINT ( 'NONE',  ( -7.723582874747322968, 47.23591325229828186, 72.45433879953087342 ) ) ;
#7897=DIRECTION ( 'NONE',  ( 0.9999689119394085113, -0.007885122365275719011, 1.526048693634352652E-16 ) ) ;
#7898=CARTESIAN_POINT ( 'NONE',  ( 0.3284977539024462323, 52.35989436107013972, 76.34474084658923232 ) ) ;
#7900=CARTESIAN_POINT ( 'NONE',  ( -7.617292153972128332, 43.16748516956134551, 75.45433879953087342 ) ) ;
#7901=CARTESIAN_POINT ( 'NONE',  ( 8.317158657711994252, 46.70735294479731436, 78.73595644658969661 ) ) ;
#7903=VERTEX_POINT ( 'NONE', #19422 ) ;
#7906=CARTESIAN_POINT ( 'NONE',  ( -3.799298760401091268, 51.89000185047994052, 75.54713691134779197 ) ) ;
#7908=CARTESIAN_POINT ( 'NONE',  ( -7.785425530191283805, 41.22750551581724210, 78.59694605312716931 ) ) ;
#7910=PLANE ( 'NONE',  #18108 ) ;
#7915=CARTESIAN_POINT ( 'NONE',  ( 5.200734800563608928, 50.89208066999871249, 76.39036821129558064 ) ) ;
#7919=FACE_OUTER_BOUND ( 'NONE', #20305, .T. ) ;
#7924=CARTESIAN_POINT ( 'NONE',  ( -5.838369852643723767, 50.43295630312090339, 76.72345405564152543 ) ) ;
#7930=EDGE_CURVE ( 'NONE', #6620, #16858, #9865, .T. ) ;
#7933=CARTESIAN_POINT ( 'NONE',  ( 5.740585635973908474, 51.24795054640212300, 75.97198585835440099 ) ) ;
#7934=ORIENTED_EDGE ( 'NONE', *, *, #11800, .T. ) ;
#7935=CARTESIAN_POINT ( 'NONE',  ( -7.014601640787291537, 47.39335580518124402, 78.31172685814304657 ) ) ;
#7937=CARTESIAN_POINT ( 'NONE',  ( -2.917199766949189588, 51.60602765227618960, 76.69845644658968808 ) ) ;
#7938=EDGE_CURVE ( 'NONE', #17046, #19575, #14845, .T. ) ;
#7939=DIRECTION ( 'NONE',  ( -0.007885122365278605591, -0.9999689119394085113, -1.805443505845548073E-16 ) ) ;
#7940=CARTESIAN_POINT ( 'NONE',  ( 9.347650859976274873, 42.80922713344904196, 78.67881838835081965 ) ) ;
#7941=CARTESIAN_POINT ( 'NONE',  ( 8.034263824280252209, 41.23734091826108283, 79.52393066155629242 ) ) ;
#7943=DIRECTION ( 'NONE',  ( 0.5941461771851693774, 0.8043570849667760481, 2.357623395011396791E-16 ) ) ;
#7945=CARTESIAN_POINT ( 'NONE',  ( -3.538420156175611897, 36.22114913392427127, 76.12177974158937843 ) ) ;
#7946=CARTESIAN_POINT ( 'NONE',  ( -4.171401865331652026, 37.44334316642215299, 76.17409373158149322 ) ) ;
#7948=ORIENTED_EDGE ( 'NONE', *, *, #13380, .T. ) ;
#7949=CARTESIAN_POINT ( 'NONE',  ( -4.850396850989176833, 37.19025346873809212, 77.31947969467269388 ) ) ;
#7952=VECTOR ( 'NONE', #10647, 1000.000000000000227 ) ;
#7958=CARTESIAN_POINT ( 'NONE',  ( -5.706182906969134550, 50.52741225482698439, 75.88700421999355683 ) ) ;
#7959=DIRECTION ( 'NONE',  ( 0.5813877811927011807, -0.8136266022444372803, -5.636455622144619183E-17 ) ) ;
#7960=CARTESIAN_POINT ( 'NONE',  ( 8.863132018971368709, 41.35709342965520818, 77.52392363563762956 ) ) ;
#7962=EDGE_LOOP ( 'NONE', ( #5705, #20672, #10480, #10837 ) ) ;
#7964=CARTESIAN_POINT ( 'NONE',  ( -0.9346256470065343880, 52.97985314436952820, 78.20877650441246942 ) ) ;
#7965=ORIENTED_EDGE ( 'NONE', *, *, #6746, .T. ) ;
#7967=CARTESIAN_POINT ( 'NONE',  ( 8.642115653336615466, 43.05911141134401277, 76.45750776978282204 ) ) ;
#7968=ADVANCED_FACE ( 'NONE', ( #5255 ), #372, .F. ) ;
#7969=CARTESIAN_POINT ( 'NONE',  ( 8.479137094719348511, 40.20623628148813111, 79.16795596456493911 ) ) ;
#7970=CARTESIAN_POINT ( 'NONE',  ( 6.920970967149330910, 50.37604745108433946, 78.34373887323252461 ) ) ;
#7971=ORIENTED_EDGE ( 'NONE', *, *, #16993, .F. ) ;
#7972=ORIENTED_EDGE ( 'NONE', *, *, #2390, .T. ) ;
#7974=FACE_OUTER_BOUND ( 'NONE', #8705, .T. ) ;
#7976=EDGE_CURVE ( 'NONE', #2983, #5644, #19627, .T. ) ;
#7977=CARTESIAN_POINT ( 'NONE',  ( 5.120163643319172841, 50.95392860687110925, 79.53967584612604469 ) ) ;
#7980=CARTESIAN_POINT ( 'NONE',  ( 6.444701727025162974, 49.83360289536132370, 78.07866327931512274 ) ) ;
#7982=CARTESIAN_POINT ( 'NONE',  ( -7.075244453723417593, 44.52209897503762193, 72.45433879953085921 ) ) ;
#7985=ORIENTED_EDGE ( 'NONE', *, *, #11092, .T. ) ;
#7986=CARTESIAN_POINT ( 'NONE',  ( 8.814092166714756260, 41.21011788141189669, 78.88950904781501094 ) ) ;
#7987=CARTESIAN_POINT ( 'NONE',  ( 5.665287683258889651, 37.02150436742986273, 75.36022115247205022 ) ) ;
#7988=CARTESIAN_POINT ( 'NONE',  ( -3.056480504853190894, 36.78428345565664159, 76.74165022305851380 ) ) ;
#7991=CARTESIAN_POINT ( 'NONE',  ( 8.395197883163783459, 39.95466513945179798, 76.21925085218815354 ) ) ;
#7992=ORIENTED_EDGE ( 'NONE', *, *, #12976, .T. ) ;
#7993=CARTESIAN_POINT ( 'NONE',  ( -0.2542917792799709864, 52.21406978104435836, 75.49651412033875886 ) ) ;
#7994=CARTESIAN_POINT ( 'NONE',  ( -4.574316323987747346, 51.33620267474496757, 79.54845644658969661 ) ) ;
#7995=CARTESIAN_POINT ( 'NONE',  ( 7.686414200152805520, 40.17302391697257491, 78.47632680691248197 ) ) ;
#7996=CARTESIAN_POINT ( 'NONE',  ( 0.6802164782827634371, 52.96490953415155190, 75.98308111960244560 ) ) ;
#7998=ORIENTED_EDGE ( 'NONE', *, *, #17843, .T. ) ;
#7999=CARTESIAN_POINT ( 'NONE',  ( -4.598246518171406727, 51.31910303412164609, 78.93669174070734584 ) ) ;
#8005=CARTESIAN_POINT ( 'NONE',  ( -7.934068236863534906, 41.70470996953825704, 78.85747680284711691 ) ) ;
#8006=B_SPLINE_SURFACE_WITH_KNOTS ( 'NONE', 3, 1, ( 
 ( #2161, #3850 ),
 ( #7889, #20548 ),
 ( #5972, #7783 ),
 ( #14264, #4674 ),
 ( #15674, #12473 ),
 ( #17668, #12779 ),
 ( #19260, #1398 ),
 ( #1094, #5880 ),
 ( #11196, #14375 ),
 ( #18852, #6179 ),
 ( #20745, #6278 ) ),
 .UNSPECIFIED., .F., .F., .F.,
 ( 4, 1, 1, 1, 1, 1, 1, 1, 4 ),
 ( 2, 2 ),
 ( 0.000000000000000000, 0.1094333067106434410, 0.2184679721593839052, 0.3300813608894926365, 0.4462978032959263319, 0.5702501687912749917, 0.7022991718047063570, 0.8456887798043180027, 0.9999999999999998890 ),
 ( 0.000000000000000000, 1.000000000000000000 ),
 .UNSPECIFIED. ) ;
#8008=CARTESIAN_POINT ( 'NONE',  ( 4.751063331615088536, 51.97887081224218520, 77.86982703766624070 ) ) ;
#8009=VERTEX_POINT ( 'NONE', #2082 ) ;
#8010=CARTESIAN_POINT ( 'NONE',  ( 0.8455950101471351177, 52.35579997042385259, 76.48963291717792856 ) ) ;
#8014=CARTESIAN_POINT ( 'NONE',  ( 1.083001295814570053, 52.34297901104275041, 76.77198585835439815 ) ) ;
#8016=CARTESIAN_POINT ( 'NONE',  ( -4.621383371311751809, 37.02109043652605180, 78.92211507803222048 ) ) ;
#8017=CARTESIAN_POINT ( 'NONE',  ( -4.491212578019011303, 51.39558556899189057, 78.91875292420674270 ) ) ;
#8022=CARTESIAN_POINT ( 'NONE',  ( -5.531051774427891310, 44.10426199826898142, 72.45432679953087529 ) ) ;
#8024=CARTESIAN_POINT ( 'NONE',  ( 4.640492351041169528, 52.06054514152135937, 78.02172882224894579 ) ) ;
#8026=CARTESIAN_POINT ( 'NONE',  ( -7.376743071288318632, 41.96049357349896525, 78.50654468188380974 ) ) ;
#8027=CARTESIAN_POINT ( 'NONE',  ( -5.396784162528952322, 49.82872168751453756, 76.45423404125398292 ) ) ;
#8030=CARTESIAN_POINT ( 'NONE',  ( -1.047061061252483327, 36.11373028406117669, 72.45433879953085921 ) ) ;
#8031=DIRECTION ( 'NONE',  ( 1.540237394707284220E-16, 1.793354297423764243E-16, -1.000000000000000000 ) ) ;
#8032=VECTOR ( 'NONE', #6052, 1000.000000000000114 ) ;
#8033=CARTESIAN_POINT ( 'NONE',  ( -3.080034802530627225, 36.80739128506166224, 77.14704031750767399 ) ) ;
#8034=EDGE_CURVE ( 'NONE', #6210, #13018, #8954, .T. ) ;
#8035=ORIENTED_EDGE ( 'NONE', *, *, #920, .T. ) ;
#8036=CARTESIAN_POINT ( 'NONE',  ( 1.996851819492591495, 52.20245025342703826, 78.99734963310253022 ) ) ;
#8037=CARTESIAN_POINT ( 'NONE',  ( -3.755902984582864867, 36.38179493852598512, 77.82155188814751057 ) ) ;
#8038=ORIENTED_EDGE ( 'NONE', *, *, #4355, .F. ) ;
#8039=CARTESIAN_POINT ( 'NONE',  ( 0.5221537403065019678, 44.16218137147968292, 72.45433879953087342 ) ) ;
#8040=CARTESIAN_POINT ( 'NONE',  ( -0.5520076040313395271, 52.29218845565640095, 75.65236789768508174 ) ) ;
#8043=CARTESIAN_POINT ( 'NONE',  ( -3.765753198988803785, 38.37823718693370978, 75.36022115247205022 ) ) ;
#8044=VERTEX_POINT ( 'NONE', #13261 ) ;
#8045=CARTESIAN_POINT ( 'NONE',  ( 0.5221537403065005245, 44.16218137147968292, 82.45433879953087342 ) ) ;
#8046=ORIENTED_EDGE ( 'NONE', *, *, #18961, .F. ) ;
#8048=CARTESIAN_POINT ( 'NONE',  ( 5.581406744796363562, 50.61539444998253856, 72.45433879953087342 ) ) ;
#8051=CARTESIAN_POINT ( 'NONE',  ( -4.790295051490115696, 37.92061980927154963, 77.33669174070733732 ) ) ;
#8052=FACE_OUTER_BOUND ( 'NONE', #13440, .T. ) ;
#8055=VERTEX_POINT ( 'NONE', #18149 ) ;
#8056=CARTESIAN_POINT ( 'NONE',  ( -4.592862224480081856, 51.32295045326188898, 75.97198585835440099 ) ) ;
#8058=EDGE_CURVE ( 'NONE', #18072, #17173, #18565, .T. ) ;
#8060=CARTESIAN_POINT ( 'NONE',  ( 8.818545868716455516, 41.22346590884859552, 77.48357784852399277 ) ) ;
#8061=CARTESIAN_POINT ( 'NONE',  ( 5.567302800327750489, 36.95148795754280258, 75.36140480012781495 ) ) ;
#8062=CARTESIAN_POINT ( 'NONE',  ( -0.7887770423231913464, 52.21626234356678253, 79.01146473771775902 ) ) ;
#8063=VECTOR ( 'NONE', #17644, 1000.000000000000000 ) ;
#8064=ORIENTED_EDGE ( 'NONE', *, *, #12013, .F. ) ;
#8066=FACE_OUTER_BOUND ( 'NONE', #14268, .T. ) ;
#8068=CARTESIAN_POINT ( 'NONE',  ( 2.119851040271389930, 52.81592988514039178, 78.16610350541323271 ) ) ;
#8069=VERTEX_POINT ( 'NONE', #3977 ) ;
#8070=EDGE_CURVE ( 'NONE', #19239, #16089, #11518, .T. ) ;
#8072=CARTESIAN_POINT ( 'NONE',  ( 9.271487163511554996, 42.58095970340946934, 75.72637824826109920 ) ) ;
#8073=FACE_OUTER_BOUND ( 'NONE', #7429, .T. ) ;
#8076=FACE_OUTER_BOUND ( 'NONE', #111, .T. ) ;
#8078=VECTOR ( 'NONE', #8660, 1000.000000000000000 ) ;
#8079=CARTESIAN_POINT ( 'NONE',  ( 0.3286341997476255883, 52.35989755568506610, 77.71750713863309556 ) ) ;
#8080=CARTESIAN_POINT ( 'NONE',  ( 6.174124403209278356, 50.00287997606557155, 77.65065976741861675 ) ) ;
#8082=CARTESIAN_POINT ( 'NONE',  ( 6.492824329076245959, 49.76746917884374000, 76.18099276316716839 ) ) ;
#8084=EDGE_CURVE ( 'NONE', #20802, #18903, #5796, .T. ) ;
#8087=CARTESIAN_POINT ( 'NONE',  ( 8.804944317620233107, 41.18270119734690837, 78.86399424569901839 ) ) ;
#8090=CARTESIAN_POINT ( 'NONE',  ( 8.949064546045571333, 41.61463866475444462, 78.77153038569251464 ) ) ;
#8091=CARTESIAN_POINT ( 'NONE',  ( 5.746684213116473039, 37.07966734754892713, 78.33482135361461474 ) ) ;
#8092=CARTESIAN_POINT ( 'NONE',  ( 8.119551934336415755, 43.80226376792169418, 72.45433879953087342 ) ) ;
#8093=CARTESIAN_POINT ( 'NONE',  ( -1.440187084481231006, 38.28092143101017797, 72.45433879953087342 ) ) ;
#8094=ORIENTED_EDGE ( 'NONE', *, *, #17420, .F. ) ;
#8095=CARTESIAN_POINT ( 'NONE',  ( -0.4650336042545967219, 52.97492497816961077, 75.60318094692254931 ) ) ;
#8097=CARTESIAN_POINT ( 'NONE',  ( 6.446960153690390882, 38.49983447822285143, 77.31245045813156480 ) ) ;
#8099=DIRECTION ( 'NONE',  ( 1.540237394707284220E-16, 1.793354297423764243E-16, -1.000000000000000000 ) ) ;
#8100=ORIENTED_EDGE ( 'NONE', *, *, #2607, .F. ) ;
#8101=CARTESIAN_POINT ( 'NONE',  ( -1.123656915330052408, 35.37488560990637865, 76.16022115247204738 ) ) ;
#8103=VERTEX_POINT ( 'NONE', #2398 ) ;
#8105=ADVANCED_FACE ( 'NONE', ( #15165 ), #10398, .T. ) ;
#8106=CARTESIAN_POINT ( 'NONE',  ( 1.167393906761340361, 52.20907389968696322, 76.77301385304936332 ) ) ;
#8107=CARTESIAN_POINT ( 'NONE',  ( 5.843112203128086435, 37.14857125875717969, 76.21413800766271152 ) ) ;
#8108=DIRECTION ( 'NONE',  ( -1.540237394707284467E-16, -1.793354297423764243E-16, 1.000000000000000000 ) ) ;
#8111=CARTESIAN_POINT ( 'NONE',  ( -4.532046673723619357, 36.95510101671939651, 76.17409373158149322 ) ) ;
#8114=LINE ( 'NONE', #1525, #5428 ) ;
#8117=VERTEX_POINT ( 'NONE', #12188 ) ;
#8119=CARTESIAN_POINT ( 'NONE',  ( -3.349688636638950889, 52.21127678364309332, 78.10580938776615767 ) ) ;
#8120=CARTESIAN_POINT ( 'NONE',  ( -4.030157702633147210, 50.97812307042602953, 78.45066232894264147 ) ) ;
#8121=CARTESIAN_POINT ( 'NONE',  ( 5.427780505986065762, 36.85179043424346190, 77.43080938776617472 ) ) ;
#8122=ORIENTED_EDGE ( 'NONE', *, *, #20735, .T. ) ;
#8123=DIRECTION ( 'NONE',  ( -0.8134066734386236064, -0.5812306281201740088, 0.02324952774876324485 ) ) ;
#8124=DIRECTION ( 'NONE',  ( 0.3014925587070406698, -0.9534141535609406137, 0.01018277142809568582 ) ) ;
#8127=CARTESIAN_POINT ( 'NONE',  ( -4.517072128342571880, 36.94403992325788977, 78.58080938776616620 ) ) ;
#8128=VECTOR ( 'NONE', #19706, 1000.000000000000000 ) ;
#8129=CARTESIAN_POINT ( 'NONE',  ( -4.735834763901007882, 50.30101192887209294, 75.43678921887351407 ) ) ;
#8132=DIRECTION ( 'NONE',  ( 1.540237394707284220E-16, 1.793354297423764243E-16, -1.000000000000000000 ) ) ;
#8134=CARTESIAN_POINT ( 'NONE',  ( 5.904402762709062280, 51.12694543383925350, 76.06909773771320715 ) ) ;
#8135=B_SPLINE_CURVE_WITH_KNOTS ( 'NONE', 3,
 ( #11713, #14882, #18284, #6798, #3506, #6901, #6993, #13403, #3816, #13303, #1911, #19775, #14997, #18187 ),
 .UNSPECIFIED., .F., .F.,
 ( 4, 2, 2, 2, 2, 2, 4 ),
 ( 0.000000000000000000, 0.0006024534355434134824, 0.0009036801533151169168, 0.001204906871086820460, 0.001506133588858523569, 0.001807360306630227328, 0.002409813742173637016 ),
 .UNSPECIFIED. ) ;
#8139=VECTOR ( 'NONE', #16869, 1000.000000000000227 ) ;
#8140=CARTESIAN_POINT ( 'NONE',  ( -3.555031842569258416, 52.06454604677990972, 75.79042024895623797 ) ) ;
#8141=EDGE_LOOP ( 'NONE', ( #1993, #18742, #987, #3195, #7335, #12561, #2584, #6317, #8773, #17058, #19617, #6657, #17634, #7465, #3573, #10524, #9347, #9263, #18451 ) ) ;
#8142=LINE ( 'NONE', #16451, #7540 ) ;
#8145=AXIS2_PLACEMENT_3D ( 'NONE', #4021, #2546, #4338 ) ;
#8146=DIRECTION ( 'NONE',  ( -0.2908163624019201587, 0.9196526680133400022, -0.2639409281927689310 ) ) ;
#8147=CARTESIAN_POINT ( 'NONE',  ( 5.561379608955574483, 51.38032281970146897, 76.39036821129558064 ) ) ;
#8148=ORIENTED_EDGE ( 'NONE', *, *, #8177, .F. ) ;
#8149=CARTESIAN_POINT ( 'NONE',  ( 5.599463258324014703, 51.35219196201597214, 78.62371398036725623 ) ) ;
#8150=DIRECTION ( 'NONE',  ( 1.540237394707284220E-16, 1.793354297423764243E-16, -1.000000000000000000 ) ) ;
#8153=CARTESIAN_POINT ( 'NONE',  ( -4.529265440370444651, 36.95304663167630821, 77.01245883157920957 ) ) ;
#8154=CARTESIAN_POINT ( 'NONE',  ( -4.990412171993382273, 37.29367714620268259, 77.90250793075740887 ) ) ;
#8155=EDGE_CURVE ( 'NONE', #19085, #5478, #19933, .T. ) ;
#8157=ORIENTED_EDGE ( 'NONE', *, *, #10247, .T. ) ;
#8158=CARTESIAN_POINT ( 'NONE',  ( -4.718161399584266391, 37.09257646755418847, 75.97198585835440099 ) ) ;
#8160=LINE ( 'NONE', #485, #9859 ) ;
#8163=VECTOR ( 'NONE', #11740, 1000.000000000000000 ) ;
#8164=CARTESIAN_POINT ( 'NONE',  ( 0.6135150644279553367, 52.34298826783862779, 76.85126224504509196 ) ) ;
#8165=DIRECTION ( 'NONE',  ( 1.540237394707283727E-16, 1.793354297423763257E-16, -1.000000000000000000 ) ) ;
#8166=CARTESIAN_POINT ( 'NONE',  ( 8.604143167063659448, 40.58088741054138637, 79.41216397796385706 ) ) ;
#8169=CARTESIAN_POINT ( 'NONE',  ( -5.510796958474739604, 38.60848837797752964, 76.73301527011911105 ) ) ;
#8170=CARTESIAN_POINT ( 'NONE',  ( 8.643862584933666326, 43.06434707616365642, 76.70850639745313515 ) ) ;
#8172=FACE_OUTER_BOUND ( 'NONE', #289, .T. ) ;
#8177=EDGE_CURVE ( 'NONE', #11143, #6944, #2237, .T. ) ;
#8179=CARTESIAN_POINT ( 'NONE',  ( 5.453344025566022601, 40.65105419805430387, 72.45432679953087529 ) ) ;
#8180=CARTESIAN_POINT ( 'NONE',  ( 6.712139372526147341, 50.53030293778272863, 77.80505143490314879 ) ) ;
#8181=CARTESIAN_POINT ( 'NONE',  ( 4.314486539155690359, 51.43278757724892358, 79.13226549199922033 ) ) ;
#8182=DIRECTION ( 'NONE',  ( -0.9485903129789527988, 0.3165065846431829311, -8.934458285744989980E-17 ) ) ;
#8184=EDGE_CURVE ( 'NONE', #8117, #188, #10850, .T. ) ;
#8185=CARTESIAN_POINT ( 'NONE',  ( 8.643718578691984789, 43.06391548032173944, 77.11956464767864361 ) ) ;
#8186=B_SPLINE_CURVE_WITH_KNOTS ( 'NONE', 3,
 ( #18365, #15500, #2194, #20162, #8693, #15174, #911, #3887, #589, #7071, #11032, #7825, #9116, #14308, #9226, #18994, #12312, #4408, #17195 ),
 .UNSPECIFIED., .F., .F.,
 ( 4, 1, 1, 1, 1, 1, 1, 1, 1, 1, 1, 1, 1, 1, 1, 1, 4 ),
 ( 0.000000000000000000, 0.08150191411353231719, 0.1574413810301363015, 0.2279254944343154510, 0.2925593756674912393, 0.3532811523109508078, 0.4087341836578463616, 0.4609809767707315764, 0.5093835833650265377, 0.5574898171909816735, 0.6095021731789963537, 0.6642568233027335012, 0.7231084493840179706, 0.7857192733158503417, 0.8528940375925012640, 0.9238451209387705809, 1.000000000000000000 ),
 .UNSPECIFIED. ) ;
#8188=EDGE_LOOP ( 'NONE', ( #8732, #15032, #9720, #3687 ) ) ;
#8189=CARTESIAN_POINT ( 'NONE',  ( -5.681413420386579816, 37.80409193316261707, 79.34222993022952153 ) ) ;
#8192=EDGE_CURVE ( 'NONE', #6620, #2983, #7817, .T. ) ;
#8193=CARTESIAN_POINT ( 'NONE',  ( -4.534577940854813249, 37.71160670378642266, 78.59503622499423159 ) ) ;
#8196=ADVANCED_FACE ( 'NONE', ( #6207 ), #3253, .F. ) ;
#8198=CARTESIAN_POINT ( 'NONE',  ( 8.572560397843592028, 40.48623184761532912, 75.53366564255911442 ) ) ;
#8200=VERTEX_POINT ( 'NONE', #16211 ) ;
#8201=CARTESIAN_POINT ( 'NONE',  ( 6.872381782841294751, 37.88404961645574076, 76.32925572521180868 ) ) ;
#8204=CARTESIAN_POINT ( 'NONE',  ( 6.870794506624137377, 37.88291540698485704, 77.55645576794258034 ) ) ;
#8206=PLANE ( 'NONE',  #4145 ) ;
#8208=CIRCLE ( 'NONE', #12292, 8.199999999999995737 ) ;
#8209=EDGE_CURVE ( 'NONE', #20868, #3406, #15581, .T. ) ;
#8211=VERTEX_POINT ( 'NONE', #1945 ) ;
#8213=CARTESIAN_POINT ( 'NONE',  ( -7.890048607039471307, 46.74575480130646099, 79.45433879953087342 ) ) ;
#8215=CARTESIAN_POINT ( 'NONE',  ( -7.365114186959480058, 41.93575649144190010, 78.75998376317852490 ) ) ;
#8216=CIRCLE ( 'NONE', #745, 8.199999999999995737 ) ;
#8217=CARTESIAN_POINT ( 'NONE',  ( 8.642937017325245108, 43.02502337403097243, 78.77838852948787007 ) ) ;
#8221=CARTESIAN_POINT ( 'NONE',  ( 0.3326973149608336566, 52.96014171822455552, 77.10139762306027933 ) ) ;
#8222=EDGE_CURVE ( 'NONE', #3298, #5674, #8346, .T. ) ;
#8223=CARTESIAN_POINT ( 'NONE',  ( 3.961507247562193523, 36.71833509068317625, 76.96022115247204454 ) ) ;
#8225=PLANE ( 'NONE',  #18656 ) ;
#8226=ORIENTED_EDGE ( 'NONE', *, *, #6992, .T. ) ;
#8227=CARTESIAN_POINT ( 'NONE',  ( 8.214799251806553571, 41.32260305165857517, 77.80727997600146750 ) ) ;
#8230=CARTESIAN_POINT ( 'NONE',  ( -3.350053155021378792, 52.21101631215288563, 78.15066919019970726 ) ) ;
#8231=CARTESIAN_POINT ( 'NONE',  ( 0.5221537403065019678, 44.16218137147968292, 72.45433879953087342 ) ) ;
#8232=ORIENTED_EDGE ( 'NONE', *, *, #5979, .T. ) ;
#8233=CARTESIAN_POINT ( 'NONE',  ( -4.404666252920439895, 51.45742840424412634, 76.10127045261064893 ) ) ;
#8235=VECTOR ( 'NONE', #12749, 1000.000000000000114 ) ;
#8237=CARTESIAN_POINT ( 'NONE',  ( 4.623413712694776301, 52.07316044369832042, 78.06776350345396054 ) ) ;
#8238=CARTESIAN_POINT ( 'NONE',  ( -6.807656070979932750, 40.62200040745536711, 77.60658645233600339 ) ) ;
#8241=CARTESIAN_POINT ( 'NONE',  ( -4.279734250126900896, 37.51515375910477701, 77.24486754123188348 ) ) ;
#8245=CARTESIAN_POINT ( 'NONE',  ( -3.231322013975681973, 36.91914105393552603, 77.52205638859560111 ) ) ;
#8246=VERTEX_POINT ( 'NONE', #3542 ) ;
#8248=FACE_OUTER_BOUND ( 'NONE', #4484, .T. ) ;
#8249=ORIENTED_EDGE ( 'NONE', *, *, #6572, .F. ) ;
#8252=VECTOR ( 'NONE', #6880, 1000.000000000000000 ) ;
#8254=CARTESIAN_POINT ( 'NONE',  ( 8.872773925109784798, 41.38599083402314704, 79.54845644658969661 ) ) ;
#8257=CARTESIAN_POINT ( 'NONE',  ( -5.176219156857807313, 38.36693177725332760, 75.60525969576029581 ) ) ;
#8263=DIRECTION ( 'NONE',  ( 0.5813877811927012917, -0.8136266022444372803, -5.636455622144620416E-17 ) ) ;
#8264=CARTESIAN_POINT ( 'NONE',  ( -4.799158982053689293, 37.15240611894265044, 77.91201545794896788 ) ) ;
#8267=VERTEX_POINT ( 'NONE', #6515 ) ;
#8272=VECTOR ( 'NONE', #16687, 1000.000000000000000 ) ;
#8274=CARTESIAN_POINT ( 'NONE',  ( 6.532049803590284753, 50.66332784790530752, 75.53514883118299394 ) ) ;
#8275=CARTESIAN_POINT ( 'NONE',  ( -4.497902711709205192, 37.67842107594061929, 76.02644968818945870 ) ) ;
#8277=CARTESIAN_POINT ( 'NONE',  ( 4.695664425361702143, 36.32864708750979332, 75.66510065906194882 ) ) ;
#8278=CARTESIAN_POINT ( 'NONE',  ( 7.769255851728997797, 40.44309521273268615, 79.16795596456493911 ) ) ;
#8280=CARTESIAN_POINT ( 'NONE',  ( -5.442413609737339009, 38.53480995828901712, 75.92268755756494159 ) ) ;
#8282=LINE ( 'NONE', #3374, #7226 ) ;
#8283=PLANE ( 'NONE',  #19425 ) ;
#8290=CARTESIAN_POINT ( 'NONE',  ( 8.951667845840693971, 41.62244091939069790, 76.38301527011910252 ) ) ;
#8295=B_SPLINE_CURVE_WITH_KNOTS ( 'NONE', 3,
 ( #16174, #8079, #4871, #15459, #12061, #981, #17056, #10588, #13752, #18757 ),
 .UNSPECIFIED., .F., .F.,
 ( 4, 2, 2, 2, 4 ),
 ( 0.000000000000000000, 0.0001324027139890673291, 0.0002648054279781346582, 0.0003972081419672020145, 0.0005296108559562693165 ),
 .UNSPECIFIED. ) ;
#8296=CARTESIAN_POINT ( 'NONE',  ( 4.097836514301406829, 51.53655020162395317, 76.55090572632929025 ) ) ;
#8297=DIRECTION ( 'NONE',  ( 0.9999689119394086223, -0.007885122365275665235, 1.526048693634353392E-16 ) ) ;
#8298=CARTESIAN_POINT ( 'NONE',  ( -4.895412223390203543, 37.22350451100091817, 76.36316342150684022 ) ) ;
#8300=ORIENTED_EDGE ( 'NONE', *, *, #19899, .F. ) ;
#8301=CARTESIAN_POINT ( 'NONE',  ( 0.3279354649297712143, 52.35625736820495035, 76.44919174070734869 ) ) ;
#8302=B_SPLINE_CURVE_WITH_KNOTS ( 'NONE', 3,
 ( #11874, #19527, #3465, #19628, #167, #16556, #5256, #1976, #13462, #478, #19734, #4942 ),
 .UNSPECIFIED., .F., .F.,
 ( 4, 2, 2, 2, 2, 4 ),
 ( 0.000000000000000000, 0.0002162791450248731536, 0.0004325582900497463071, 0.0006488374350746195420, 0.0007569770075870690344, 0.0008651165800995185267 ),
 .UNSPECIFIED. ) ;
#8303=EDGE_CURVE ( 'NONE', #8200, #5130, #19595, .T. ) ;
#8304=CARTESIAN_POINT ( 'NONE',  ( 8.912702722122396892, 41.50565997170561161, 78.91042349786003740 ) ) ;
#8305=CARTESIAN_POINT ( 'NONE',  ( 8.636008417968735529, 42.97537321702968427, 75.95421592775571185 ) ) ;
#8306=CARTESIAN_POINT ( 'NONE',  ( -4.032264951078912141, 50.98107207184723677, 72.45433879953087342 ) ) ;
#8308=CARTESIAN_POINT ( 'NONE',  ( -5.838428831739583380, 50.43291415881836315, 78.10580938776615767 ) ) ;
#8310=EDGE_LOOP ( 'NONE', ( #9894, #16453, #10783, #1798 ) ) ;
#8311=CARTESIAN_POINT ( 'NONE',  ( 6.658811665516601863, 37.73144022991658630, 75.70392102816973079 ) ) ;
#8312=CARTESIAN_POINT ( 'NONE',  ( -0.1077981546206782937, 52.97333330572794807, 79.46489189366771200 ) ) ;
#8314=FACE_OUTER_BOUND ( 'NONE', #15556, .T. ) ;
#8318=CARTESIAN_POINT ( 'NONE',  ( 8.945167944750011202, 41.60296030347588214, 76.15680935856015310 ) ) ;
#8320=EDGE_LOOP ( 'NONE', ( #14393, #12008, #13877, #9232 ) ) ;
#8322=CARTESIAN_POINT ( 'NONE',  ( -7.783335128423334304, 41.22810361570975601, 78.64066830726386570 ) ) ;
#8323=CARTESIAN_POINT ( 'NONE',  ( 5.847829093480187979, 37.15194177590640834, 76.49330797698027595 ) ) ;
#8325=FACE_OUTER_BOUND ( 'NONE', #10975, .T. ) ;
#8329=CARTESIAN_POINT ( 'NONE',  ( -7.472485363237701961, 47.84165176951479737, 78.32453815152756249 ) ) ;
#8333=LINE ( 'NONE', #5228, #19463 ) ;
#8334=DIRECTION ( 'NONE',  ( 0.3193833840016667702, -0.1065654399787158285, 0.9416146032352017414 ) ) ;
#8338=VERTEX_POINT ( 'NONE', #5652 ) ;
#8340=VERTEX_POINT ( 'NONE', #11955 ) ;
#8341=CARTESIAN_POINT ( 'NONE',  ( 9.205318032915601023, 42.38264662132202432, 79.33312187154012918 ) ) ;
#8342=EDGE_CURVE ( 'NONE', #5069, #158, #18431, .T. ) ;
#8343=CARTESIAN_POINT ( 'NONE',  ( -7.470920617401620945, 40.23538427955658392, 77.87635769503857830 ) ) ;
#8344=CARTESIAN_POINT ( 'NONE',  ( -4.423078977246956534, 37.62101209537413382, 77.30960331605402303 ) ) ;
#8346=B_SPLINE_CURVE_WITH_KNOTS ( 'NONE', 3,
 ( #8437, #3327, #18012, #14916, #14503, #4911, #1852, #11431, #5018, #17904, #6723, #341, #14610, #38, #16319 ),
 .UNSPECIFIED., .F., .F.,
 ( 4, 1, 1, 1, 1, 1, 1, 1, 1, 1, 1, 1, 4 ),
 ( 0.000000000000000000, 0.1124872259413081665, 0.2145177594606929306, 0.3061691560909166610, 0.3877635431594634863, 0.4596729905988826692, 0.5233009716387192478, 0.5766443983521717387, 0.6225226080321302202, 0.7076769590374641927, 0.7964950891574525960, 0.8912003305064800651, 1.000000000000000000 ),
 .UNSPECIFIED. ) ;
#8348=LINE ( 'NONE', #2271, #11968 ) ;
#8349=ADVANCED_FACE ( 'NONE', ( #15140 ), #5764, .F. ) ;
#8353=EDGE_LOOP ( 'NONE', ( #4950, #12063, #870, #11981 ) ) ;
#8355=DIRECTION ( 'NONE',  ( 0.007885122365275663500, 0.9999689119394085113, 1.805443505845543142E-16 ) ) ;
#8360=ORIENTED_EDGE ( 'NONE', *, *, #763, .T. ) ;
#8362=CARTESIAN_POINT ( 'NONE',  ( -4.309294135009902327, 37.72656918548430127, 75.36046818803191627 ) ) ;
#8363=ORIENTED_EDGE ( 'NONE', *, *, #19058, .F. ) ;
#8367=ORIENTED_EDGE ( 'NONE', *, *, #20772, .F. ) ;
#8369=CARTESIAN_POINT ( 'NONE',  ( -4.525688498162991458, 36.95040448855564108, 78.17872471894986575 ) ) ;
#8370=VERTEX_POINT ( 'NONE', #8757 ) ;
#8372=CARTESIAN_POINT ( 'NONE',  ( 0.5221537403065019678, 44.16218137147968292, 72.45433879953087342 ) ) ;
#8373=EDGE_CURVE ( 'NONE', #10515, #18997, #15456, .T. ) ;
#8374=CARTESIAN_POINT ( 'NONE',  ( 6.241727703577843123, 50.87777708829695200, 75.41423045364997790 ) ) ;
#8375=CARTESIAN_POINT ( 'NONE',  ( -0.1994209430448784792, 35.36759766960258844, 76.86610350541323555 ) ) ;
#8377=CARTESIAN_POINT ( 'NONE',  ( 4.753159030984773992, 36.36973062767617648, 75.61597629374708163 ) ) ;
#8378=CARTESIAN_POINT ( 'NONE',  ( 8.386782761808312614, 39.92944448690413140, 78.16120960217517677 ) ) ;
#8381=CARTESIAN_POINT ( 'NONE',  ( 8.530801708727521415, 42.72549645772559046, 75.64289537645213102 ) ) ;
#8382=PLANE ( 'NONE',  #5477 ) ;
#8383=CARTESIAN_POINT ( 'NONE',  ( 1.851994483447819917, 52.86147903094889244, 79.19202123453014508 ) ) ;
#8386=CARTESIAN_POINT ( 'NONE',  ( 5.393087686338802200, 50.75151780712508298, 78.93669174070734584 ) ) ;
#8389=B_SPLINE_CURVE_WITH_KNOTS ( 'NONE', 3,
 ( #2336, #11927, #17018, #9046, #7109, #15534, #15328, #17127, #8634, #8832, #7440, #5845, #738, #16709, #7223, #13721, #15114, #2448, #7002 ),
 .UNSPECIFIED., .F., .F.,
 ( 4, 1, 1, 1, 1, 1, 1, 1, 1, 1, 1, 1, 1, 1, 1, 1, 4 ),
 ( 0.000000000000000000, 0.09593561818428578136, 0.1790132514218915338, 0.2495659677033479074, 0.3103928923273128748, 0.3657232523743771391, 0.4198889549570182789, 0.4761292045875803458, 0.5349114402766786958, 0.5687027968553886037, 0.6100175737345402416, 0.6575813992106814831, 0.7121752348458817439, 0.7738275843818921418, 0.8419112148355063496, 0.9177342363179752383, 1.000000000000000000 ),
 .UNSPECIFIED. ) ;
#8392=FACE_OUTER_BOUND ( 'NONE', #4107, .T. ) ;
#8393=CARTESIAN_POINT ( 'NONE',  ( 8.378259716512932442, 41.81237273359645457, 77.23509376690508077 ) ) ;
#8394=CARTESIAN_POINT ( 'NONE',  ( 4.419036743624424446, 51.37729090045076674, 79.26137706927028148 ) ) ;
#8397=CARTESIAN_POINT ( 'NONE',  ( 6.477080015414021119, 49.77909886912638626, 76.08942471621537607 ) ) ;
#8398=CARTESIAN_POINT ( 'NONE',  ( 4.149796636236800396, 51.49816935263167039, 76.01224951307210631 ) ) ;
#8399=CARTESIAN_POINT ( 'NONE',  ( -3.080359849264385552, 36.80763138399021273, 76.21065298426071877 ) ) ;
#8403=VERTEX_POINT ( 'NONE', #8869 ) ;
#8405=DIRECTION ( 'NONE',  ( 0.5813877811927012917, -0.8136266022444372803, -5.636455622144620416E-17 ) ) ;
#8406=LINE ( 'NONE', #13407, #6539 ) ;
#8408=CARTESIAN_POINT ( 'NONE',  ( 0.3201111382462866750, 51.36399839264385037, 77.76169174070734869 ) ) ;
#8409=CARTESIAN_POINT ( 'NONE',  ( 0.5221537403065005245, 44.16218137147968292, 82.45433879953087342 ) ) ;
#8410=CARTESIAN_POINT ( 'NONE',  ( 8.596205818237969254, 40.55709867257476731, 75.50010622114506020 ) ) ;
#8412=ORIENTED_EDGE ( 'NONE', *, *, #13526, .F. ) ;
#8414=CARTESIAN_POINT ( 'NONE',  ( 0.1758192580184792242, 52.20865614724360881, 79.52116152017964623 ) ) ;
#8415=CARTESIAN_POINT ( 'NONE',  ( 6.326494392126531530, 38.41375405554234845, 78.00072712051441215 ) ) ;
#8417=CARTESIAN_POINT ( 'NONE',  ( 0.8485541085179806320, 52.95612604475941509, 76.28587793549699825 ) ) ;
#8418=ORIENTED_EDGE ( 'NONE', *, *, #13517, .T. ) ;
#8419=CARTESIAN_POINT ( 'NONE',  ( -4.414789981656704221, 51.45019435834255717, 78.82303764823565473 ) ) ;
#8420=LINE ( 'NONE', #10460, #6450 ) ;
#8421=EDGE_CURVE ( 'NONE', #8103, #2109, #20985, .T. ) ;
#8424=AXIS2_PLACEMENT_3D ( 'NONE', #10899, #17368, #12582 ) ;
#8427=DIRECTION ( 'NONE',  ( -0.9534635866061451637, -0.3015081906286224411, -2.009271279954815058E-16 ) ) ;
#8429=LINE ( 'NONE', #544, #49 ) ;
#8432=LINE ( 'NONE', #19389, #9165 ) ;
#8437=CARTESIAN_POINT ( 'NONE',  ( 5.939900590116411472, 51.10072461867315496, 76.38301527011910252 ) ) ;
#8439=CARTESIAN_POINT ( 'NONE',  ( 5.076572431691916520, 37.34329067111212197, 72.45433879953087342 ) ) ;
#8440=ORIENTED_EDGE ( 'NONE', *, *, #8462, .T. ) ;
#8441=CARTESIAN_POINT ( 'NONE',  ( -4.182948190183843451, 50.86894458203908442, 75.97373057797423712 ) ) ;
#8442=EDGE_CURVE ( 'NONE', #19492, #2056, #8658, .T. ) ;
#8443=ORIENTED_EDGE ( 'NONE', *, *, #2589, .T. ) ;
#8444=DIRECTION ( 'NONE',  ( -0.3165065846431826535, -0.9485903129789529098, -2.188653791613874008E-16 ) ) ;
#8445=CARTESIAN_POINT ( 'NONE',  ( -7.435799528285976123, 40.12432036608910124, 78.15415281222085753 ) ) ;
#8446=FACE_OUTER_BOUND ( 'NONE', #15300, .T. ) ;
#8451=B_SPLINE_CURVE_WITH_KNOTS ( 'NONE', 3,
 ( #101, #10984, #14469, #11085, #3088, #6166, #17455, #20933 ),
 .UNSPECIFIED., .F., .F.,
 ( 4, 2, 2, 4 ),
 ( 0.000000000000000000, 0.0001360895826664835205, 0.0002721791653329670409, 0.0005443583306659316966 ),
 .UNSPECIFIED. ) ;
#8453=CARTESIAN_POINT ( 'NONE',  ( -7.548577791137153881, 47.77306291863948928, 78.32234914140835258 ) ) ;
#8454=VECTOR ( 'NONE', #7782, 1000.000000000000000 ) ;
#8455=CARTESIAN_POINT ( 'NONE',  ( -4.004103039135145536, 51.74365621125981107, 75.44813358671753178 ) ) ;
#8457=CARTESIAN_POINT ( 'NONE',  ( 0.6452515144483527143, 52.96578307438453237, 79.54845644658969661 ) ) ;
#8458=CARTESIAN_POINT ( 'NONE',  ( 5.308031450093095849, 37.52402081283153734, 78.30432351818811298 ) ) ;
#8461=CARTESIAN_POINT ( 'NONE',  ( 0.8503282811412331554, 52.95606000782370870, 78.52566232894263010 ) ) ;
#8462=EDGE_CURVE ( 'NONE', #9068, #15270, #17468, .T. ) ;
#8467=ORIENTED_EDGE ( 'NONE', *, *, #19236, .F. ) ;
#8469=CARTESIAN_POINT ( 'NONE',  ( 0.4729456550870366205, 52.96207995487667120, 75.98649297057549745 ) ) ;
#8472=EDGE_CURVE ( 'NONE', #8686, #14654, #4476, .T. ) ;
#8476=ORIENTED_EDGE ( 'NONE', *, *, #15698, .T. ) ;
#8477=CARTESIAN_POINT ( 'NONE',  ( -4.442047047865082199, 50.68380202455470851, 76.19771883405211099 ) ) ;
#8478=CARTESIAN_POINT ( 'NONE',  ( 2.080558424246795379, 52.82310755624531140, 76.12927713265780483 ) ) ;
#8479=EDGE_CURVE ( 'NONE', #20066, #1091, #18285, .T. ) ;
#8480=CIRCLE ( 'NONE', #13911, 8.199999999999995737 ) ;
#8481=DIRECTION ( 'NONE',  ( -0.5813877811926999595, 0.8136266022444381685, 5.636455622144657394E-17 ) ) ;
#8483=CARTESIAN_POINT ( 'NONE',  ( -7.203028914707078734, 41.41235317899835877, 78.58228193349691537 ) ) ;
#8484=ORIENTED_EDGE ( 'NONE', *, *, #7426, .T. ) ;
#8487=CARTESIAN_POINT ( 'NONE',  ( 7.677770335231880239, 40.16890731605786158, 78.28891658965622469 ) ) ;
#8490=CARTESIAN_POINT ( 'NONE',  ( 8.405938446954575483, 42.35127334101444063, 75.45386443748748206 ) ) ;
#8493=( BOUNDED_CURVE ( )  B_SPLINE_CURVE ( 3, ( #16741, #5659, #7475, #984 ),
 .UNSPECIFIED., .F., .T. ) 
 B_SPLINE_CURVE_WITH_KNOTS ( ( 4, 4 ),
 ( 4.530614858972014325, 4.536446781922521154 ),
 .UNSPECIFIED. ) 
 CURVE ( )  GEOMETRIC_REPRESENTATION_ITEM ( )  RATIONAL_B_SPLINE_CURVE ( ( 1.000000000000000000, 0.9999971657248998280, 0.9999971657248998280, 1.000000000000000000 ) ) 
 REPRESENTATION_ITEM ( '' )  );
#8495=ORIENTED_EDGE ( 'NONE', *, *, #15524, .T. ) ;
#8496=VECTOR ( 'NONE', #4580, 1000.000000000000000 ) ;
#8497=EDGE_CURVE ( 'NONE', #5056, #10886, #13963, .T. ) ;
#8499=EDGE_LOOP ( 'NONE', ( #6185, #20253, #5913, #12783 ) ) ;
#8500=CARTESIAN_POINT ( 'NONE',  ( 5.421579169047436864, 50.73772679352408232, 75.97340973669622599 ) ) ;
#8502=CARTESIAN_POINT ( 'NONE',  ( -7.349889430531795220, 41.86589664987295123, 78.88458194038388172 ) ) ;
#8503=CARTESIAN_POINT ( 'NONE',  ( 0.1203869048799174335, 52.95380583232233818, 75.39536708303639045 ) ) ;
#8505=CARTESIAN_POINT ( 'NONE',  ( 8.788905609664558582, 41.13463217212708400, 76.28640183395299346 ) ) ;
#8506=VECTOR ( 'NONE', #159, 999.9999999999998863 ) ;
#8507=CARTESIAN_POINT ( 'NONE',  ( -4.340948238162491535, 40.55733868359232730, 72.45432679953087529 ) ) ;
#8508=CARTESIAN_POINT ( 'NONE',  ( 6.433553176315260913, 38.47928099333162777, 75.45433879953088763 ) ) ;
#8510=AXIS2_PLACEMENT_3D ( 'NONE', #15916, #1338, #7827 ) ;
#8511=VECTOR ( 'NONE', #13265, 1000.000000000000000 ) ;
#8513=ORIENTED_EDGE ( 'NONE', *, *, #8342, .T. ) ;
#8514=CARTESIAN_POINT ( 'NONE',  ( 0.3366241274589152899, 52.96752759352020945, 76.19791476666895846 ) ) ;
#8515=DIRECTION ( 'NONE',  ( -1.540237394707284220E-16, -1.793354297423764243E-16, 1.000000000000000000 ) ) ;
#8516=CARTESIAN_POINT ( 'NONE',  ( -5.528784567355424784, 50.65417461334718752, 79.23104009678212378 ) ) ;
#8519=CARTESIAN_POINT ( 'NONE',  ( 8.933414522996312002, 41.56773455285687646, 77.44430071719698105 ) ) ;
#8525=CARTESIAN_POINT ( 'NONE',  ( 6.522560395309022319, 49.75102024682771429, 76.63889762306028786 ) ) ;
#8526=CARTESIAN_POINT ( 'NONE',  ( 5.240387607648463231, 50.87148932128918943, 75.36192990029346106 ) ) ;
#8527=CARTESIAN_POINT ( 'NONE',  ( -4.315618344801259276, 37.54118080996789786, 78.93496803530179307 ) ) ;
#8528=ORIENTED_EDGE ( 'NONE', *, *, #5029, .T. ) ;
#8535=CARTESIAN_POINT ( 'NONE',  ( 1.926405151277293504, 52.94175334346884654, 77.08393542551461053 ) ) ;
#8537=B_SPLINE_SURFACE_WITH_KNOTS ( 'NONE', 3, 1, ( 
 ( #5883, #2682 ),
 ( #20222, #18758 ),
 ( #4172, #20645 ),
 ( #19070, #13967 ),
 ( #1097, #5975 ),
 ( #6075, #10589 ),
 ( #11001, #2897 ),
 ( #9189, #7257 ),
 ( #17472, #9080 ),
 ( #17057, #4480 ),
 ( #7685, #12476 ),
 ( #15787, #12381 ),
 ( #5657, #20449 ),
 ( #20333, #2796 ),
 ( #7585, #18957 ),
 ( #12164, #12580 ),
 ( #4267, #9297 ),
 ( #10697, #17159 ),
 ( #18645, #982 ) ),
 .UNSPECIFIED., .F., .F., .F.,
 ( 4, 1, 1, 1, 1, 1, 1, 1, 1, 1, 1, 1, 1, 1, 1, 1, 4 ),
 ( 2, 2 ),
 ( 0.000000000000000000, 0.1010931020334112918, 0.1936883160783454683, 0.2783829231069467891, 0.3553896825508546242, 0.4249031060497730494, 0.4877225005288854942, 0.5445694316561201509, 0.5961453798982884189, 0.6449762784811632343, 0.6930678288708707058, 0.7409100032456262808, 0.7895445362486890328, 0.8390228595812658785, 0.8900783947972482624, 0.9435774522572311085, 1.000000000000000000 ),
 ( 0.000000000000000000, 1.000000000000000000 ),
 .UNSPECIFIED. ) ;
#8540=PLANE ( 'NONE',  #4504 ) ;
#8543=AXIS2_PLACEMENT_3D ( 'NONE', #9486, #4567, #10779 ) ;
#8545=ORIENTED_EDGE ( 'NONE', *, *, #2339, .F. ) ;
#8547=CARTESIAN_POINT ( 'NONE',  ( -5.953540064417263800, 38.00510092317821886, 78.67637590524894620 ) ) ;
#8548=CARTESIAN_POINT ( 'NONE',  ( 5.508100443945853186, 47.59510827513957310, 75.45433879953087342 ) ) ;
#8549=FACE_OUTER_BOUND ( 'NONE', #3775, .T. ) ;
#8550=LINE ( 'NONE', #8439, #14347 ) ;
#8552=DIRECTION ( 'NONE',  ( -1.540237394707284220E-16, -1.793354297423764243E-16, 1.000000000000000000 ) ) ;
#8554=FACE_OUTER_BOUND ( 'NONE', #17160, .T. ) ;
#8555=CARTESIAN_POINT ( 'NONE',  ( -6.823472211661642639, 40.67201601130748401, 77.53559663939034863 ) ) ;
#8556=ADVANCED_FACE ( 'NONE', ( #2988 ), #1034, .F. ) ;
#8557=CARTESIAN_POINT ( 'NONE',  ( -4.924280525269182363, 51.08613106951644767, 75.37785507730471579 ) ) ;
#8558=CARTESIAN_POINT ( 'NONE',  ( 6.701747691083868474, 50.53797885426168079, 79.21482656134288902 ) ) ;
#8559=ADVANCED_FACE ( 'NONE', ( #16291 ), #18691, .T. ) ;
#8563=CARTESIAN_POINT ( 'NONE',  ( 5.848951923618479931, 37.15274410921379911, 76.58742703482498371 ) ) ;
#8564=MECHANICAL_DESIGN_GEOMETRIC_PRESENTATION_REPRESENTATION('',(#7877),#15710);
#8565=ORIENTED_EDGE ( 'NONE', *, *, #12393, .F. ) ;
#8566=CARTESIAN_POINT ( 'NONE',  ( 0.8417336166835989175, 52.96423374080004720, 79.54553221853565503 ) ) ;
#8573=ORIENTED_EDGE ( 'NONE', *, *, #1941, .T. ) ;
#8574=CARTESIAN_POINT ( 'NONE',  ( 8.804199926738755622, 41.18047021065184055, 77.88643322029270166 ) ) ;
#8575=CARTESIAN_POINT ( 'NONE',  ( -5.486635640793876334, 38.59622392959819592, 76.24300064276494027 ) ) ;
#8579=B_SPLINE_CURVE_WITH_KNOTS ( 'NONE', 3,
 ( #9473, #4653, #15959, #9052, #17342, #17643, #17857, #21030, #1592, #16268, #3493, #19450, #13079, #6465, #3185, #192, #11598, #12969 ),
 .UNSPECIFIED., .F., .F.,
 ( 4, 2, 2, 2, 2, 2, 2, 2, 4 ),
 ( 0.000000000000000000, 0.0007105477805655377281, 0.001065821670848306592, 0.001421095561131075456, 0.001598732506272453275, 0.001776369451413830876, 0.001954006396555208695, 0.002131643341696586296, 0.002842191122262097136 ),
 .UNSPECIFIED. ) ;
#8580=CARTESIAN_POINT ( 'NONE',  ( 5.605329808110463219, 51.34785857800776654, 78.76051003739772227 ) ) ;
#8581=CARTESIAN_POINT ( 'NONE',  ( 3.212180877488374886, 51.27651577472676792, 72.45432679953087529 ) ) ;
#8585=CARTESIAN_POINT ( 'NONE',  ( -2.167873396875370950, 37.04784696823259793, 72.45433879953085921 ) ) ;
#8587=ORIENTED_EDGE ( 'NONE', *, *, #2329, .F. ) ;
#8592=EDGE_CURVE ( 'NONE', #16784, #8044, #14673, .T. ) ;
#8594=CARTESIAN_POINT ( 'NONE',  ( 6.740887235739653427, 50.50906804926147942, 75.70960632971019777 ) ) ;
#8595=CARTESIAN_POINT ( 'NONE',  ( 5.581367357135656349, 50.61542532950539197, 76.94912097791375061 ) ) ;
#8596=VECTOR ( 'NONE', #16912, 1000.000000000000000 ) ;
#8597=DIRECTION ( 'NONE',  ( -0.9539696396349525154, 0.2999031954727373050, -9.315070279690336121E-17 ) ) ;
#8599=ORIENTED_EDGE ( 'NONE', *, *, #2583, .F. ) ;
#8601=CARTESIAN_POINT ( 'NONE',  ( 4.208856430796397596, 36.90056750005005171, 75.71841013695411959 ) ) ;
#8602=VECTOR ( 'NONE', #13183, 1000.000000000000000 ) ;
#8603=CARTESIAN_POINT ( 'NONE',  ( 8.414968994577074923, 40.01392041461337357, 78.89537297773202340 ) ) ;
#8604=ORIENTED_EDGE ( 'NONE', *, *, #13724, .T. ) ;
#8605=CARTESIAN_POINT ( 'NONE',  ( -4.359893715479207899, 37.57388776543446340, 75.36022115247205022 ) ) ;
#8606=CARTESIAN_POINT ( 'NONE',  ( 0.5221537403065009686, 44.16218137147968292, 79.45433879953087342 ) ) ;
#8608=ORIENTED_EDGE ( 'NONE', *, *, #15219, .F. ) ;
#8610=VERTEX_POINT ( 'NONE', #13858 ) ;
#8611=CARTESIAN_POINT ( 'NONE',  ( 0.6452163281857689059, 52.96132085210302165, 79.54845644658969661 ) ) ;
#8612=AXIS2_PLACEMENT_3D ( 'NONE', #1462, #16350, #6331 ) ;
#8614=CARTESIAN_POINT ( 'NONE',  ( 4.546108750497564799, 52.13026250523957827, 76.88467537290178200 ) ) ;
#8615=CARTESIAN_POINT ( 'NONE',  ( 2.813615989083933844, 36.91585811327295374, 72.45432679953087529 ) ) ;
#8617=CARTESIAN_POINT ( 'NONE',  ( 8.798005484913860030, 41.16190507553456968, 76.10950202369875228 ) ) ;
#8618=B_SPLINE_CURVE_WITH_KNOTS ( 'NONE', 3,
 ( #6095, #14398, #20467, #17694, #3121, #12702, #9316, #20661, #19179, #12491, #6200, #17488, #9624, #17585, #16106, #12399, #4593, #10812, #2914, #17278, #3013, #14182, #9210, #15696, #18978, #7604, #14087 ),
 .UNSPECIFIED., .F., .F.,
 ( 4, 1, 1, 1, 1, 1, 1, 1, 1, 1, 1, 1, 1, 1, 1, 1, 1, 1, 1, 1, 1, 1, 1, 1, 4 ),
 ( 0.000000000000000000, 0.05111620615384394190, 0.09904209687041264087, 0.1432334450931441461, 0.1843589373079111415, 0.2222937343119009146, 0.2574440974212286459, 0.2893637488079585096, 0.3188910630028964910, 0.3474602836591745292, 0.3767670824238625316, 0.4074295047838343287, 0.4392621747742110894, 0.4730325979957886173, 0.5084852716492808122, 0.5462542205972961140, 0.5860610780164621225, 0.6283505634423164343, 0.6729648726644925638, 0.7201947540188263774, 0.7701882088044430530, 0.8230700400259792771, 0.8789456997408242600, 0.9378877171948971636, 1.000000000000000000 ),
 .UNSPECIFIED. ) ;
#8619=CARTESIAN_POINT ( 'NONE',  ( 8.527988662190095326, 48.03182059810101379, 79.44551527011911674 ) ) ;
#8620=CARTESIAN_POINT ( 'NONE',  ( 4.544296722651392173, 52.13160097721661401, 76.36737811492949390 ) ) ;
#8624=EDGE_LOOP ( 'NONE', ( #15986, #10185, #3715, #6686 ) ) ;
#8626=DIRECTION ( 'NONE',  ( -1.540237394707284220E-16, -1.793354297423764243E-16, 1.000000000000000000 ) ) ;
#8628=ADVANCED_FACE ( 'NONE', ( #563 ), #13545, .F. ) ;
#8630=DIRECTION ( 'NONE',  ( 0.007885122365275663500, 0.9999689119394085113, 1.805443505845543142E-16 ) ) ;
#8632=CARTESIAN_POINT ( 'NONE',  ( -4.361349971946749449, 37.58365018120226608, 78.93613021445058564 ) ) ;
#8634=CARTESIAN_POINT ( 'NONE',  ( -4.686954935604242145, 37.06952550968519233, 77.27854074750605662 ) ) ;
#8635=CARTESIAN_POINT ( 'NONE',  ( 0.5221537403065005245, 44.16218137147968292, 82.45433879953087342 ) ) ;
#8636=ADVANCED_FACE ( 'NONE', ( #5455 ), #16953, .F. ) ;
#8638=VERTEX_POINT ( 'NONE', #16537 ) ;
#8639=CARTESIAN_POINT ( 'NONE',  ( 8.281036760714160394, 41.97693506373668271, 79.53018343098241871 ) ) ;
#8641=CARTESIAN_POINT ( 'NONE',  ( 5.499753608866646104, 50.67865541357578252, 77.99542992962396681 ) ) ;
#8643=PLANE ( 'NONE',  #16091 ) ;
#8644=FACE_OUTER_BOUND ( 'NONE', #16427, .T. ) ;
#8646=DIRECTION ( 'NONE',  ( -1.540237394707284220E-16, -1.793354297423764243E-16, 1.000000000000000000 ) ) ;
#8648=CARTESIAN_POINT ( 'NONE',  ( 1.706499989092010949, 52.94348737648915204, 76.92027168626151479 ) ) ;
#8653=ORIENTED_EDGE ( 'NONE', *, *, #13000, .T. ) ;
#8657=CARTESIAN_POINT ( 'NONE',  ( -4.592862224480082745, 51.32295045326189609, 75.97198585835440099 ) ) ;
#8658=LINE ( 'NONE', #18321, #9483 ) ;
#8660=DIRECTION ( 'NONE',  ( 1.540237394707284467E-16, 1.793354297423764243E-16, -1.000000000000000000 ) ) ;
#8661=CARTESIAN_POINT ( 'NONE',  ( 5.562547263452509938, 51.37946032036057886, 77.00567114208729436 ) ) ;
#8662=LINE ( 'NONE', #556, #12666 ) ;
#8663=ORIENTED_EDGE ( 'NONE', *, *, #15753, .F. ) ;
#8665=ORIENTED_EDGE ( 'NONE', *, *, #15289, .T. ) ;
#8666=ADVANCED_FACE ( 'NONE', ( #244 ), #1957, .T. ) ;
#8667=DIRECTION ( 'NONE',  ( 1.540237394707283727E-16, 1.793354297423763257E-16, -1.000000000000000000 ) ) ;
#8668=CARTESIAN_POINT ( 'NONE',  ( -7.885128509680407127, 41.54523971581953390, 76.16022115247204738 ) ) ;
#8670=CARTESIAN_POINT ( 'NONE',  ( 7.691771551572206711, 40.18266124458227750, 72.45433879953087342 ) ) ;
#8673=EDGE_LOOP ( 'NONE', ( #4907, #10181, #8784, #15703 ) ) ;
#8674=CARTESIAN_POINT ( 'NONE',  ( 8.274641112204461635, 41.51360698326416809, 78.93505401271374922 ) ) ;
#8677=B_SPLINE_CURVE_WITH_KNOTS ( 'NONE', 3,
 ( #16392, #3399, #17551, #16283, #2978, #7986, #8087, #14576, #9911, #14471, #7773, #14250, #6370, #20733, #12673 ),
 .UNSPECIFIED., .F., .F.,
 ( 4, 1, 1, 1, 1, 1, 1, 1, 1, 1, 1, 1, 4 ),
 ( 0.000000000000000000, 0.07527217715292475186, 0.1459465445934834404, 0.2117756949130734923, 0.2766029815265222958, 0.3381147468631120478, 0.3951637252042238257, 0.4534551218168583753, 0.5124046679576552688, 0.5890284689491043224, 0.6947781202056673155, 0.8321371544603952675, 0.9999999999999998890 ),
 .UNSPECIFIED. ) ;
#8678=ADVANCED_FACE ( 'NONE', ( #352 ), #20457, .F. ) ;
#8681=ORIENTED_EDGE ( 'NONE', *, *, #13097, .F. ) ;
#8686=VERTEX_POINT ( 'NONE', #9089 ) ;
#8688=ORIENTED_EDGE ( 'NONE', *, *, #11507, .F. ) ;
#8689=CARTESIAN_POINT ( 'NONE',  ( -4.774380534136511756, 51.19324411499089678, 76.08363728426196815 ) ) ;
#8690=DIRECTION ( 'NONE',  ( -0.9999689119394086223, 0.007885122365275665235, -1.526048693634353392E-16 ) ) ;
#8693=CARTESIAN_POINT ( 'NONE',  ( -3.545047478496393456, 36.22604446995779881, 78.23707788297487298 ) ) ;
#8696=CARTESIAN_POINT ( 'NONE',  ( -3.098709854545130593, 36.80491647020841128, 78.46683879953087626 ) ) ;
#8700=EDGE_CURVE ( 'NONE', #11467, #15461, #14078, .T. ) ;
#8703=CARTESIAN_POINT ( 'NONE',  ( 0.4250111554052659057, 52.35549180149831727, 77.42486900944150818 ) ) ;
#8705=EDGE_LOOP ( 'NONE', ( #103, #17370, #17586, #1420 ) ) ;
#8706=CARTESIAN_POINT ( 'NONE',  ( 6.885459498894642927, 50.40227834219487590, 78.84682786933051091 ) ) ;
#8709=CARTESIAN_POINT ( 'NONE',  ( 6.882377701754223587, 37.89119233413698140, 76.59354538285809610 ) ) ;
#8711=CARTESIAN_POINT ( 'NONE',  ( -3.552306130656605720, 51.28101034580461004, 79.43132126585329900 ) ) ;
#8712=CARTESIAN_POINT ( 'NONE',  ( -0.5476599173704348456, 52.89753068181172324, 75.65267637979816584 ) ) ;
#8713=FACE_OUTER_BOUND ( 'NONE', #7170, .T. ) ;
#8715=CARTESIAN_POINT ( 'NONE',  ( 8.868817592801745420, 41.37413345511091478, 75.97198585835440099 ) ) ;
#8716=LINE ( 'NONE', #7209, #19685 ) ;
#8719=CARTESIAN_POINT ( 'NONE',  ( 8.346529106983265223, 41.70870148392067023, 76.02106044755406344 ) ) ;
#8722=LINE ( 'NONE', #7103, #17329 ) ;
#8723=CARTESIAN_POINT ( 'NONE',  ( 8.214799251806553571, 41.32260305165857517, 78.45948585835439815 ) ) ;
#8728=DIRECTION ( 'NONE',  ( 1.540237394707284220E-16, 1.793354297423764243E-16, -1.000000000000000000 ) ) ;
#8731=CARTESIAN_POINT ( 'NONE',  ( 5.761154613439540384, 51.23275707131721646, 77.94923276678728996 ) ) ;
#8732=ORIENTED_EDGE ( 'NONE', *, *, #12606, .F. ) ;
#8734=CARTESIAN_POINT ( 'NONE',  ( 6.507769556168451430, 49.76686128376767471, 77.01032402965913093 ) ) ;
#8735=CARTESIAN_POINT ( 'NONE',  ( -4.680892486399498509, 37.06504742266799468, 75.36060488990274564 ) ) ;
#8736=ADVANCED_FACE ( 'NONE', ( #991 ), #5985, .T. ) ;
#8738=ORIENTED_EDGE ( 'NONE', *, *, #13380, .F. ) ;
#8739=CARTESIAN_POINT ( 'NONE',  ( 0.5351667827239598996, 52.36231569124743146, 78.93477473415802592 ) ) ;
#8740=DIRECTION ( 'NONE',  ( -0.5941461771851693774, -0.8043570849667760481, -2.357623395011396791E-16 ) ) ;
#8741=EDGE_CURVE ( 'NONE', #15118, #2200, #15471, .T. ) ;
#8742=AXIS2_PLACEMENT_3D ( 'NONE', #13343, #13443, #15042 ) ;
#8745=( BOUNDED_CURVE ( )  B_SPLINE_CURVE ( 3, ( #14625, #1764, #14730, #11134 ),
 .UNSPECIFIED., .F., .F. ) 
 B_SPLINE_CURVE_WITH_KNOTS ( ( 4, 4 ),
 ( 1.415673517910795987, 1.520829339303995331 ),
 .UNSPECIFIED. ) 
 CURVE ( )  GEOMETRIC_REPRESENTATION_ITEM ( )  RATIONAL_B_SPLINE_CURVE ( ( 1.000000000000000000, 0.9990787333635395839, 0.9990787333635395839, 1.000000000000000000 ) ) 
 REPRESENTATION_ITEM ( '' )  );
#8746=CARTESIAN_POINT ( 'NONE',  ( -7.783107710516365962, 41.22738444886793729, 78.61536821129558916 ) ) ;
#8750=LINE ( 'NONE', #15238, #4460 ) ;
#8753=CARTESIAN_POINT ( 'NONE',  ( -4.265367546595294712, 50.81005072751269580, 78.93596273702843291 ) ) ;
#8755=VERTEX_POINT ( 'NONE', #15369 ) ;
#8756=DIRECTION ( 'NONE',  ( 0.6080936526121289987, 0.7938652969193448206, 2.360290325043240801E-16 ) ) ;
#8757=CARTESIAN_POINT ( 'NONE',  ( -4.158578283022522193, 37.42937009194850617, 76.81463291717793140 ) ) ;
#8758=CARTESIAN_POINT ( 'NONE',  ( -3.343753456003188518, 51.29574226414619886, 79.34012906335151172 ) ) ;
#8759=LINE ( 'NONE', #10477, #5344 ) ;
#8760=DIRECTION ( 'NONE',  ( 1.540237394707284220E-16, 1.793354297423764243E-16, -1.000000000000000000 ) ) ;
#8763=VERTEX_POINT ( 'NONE', #5782 ) ;
#8764=CARTESIAN_POINT ( 'NONE',  ( 5.241898597225179479, 50.86770213969851540, 78.23114816710980790 ) ) ;
#8765=VECTOR ( 'NONE', #3416, 1000.000000000000000 ) ;
#8766=VERTEX_POINT ( 'NONE', #4379 ) ;
#8770=DIRECTION ( 'NONE',  ( -1.540237394707284220E-16, -1.793354297423764243E-16, 1.000000000000000000 ) ) ;
#8772=CARTESIAN_POINT ( 'NONE',  ( 1.652727357819364640, 35.35299279957455809, 75.45433879953087342 ) ) ;
#8773=ORIENTED_EDGE ( 'NONE', *, *, #20113, .T. ) ;
#8774=CARTESIAN_POINT ( 'NONE',  ( 4.103056440471904764, 51.53898521715114356, 76.82013224188756340 ) ) ;
#8777=CARTESIAN_POINT ( 'NONE',  ( -4.387981331227590154, 51.46935083841186298, 75.37146543928014353 ) ) ;
#8780=ORIENTED_EDGE ( 'NONE', *, *, #2197, .T. ) ;
#8781=B_SPLINE_CURVE_WITH_KNOTS ( 'NONE', 3,
 ( #2722, #4514, #9227, #11033, #15715, #1133, #7621, #14103, #4410, #17503, #20585, #2927, #6013, #9429, #7721 ),
 .UNSPECIFIED., .F., .F.,
 ( 4, 1, 1, 1, 1, 1, 1, 1, 1, 1, 1, 1, 4 ),
 ( 0.000000000000000000, 0.1107947361882193060, 0.2116365373969002206, 0.3025951166517907298, 0.3827141919669941328, 0.4557983700405009997, 0.5187458605491411801, 0.5729830782426720281, 0.6198356358567430613, 0.7053145269299332387, 0.7944869293383459707, 0.8901174066118697770, 1.000000000000000000 ),
 .UNSPECIFIED. ) ;
#8782=CARTESIAN_POINT ( 'NONE',  ( -4.409036544953043979, 47.67330854490502645, 75.45433879953087342 ) ) ;
#8784=ORIENTED_EDGE ( 'NONE', *, *, #20820, .T. ) ;
#8787=ORIENTED_EDGE ( 'NONE', *, *, #16781, .F. ) ;
#8790=EDGE_LOOP ( 'NONE', ( #12887, #4667, #2421, #16916 ) ) ;
#8791=CARTESIAN_POINT ( 'NONE',  ( -4.762271096064603526, 51.20189707608225405, 76.05031124229590489 ) ) ;
#8792=PLANE ( 'NONE',  #15649 ) ;
#8793=VECTOR ( 'NONE', #18953, 1000.000000000000000 ) ;
#8797=DIRECTION ( 'NONE',  ( -0.5813877811927011807, 0.8136266022444372803, 5.636455622144619183E-17 ) ) ;
#8800=CARTESIAN_POINT ( 'NONE',  ( 1.972616468458138650, 52.95547850198470030, 75.87378281519762879 ) ) ;
#8802=CARTESIAN_POINT ( 'NONE',  ( 6.876224750190004897, 50.40909967906462441, 75.93520998463665705 ) ) ;
#8805=EDGE_LOOP ( 'NONE', ( #15479, #14486, #10, #5374 ) ) ;
#8806=AXIS2_PLACEMENT_3D ( 'NONE', #14611, #16320, #9731 ) ;
#8808=LINE ( 'NONE', #15302, #8272 ) ;
#8810=CARTESIAN_POINT ( 'NONE',  ( -3.579922675594000125, 36.25180537319517526, 77.38751485876633751 ) ) ;
#8812=CARTESIAN_POINT ( 'NONE',  ( -4.804644443005472887, 51.17161863374555963, 76.44036821129557779 ) ) ;
#8813=DIRECTION ( 'NONE',  ( -1.540237394707283727E-16, -1.793354297423763257E-16, 1.000000000000000000 ) ) ;
#8814=CARTESIAN_POINT ( 'NONE',  ( -7.578484755904182357, 42.88833611937010915, 79.14296897072306081 ) ) ;
#8816=CARTESIAN_POINT ( 'NONE',  ( 0.5915713968613123264, 52.96553219837200999, 77.38375056423674891 ) ) ;
#8818=CARTESIAN_POINT ( 'NONE',  ( 4.566945366853153665, 51.19003838910122539, 75.50506468444432073 ) ) ;
#8820=AXIS2_PLACEMENT_3D ( 'NONE', #2017, #8515, #11810 ) ;
#8821=EDGE_CURVE ( 'NONE', #10817, #7197, #10599, .T. ) ;
#8823=VERTEX_POINT ( 'NONE', #4487 ) ;
#8825=AXIS2_PLACEMENT_3D ( 'NONE', #13450, #13352, #3656 ) ;
#8828=LINE ( 'NONE', #20297, #12636 ) ;
#8829=CARTESIAN_POINT ( 'NONE',  ( -3.350758615681482144, 52.21051221579373447, 78.23748737924660190 ) ) ;
#8831=VECTOR ( 'NONE', #20042, 1000.000000000000000 ) ;
#8832=CARTESIAN_POINT ( 'NONE',  ( -4.730130202819497143, 37.10141734037124905, 77.29630340639747033 ) ) ;
#8833=CARTESIAN_POINT ( 'NONE',  ( -6.859224089373359590, 47.65557686534583581, 78.82648837639791850 ) ) ;
#8834=CARTESIAN_POINT ( 'NONE',  ( -3.621797592085240769, 36.28273668718272660, 77.97675128563095370 ) ) ;
#8836=LINE ( 'NONE', #10345, #14922 ) ;
#8837=VECTOR ( 'NONE', #17841, 1000.000000000000114 ) ;
#8838=ORIENTED_EDGE ( 'NONE', *, *, #15208, .T. ) ;
#8842=CARTESIAN_POINT ( 'NONE',  ( 6.490071791215038743, 49.78570669403264048, 77.16764180776988269 ) ) ;
#8844=LINE ( 'NONE', #18834, #3139 ) ;
#8847=AXIS2_PLACEMENT_3D ( 'NONE', #15515, #4436, #17421 ) ;
#8848=CARTESIAN_POINT ( 'NONE',  ( -8.190968255476823501, 42.92868192021149554, 75.86215881574817388 ) ) ;
#8850=EDGE_CURVE ( 'NONE', #14271, #12459, #8987, .T. ) ;
#8851=CARTESIAN_POINT ( 'NONE',  ( -0.8303902511565894873, 52.85771897673274111, 78.94509925486606505 ) ) ;
#8854=CARTESIAN_POINT ( 'NONE',  ( -6.962266735612947066, 47.40375324003255741, 78.31366413292410300 ) ) ;
#8856=VECTOR ( 'NONE', #11191, 999.9999999999998863 ) ;
#8859=ORIENTED_EDGE ( 'NONE', *, *, #2214, .F. ) ;
#8860=ADVANCED_FACE ( 'NONE', ( #4181 ), #17575, .F. ) ;
#8861=CARTESIAN_POINT ( 'NONE',  ( 1.485376517908854721, 52.30695239789775997, 75.48605119142476383 ) ) ;
#8862=ORIENTED_EDGE ( 'NONE', *, *, #20534, .F. ) ;
#8869=CARTESIAN_POINT ( 'NONE',  ( 0.5915428171209280439, 52.96190779654647685, 77.38375056423674891 ) ) ;
#8870=CARTESIAN_POINT ( 'NONE',  ( -3.350758615681482144, 52.21051221579373447, 78.23748737924660190 ) ) ;
#8871=CARTESIAN_POINT ( 'NONE',  ( 0.7375380209976891699, 52.95956711614144297, 77.42541598925475910 ) ) ;
#8872=CARTESIAN_POINT ( 'NONE',  ( 5.633915549615357676, 51.32674344226200702, 77.24912405724838038 ) ) ;
#8873=CARTESIAN_POINT ( 'NONE',  ( -7.600593896485818846, 45.28511094584521146, 72.45433879953085921 ) ) ;
#8876=CARTESIAN_POINT ( 'NONE',  ( 8.286596668832688195, 41.52487556862202922, 77.52280427046368061 ) ) ;
#8878=CARTESIAN_POINT ( 'NONE',  ( 6.352353975415561571, 49.92870928545907816, 77.86676136243460178 ) ) ;
#8880=FACE_OUTER_BOUND ( 'NONE', #3998, .T. ) ;
#8882=DIRECTION ( 'NONE',  ( 0.02533578529877050789, 0.9996789974703352843, 1.831801750099146688E-16 ) ) ;
#8884=EDGE_CURVE ( 'NONE', #4878, #5410, #18302, .T. ) ;
#8885=CARTESIAN_POINT ( 'NONE',  ( -5.056163503743585252, 37.34224500634140043, 75.38158877174898009 ) ) ;
#8888=CARTESIAN_POINT ( 'NONE',  ( -0.7567330459223939876, 36.05414901439895914, 77.72082377648446538 ) ) ;
#8889=VECTOR ( 'NONE', #1933, 1000.000000000000114 ) ;
#8890=ORIENTED_EDGE ( 'NONE', *, *, #555, .T. ) ;
#8894=B_SPLINE_SURFACE_WITH_KNOTS ( 'NONE', 3, 1, ( 
 ( #6567, #12755 ),
 ( #16372, #4862 ),
 ( #9996, #14765 ),
 ( #186, #17854 ),
 ( #9685, #19234 ),
 ( #3279, #3375 ),
 ( #17753, #16263 ),
 ( #16061, #9891 ),
 ( #7970, #17960 ),
 ( #17638, #18066 ),
 ( #1691, #1587 ) ),
 .UNSPECIFIED., .F., .F., .F.,
 ( 4, 1, 1, 1, 1, 1, 1, 1, 4 ),
 ( 2, 2 ),
 ( 0.000000000000000000, 0.1230989878275519644, 0.2403818709996815850, 0.3547287725962395277, 0.4701889909135318901, 0.5896219003167558759, 0.7153806559642975627, 0.8522030906580475573, 1.000000000000000000 ),
 ( 0.000000000000000000, 1.000000000000000000 ),
 .UNSPECIFIED. ) ;
#8895=CARTESIAN_POINT ( 'NONE',  ( -7.250832141565055622, 41.98755119451053730, 77.57193099691271243 ) ) ;
#8898=CARTESIAN_POINT ( 'NONE',  ( 0.5915428171209280439, 52.96190779654647685, 77.38375056423674891 ) ) ;
#8901=VERTEX_POINT ( 'NONE', #7792 ) ;
#8902=FACE_BOUND ( 'NONE', #18328, .T. ) ;
#8905=ORIENTED_EDGE ( 'NONE', *, *, #9488, .T. ) ;
#8910=CARTESIAN_POINT ( 'NONE',  ( 8.378637954445377289, 41.81363803720061867, 72.45433879953087342 ) ) ;
#8911=CARTESIAN_POINT ( 'NONE',  ( 0.5398981455733474766, 52.96229826333378554, 78.93477474516929249 ) ) ;
#8912=PLANE ( 'NONE',  #13325 ) ;
#8914=CARTESIAN_POINT ( 'NONE',  ( 1.932080035760362247, 52.95579814665390472, 75.81376357423876300 ) ) ;
#8915=EDGE_LOOP ( 'NONE', ( #4983, #11875, #13765, #2181 ) ) ;
#8916=AXIS2_PLACEMENT_3D ( 'NONE', #5949, #4028, #12038 ) ;
#8917=CARTESIAN_POINT ( 'NONE',  ( 6.955656837306707807, 50.35042639603116044, 76.39262467917644983 ) ) ;
#8918=DIRECTION ( 'NONE',  ( 0.9534635866061452747, 0.3015081906286224411, 2.009271279954815304E-16 ) ) ;
#8921=DIRECTION ( 'NONE',  ( -0.9999689119394086223, 0.007885122365275665235, -1.526048693634353392E-16 ) ) ;
#8922=VERTEX_POINT ( 'NONE', #11315 ) ;
#8923=CARTESIAN_POINT ( 'NONE',  ( 5.018290002877273892, 50.86746622949960539, 79.53290755650829169 ) ) ;
#8926=DIRECTION ( 'NONE',  ( -1.540237394707284467E-16, -1.793354297423764243E-16, 1.000000000000000000 ) ) ;
#8929=CARTESIAN_POINT ( 'NONE',  ( 0.8251303722654924622, 52.35233671442713899, 77.55588632845071118 ) ) ;
#8930=AXIS2_PLACEMENT_3D ( 'NONE', #16198, #20654, #19273 ) ;
#8934=VECTOR ( 'NONE', #15460, 1000.000000000000000 ) ;
#8935=CARTESIAN_POINT ( 'NONE',  ( -7.956935296483398368, 41.77702279339499825, 78.50654468188380974 ) ) ;
#8936=CARTESIAN_POINT ( 'NONE',  ( 8.787829143201870252, 41.13140593384865440, 76.40801527011910821 ) ) ;
#8940=VECTOR ( 'NONE', #1425, 1000.000000000000114 ) ;
#8942=CARTESIAN_POINT ( 'NONE',  ( -7.857211665749059826, 46.86741566905539713, 79.32924967153994089 ) ) ;
#8944=EDGE_CURVE ( 'NONE', #13012, #13982, #957, .T. ) ;
#8945=FACE_OUTER_BOUND ( 'NONE', #12190, .T. ) ;
#8948=CARTESIAN_POINT ( 'NONE',  ( 8.569783991210568885, 42.84232883131717529, 79.15097751326614173 ) ) ;
#8951=B_SPLINE_CURVE_WITH_KNOTS ( 'NONE', 3,
 ( #11060, #6449, #1681, #20610, #17845, #14443, #9568, #16154, #12748, #4641, #11374, #7958, #12955, #2953, #4742, #19434, #21014, #17432, #14343, #17741, #20818, #9357, #6246 ),
 .UNSPECIFIED., .F., .F.,
 ( 4, 1, 1, 1, 1, 1, 1, 1, 1, 1, 1, 1, 1, 1, 1, 1, 1, 1, 1, 1, 4 ),
 ( 0.000000000000000000, 0.04683093660151300269, 0.09055667580802433114, 0.1312013806050136844, 0.1681729499244319359, 0.2024082766003676426, 0.2330515569695218725, 0.2607881417524846590, 0.2857054801288026469, 0.3326652789510584074, 0.3814982805224741425, 0.4333318279156733732, 0.4889629060548432160, 0.5467408684218817427, 0.6046224851005120859, 0.6645427963802341687, 0.7261481924644412889, 0.7902890061914499276, 0.8570127982043956871, 0.9269126820953633716, 1.000000000000000000 ),
 .UNSPECIFIED. ) ;
#8954=B_SPLINE_CURVE_WITH_KNOTS ( 'NONE', 3,
 ( #3464, #8149, #9975, #8580, #15064, #477, #11673, #12944, #14639, #3355, #1876 ),
 .UNSPECIFIED., .F., .F.,
 ( 4, 1, 1, 1, 1, 1, 1, 1, 4 ),
 ( 0.000000000000000000, 0.2096989846417539882, 0.3830033715279665407, 0.5180517223345033617, 0.6192761841629320640, 0.7029005363942016915, 0.7892332632667665715, 0.8867012962659018838, 1.000000000000000000 ),
 .UNSPECIFIED. ) ;
#8955=CARTESIAN_POINT ( 'NONE',  ( 9.106328434870372135, 42.08596851619746104, 78.11626675975762168 ) ) ;
#8957=CARTESIAN_POINT ( 'NONE',  ( -4.412197277429617870, 51.45204700985827628, 76.06958028623719770 ) ) ;
#8959=EDGE_CURVE ( 'NONE', #6196, #19924, #16506, .T. ) ;
#8960=CARTESIAN_POINT ( 'NONE',  ( -7.088677424969694663, 47.02489238468576360, 77.68791732120209304 ) ) ;
#8962=CARTESIAN_POINT ( 'NONE',  ( 6.814395614697851933, 37.84261482370956031, 75.97427057108799886 ) ) ;
#8964=CARTESIAN_POINT ( 'NONE',  ( 5.924340528221679669, 51.11221820959726614, 77.13671500005938242 ) ) ;
#8965=EDGE_CURVE ( 'NONE', #8763, #19237, #14489, .T. ) ;
#8969=ORIENTED_EDGE ( 'NONE', *, *, #12127, .T. ) ;
#8971=DIRECTION ( 'NONE',  ( -0.8136266022444372803, -0.5813877811927011807, -2.295812393977109100E-16 ) ) ;
#8972=EDGE_CURVE ( 'NONE', #15539, #15079, #12899, .T. ) ;
#8974=CARTESIAN_POINT ( 'NONE',  ( -3.165193363162642104, 51.42333476898780020, 79.18928797456808866 ) ) ;
#8976=FACE_OUTER_BOUND ( 'NONE', #20065, .T. ) ;
#8977=CARTESIAN_POINT ( 'NONE',  ( 6.961907239250668233, 50.34580947589670075, 76.63889762306028786 ) ) ;
#8981=ORIENTED_EDGE ( 'NONE', *, *, #5746, .F. ) ;
#8983=CARTESIAN_POINT ( 'NONE',  ( 4.540095451430588902, 52.13470428702989068, 76.74217282813371810 ) ) ;
#8984=CARTESIAN_POINT ( 'NONE',  ( 7.864691922653266332, 47.81281597943210215, 78.56977997600147035 ) ) ;
#8985=ADVANCED_FACE ( 'NONE', ( #2999 ), #15474, .F. ) ;
#8986=CARTESIAN_POINT ( 'NONE',  ( 6.885459498894642927, 50.40227834219487590, 78.84682786933051091 ) ) ;
#8987=LINE ( 'NONE', #886, #4352 ) ;
#8988=CARTESIAN_POINT ( 'NONE',  ( 5.839584039462725862, 37.14605016217623046, 76.11636564480957645 ) ) ;
#8989=CARTESIAN_POINT ( 'NONE',  ( -4.716387082485073989, 37.09126585098686490, 75.36022115247205022 ) ) ;
#8991=CARTESIAN_POINT ( 'NONE',  ( 8.787893756631275366, 41.13159958439556618, 78.49453464888588883 ) ) ;
#8993=CARTESIAN_POINT ( 'NONE',  ( -3.952897528319690323, 50.86047021225675024, 75.37146543928014353 ) ) ;
#8995=CARTESIAN_POINT ( 'NONE',  ( -8.178850963866057810, 42.47164029129891105, 76.61471288230795551 ) ) ;
#8996=EDGE_LOOP ( 'NONE', ( #15582, #4885, #15186, #401 ) ) ;
#8997=ADVANCED_FACE ( 'NONE', ( #18305 ), #16990, .F. ) ;
#9002=CARTESIAN_POINT ( 'NONE',  ( 5.288291328326708118, 36.75211657491283290, 75.39318197153889400 ) ) ;
#9005=VERTEX_POINT ( 'NONE', #325 ) ;
#9006=CARTESIAN_POINT ( 'NONE',  ( 1.847086472663199253, 52.25482134247464927, 79.19213266016700459 ) ) ;
#9009=CARTESIAN_POINT ( 'NONE',  ( -4.633747169617723927, 50.53922380117749213, 79.50315915470658013 ) ) ;
#9015=DIRECTION ( 'NONE',  ( -1.540237394707284220E-16, -1.793354297423764243E-16, 1.000000000000000000 ) ) ;
#9016=CARTESIAN_POINT ( 'NONE',  ( 5.245411638781020791, 50.86060015470197726, 78.76051003739772227 ) ) ;
#9019=CARTESIAN_POINT ( 'NONE',  ( 2.120607010463642528, 52.95431154217356351, 76.45922371407752394 ) ) ;
#9022=CARTESIAN_POINT ( 'NONE',  ( 0.3279354642263507258, 52.35625727899917337, 77.76169174070734869 ) ) ;
#9025=FACE_OUTER_BOUND ( 'NONE', #16184, .T. ) ;
#9027=CARTESIAN_POINT ( 'NONE',  ( 4.772654808018759631, 51.96292205838052070, 79.19424447893550223 ) ) ;
#9029=CARTESIAN_POINT ( 'NONE',  ( 8.395197883163783459, 39.95466513945179798, 76.21925085218815354 ) ) ;
#9030=CARTESIAN_POINT ( 'NONE',  ( -4.525688498162968365, 36.95040448855567661, 78.17872471894986575 ) ) ;
#9031=CARTESIAN_POINT ( 'NONE',  ( -6.771957287108766543, 40.50912055441206405, 79.09912640779528203 ) ) ;
#9032=DIRECTION ( 'NONE',  ( 1.540237394707284220E-16, 1.793354297423764243E-16, -1.000000000000000000 ) ) ;
#9036=CARTESIAN_POINT ( 'NONE',  ( -5.390530271885531022, 49.83319048879877045, 76.36675183022860836 ) ) ;
#9037=CARTESIAN_POINT ( 'NONE',  ( 4.826069222465897646, 51.92346698209227895, 75.62563104034643402 ) ) ;
#9039=CARTESIAN_POINT ( 'NONE',  ( -7.291677074388141833, 40.11445521940208891, 78.59658243778928011 ) ) ;
#9041=CARTESIAN_POINT ( 'NONE',  ( 8.934486310075088866, 41.57094676672487310, 78.86350455626283917 ) ) ;
#9042=FACE_OUTER_BOUND ( 'NONE', #11672, .T. ) ;
#9044=CARTESIAN_POINT ( 'NONE',  ( -3.350053155021378792, 52.21101631215288563, 78.15066919019970726 ) ) ;
#9046=CARTESIAN_POINT ( 'NONE',  ( -4.529265440370440210, 36.95304663167631531, 77.01245883157920957 ) ) ;
#9047=CARTESIAN_POINT ( 'NONE',  ( -7.465715295087656855, 42.67411418385548671, 79.33973788556694728 ) ) ;
#9048=CARTESIAN_POINT ( 'NONE',  ( 8.641107047301593624, 43.01204830781416888, 77.56292432728525910 ) ) ;
#9049=EDGE_CURVE ( 'NONE', #19214, #11104, #18839, .T. ) ;
#9050=CARTESIAN_POINT ( 'NONE',  ( -4.616992131696503243, 37.01784680471218536, 75.99117330331094422 ) ) ;
#9051=ORIENTED_EDGE ( 'NONE', *, *, #20629, .T. ) ;
#9052=CARTESIAN_POINT ( 'NONE',  ( 8.025069409823680999, 40.85162907203753946, 75.45988996333271359 ) ) ;
#9053=DIRECTION ( 'NONE',  ( -0.3165065846431825980, -0.9485903129789530208, 0.000000000000000000 ) ) ;
#9057=CARTESIAN_POINT ( 'NONE',  ( 5.748274343403736886, 51.24227120794373747, 77.94845644658968808 ) ) ;
#9065=CARTESIAN_POINT ( 'NONE',  ( 6.866536783559561208, 37.87987299396810670, 76.25518385353585415 ) ) ;
#9066=ORIENTED_EDGE ( 'NONE', *, *, #2976, .T. ) ;
#9067=CARTESIAN_POINT ( 'NONE',  ( 5.755371611800503828, 51.23702874167446453, 77.28963291717792572 ) ) ;
#9068=VERTEX_POINT ( 'NONE', #15341 ) ;
#9069=CARTESIAN_POINT ( 'NONE',  ( -4.443144554159853321, 50.68301778673873059, 78.71090438869831019 ) ) ;
#9076=EDGE_CURVE ( 'NONE', #11628, #9753, #11108, .T. ) ;
#9077=CARTESIAN_POINT ( 'NONE',  ( -3.746334366659155979, 51.00807268481932510, 79.50772166908967620 ) ) ;
#9078=LINE ( 'NONE', #875, #7750 ) ;
#9080=CARTESIAN_POINT ( 'NONE',  ( -3.874372605692208094, 36.46930367539203388, 79.33401574558745040 ) ) ;
#9082=CARTESIAN_POINT ( 'NONE',  ( 6.522436035574397550, 49.75115376156129798, 72.45433879953087342 ) ) ;
#9084=ORIENTED_EDGE ( 'NONE', *, *, #2977, .F. ) ;
#9086=FACE_OUTER_BOUND ( 'NONE', #17351, .T. ) ;
#9087=CARTESIAN_POINT ( 'NONE',  ( 6.545534159973747990, 50.65336749702785113, 77.68963291717794561 ) ) ;
#9089=CARTESIAN_POINT ( 'NONE',  ( -6.647464070959230753, 48.14170149837704571, 72.45433879953087342 ) ) ;
#9090=DIRECTION ( 'NONE',  ( -0.9534635866061452747, -0.3015081906286225522, -2.009271279954815797E-16 ) ) ;
#9092=CONICAL_SURFACE ( 'NONE', #20945, 6.200000000000020606, 1.047197551196600518 ) ;
#9093=VERTEX_POINT ( 'NONE', #18525 ) ;
#9094=CARTESIAN_POINT ( 'NONE',  ( 4.100647748703544870, 51.54014729097003311, 76.70496318590288354 ) ) ;
#9096=CARTESIAN_POINT ( 'NONE',  ( -4.472548095981605520, 51.40892252450552036, 75.36471306604558151 ) ) ;
#9098=ORIENTED_EDGE ( 'NONE', *, *, #7398, .T. ) ;
#9101=CARTESIAN_POINT ( 'NONE',  ( 6.433553176315263578, 38.47928099333162777, 72.45433879953087342 ) ) ;
#9104=CARTESIAN_POINT ( 'NONE',  ( 9.176231272041631470, 45.98187388689780164, 75.44992703482499508 ) ) ;
#9105=EDGE_CURVE ( 'NONE', #10886, #16595, #7285, .T. ) ;
#9112=CARTESIAN_POINT ( 'NONE',  ( -5.195654067311837210, 50.04042785407680327, 79.16788338592567698 ) ) ;
#9113=CARTESIAN_POINT ( 'NONE',  ( 5.110857744515833190, 37.36631113118844638, 76.10944558133218152 ) ) ;
#9116=CARTESIAN_POINT ( 'NONE',  ( -3.716800330428157384, 36.35291138305289849, 77.85659439586764563 ) ) ;
#9117=CARTESIAN_POINT ( 'NONE',  ( 5.478721299898049679, 36.88819086051147167, 76.06572720930677178 ) ) ;
#9119=CARTESIAN_POINT ( 'NONE',  ( -7.609845089999874190, 43.10833364818387992, 76.06610350541322418 ) ) ;
#9120=EDGE_CURVE ( 'NONE', #559, #8246, #17683, .T. ) ;
#9122=FACE_OUTER_BOUND ( 'NONE', #7962, .T. ) ;
#9123=ORIENTED_EDGE ( 'NONE', *, *, #8184, .T. ) ;
#9124=CARTESIAN_POINT ( 'NONE',  ( -0.5095519206278340540, 52.29771471936252425, 79.29519679866520221 ) ) ;
#9125=EDGE_CURVE ( 'NONE', #9436, #4858, #20473, .T. ) ;
#9129=ORIENTED_EDGE ( 'NONE', *, *, #8472, .T. ) ;
#9131=EDGE_LOOP ( 'NONE', ( #12073, #11975, #17719, #13853, #9591, #6437, #19408, #8681, #13816, #6797, #20524, #15776, #3167, #19064, #12722, #11385, #13958, #5446, #12129, #20545, #12316, #18038, #17923, #5335 ) ) ;
#9132=ADVANCED_FACE ( 'NONE', ( #16689 ), #402, .F. ) ;
#9135=CARTESIAN_POINT ( 'NONE',  ( 8.387016861607721196, 39.93014609885396027, 76.70090004521539129 ) ) ;
#9136=VECTOR ( 'NONE', #7034, 1000.000000000000000 ) ;
#9137=VERTEX_POINT ( 'NONE', #18175 ) ;
#9138=CARTESIAN_POINT ( 'NONE',  ( -4.990412171993358292, 37.29367714620271101, 77.90250793075740887 ) ) ;
#9139=CARTESIAN_POINT ( 'NONE',  ( 5.884818748728627646, 51.14141135607439992, 78.06587361566768379 ) ) ;
#9142=PLANE ( 'NONE',  #7387 ) ;
#9143=CARTESIAN_POINT ( 'NONE',  ( -5.347586347461742662, 49.86387664491459049, 76.07566230427023868 ) ) ;
#9147=CARTESIAN_POINT ( 'NONE',  ( 8.951667845840693971, 41.62244091939069790, 78.41904468188381827 ) ) ;
#9150=ORIENTED_EDGE ( 'NONE', *, *, #14442, .F. ) ;
#9151=CARTESIAN_POINT ( 'NONE',  ( -7.611372734017124664, 43.12018948500615778, 75.45433879953087342 ) ) ;
#9152=CARTESIAN_POINT ( 'NONE',  ( 0.5627506536433498630, 51.36208509089345142, 75.97198585835440099 ) ) ;
#9154=CARTESIAN_POINT ( 'NONE',  ( -3.363202728395832342, 52.20162010845611178, 78.48078762820125576 ) ) ;
#9156=CARTESIAN_POINT ( 'NONE',  ( 9.353817388681445522, 42.82770861117572281, 78.41904468188381827 ) ) ;
#9158=CARTESIAN_POINT ( 'NONE',  ( 5.430298293217690642, 36.85358955281711246, 77.55899030588862786 ) ) ;
#9161=CARTESIAN_POINT ( 'NONE',  ( -4.092474520164236296, 50.94051422294817399, 76.01547346202475808 ) ) ;
#9162=CARTESIAN_POINT ( 'NONE',  ( 0.3821786226492927541, 35.36301154328572949, 76.16022115247204738 ) ) ;
#9163=CARTESIAN_POINT ( 'NONE',  ( 5.755371611800503828, 51.23702874167446453, 77.28963291717792572 ) ) ;
#9164=CARTESIAN_POINT ( 'NONE',  ( 5.734785278855812685, 51.25223503655262647, 77.94915300234312383 ) ) ;
#9165=VECTOR ( 'NONE', #18008, 1000.000000000000227 ) ;
#9166=CARTESIAN_POINT ( 'NONE',  ( 9.242846470233811118, 42.49512172872434945, 77.95057265855270145 ) ) ;
#9170=ORIENTED_EDGE ( 'NONE', *, *, #9675, .F. ) ;
#9172=VECTOR ( 'NONE', #15220, 1000.000000000000114 ) ;
#9173=CARTESIAN_POINT ( 'NONE',  ( -6.792737292293178797, 47.86790251333490431, 78.78375056423675460 ) ) ;
#9175=CARTESIAN_POINT ( 'NONE',  ( 0.5934291639749685876, 52.36187159818830850, 75.36022115247205022 ) ) ;
#9176=AXIS2_PLACEMENT_3D ( 'NONE', #2959, #12752, #14556 ) ;
#9177=ORIENTED_EDGE ( 'NONE', *, *, #5040, .T. ) ;
#9183=CARTESIAN_POINT ( 'NONE',  ( -0.9175459788215616364, 52.21929978415766982, 76.23506554152810111 ) ) ;
#9184=AXIS2_PLACEMENT_3D ( 'NONE', #12740, #16147, #6334 ) ;
#9185=AXIS2_PLACEMENT_3D ( 'NONE', #5453, #784, #16851 ) ;
#9186=CARTESIAN_POINT ( 'NONE',  ( -4.330063686617302565, 50.77263821455978388, 75.97757385978665923 ) ) ;
#9189=CARTESIAN_POINT ( 'NONE',  ( -3.527921555204845738, 37.12740924552473842, 79.39152984579853012 ) ) ;
#9190=ORIENTED_EDGE ( 'NONE', *, *, #7673, .T. ) ;
#9193=EDGE_LOOP ( 'NONE', ( #18009, #8545, #9634, #453 ) ) ;
#9194=CARTESIAN_POINT ( 'NONE',  ( 5.230203880350988044, 37.63038499358497546, 75.36022115247205022 ) ) ;
#9200=DIRECTION ( 'NONE',  ( -1.540237394707283727E-16, -1.793354297423763257E-16, 1.000000000000000000 ) ) ;
#9201=FACE_OUTER_BOUND ( 'NONE', #9405, .T. ) ;
#9202=CARTESIAN_POINT ( 'NONE',  ( 5.655950003444441876, 37.76811099897118851, 78.37198585835440667 ) ) ;
#9203=B_SPLINE_SURFACE_WITH_KNOTS ( 'NONE', 3, 1, ( 
 ( #5479, #3574 ),
 ( #10186, #20156 ),
 ( #13467, #19939 ),
 ( #10079, #5366 ),
 ( #18359, #16561 ),
 ( #8791, #18572 ),
 ( #8689, #7180 ),
 ( #10405, #15394 ),
 ( #15070, #6866 ),
 ( #1982, #8477 ),
 ( #3779, #15281 ),
 ( #15170, #18466 ),
 ( #16669, #701 ),
 ( #586, #3881 ),
 ( #2293, #16973 ) ),
 .UNSPECIFIED., .F., .F., .F.,
 ( 4, 1, 1, 1, 1, 1, 1, 1, 1, 1, 1, 1, 4 ),
 ( 2, 2 ),
 ( 0.000000000000000000, 0.1176523470896303353, 0.2161622001139844318, 0.3003057309359747351, 0.3785980537073788676, 0.4226998745584166772, 0.4746596431302817498, 0.5370400780653459272, 0.6084305140821594238, 0.6909958779695384301, 0.7839813792576545426, 0.8861497511813531958, 0.9999999999999998890 ),
 ( 0.000000000000000000, 1.000000000000000000 ),
 .UNSPECIFIED. ) ;
#9205=CARTESIAN_POINT ( 'NONE',  ( 8.214833241226736860, 41.32269513172508368, 76.35929938113996229 ) ) ;
#9206=VERTEX_POINT ( 'NONE', #606 ) ;
#9207=DIRECTION ( 'NONE',  ( 0.5941461771851728191, 0.8043570849667734945, 2.357623395011397284E-16 ) ) ;
#9210=CARTESIAN_POINT ( 'NONE',  ( 5.429452001895136881, 51.47777242866884251, 75.37972891991934432 ) ) ;
#9213=CARTESIAN_POINT ( 'NONE',  ( -5.323589340698339001, 50.80079960963960417, 79.37256909934775706 ) ) ;
#9215=CARTESIAN_POINT ( 'NONE',  ( 6.114519447167765520, 37.34250893849451813, 78.36972961004526894 ) ) ;
#9216=CARTESIAN_POINT ( 'NONE',  ( 5.209619950776937181, 50.88551756745181365, 76.17377400622436312 ) ) ;
#9219=DIRECTION ( 'NONE',  ( -0.3015081906286224966, 0.9534635866061452747, 1.245503830460468587E-16 ) ) ;
#9221=EDGE_CURVE ( 'NONE', #8340, #12307, #7200, .T. ) ;
#9222=VERTEX_POINT ( 'NONE', #4006 ) ;
#9223=CARTESIAN_POINT ( 'NONE',  ( -5.005367866107262032, 50.21986932831274686, 79.33799273367436911 ) ) ;
#9224=PLANE ( 'NONE',  #1366 ) ;
#9226=CARTESIAN_POINT ( 'NONE',  ( -3.799282117832333494, 36.41383735683930212, 77.78682928037112276 ) ) ;
#9227=CARTESIAN_POINT ( 'NONE',  ( 8.787869161997047485, 41.13152587271654426, 76.34522901481825841 ) ) ;
#9230=VERTEX_POINT ( 'NONE', #14219 ) ;
#9231=CARTESIAN_POINT ( 'NONE',  ( 2.064224670253138605, 52.95475613764697442, 76.07541412571639228 ) ) ;
#9232=ORIENTED_EDGE ( 'NONE', *, *, #3722, .T. ) ;
#9233=CARTESIAN_POINT ( 'NONE',  ( 6.591015671753180705, 50.61977213638343187, 75.57514290624801845 ) ) ;
#9234=CARTESIAN_POINT ( 'NONE',  ( 5.330578599509985693, 37.52924894288483415, 77.75763958275959453 ) ) ;
#9239=CARTESIAN_POINT ( 'NONE',  ( -4.611439147851055687, 37.01374503923339176, 75.36135576041903050 ) ) ;
#9242=ORIENTED_EDGE ( 'NONE', *, *, #19379, .T. ) ;
#9244=EDGE_CURVE ( 'NONE', #445, #4372, #2426, .T. ) ;
#9245=FACE_OUTER_BOUND ( 'NONE', #2341, .T. ) ;
#9247=EDGE_CURVE ( 'NONE', #19774, #1868, #20276, .T. ) ;
#9250=CARTESIAN_POINT ( 'NONE',  ( -7.435811987448031068, 40.12253007576792641, 78.82487260570216847 ) ) ;
#9254=FACE_OUTER_BOUND ( 'NONE', #4651, .T. ) ;
#9255=ADVANCED_FACE ( 'NONE', ( #928 ), #13906, .T. ) ;
#9256=EDGE_CURVE ( 'NONE', #12581, #11222, #7636, .T. ) ;
#9260=CARTESIAN_POINT ( 'NONE',  ( 8.949918141112842562, 41.61719694332212072, 78.74360054667872078 ) ) ;
#9263=ORIENTED_EDGE ( 'NONE', *, *, #19610, .T. ) ;
#9265=FACE_OUTER_BOUND ( 'NONE', #20854, .T. ) ;
#9266=CARTESIAN_POINT ( 'NONE',  ( 8.515342467852711650, 40.31474608159486195, 79.26294543469528264 ) ) ;
#9270=CARTESIAN_POINT ( 'NONE',  ( 8.641109729321982513, 43.05609659325752858, 78.59572304307680213 ) ) ;
#9271=CARTESIAN_POINT ( 'NONE',  ( -4.751859364981149803, 37.11746779715601718, 79.54765774203875139 ) ) ;
#9273=DIRECTION ( 'NONE',  ( -0.5941461771851691553, -0.8043570849667760481, -2.357623395011396791E-16 ) ) ;
#9280=ADVANCED_FACE ( 'NONE', ( #1041 ), #1381, .T. ) ;
#9284=CARTESIAN_POINT ( 'NONE',  ( -4.630794176838950449, 51.29584566888366481, 79.54703672271651271 ) ) ;
#9285=VECTOR ( 'NONE', #5625, 999.9999999999998863 ) ;
#9286=ORIENTED_EDGE ( 'NONE', *, *, #20418, .F. ) ;
#9287=CARTESIAN_POINT ( 'NONE',  ( 5.873343927958857513, 51.14988734394304970, 77.25083512729199242 ) ) ;
#9288=EDGE_LOOP ( 'NONE', ( #1538, #1484, #19335, #19115 ) ) ;
#9291=ORIENTED_EDGE ( 'NONE', *, *, #19459, .T. ) ;
#9293=CARTESIAN_POINT ( 'NONE',  ( -0.9343110595793820972, 52.97862540336715398, 76.74746709665741662 ) ) ;
#9294=CARTESIAN_POINT ( 'NONE',  ( -4.244029479098209379, 50.83477438462418974, 75.97198585835440099 ) ) ;
#9296=CARTESIAN_POINT ( 'NONE',  ( 0.7930981759416947385, 52.96401942048080969, 76.04568394904065087 ) ) ;
#9297=CARTESIAN_POINT ( 'NONE',  ( -3.535132420242974138, 36.21872061582890723, 78.58910375170351870 ) ) ;
#9300=VECTOR ( 'NONE', #19806, 999.9999999999998863 ) ;
#9302=VERTEX_POINT ( 'NONE', #11050 ) ;
#9307=CARTESIAN_POINT ( 'NONE',  ( 5.694963103159264683, 37.04270933600420079, 75.97340568087561508 ) ) ;
#9308=CARTESIAN_POINT ( 'NONE',  ( -5.907462774012221196, 37.97106548486249267, 76.06004113464240390 ) ) ;
#9310=CARTESIAN_POINT ( 'NONE',  ( 2.813615989083933844, 36.91585811327294664, 75.45433879953087342 ) ) ;
#9312=EDGE_LOOP ( 'NONE', ( #8094, #2375, #16847, #15378 ) ) ;
#9313=AXIS2_PLACEMENT_3D ( 'NONE', #16977, #20261, #14778 ) ;
#9316=CARTESIAN_POINT ( 'NONE',  ( 4.575658464751415799, 52.10843532165534953, 76.08931382966170531 ) ) ;
#9320=CARTESIAN_POINT ( 'NONE',  ( -4.518589064258795140, 36.94516042271329326, 78.67445481091525039 ) ) ;
#9321=ADVANCED_FACE ( 'NONE', ( #14432 ), #20384, .F. ) ;
#9323=ORIENTED_EDGE ( 'NONE', *, *, #17525, .F. ) ;
#9326=ORIENTED_EDGE ( 'NONE', *, *, #15324, .T. ) ;
#9327=CARTESIAN_POINT ( 'NONE',  ( 0.5221537403065015237, 44.16218137147968292, 75.45433879953088763 ) ) ;
#9333=CARTESIAN_POINT ( 'NONE',  ( -7.211434918694761720, 41.43606403771804025, 78.45489642720582424 ) ) ;
#9335=CARTESIAN_POINT ( 'NONE',  ( -7.154059339130676598, 47.04588606493869918, 77.58227997600145898 ) ) ;
#9336=EDGE_CURVE ( 'NONE', #16327, #15690, #15222, .T. ) ;
#9338=LINE ( 'NONE', #20889, #11913 ) ;
#9339=CARTESIAN_POINT ( 'NONE',  ( 5.769916034762062829, 37.09626795672559041, 77.71701144737939160 ) ) ;
#9342=ORIENTED_EDGE ( 'NONE', *, *, #15289, .F. ) ;
#9344=ORIENTED_EDGE ( 'NONE', *, *, #16125, .F. ) ;
#9345=CARTESIAN_POINT ( 'NONE',  ( -3.878807879564845962, 37.39741278052461837, 75.39293290059653430 ) ) ;
#9346=CARTESIAN_POINT ( 'NONE',  ( -5.405803290722375642, 49.82780803385384871, 76.66164947481811964 ) ) ;
#9347=ORIENTED_EDGE ( 'NONE', *, *, #10271, .T. ) ;
#9348=CARTESIAN_POINT ( 'NONE',  ( 4.202207491541066098, 51.47027350681489111, 78.92424046551381878 ) ) ;
#9349=CARTESIAN_POINT ( 'NONE',  ( -6.716320333671362164, 40.30932109133388508, 78.68352653107739059 ) ) ;
#9350=CARTESIAN_POINT ( 'NONE',  ( 8.389283321988518338, 39.93693882439677623, 76.47636794762235013 ) ) ;
#9351=ADVANCED_FACE ( 'NONE', ( #11364 ), #17834, .T. ) ;
#9353=CARTESIAN_POINT ( 'NONE',  ( 5.987192815050652150, 50.27622337231140648, 75.44981441668713273 ) ) ;
#9354=CARTESIAN_POINT ( 'NONE',  ( 5.819883890974968388, 51.18937611976139834, 77.96367690144739981 ) ) ;
#9355=CARTESIAN_POINT ( 'NONE',  ( 6.450247442662826458, 38.49669771550791353, 76.69330938776616335 ) ) ;
#9357=CARTESIAN_POINT ( 'NONE',  ( -4.699374957658429608, 51.24684035381270064, 75.36124333316173818 ) ) ;
#9362=B_SPLINE_CURVE_WITH_KNOTS ( 'NONE', 3,
 ( #16257, #7960, #3367, #14445, #8060, #20913, #14758, #14552, #12849, #4745, #6453 ),
 .UNSPECIFIED., .F., .F.,
 ( 4, 1, 1, 1, 1, 1, 1, 1, 4 ),
 ( 0.000000000000000000, 0.1182921183292337947, 0.2229146666077276573, 0.3191072744444787279, 0.4123240778398947204, 0.5160602913484956256, 0.6446607815519475038, 0.8056994663548258107, 1.000000000000000000 ),
 .UNSPECIFIED. ) ;
#9363=CARTESIAN_POINT ( 'NONE',  ( 4.539372959821318609, 52.13523796247791608, 76.58963291717793709 ) ) ;
#9365=CARTESIAN_POINT ( 'NONE',  ( 5.575778192174150050, 51.36968716628822307, 76.13411024644928204 ) ) ;
#9367=ORIENTED_EDGE ( 'NONE', *, *, #4787, .F. ) ;
#9368=CARTESIAN_POINT ( 'NONE',  ( -7.594489630341222153, 43.08133907316179290, 78.79856413697085316 ) ) ;
#9369=FACE_OUTER_BOUND ( 'NONE', #13457, .T. ) ;
#9370=ORIENTED_EDGE ( 'NONE', *, *, #5694, .F. ) ;
#9371=CARTESIAN_POINT ( 'NONE',  ( 8.214956227423224178, 41.32302818927274757, 78.56413997391275927 ) ) ;
#9372=CARTESIAN_POINT ( 'NONE',  ( -4.069601230858992835, 36.61351119651401120, 79.44037905412795908 ) ) ;
#9373=CARTESIAN_POINT ( 'NONE',  ( 5.076572431691917409, 37.34329067111212197, 77.43080938776617472 ) ) ;
#9375=B_SPLINE_SURFACE_WITH_KNOTS ( 'NONE', 3, 1, ( 
 ( #10200, #11479 ),
 ( #19440, #3370 ),
 ( #1890, #19850 ),
 ( #13278, #19543 ),
 ( #8378, #14972 ),
 ( #19747, #8487 ),
 ( #6877, #5169 ),
 ( #16570, #3581 ),
 ( #391, #13381 ),
 ( #10088, #4959 ),
 ( #3480, #11786 ),
 ( #8603, #18261 ),
 ( #11379, #14760 ),
 ( #1797, #5271 ),
 ( #13068, #8278 ),
 ( #1992, #3681 ),
 ( #16678, #2101 ),
 ( #17849, #15081 ),
 ( #3273, #495 ),
 ( #9779, #1685 ),
 ( #8166, #14653 ),
 ( #14424, #11252 ),
 ( #16033, #19416 ),
 ( #12938, #7941 ),
 ( #7838, #11142 ),
 ( #3042, #19114 ),
 ( #7730, #19005 ) ),
 .UNSPECIFIED., .F., .F., .F.,
 ( 4, 1, 1, 1, 1, 1, 1, 1, 1, 1, 1, 1, 1, 1, 1, 1, 1, 1, 1, 1, 1, 1, 1, 1, 4 ),
 ( 2, 2 ),
 ( 0.000000000000000000, 0.05993306358482522467, 0.1145105083304139432, 0.1639926324650750333, 0.2083799252409545000, 0.2474206522578790979, 0.2813744068707942358, 0.3102651545178817805, 0.3340707221093189849, 0.3764843156245091249, 0.4195869878574357559, 0.4649490021377667981, 0.5131068515344550107, 0.5381792345077858197, 0.5638273912065150384, 0.5896398555221948889, 0.6163062535856453916, 0.6433841197412238921, 0.6712141767968796691, 0.7000136030487154049, 0.7297781433983795418, 0.7919609919944711196, 0.8575419152218471952, 0.9267698348267595643, 1.000000000000000000 ),
 ( 0.000000000000000000, 1.000000000000000000 ),
 .UNSPECIFIED. ) ;
#9376=CARTESIAN_POINT ( 'NONE',  ( 5.374867109526370257, 50.76497661324683719, 77.94915300234312383 ) ) ;
#9382=CARTESIAN_POINT ( 'NONE',  ( -5.261478123908109872, 50.84518201112111058, 79.40394833312912226 ) ) ;
#9383=EDGE_CURVE ( 'NONE', #10724, #13622, #8759, .T. ) ;
#9384=CARTESIAN_POINT ( 'NONE',  ( 5.248942363195014948, 50.86274201606274659, 78.77059126715526816 ) ) ;
#9385=EDGE_LOOP ( 'NONE', ( #18245, #14638, #2397, #6874 ) ) ;
#9386=DIRECTION ( 'NONE',  ( 1.540237394707284220E-16, 1.793354297423764243E-16, -1.000000000000000000 ) ) ;
#9387=B_SPLINE_CURVE_WITH_KNOTS ( 'NONE', 3,
 ( #19657, #3594, #13489, #8503, #14988, #10005, #5390, #8712, #1904, #6892, #14772, #5083, #11601, #13396, #18076, #2746, #18704, #7317 ),
 .UNSPECIFIED., .F., .F.,
 ( 4, 2, 2, 2, 2, 2, 2, 2, 4 ),
 ( 0.000000000000000000, 0.0003586288075955534156, 0.0007172576151911068312, 0.001075886422786660138, 0.001434515230382213662, 0.001793144037977766969, 0.001972458441775543948, 0.002151772845573320277, 0.002869030460764344492 ),
 .UNSPECIFIED. ) ;
#9390=ORIENTED_EDGE ( 'NONE', *, *, #15208, .F. ) ;
#9391=CARTESIAN_POINT ( 'NONE',  ( 5.753005855668248181, 51.23877623043087937, 78.93669174070734584 ) ) ;
#9392=CARTESIAN_POINT ( 'NONE',  ( -0.9278697225093164302, 52.97857461105712673, 76.50701133828320621 ) ) ;
#9393=CARTESIAN_POINT ( 'NONE',  ( 4.989364768915854675, 51.80284713987553857, 79.39429067157672648 ) ) ;
#9395=PLANE ( 'NONE',  #12145 ) ;
#9397=EDGE_LOOP ( 'NONE', ( #16615, #8608, #17498, #11784 ) ) ;
#9398=CARTESIAN_POINT ( 'NONE',  ( 2.119851040271390374, 52.81592988514039178, 77.84551527011910821 ) ) ;
#9399=ORIENTED_EDGE ( 'NONE', *, *, #17785, .F. ) ;
#9403=PLANE ( 'NONE',  #5917 ) ;
#9404=CARTESIAN_POINT ( 'NONE',  ( -5.955289093497882824, 38.00639286050488863, 76.68644156968609593 ) ) ;
#9405=EDGE_LOOP ( 'NONE', ( #3557, #20714, #15680, #10394 ) ) ;
#9406=PLANE ( 'NONE',  #15278 ) ;
#9409=CARTESIAN_POINT ( 'NONE',  ( -3.906146384357795043, 51.81365245034167799, 75.48713596493043099 ) ) ;
#9410=EDGE_CURVE ( 'NONE', #17793, #8117, #9078, .T. ) ;
#9413=VERTEX_POINT ( 'NONE', #16942 ) ;
#9414=CARTESIAN_POINT ( 'NONE',  ( -5.181694682358441995, 49.98224533783228907, 79.13778479689705136 ) ) ;
#9416=ORIENTED_EDGE ( 'NONE', *, *, #6268, .T. ) ;
#9417=CARTESIAN_POINT ( 'NONE',  ( 4.753159030984773992, 36.36973062767617648, 75.61597629374708163 ) ) ;
#9418=CARTESIAN_POINT ( 'NONE',  ( 5.570264759168902735, 51.37375971715457013, 76.17377400622436312 ) ) ;
#9420=LINE ( 'NONE', #20876, #19353 ) ;
#9424=FACE_OUTER_BOUND ( 'NONE', #15554, .T. ) ;
#9426=AXIS2_PLACEMENT_3D ( 'NONE', #18435, #8760, #12380 ) ;
#9429=CARTESIAN_POINT ( 'NONE',  ( 8.862035351310685982, 41.35380664710483245, 75.97281361087948426 ) ) ;
#9430=CARTESIAN_POINT ( 'NONE',  ( 5.928804517645879457, 51.10892084043006633, 76.16996516156804375 ) ) ;
#9431=B_SPLINE_CURVE_WITH_KNOTS ( 'NONE', 3,
 ( #17406, #10935, #11245, #3035, #1445, #17718, #11350, #12623, #20588, #6016, #20792, #12516, #7830, #18998 ),
 .UNSPECIFIED., .F., .F.,
 ( 4, 2, 2, 2, 2, 2, 4 ),
 ( 0.000000000000000000, 0.0004302987682907632766, 0.0006454481524361446168, 0.0008605975365815261196, 0.001075746920726907731, 0.001290896304872289017, 0.001721195073163036627 ),
 .UNSPECIFIED. ) ;
#9433=CARTESIAN_POINT ( 'NONE',  ( -7.145525873512015735, 47.06850347111571864, 78.12199217155379927 ) ) ;
#9434=CARTESIAN_POINT ( 'NONE',  ( 5.981342461385748877, 37.24734554037533485, 78.37107466246847309 ) ) ;
#9435=CARTESIAN_POINT ( 'NONE',  ( -6.753843712027885360, 40.38066566033639759, 75.45433879953087342 ) ) ;
#9436=VERTEX_POINT ( 'NONE', #11957 ) ;
#9437=DIRECTION ( 'NONE',  ( 0.5813877811926998485, -0.8136266022444382795, -5.636455622144657394E-17 ) ) ;
#9438=CARTESIAN_POINT ( 'NONE',  ( 0.5221537403065015237, 44.16218137147968292, 75.45433879953088763 ) ) ;
#9440=B_SPLINE_CURVE_WITH_KNOTS ( 'NONE', 3,
 ( #17553, #17245, #2980, #2669, #14472, #1284, #10882, #11187, #20538, #19059, #7672, #12461, #1083, #5866 ),
 .UNSPECIFIED., .F., .F.,
 ( 4, 2, 2, 2, 2, 2, 4 ),
 ( 0.000000000000000000, 0.0001389616711475478018, 0.0002779233422950956036, 0.0003474041778688886678, 0.0004168850134426816778, 0.0004863658490164747420, 0.0005558466845902677519 ),
 .UNSPECIFIED. ) ;
#9443=ORIENTED_EDGE ( 'NONE', *, *, #9244, .F. ) ;
#9445=CARTESIAN_POINT ( 'NONE',  ( -3.165374202885676613, 36.87042806242320125, 75.89423958357750166 ) ) ;
#9446=CARTESIAN_POINT ( 'NONE',  ( 8.355456706376745757, 41.73731273165762445, 78.88551942360874136 ) ) ;
#9447=CARTESIAN_POINT ( 'NONE',  ( 5.830039445700249345, 50.26785961534839942, 79.48482414599367019 ) ) ;
#9448=ORIENTED_EDGE ( 'NONE', *, *, #17925, .F. ) ;
#9449=CARTESIAN_POINT ( 'NONE',  ( -4.480134106163296437, 37.69151641300361177, 77.31947969467269388 ) ) ;
#9450=CARTESIAN_POINT ( 'NONE',  ( 8.221051890839362386, 41.35279423182788605, 77.39661844205990349 ) ) ;
#9453=CARTESIAN_POINT ( 'NONE',  ( 5.497743849324331578, 37.64424434608246628, 77.37492703482499223 ) ) ;
#9454=CARTESIAN_POINT ( 'NONE',  ( -7.835841657577859998, 41.38754952096324047, 79.54638463348854316 ) ) ;
#9455=CARTESIAN_POINT ( 'NONE',  ( -5.510796958474740492, 38.60848837797752964, 78.53742703482498655 ) ) ;
#9458=VECTOR ( 'NONE', #13916, 1000.000000000000000 ) ;
#9460=CARTESIAN_POINT ( 'NONE',  ( 5.308657174530695855, 50.64216575474389970, 75.36022115247205022 ) ) ;
#9463=DIRECTION ( 'NONE',  ( 0.3165065846431827645, 0.9485903129789529098, 0.000000000000000000 ) ) ;
#9464=CARTESIAN_POINT ( 'NONE',  ( -0.9429997834273105006, 52.21747844655818227, 77.93056416558285093 ) ) ;
#9465=ORIENTED_EDGE ( 'NONE', *, *, #15478, .T. ) ;
#9466=CARTESIAN_POINT ( 'NONE',  ( -4.267481014617145796, 37.50633945324470631, 75.98838203353618326 ) ) ;
#9468=CARTESIAN_POINT ( 'NONE',  ( 8.392124750090893315, 39.94545476467643397, 78.58253683706189463 ) ) ;
#9472=ORIENTED_EDGE ( 'NONE', *, *, #8700, .T. ) ;
#9473=CARTESIAN_POINT ( 'NONE',  ( 8.318328750355229673, 41.62059619433301094, 75.36022115247205022 ) ) ;
#9474=CARTESIAN_POINT ( 'NONE',  ( -4.473072018670158911, 36.91153881467540998, 79.53329352641277694 ) ) ;
#9475=CARTESIAN_POINT ( 'NONE',  ( 5.427780505986065762, 36.85179043424346190, 76.70433879953087342 ) ) ;
#9479=CARTESIAN_POINT ( 'NONE',  ( 6.680635945739894055, 50.55357325011429026, 77.60602934391619101 ) ) ;
#9482=B_SPLINE_CURVE_WITH_KNOTS ( 'NONE', 3,
 ( #1956, #12174, #10273, #4180, #8986, #16749, #13760, #4071, #8558, #10706, #676, #2381, #7045, #10598, #3860, #15368, #5664, #785, #7265 ),
 .UNSPECIFIED., .F., .F.,
 ( 4, 1, 1, 1, 1, 1, 1, 1, 1, 1, 1, 1, 1, 1, 1, 1, 4 ),
 ( 0.000000000000000000, 0.06302581646095750667, 0.1222495429959427476, 0.1789669701231155763, 0.2332877456213924006, 0.2860909212508800925, 0.3384954837963008445, 0.3911857795644178570, 0.4453574251251987137, 0.5015394511440722791, 0.5602660668541803446, 0.6223358252984214634, 0.6886061413240012197, 0.7590929558684775813, 0.8342439359547982880, 0.9143471077142913961, 1.000000000000000000 ),
 .UNSPECIFIED. ) ;
#9483=VECTOR ( 'NONE', #16940, 1000.000000000000227 ) ;
#9486=CARTESIAN_POINT ( 'NONE',  ( 2.337612517491833852, 49.93701999136722947, 72.45432679953087529 ) ) ;
#9487=CARTESIAN_POINT ( 'NONE',  ( -5.927888611570137911, 47.57933715648534445, 78.32492703482499508 ) ) ;
#9488=EDGE_CURVE ( 'NONE', #8267, #10926, #15142, .T. ) ;
#9490=FACE_OUTER_BOUND ( 'NONE', #15693, .T. ) ;
#9493=CARTESIAN_POINT ( 'NONE',  ( 4.432284427945813121, 36.14044538431356557, 77.43080938776617472 ) ) ;
#9495=CARTESIAN_POINT ( 'NONE',  ( -0.7807185704487904498, 52.97741427014419457, 75.89928829349869943 ) ) ;
#9496=CARTESIAN_POINT ( 'NONE',  ( 5.706854332355044690, 51.27286650160559134, 79.54768974400036541 ) ) ;
#9497=CARTESIAN_POINT ( 'NONE',  ( -2.917199766949190476, 51.60602765227618960, 78.10580938776615767 ) ) ;
#9501=EDGE_CURVE ( 'NONE', #8403, #492, #19965, .T. ) ;
#9506=CARTESIAN_POINT ( 'NONE',  ( -6.851854717395867489, 47.75120794669041402, 78.80861213953217259 ) ) ;
#9507=CARTESIAN_POINT ( 'NONE',  ( 1.110644313093400504, 52.20952139108884893, 76.77233108029956554 ) ) ;
#9509=CARTESIAN_POINT ( 'NONE',  ( 8.496652696354052736, 46.09822506120844565, 76.54154894328375747 ) ) ;
#9513=CARTESIAN_POINT ( 'NONE',  ( 4.582010541884842247, 52.10374329815417127, 78.30859729819620441 ) ) ;
#9514=ORIENTED_EDGE ( 'NONE', *, *, #13272, .F. ) ;
#9519=CARTESIAN_POINT ( 'NONE',  ( -8.192078482032011166, 42.93655631659661509, 72.45433879953085921 ) ) ;
#9520=ORIENTED_EDGE ( 'NONE', *, *, #4663, .F. ) ;
#9521=CARTESIAN_POINT ( 'NONE',  ( -5.376400592477268425, 49.84311562309974164, 78.65111229433956908 ) ) ;
#9523=CARTESIAN_POINT ( 'NONE',  ( -4.178795553179217137, 37.44880458579923044, 78.81995494622690046 ) ) ;
#9524=CARTESIAN_POINT ( 'NONE',  ( 5.575778192174150050, 51.36968716628822307, 76.13411024644928204 ) ) ;
#9525=DIRECTION ( 'NONE',  ( 0.003131479924976700649, -0.009902722955645586189, -0.9999460635011987453 ) ) ;
#9527=VECTOR ( 'NONE', #11996, 1000.000000000000114 ) ;
#9530=FACE_OUTER_BOUND ( 'NONE', #12477, .T. ) ;
#9535=CIRCLE ( 'NONE', #8510, 6.000000000000002665 ) ;
#9536=CARTESIAN_POINT ( 'NONE',  ( 0.7926596301127065702, 52.95803722965069227, 78.84197725022382031 ) ) ;
#9540=EDGE_CURVE ( 'NONE', #12039, #496, #7360, .T. ) ;
#9542=CARTESIAN_POINT ( 'NONE',  ( 5.933960187751527116, 51.10511255460609448, 76.21496574784163158 ) ) ;
#9544=CARTESIAN_POINT ( 'NONE',  ( 2.069840415553682700, 52.20187471152334524, 78.81257284323012868 ) ) ;
#9546=ORIENTED_EDGE ( 'NONE', *, *, #5944, .T. ) ;
#9547=CARTESIAN_POINT ( 'NONE',  ( -5.917125461193805336, 40.64525615903904310, 76.16022115247204738 ) ) ;
#9548=EDGE_CURVE ( 'NONE', #19487, #12818, #2577, .T. ) ;
#9549=CARTESIAN_POINT ( 'NONE',  ( 5.485216391323153751, 37.63974744726360910, 77.55803991379978868 ) ) ;
#9550=CARTESIAN_POINT ( 'NONE',  ( 9.318068138769051600, 42.72056584129816059, 78.97126489842982267 ) ) ;
#9551=B_SPLINE_SURFACE_WITH_KNOTS ( 'NONE', 3, 1, ( 
 ( #14403, #6002 ),
 ( #17591, #1325 ),
 ( #4600, #7810 ),
 ( #19093, #19394 ),
 ( #1221, #6303 ),
 ( #12913, #4810 ),
 ( #6406, #12607 ),
 ( #2817, #3018 ),
 ( #9524, #1533 ),
 ( #9418, #9216 ),
 ( #6100, #1122 ),
 ( #4503, #15906 ),
 ( #7710, #16008 ),
 ( #3127, #12804 ),
 ( #2710, #7915 ) ),
 .UNSPECIFIED., .F., .F., .F.,
 ( 4, 1, 1, 1, 1, 1, 1, 1, 1, 1, 1, 1, 4 ),
 ( 2, 2 ),
 ( 0.000000000000000000, 0.1100843045400305420, 0.2037028897711227471, 0.2865965782701816456, 0.3664837514983516065, 0.4113922274074651164, 0.4651658430714658010, 0.5281943374952151604, 0.6014928947756199573, 0.6850328536222562992, 0.7789954854465236389, 0.8848457782734755472, 1.000000000000000000 ),
 ( 0.000000000000000000, 1.000000000000000000 ),
 .UNSPECIFIED. ) ;
#9553=DIRECTION ( 'NONE',  ( 0.9999689119394085113, -0.007885122365275831768, 1.526048693634352652E-16 ) ) ;
#9554=ORIENTED_EDGE ( 'NONE', *, *, #4824, .F. ) ;
#9557=CARTESIAN_POINT ( 'NONE',  ( -4.664487479516255419, 37.05292970491732518, 75.97486526700035370 ) ) ;
#9558=LINE ( 'NONE', #19011, #20139 ) ;
#9560=CARTESIAN_POINT ( 'NONE',  ( -4.399781695603910414, 37.63216332411592191, 77.30667006270941499 ) ) ;
#9561=CARTESIAN_POINT ( 'NONE',  ( 8.274195582100176694, 41.51206924590946556, 77.52203278780699236 ) ) ;
#9564=CARTESIAN_POINT ( 'NONE',  ( -7.775939518413485629, 41.23271989474202570, 78.69802408570997443 ) ) ;
#9566=CARTESIAN_POINT ( 'NONE',  ( -5.488960544945736153, 38.58484428221787965, 78.87558661569313756 ) ) ;
#9568=CARTESIAN_POINT ( 'NONE',  ( -5.818890812078571173, 50.44687531233557110, 76.28720437108826502 ) ) ;
#9569=CARTESIAN_POINT ( 'NONE',  ( -8.080465354403330025, 46.01554175503538602, 72.45433879953085921 ) ) ;
#9570=PLANE ( 'NONE',  #16632 ) ;
#9571=CARTESIAN_POINT ( 'NONE',  ( -0.8447986058118214237, 52.97914482513772327, 78.90127229107831397 ) ) ;
#9573=CARTESIAN_POINT ( 'NONE',  ( 8.643936145691096584, 43.06456754242027074, 76.74257409364852833 ) ) ;
#9576=VECTOR ( 'NONE', #6638, 1000.000000000000114 ) ;
#9577=VERTEX_POINT ( 'NONE', #4478 ) ;
#9578=ORIENTED_EDGE ( 'NONE', *, *, #741, .F. ) ;
#9579=CARTESIAN_POINT ( 'NONE',  ( 9.332226353535185481, 42.76299890913265500, 76.00948821603452643 ) ) ;
#9581=CARTESIAN_POINT ( 'NONE',  ( -4.886362818588793289, 37.21682008020638222, 78.74088963820604192 ) ) ;
#9584=DIRECTION ( 'NONE',  ( -1.540237394707284220E-16, -1.793354297423764243E-16, 1.000000000000000000 ) ) ;
#9585=CARTESIAN_POINT ( 'NONE',  ( -3.057592722523234219, 36.78482279269636734, 76.43665125469834720 ) ) ;
#9587=B_SPLINE_CURVE_WITH_KNOTS ( 'NONE', 3,
 ( #1737, #18501, #16305, #19582, #17891, #8719, #10332, #15204, #10440, #3913, #3313, #7098, #16804, #14704 ),
 .UNSPECIFIED., .F., .F.,
 ( 4, 2, 2, 2, 2, 2, 4 ),
 ( 0.000000000000000000, 6.877694998478215750E-05, 0.0001375538999695643150, 0.0002063308499543464725, 0.0002751077999391286300, 0.0004126616999087005886, 0.0005502155998782725472 ),
 .UNSPECIFIED. ) ;
#9591=ORIENTED_EDGE ( 'NONE', *, *, #15209, .F. ) ;
#9592=LINE ( 'NONE', #1712, #3084 ) ;
#9595=CARTESIAN_POINT ( 'NONE',  ( 5.518796429342951448, 36.91682708076865538, 78.21801395346943764 ) ) ;
#9598=LINE ( 'NONE', #17557, #8856 ) ;
#9599=VECTOR ( 'NONE', #5854, 1000.000000000000114 ) ;
#9600=CARTESIAN_POINT ( 'NONE',  ( 8.887668352622405621, 41.43063037816333605, 75.36022115247205022 ) ) ;
#9602=CARTESIAN_POINT ( 'NONE',  ( 5.833066520072705430, 37.14139298144173296, 75.36337631951366234 ) ) ;
#9603=CARTESIAN_POINT ( 'NONE',  ( 1.652727357819364418, 35.35299279957455099, 76.16022115247204738 ) ) ;
#9604=CARTESIAN_POINT ( 'NONE',  ( 5.777481493531589685, 38.02144953885154877, 78.35997004935869370 ) ) ;
#9605=CARTESIAN_POINT ( 'NONE',  ( 0.5753960310588919214, 52.96573608190006865, 75.97198585835440099 ) ) ;
#9606=DIRECTION ( 'NONE',  ( 0.5813877811927011807, -0.8136266022444372803, -5.636455622144619183E-17 ) ) ;
#9608=CARTESIAN_POINT ( 'NONE',  ( 0.3869120917952217908, 35.96329670974014192, 72.45433879953085921 ) ) ;
#9610=ORIENTED_EDGE ( 'NONE', *, *, #16773, .T. ) ;
#9613=DIRECTION ( 'NONE',  ( 0.3165065846431829311, 0.9485903129789527988, 2.188653791613874255E-16 ) ) ;
#9615=CARTESIAN_POINT ( 'NONE',  ( -7.923612069094863486, 41.67164428332228709, 78.89026057757155286 ) ) ;
#9618=ORIENTED_EDGE ( 'NONE', *, *, #17946, .F. ) ;
#9622=CARTESIAN_POINT ( 'NONE',  ( 6.450247442662827346, 38.49669771550791353, 72.45433879953087342 ) ) ;
#9624=CARTESIAN_POINT ( 'NONE',  ( 4.732847133705871734, 51.99232638384451377, 75.72008365543779007 ) ) ;
#9626=CARTESIAN_POINT ( 'NONE',  ( -5.403135505393695581, 49.82401183315728588, 78.21416447440572028 ) ) ;
#9629=CARTESIAN_POINT ( 'NONE',  ( 4.695664425361702143, 36.32864708750979332, 75.66510065906194882 ) ) ;
#9633=FACE_OUTER_BOUND ( 'NONE', #16446, .T. ) ;
#9634=ORIENTED_EDGE ( 'NONE', *, *, #14201, .T. ) ;
#9635=DIRECTION ( 'NONE',  ( 0.9485903129789529098, -0.3165065846431826535, 8.934458285744997376E-17 ) ) ;
#9636=B_SPLINE_CURVE_WITH_KNOTS ( 'NONE', 3,
 ( #14212, #1142, #2838, #2734, #2936, #7630, #19307, #4427, #10940, #14111, #1558, #9656, #19206, #16138, #6324, #4622, #15827, #1238 ),
 .UNSPECIFIED., .F., .F.,
 ( 4, 2, 2, 2, 2, 2, 2, 2, 4 ),
 ( 0.000000000000000000, 0.0006084283796061584065, 0.0009126425694092466087, 0.001216856759212335028, 0.001521070949015423121, 0.001825285138818511432, 0.001977392233720055587, 0.002129499328621599959, 0.002433713518424688270 ),
 .UNSPECIFIED. ) ;
#9638=VERTEX_POINT ( 'NONE', #6180 ) ;
#9639=CARTESIAN_POINT ( 'NONE',  ( 4.145197572768899441, 51.51238443731228500, 78.30859729819620441 ) ) ;
#9640=CARTESIAN_POINT ( 'NONE',  ( 5.309255083855641821, 37.50457964663987553, 75.97198585835440099 ) ) ;
#9642=CARTESIAN_POINT ( 'NONE',  ( -5.838428831739582492, 50.43291415881836315, 76.76022115247205591 ) ) ;
#9645=DIRECTION ( 'NONE',  ( -1.540237394707283727E-16, -1.793354297423763257E-16, 1.000000000000000000 ) ) ;
#9646=VECTOR ( 'NONE', #7897, 1000.000000000000114 ) ;
#9647=CARTESIAN_POINT ( 'NONE',  ( 5.913630530257057316, 51.12012925366870064, 76.09715583564816654 ) ) ;
#9649=CARTESIAN_POINT ( 'NONE',  ( -7.150130606013386014, 47.05633550303845425, 78.03747806989589719 ) ) ;
#9650=EDGE_CURVE ( 'NONE', #11138, #8922, #14145, .T. ) ;
#9651=ORIENTED_EDGE ( 'NONE', *, *, #8462, .F. ) ;
#9655=CARTESIAN_POINT ( 'NONE',  ( 8.908783915644443496, 41.49391506008672792, 75.36120592425527320 ) ) ;
#9656=CARTESIAN_POINT ( 'NONE',  ( -2.964841284551051892, 51.58385076907617162, 76.14610479913682184 ) ) ;
#9657=VERTEX_POINT ( 'NONE', #9497 ) ;
#9658=CARTESIAN_POINT ( 'NONE',  ( 5.647726803872021861, 51.31654162509386907, 77.98642840401727483 ) ) ;
#9659=ORIENTED_EDGE ( 'NONE', *, *, #19651, .T. ) ;
#9660=CARTESIAN_POINT ( 'NONE',  ( 0.8455950101471348956, 52.35579997042385259, 77.76169174070734869 ) ) ;
#9661=CARTESIAN_POINT ( 'NONE',  ( -4.522047388140567392, 36.94771494725497973, 76.29203488853940485 ) ) ;
#9664=VERTEX_POINT ( 'NONE', #4576 ) ;
#9665=CARTESIAN_POINT ( 'NONE',  ( -4.717136037229297862, 37.86658019246193163, 77.33565342272370913 ) ) ;
#9666=CARTESIAN_POINT ( 'NONE',  ( 8.211514564676907213, 41.32421026028232092, 77.18134264024645574 ) ) ;
#9670=ORIENTED_EDGE ( 'NONE', *, *, #18444, .T. ) ;
#9671=CARTESIAN_POINT ( 'NONE',  ( -4.649709362898930998, 51.28232956945436882, 75.97399450257033493 ) ) ;
#9675=EDGE_CURVE ( 'NONE', #19686, #12584, #2894, .T. ) ;
#9676=CARTESIAN_POINT ( 'NONE',  ( 5.772314152670717569, 37.86287365998423127, 78.36882016909345339 ) ) ;
#9678=CARTESIAN_POINT ( 'NONE',  ( 0.7150189969462155126, 52.34218787202741652, 76.81551440955847454 ) ) ;
#9679=CARTESIAN_POINT ( 'NONE',  ( 5.230203880350988044, 37.63038499358497546, 75.36022115247205022 ) ) ;
#9680=CARTESIAN_POINT ( 'NONE',  ( -0.4905242218931977205, 52.21391051046797571, 79.30111418114536548 ) ) ;
#9681=VERTEX_POINT ( 'NONE', #17567 ) ;
#9682=DIRECTION ( 'NONE',  ( 0.5941461771851782592, 0.8043570849667694977, 2.357623395011398763E-16 ) ) ;
#9684=CARTESIAN_POINT ( 'NONE',  ( 0.8455950101471351177, 52.35579997042385259, 76.48963291717792856 ) ) ;
#9685=CARTESIAN_POINT ( 'NONE',  ( 6.778550821858020825, 50.48124747537763568, 77.88538524077617353 ) ) ;
#9686=VERTEX_POINT ( 'NONE', #15984 ) ;
#9688=EDGE_LOOP ( 'NONE', ( #15560, #3560, #14575, #2235, #10797, #3257 ) ) ;
#9689=( BOUNDED_CURVE ( )  B_SPLINE_CURVE ( 3, ( #20517, #18824, #945, #9151 ),
 .UNSPECIFIED., .F., .F. ) 
 B_SPLINE_CURVE_WITH_KNOTS ( ( 4, 4 ),
 ( 1.748195931235267064, 1.749653718118951762 ),
 .UNSPECIFIED. ) 
 CURVE ( )  GEOMETRIC_REPRESENTATION_ITEM ( )  RATIONAL_B_SPLINE_CURVE ( ( 1.000000000000000000, 0.9999998229047912801, 0.9999998229047912801, 1.000000000000000000 ) ) 
 REPRESENTATION_ITEM ( '' )  );
#9690=DIRECTION ( 'NONE',  ( 0.3165065846431827645, 0.9485903129789529098, 0.000000000000000000 ) ) ;
#9692=DIRECTION ( 'NONE',  ( -1.540237394707284220E-16, -1.793354297423764243E-16, 1.000000000000000000 ) ) ;
#9693=CARTESIAN_POINT ( 'NONE',  ( 4.903749685900197441, 51.09391985211853893, 79.50087752586969714 ) ) ;
#9694=LINE ( 'NONE', #20928, #2159 ) ;
#9695=CARTESIAN_POINT ( 'NONE',  ( 5.599231707071657738, 51.35236299959863970, 78.30875056423674607 ) ) ;
#9696=FACE_OUTER_BOUND ( 'NONE', #19518, .T. ) ;
#9697=CARTESIAN_POINT ( 'NONE',  ( 9.277577006266444215, 42.59921134847828483, 77.86785210695053649 ) ) ;
#9699=EDGE_LOOP ( 'NONE', ( #12431, #13799, #3631 ) ) ;
#9700=CARTESIAN_POINT ( 'NONE',  ( -5.210464978622037613, 37.45622129019157143, 79.52089765539699329 ) ) ;
#9701=PLANE ( 'NONE',  #2090 ) ;
#9702=CARTESIAN_POINT ( 'NONE',  ( 5.282313327535892000, 50.83908068768521815, 78.88513556223540490 ) ) ;
#9703=CARTESIAN_POINT ( 'NONE',  ( 8.869748494521283888, 41.37692342661967615, 77.52492703482499792 ) ) ;
#9704=CARTESIAN_POINT ( 'NONE',  ( 8.774405178022840701, 41.09117345860662596, 75.37437276336991943 ) ) ;
#9705=ORIENTED_EDGE ( 'NONE', *, *, #10808, .T. ) ;
#9706=CARTESIAN_POINT ( 'NONE',  ( 6.136807603568960268, 37.35843523903731977, 75.40772603260481333 ) ) ;
#9707=CARTESIAN_POINT ( 'NONE',  ( 4.578029447411149810, 52.10668397227361481, 78.50413411530853125 ) ) ;
#9708=CARTESIAN_POINT ( 'NONE',  ( 6.830172062167755520, 37.85388809545894873, 77.80469260682309596 ) ) ;
#9709=CARTESIAN_POINT ( 'NONE',  ( 4.102496745554329749, 51.53925067467379506, 76.40131969043289928 ) ) ;
#9710=CARTESIAN_POINT ( 'NONE',  ( -0.9199438314403606265, 52.23437776363726215, 75.45433879953088763 ) ) ;
#9711=ORIENTED_EDGE ( 'NONE', *, *, #17552, .F. ) ;
#9712=CARTESIAN_POINT ( 'NONE',  ( 8.345083808671303061, 41.72452575800834751, 76.03029119948048731 ) ) ;
#9715=ADVANCED_FACE ( 'NONE', ( #12578 ), #12424, .T. ) ;
#9716=CARTESIAN_POINT ( 'NONE',  ( 0.4436773671319499401, 52.36183473419609413, 75.99664209308157581 ) ) ;
#9717=CARTESIAN_POINT ( 'NONE',  ( -3.096195867026992232, 36.80851087063928873, 78.43912781517941823 ) ) ;
#9718=DIRECTION ( 'NONE',  ( -1.540237394707284220E-16, -1.793354297423764243E-16, 1.000000000000000000 ) ) ;
#9719=B_SPLINE_SURFACE_WITH_KNOTS ( 'NONE', 3, 1, ( 
 ( #1301, #6184 ),
 ( #12688, #15987 ),
 ( #19167, #12383 ),
 ( #17571, #18858 ),
 ( #19576, #1832 ),
 ( #1923, #9712 ),
 ( #4788, #319 ),
 ( #19371, #9813 ),
 ( #14896, #20952 ),
 ( #8318, #3306 ),
 ( #16297, #19683 ),
 ( #16508, #11729 ),
 ( #17783, #11311 ),
 ( #6812, #5108 ),
 ( #11626, #3210 ) ),
 .UNSPECIFIED., .F., .F., .F.,
 ( 4, 1, 1, 1, 1, 1, 1, 1, 1, 1, 1, 1, 4 ),
 ( 2, 2 ),
 ( 0.000000000000000000, 0.07577303389073718198, 0.1558117613168219784, 0.2417361372947465226, 0.3357870204060591224, 0.3882587240527491379, 0.4455552461494497463, 0.5113167710153618817, 0.5866953322903324386, 0.6731791507778834838, 0.7705825181721650541, 0.8794626622360116608, 1.000000000000000000 ),
 ( 0.000000000000000000, 1.000000000000000000 ),
 .UNSPECIFIED. ) ;
#9720=ORIENTED_EDGE ( 'NONE', *, *, #8442, .T. ) ;
#9721=CARTESIAN_POINT ( 'NONE',  ( -4.517374237173715557, 36.94426307888177519, 76.44623874561141008 ) ) ;
#9722=EDGE_CURVE ( 'NONE', #5725, #3856, #19367, .T. ) ;
#9723=VERTEX_POINT ( 'NONE', #14586 ) ;
#9728=CARTESIAN_POINT ( 'NONE',  ( -5.811565481342516826, 50.45210972548208161, 78.65111229433956908 ) ) ;
#9729=CARTESIAN_POINT ( 'NONE',  ( 0.3869120917952217908, 35.96329670974014192, 72.45433879953085921 ) ) ;
#9731=DIRECTION ( 'NONE',  ( -0.3165065846431827645, -0.9485903129789529098, 0.000000000000000000 ) ) ;
#9735=DIRECTION ( 'NONE',  ( -0.9999542261909885044, -0.009567942452870459302, -1.557325602890304767E-16 ) ) ;
#9736=ORIENTED_EDGE ( 'NONE', *, *, #11100, .F. ) ;
#9738=PLANE ( 'NONE',  #18941 ) ;
#9739=SHAPE_REPRESENTATION ( 'Number Dial Wheels', ( #18366 ), #19057 ) ;
#9740=CARTESIAN_POINT ( 'NONE',  ( -5.644616003178662744, 50.57140571016744701, 75.79002994479621691 ) ) ;
#9743=CARTESIAN_POINT ( 'NONE',  ( 0.6404851603139647409, 52.36132752672286017, 79.54845644658969661 ) ) ;
#9745=CARTESIAN_POINT ( 'NONE',  ( 5.579255781724441476, 50.61248246897039138, 76.38301527011910252 ) ) ;
#9746=EDGE_LOOP ( 'NONE', ( #8360, #8440, #17024, #6833 ) ) ;
#9747=CARTESIAN_POINT ( 'NONE',  ( 1.756236358059617642, 52.20434759476808040, 79.26556901187228732 ) ) ;
#9748=VERTEX_POINT ( 'NONE', #16406 ) ;
#9750=EDGE_CURVE ( 'NONE', #4844, #20845, #19786, .T. ) ;
#9751=LINE ( 'NONE', #3562, #6500 ) ;
#9752=CARTESIAN_POINT ( 'NONE',  ( 9.279665234200917823, 42.60546990007262025, 79.15097751326614173 ) ) ;
#9753=VERTEX_POINT ( 'NONE', #17879 ) ;
#9755=CARTESIAN_POINT ( 'NONE',  ( -5.394504046100737860, 38.52817003188538081, 75.85972562479176418 ) ) ;
#9756=ORIENTED_EDGE ( 'NONE', *, *, #17392, .F. ) ;
#9760=ORIENTED_EDGE ( 'NONE', *, *, #15601, .F. ) ;
#9761=CARTESIAN_POINT ( 'NONE',  ( 5.389492195292208798, 36.82443100924615464, 78.79551527011911105 ) ) ;
#9762=CARTESIAN_POINT ( 'NONE',  ( -4.620149427167481448, 37.79494009046823777, 77.90250793075740887 ) ) ;
#9764=AXIS2_PLACEMENT_3D ( 'NONE', #12977, #6474, #11394 ) ;
#9765=ORIENTED_EDGE ( 'NONE', *, *, #5329, .F. ) ;
#9766=CARTESIAN_POINT ( 'NONE',  ( 9.353817388681445522, 42.82770861117572281, 77.06316232894263862 ) ) ;
#9771=B_SPLINE_CURVE_WITH_KNOTS ( 'NONE', 3,
 ( #20519, #7546, #5843, #20193, #12346, #4234, #18508, #3921, #18827, #17225 ),
 .UNSPECIFIED., .F., .F.,
 ( 4, 2, 2, 2, 4 ),
 ( 0.000000000000000000, 0.0003230938241351131719, 0.0004038672801688700112, 0.0004846407362026268506, 0.0006461876482701230193 ),
 .UNSPECIFIED. ) ;
#9772=UNCERTAINTY_MEASURE_WITH_UNIT (LENGTH_MEASURE( 1.000000000000000082E-05 ), #15646, 'distance_accuracy_value', 'NONE');
#9773=EDGE_CURVE ( 'NONE', #8610, #17907, #2599, .T. ) ;
#9774=CARTESIAN_POINT ( 'NONE',  ( 6.244022549736605754, 38.28825185105232265, 78.16399671769941904 ) ) ;
#9776=EDGE_CURVE ( 'NONE', #19886, #11899, #14629, .T. ) ;
#9777=CARTESIAN_POINT ( 'NONE',  ( -5.478128554961354091, 38.57320898139802523, 72.45433879953085921 ) ) ;
#9778=EDGE_CURVE ( 'NONE', #15408, #16784, #19711, .T. ) ;
#9779=CARTESIAN_POINT ( 'NONE',  ( 8.579956030688345336, 40.50839702842124268, 79.37958223971880045 ) ) ;
#9785=EDGE_CURVE ( 'NONE', #15919, #2938, #4633, .T. ) ;
#9786=ORIENTED_EDGE ( 'NONE', *, *, #8070, .T. ) ;
#9787=VECTOR ( 'NONE', #15521, 1000.000000000000000 ) ;
#9788=CARTESIAN_POINT ( 'NONE',  ( 6.634437729966897734, 50.58769801112816111, 77.73730439759678745 ) ) ;
#9789=CARTESIAN_POINT ( 'NONE',  ( 4.614533305268312624, 51.26839818186464726, 79.40329896012910638 ) ) ;
#9791=DIRECTION ( 'NONE',  ( 0.3165065846431826535, 0.9485903129789529098, 2.188653791613874008E-16 ) ) ;
#9793=CARTESIAN_POINT ( 'NONE',  ( 9.353817388681445522, 42.82770861117572281, 77.06316232894263862 ) ) ;
#9795=CARTESIAN_POINT ( 'NONE',  ( 6.519002636616433755, 49.74813231759035403, 76.51259071708746262 ) ) ;
#9797=ORIENTED_EDGE ( 'NONE', *, *, #555, .F. ) ;
#9798=ADVANCED_FACE ( 'NONE', ( #18409 ), #13944, .T. ) ;
#9802=PLANE ( 'NONE',  #6486 ) ;
#9803=DIRECTION ( 'NONE',  ( 0.3014921695764776199, -0.9534129230078944861, 0.01030873055283977775 ) ) ;
#9804=CARTESIAN_POINT ( 'NONE',  ( 9.341681937738675501, 42.79133789484158967, 77.50995918449682165 ) ) ;
#9807=CARTESIAN_POINT ( 'NONE',  ( 0.3848670358072697195, 52.20902977889265628, 75.36353278631986541 ) ) ;
#9809=CARTESIAN_POINT ( 'NONE',  ( 5.953729262864296601, 38.14738974197400978, 78.31663032931759005 ) ) ;
#9810=CARTESIAN_POINT ( 'NONE',  ( 4.391355930538122010, 51.39239564774072022, 75.64582075504121406 ) ) ;
#9812=ORIENTED_EDGE ( 'NONE', *, *, #19274, .T. ) ;
#9813=CARTESIAN_POINT ( 'NONE',  ( 8.359590704656968185, 41.76800384557771650, 76.08336210994360727 ) ) ;
#9819=CARTESIAN_POINT ( 'NONE',  ( 5.385255718775495026, 47.76702405936703855, 75.45433879953087342 ) ) ;
#9820=B_SPLINE_CURVE_WITH_KNOTS ( 'NONE', 3,
 ( #8254, #16032, #14319, #12728, #19621, #19521, #4935, #17823, #20891, #5042, #3252, #1453, #20994, #17611, #11141, #9752, #14633, #16235, #9550, #14740, #18036, #60, #7940, #11561, #17927, #14423, #6323 ),
 .UNSPECIFIED., .F., .F.,
 ( 4, 1, 1, 1, 1, 1, 1, 1, 1, 1, 1, 1, 1, 1, 1, 1, 1, 1, 1, 1, 1, 1, 1, 1, 4 ),
 ( 0.000000000000000000, 0.06037445285962812075, 0.1180910611743953287, 0.1732658017268006723, 0.2259310541736886668, 0.2758310469819637567, 0.3235430165773793276, 0.3690552752481174870, 0.4126046436208182233, 0.4542408720228611196, 0.4938267050212239995, 0.5316899362873784840, 0.5681969051958857264, 0.6035856803598054210, 0.6378784996589128564, 0.6713567270158068423, 0.7043713979572046036, 0.7376082755227613141, 0.7714571943499641815, 0.8061103333465380327, 0.8420729482554840661, 0.8794516251380997129, 0.9177737848194706949, 0.9579350591099196066, 1.000000000000000000 ),
 .UNSPECIFIED. ) ;
#9821=CARTESIAN_POINT ( 'NONE',  ( 8.619779459752459516, 42.86892843748081816, 79.10813152944312776 ) ) ;
#9823=AXIS2_PLACEMENT_3D ( 'NONE', #15691, #14177, #15998 ) ;
#9825=CARTESIAN_POINT ( 'NONE',  ( -7.723289445447552914, 47.23670041943413622, 77.69607208529100717 ) ) ;
#9829=EDGE_CURVE ( 'NONE', #5214, #18140, #11376, .T. ) ;
#9830=CARTESIAN_POINT ( 'NONE',  ( -5.403263942874336756, 49.82392005643602317, 78.10580938776615767 ) ) ;
#9831=DIRECTION ( 'NONE',  ( 0.9467234622824005630, -0.007465262426704777701, -0.3219611091745780973 ) ) ;
#9837=CARTESIAN_POINT ( 'NONE',  ( 0.8448994723799378992, 52.35218080436352039, 78.59044740879555491 ) ) ;
#9838=ORIENTED_EDGE ( 'NONE', *, *, #2197, .F. ) ;
#9840=CARTESIAN_POINT ( 'NONE',  ( -7.674646407923283675, 40.87962920872410422, 76.96732277425439861 ) ) ;
#9842=CARTESIAN_POINT ( 'NONE',  ( 0.5221537403065019678, 44.16218137147968292, 72.45433879953087342 ) ) ;
#9846=CARTESIAN_POINT ( 'NONE',  ( -7.611372734017124664, 43.12018948500615778, 72.45433879953085921 ) ) ;
#9848=CARTESIAN_POINT ( 'NONE',  ( 5.756838674491786101, 51.23594508156129734, 75.97260389846793771 ) ) ;
#9850=CARTESIAN_POINT ( 'NONE',  ( -7.308127660158699967, 41.72770130593617210, 76.16022115247204738 ) ) ;
#9851=CARTESIAN_POINT ( 'NONE',  ( 6.691294758883309157, 37.75465145915448062, 78.79551527011911105 ) ) ;
#9852=AXIS2_PLACEMENT_3D ( 'NONE', #16024, #9645, #16126 ) ;
#9853=B_SPLINE_CURVE_WITH_KNOTS ( 'NONE', 3,
 ( #8169, #83, #14656, #6564, #8280, #19644, #6666, #3483, #14863, #13171, #5496, #598, #2104, #7079, #10311, #8605 ),
 .UNSPECIFIED., .F., .F.,
 ( 4, 2, 2, 2, 2, 2, 2, 4 ),
 ( 0.000000000000000000, 0.0006122100410275824493, 0.0009183150615413739450, 0.001224420082055165115, 0.001377472592312054900, 0.001530525102568944468, 0.001836630123082723604, 0.002448840164110273852 ),
 .UNSPECIFIED. ) ;
#9854=VERTEX_POINT ( 'NONE', #19240 ) ;
#9855=LINE ( 'NONE', #16341, #8506 ) ;
#9856=EDGE_CURVE ( 'NONE', #13175, #18406, #10767, .T. ) ;
#9857=CARTESIAN_POINT ( 'NONE',  ( 5.241460166982748525, 50.86801069014953924, 78.30875056423674607 ) ) ;
#9858=CARTESIAN_POINT ( 'NONE',  ( 8.177787109632054907, 41.66748930940789108, 75.36022115247205022 ) ) ;
#9859=VECTOR ( 'NONE', #6867, 1000.000000000000114 ) ;
#9863=CARTESIAN_POINT ( 'NONE',  ( -5.943920255163966715, 37.99799515759236357, 76.35020017089209432 ) ) ;
#9864=EDGE_LOOP ( 'NONE', ( #3095, #4914, #12374, #15346 ) ) ;
#9865=LINE ( 'NONE', #11771, #20314 ) ;
#9869=CARTESIAN_POINT ( 'NONE',  ( -5.160557796315995205, 37.41935686500602287, 77.33669174070733732 ) ) ;
#9873=ORIENTED_EDGE ( 'NONE', *, *, #13956, .F. ) ;
#9874=CARTESIAN_POINT ( 'NONE',  ( -0.8071739151948670310, 40.17810205696807913, 82.45433879953087342 ) ) ;
#9875=CARTESIAN_POINT ( 'NONE',  ( 1.652727357819364418, 35.35299279957455099, 76.86610350541323555 ) ) ;
#9876=CARTESIAN_POINT ( 'NONE',  ( 1.490046680165512782, 52.91022367065997400, 75.48600500139500014 ) ) ;
#9880=VECTOR ( 'NONE', #16721, 1000.000000000000114 ) ;
#9881=CARTESIAN_POINT ( 'NONE',  ( 8.648170029844118645, 43.06315486489794608, 78.41904468188381827 ) ) ;
#9883=CARTESIAN_POINT ( 'NONE',  ( 0.8277711449680080769, 52.34129877990315549, 76.79008513575435302 ) ) ;
#9884=CARTESIAN_POINT ( 'NONE',  ( 4.943220423779688844, 37.42531712265408572, 75.37835156746757548 ) ) ;
#9887=ORIENTED_EDGE ( 'NONE', *, *, #9488, .F. ) ;
#9888=CARTESIAN_POINT ( 'NONE',  ( -4.159067576658533660, 37.42968809036762678, 76.29677174223795078 ) ) ;
#9891=CARTESIAN_POINT ( 'NONE',  ( 6.466516115726876457, 49.79771993804390462, 78.20944795639196911 ) ) ;
#9893=EDGE_CURVE ( 'NONE', #10515, #13636, #4970, .T. ) ;
#9894=ORIENTED_EDGE ( 'NONE', *, *, #7, .T. ) ;
#9895=CARTESIAN_POINT ( 'NONE',  ( 5.406592671645608306, 50.74154221849293833, 78.93606911575150775 ) ) ;
#9897=ORIENTED_EDGE ( 'NONE', *, *, #7938, .F. ) ;
#9898=ADVANCED_FACE ( 'NONE', ( #2658 ), #7554, .T. ) ;
#9899=CARTESIAN_POINT ( 'NONE',  ( -8.080465354403331801, 46.01554175503538602, 75.45433879953087342 ) ) ;
#9900=CARTESIAN_POINT ( 'NONE',  ( 5.008975552073978932, 51.78836144432716537, 77.68963291717794561 ) ) ;
#9902=CARTESIAN_POINT ( 'NONE',  ( 2.029186242314200861, 35.35002428291939225, 76.16022115247204738 ) ) ;
#9903=CARTESIAN_POINT ( 'NONE',  ( -5.160557796315992540, 37.41935686500602287, 77.33669174070733732 ) ) ;
#9906=CARTESIAN_POINT ( 'NONE',  ( 9.341681937738675501, 42.79133789484158967, 77.50995918449682165 ) ) ;
#9907=CARTESIAN_POINT ( 'NONE',  ( -3.059371429944726550, 36.79212808410388647, 76.40804902690982203 ) ) ;
#9908=CARTESIAN_POINT ( 'NONE',  ( -4.406172944158208260, 37.61675910519541333, 75.97348137399042400 ) ) ;
#9910=ORIENTED_EDGE ( 'NONE', *, *, #4239, .F. ) ;
#9911=CARTESIAN_POINT ( 'NONE',  ( 8.792941515635110505, 41.14672803835393466, 78.80099766627323277 ) ) ;
#9912=CARTESIAN_POINT ( 'NONE',  ( -7.154059339130676598, 47.04588606493869918, 77.58227997600145898 ) ) ;
#9913=CARTESIAN_POINT ( 'NONE',  ( -4.879976564110340753, 37.21210281127717678, 78.77850703318271997 ) ) ;
#9914=LINE ( 'NONE', #3295, #2736 ) ;
#9916=CARTESIAN_POINT ( 'NONE',  ( 8.677276008184190204, 40.80007117484056067, 75.42295143068700725 ) ) ;
#9917=ORIENTED_EDGE ( 'NONE', *, *, #5062, .T. ) ;
#9918=CARTESIAN_POINT ( 'NONE',  ( 6.339841751912436152, 38.42329159016732376, 75.87985893138584004 ) ) ;
#9919=VECTOR ( 'NONE', #5757, 1000.000000000000000 ) ;
#9920=CARTESIAN_POINT ( 'NONE',  ( 0.07956630390167138134, 52.97185586811492897, 79.50648293536016809 ) ) ;
#9921=CARTESIAN_POINT ( 'NONE',  ( 6.663926478743484871, 37.73509508818325031, 78.14418354478426920 ) ) ;
#9922=CARTESIAN_POINT ( 'NONE',  ( -3.674734132037354772, 36.32183877683145568, 75.77010869825431882 ) ) ;
#9923=EDGE_CURVE ( 'NONE', #5122, #3672, #8579, .T. ) ;
#9925=ORIENTED_EDGE ( 'NONE', *, *, #13030, .T. ) ;
#9927=CARTESIAN_POINT ( 'NONE',  ( -4.491212578019011303, 51.39558556899189057, 78.91875292420674270 ) ) ;
#9928=EDGE_CURVE ( 'NONE', #5725, #10089, #1488, .T. ) ;
#9931=CARTESIAN_POINT ( 'NONE',  ( 1.633003964141607867, 52.20540239326999910, 76.88486154722851040 ) ) ;
#9933=AXIS2_PLACEMENT_3D ( 'NONE', #953, #4136, #10449 ) ;
#9936=VECTOR ( 'NONE', #8031, 1000.000000000000000 ) ;
#9939=LINE ( 'NONE', #16423, #2380 ) ;
#9941=CARTESIAN_POINT ( 'NONE',  ( 4.470572738639666532, 36.16780480931087283, 79.45433879953087342 ) ) ;
#9942=ORIENTED_EDGE ( 'NONE', *, *, #4257, .F. ) ;
#9944=CARTESIAN_POINT ( 'NONE',  ( 8.559588968570775336, 45.78687671259945802, 75.44992703482499508 ) ) ;
#9945=CARTESIAN_POINT ( 'NONE',  ( -5.838428831739583380, 50.43291415881836315, 78.10580938776615767 ) ) ;
#9946=DIRECTION ( 'NONE',  ( -0.3165065846431827090, -0.9485903129789527988, 0.000000000000000000 ) ) ;
#9947=ADVANCED_FACE ( 'NONE', ( #11388 ), #3283, .T. ) ;
#9948=CARTESIAN_POINT ( 'NONE',  ( 8.889576793745449734, 46.88836537034026719, 78.73595644658969661 ) ) ;
#9950=CARTESIAN_POINT ( 'NONE',  ( -4.039182523966593052, 50.97167426352094566, 76.19049300047602458 ) ) ;
#9954=CARTESIAN_POINT ( 'NONE',  ( 4.890314246961300348, 51.87601177044496836, 77.76130678786321937 ) ) ;
#9960=CARTESIAN_POINT ( 'NONE',  ( 5.490969714706527505, 37.64385856151075416, 76.26708001093082601 ) ) ;
#9965=ORIENTED_EDGE ( 'NONE', *, *, #15096, .F. ) ;
#9969=CARTESIAN_POINT ( 'NONE',  ( -0.02883801100815608018, 35.36625256049322275, 79.45433879953087342 ) ) ;
#9973=CARTESIAN_POINT ( 'NONE',  ( -5.772695632942807187, 37.87151842650609268, 75.75097338717934292 ) ) ;
#9975=CARTESIAN_POINT ( 'NONE',  ( 5.599886173630381769, 51.35187957151522653, 78.68193220087633222 ) ) ;
#9976=CARTESIAN_POINT ( 'NONE',  ( 0.3332310122597790802, 52.96015324592079310, 76.34474143055572881 ) ) ;
#9979=CARTESIAN_POINT ( 'NONE',  ( -4.578768572918487045, 36.98961260158169040, 78.00876120161012750 ) ) ;
#9982=CARTESIAN_POINT ( 'NONE',  ( 8.449576249518734983, 46.30180237598475657, 78.74038740353792321 ) ) ;
#9986=VECTOR ( 'NONE', #11903, 1000.000000000000114 ) ;
#9989=DIRECTION ( 'NONE',  ( -1.540237394707284220E-16, -1.793354297423764243E-16, 1.000000000000000000 ) ) ;
#9990=CARTESIAN_POINT ( 'NONE',  ( 4.055885703770254480, 36.79126021913294409, 75.97723610431854979 ) ) ;
#9991=FACE_OUTER_BOUND ( 'NONE', #12290, .T. ) ;
#9994=CARTESIAN_POINT ( 'NONE',  ( 8.643719690846561221, 43.06391881351956386, 76.64232882509132594 ) ) ;
#9996=CARTESIAN_POINT ( 'NONE',  ( 6.634437729966897734, 50.58769801112816111, 77.73730439759678745 ) ) ;
#9998=ORIENTED_EDGE ( 'NONE', *, *, #3974, .T. ) ;
#10000=EDGE_CURVE ( 'NONE', #20886, #12245, #10361, .T. ) ;
#10001=DIRECTION ( 'NONE',  ( -0.8043570849667761591, 0.5941461771851690443, -1.733862608106491891E-17 ) ) ;
#10002=ORIENTED_EDGE ( 'NONE', *, *, #19772, .T. ) ;
#10004=LINE ( 'NONE', #12970, #20626 ) ;
#10005=CARTESIAN_POINT ( 'NONE',  ( -0.2286725555534918908, 52.93086078304144593, 75.48599683584926368 ) ) ;
#10009=CARTESIAN_POINT ( 'NONE',  ( 4.591779561242093521, 52.09652731707507201, 76.01224951307210631 ) ) ;
#10010=CARTESIAN_POINT ( 'NONE',  ( 6.882736312352589536, 37.89144858414100270, 76.69330938776616335 ) ) ;
#10013=ORIENTED_EDGE ( 'NONE', *, *, #2246, .F. ) ;
#10014=CARTESIAN_POINT ( 'NONE',  ( 0.3346339570403927821, 52.96754328674535373, 76.26461983994238381 ) ) ;
#10015=DIRECTION ( 'NONE',  ( 1.540237394707284220E-16, 1.793354297423764243E-16, -1.000000000000000000 ) ) ;
#10018=CARTESIAN_POINT ( 'NONE',  ( 9.292527943876132568, 42.64402025696431764, 77.82525376769920911 ) ) ;
#10020=VERTEX_POINT ( 'NONE', #4757 ) ;
#10022=CARTESIAN_POINT ( 'NONE',  ( 7.680032241523795378, 40.16158449578585277, 77.69330938776616335 ) ) ;
#10023=CARTESIAN_POINT ( 'NONE',  ( -3.763323997310421554, 36.38727654169122161, 75.66260743385902288 ) ) ;
#10025=VERTEX_POINT ( 'NONE', #19760 ) ;
#10026=DIRECTION ( 'NONE',  ( -0.5941461771851693774, -0.8043570849667760481, -2.357623395011396791E-16 ) ) ;
#10027=CARTESIAN_POINT ( 'NONE',  ( 9.273778039597953438, 45.67340037358405169, 78.74919174070734584 ) ) ;
#10028=VERTEX_POINT ( 'NONE', #9899 ) ;
#10031=CARTESIAN_POINT ( 'NONE',  ( 1.822474108708594720, 52.20390835154866238, 76.99833242929096855 ) ) ;
#10034=CARTESIAN_POINT ( 'NONE',  ( 6.882736312352589536, 37.89144858414100270, 77.26022115247205591 ) ) ;
#10035=VERTEX_POINT ( 'NONE', #6675 ) ;
#10036=EDGE_CURVE ( 'NONE', #11820, #5798, #16415, .T. ) ;
#10038=ADVANCED_FACE ( 'NONE', ( #20071 ), #11907, .T. ) ;
#10039=ORIENTED_EDGE ( 'NONE', *, *, #6763, .T. ) ;
#10045=CARTESIAN_POINT ( 'NONE',  ( 8.095626740731175275, 41.43801618066453329, 75.36738766396204880 ) ) ;
#10047=CARTESIAN_POINT ( 'NONE',  ( -4.383821200644077543, 51.47232351541473605, 78.52322435057745054 ) ) ;
#10050=B_SPLINE_CURVE_WITH_KNOTS ( 'NONE', 3,
 ( #8227, #14714, #19593, #11533, #5015, #660, #18319, #13435, #20003, #16629, #2050, #15244 ),
 .UNSPECIFIED., .F., .F.,
 ( 4, 2, 2, 2, 2, 4 ),
 ( 0.000000000000000000, 0.0001072365356795881180, 0.0002144730713591762360, 0.0004289461427183928585, 0.0006434192140776094811, 0.0008578922854368260494 ),
 .UNSPECIFIED. ) ;
#10054=CARTESIAN_POINT ( 'NONE',  ( -6.714292542261278030, 40.32675560908123913, 78.24455606223649795 ) ) ;
#10057=DIRECTION ( 'NONE',  ( -1.540237394707283727E-16, -1.793354297423763257E-16, 1.000000000000000000 ) ) ;
#10059=CARTESIAN_POINT ( 'NONE',  ( 5.840776426723270021, 37.14690219845653019, 76.14207271482608519 ) ) ;
#10060=CARTESIAN_POINT ( 'NONE',  ( -7.496206882273947159, 47.93002185485102018, 78.32480289656686523 ) ) ;
#10061=VERTEX_POINT ( 'NONE', #11798 ) ;
#10063=CARTESIAN_POINT ( 'NONE',  ( 0.5221537403065019678, 44.16218137147968292, 72.45433879953087342 ) ) ;
#10064=CARTESIAN_POINT ( 'NONE',  ( 5.031028746841824884, 37.32608482280444662, 78.09625056423674039 ) ) ;
#10069=B_SPLINE_SURFACE_WITH_KNOTS ( 'NONE', 3, 1, ( 
 ( #2449, #7332 ),
 ( #5731, #7549 ),
 ( #13933, #12446 ),
 ( #15535, #15647 ),
 ( #14238, #1266 ),
 ( #9368, #2868 ),
 ( #15851, #952 ),
 ( #6049, #15431 ),
 ( #7656, #4342 ),
 ( #20302, #20719 ),
 ( #2552, #5846 ),
 ( #9047, #10867 ),
 ( #20618, #7441 ),
 ( #20416, #18830 ),
 ( #1064, #20521 ),
 ( #12549, #17444 ),
 ( #6432, #4237 ),
 ( #10764, #5948 ),
 ( #12941, #2766 ) ),
 .UNSPECIFIED., .F., .F., .F.,
 ( 4, 1, 1, 1, 1, 1, 1, 1, 1, 1, 1, 1, 1, 1, 1, 1, 4 ),
 ( 2, 2 ),
 ( 0.000000000000000000, 0.07118833779177360932, 0.1347494984424237596, 0.1905117199385542026, 0.2387103502848646475, 0.2842577524993954441, 0.3323041331166366463, 0.3837985941886438157, 0.4397333780097005262, 0.4984292962743230304, 0.5584994700834656767, 0.6208277070730616742, 0.6868513727233629407, 0.7572275588454563389, 0.8323608126527687334, 0.9133389214536370426, 1.000000000000000000 ),
 ( 0.000000000000000000, 1.000000000000000000 ),
 .UNSPECIFIED. ) ;
#10071=CARTESIAN_POINT ( 'NONE',  ( 8.787829143201870252, 41.13140593384865440, 77.80727997600146750 ) ) ;
#10072=CARTESIAN_POINT ( 'NONE',  ( -5.955289093497887265, 38.00639286050488153, 76.68644156968609593 ) ) ;
#10073=VERTEX_POINT ( 'NONE', #18493 ) ;
#10075=CARTESIAN_POINT ( 'NONE',  ( 0.4484089342563315483, 52.96189929305592869, 75.99664213318317252 ) ) ;
#10076=ORIENTED_EDGE ( 'NONE', *, *, #5316, .F. ) ;
#10077=CARTESIAN_POINT ( 'NONE',  ( -4.347163611243005654, 37.59329646478425246, 77.92182307551118470 ) ) ;
#10078=EDGE_LOOP ( 'NONE', ( #11145, #7039, #13549, #2078 ) ) ;
#10079=CARTESIAN_POINT ( 'NONE',  ( -4.699529792962120034, 51.24672971417357559, 75.98997946140892168 ) ) ;
#10080=FACE_OUTER_BOUND ( 'NONE', #15979, .T. ) ;
#10083=CARTESIAN_POINT ( 'NONE',  ( 6.253655717016493476, 49.94413339827291765, 75.66183449524544358 ) ) ;
#10084=CARTESIAN_POINT ( 'NONE',  ( -5.955451856753747997, 38.00651308716548726, 78.53742703482498655 ) ) ;
#10085=DIRECTION ( 'NONE',  ( -1.540237394707284220E-16, -1.793354297423764243E-16, 1.000000000000000000 ) ) ;
#10087=CARTESIAN_POINT ( 'NONE',  ( 3.975681152273106367, 36.73394898310913703, 76.35980278528342069 ) ) ;
#10088=CARTESIAN_POINT ( 'NONE',  ( 8.394097411062748648, 39.95136695475236621, 78.67376765716130649 ) ) ;
#10089=VERTEX_POINT ( 'NONE', #18176 ) ;
#10091=CARTESIAN_POINT ( 'NONE',  ( 9.009194133669925719, 41.79485085341455886, 75.38196330830126612 ) ) ;
#10092=CARTESIAN_POINT ( 'NONE',  ( 0.3869120917952211802, 35.96329670974014192, 76.86610350541323555 ) ) ;
#10094=ORIENTED_EDGE ( 'NONE', *, *, #2222, .T. ) ;
#10096=AXIS2_PLACEMENT_3D ( 'NONE', #21009, #11370, #13061 ) ;
#10099=CARTESIAN_POINT ( 'NONE',  ( -3.711266317373841161, 36.34882363053332455, 77.55767546204062057 ) ) ;
#10102=CARTESIAN_POINT ( 'NONE',  ( 4.668718747243733702, 52.03969543967511413, 77.44183710417100031 ) ) ;
#10103=CARTESIAN_POINT ( 'NONE',  ( 2.484494565094233831, 50.04344131194918788, 72.45433879953087342 ) ) ;
#10105=CARTESIAN_POINT ( 'NONE',  ( 8.211361072458180033, 41.32375023436543415, 76.40801527011910821 ) ) ;
#10106=CARTESIAN_POINT ( 'NONE',  ( 8.661599634585137153, 45.15687757339797059, 72.45433879953087342 ) ) ;
#10107=DIRECTION ( 'NONE',  ( -0.5941461771851693774, -0.8043570849667760481, -2.357623395011396791E-16 ) ) ;
#10111=EDGE_LOOP ( 'NONE', ( #10632, #14849, #12930, #17795 ) ) ;
#10112=FACE_OUTER_BOUND ( 'NONE', #20155, .T. ) ;
#10116=CARTESIAN_POINT ( 'NONE',  ( 5.396517835962451493, 50.75616155517602834, 78.93669174070734584 ) ) ;
#10118=VECTOR ( 'NONE', #3522, 1000.000000000000000 ) ;
#10119=DIRECTION ( 'NONE',  ( 0.02533578529877050789, 0.9996789974703352843, 1.831801750099146688E-16 ) ) ;
#10121=CARTESIAN_POINT ( 'NONE',  ( -1.883296302981685599, 36.95289499283964574, 72.45433879953085921 ) ) ;
#10126=CARTESIAN_POINT ( 'NONE',  ( 7.721391190447019603, 40.23635033321865961, 78.89153941383322888 ) ) ;
#10127=CARTESIAN_POINT ( 'NONE',  ( 4.535172733565821623, 51.31357302830301848, 75.54762311074527759 ) ) ;
#10128=LINE ( 'NONE', #3830, #16055 ) ;
#10132=ORIENTED_EDGE ( 'NONE', *, *, #5168, .T. ) ;
#10134=VECTOR ( 'NONE', #5983, 1000.000000000000000 ) ;
#10135=CARTESIAN_POINT ( 'NONE',  ( 2.027628481303231922, 52.94095516031140392, 77.22796645847455466 ) ) ;
#10140=CARTESIAN_POINT ( 'NONE',  ( -4.409036544953043979, 47.67330854490502645, 72.45433879953087342 ) ) ;
#10141=ORIENTED_EDGE ( 'NONE', *, *, #13298, .T. ) ;
#10142=DIRECTION ( 'NONE',  ( -0.5813877811927011807, 0.8136266022444372803, 5.636455622144619183E-17 ) ) ;
#10150=FACE_OUTER_BOUND ( 'NONE', #10111, .T. ) ;
#10153=CARTESIAN_POINT ( 'NONE',  ( 0.5221537403065010796, 44.16218137147968292, 78.25433879953088478 ) ) ;
#10154=CARTESIAN_POINT ( 'NONE',  ( 0.3419587093557019397, 52.35614670350682331, 78.72223189599347393 ) ) ;
#10156=CARTESIAN_POINT ( 'NONE',  ( -4.035110498892168884, 50.97458398355276898, 76.24813767079230331 ) ) ;
#10158=CARTESIAN_POINT ( 'NONE',  ( -3.499239294549248758, 37.01553787106989546, 77.72465150895241948 ) ) ;
#10159=CARTESIAN_POINT ( 'NONE',  ( -6.721687221504229370, 40.35013990712663201, 78.15415281222085753 ) ) ;
#10164=CARTESIAN_POINT ( 'NONE',  ( 8.559588968570775336, 45.78687671259945802, 75.44992703482499508 ) ) ;
#10165=AXIS2_PLACEMENT_3D ( 'NONE', #800, #18666, #900 ) ;
#10167=DIRECTION ( 'NONE',  ( 1.540237394707284220E-16, 1.793354297423764243E-16, -1.000000000000000000 ) ) ;
#10168=DIRECTION ( 'NONE',  ( -0.5813877811927011807, 0.8136266022444372803, 5.636455622144619183E-17 ) ) ;
#10169=ORIENTED_EDGE ( 'NONE', *, *, #16165, .T. ) ;
#10170=B_SPLINE_CURVE_WITH_KNOTS ( 'NONE', 3,
 ( #10763, #17227, #11254, #14322, #9658, #1457, #4624, #11357, #14531, #17825, #1560 ),
 .UNSPECIFIED., .F., .F.,
 ( 4, 1, 1, 1, 1, 1, 1, 1, 4 ),
 ( 0.000000000000000000, 0.1077815449370134182, 0.2006545494464173907, 0.2847368448845932765, 0.3681045469499393263, 0.4695596479522798350, 0.6076740370479670750, 0.7836404280850621795, 1.000000000000000000 ),
 .UNSPECIFIED. ) ;
#10171=CARTESIAN_POINT ( 'NONE',  ( -4.244029479098209379, 50.83477438462418974, 75.97198585835440099 ) ) ;
#10174=EDGE_LOOP ( 'NONE', ( #16883, #15790, #20152, #16266 ) ) ;
#10176=CARTESIAN_POINT ( 'NONE',  ( -5.325372805274120047, 38.47710556906300639, 75.75097338717934292 ) ) ;
#10178=CARTESIAN_POINT ( 'NONE',  ( 0.5221537403065005245, 44.16218137147968292, 82.45433879953087342 ) ) ;
#10180=ADVANCED_FACE ( 'NONE', ( #10323 ), #2212, .T. ) ;
#10181=ORIENTED_EDGE ( 'NONE', *, *, #14151, .T. ) ;
#10185=ORIENTED_EDGE ( 'NONE', *, *, #19385, .F. ) ;
#10186=CARTESIAN_POINT ( 'NONE',  ( -4.612897897929109980, 51.30863369456805145, 75.97269380145769446 ) ) ;
#10187=CARTESIAN_POINT ( 'NONE',  ( 2.118846216502994650, 52.81611540061026489, 76.39834847206340385 ) ) ;
#10191=CARTESIAN_POINT ( 'NONE',  ( 5.881110887899452244, 50.21931725652056855, 75.43719735689487038 ) ) ;
#10192=CARTESIAN_POINT ( 'NONE',  ( 5.570062599089864896, 50.62428647915746183, 77.12188467626378952 ) ) ;
#10193=VECTOR ( 'NONE', #10680, 1000.000000000000000 ) ;
#10196=EDGE_CURVE ( 'NONE', #6954, #10817, #1929, .T. ) ;
#10197=CARTESIAN_POINT ( 'NONE',  ( 4.394792124162911762, 36.11365475671116343, 76.60595702694484999 ) ) ;
#10199=B_SPLINE_CURVE_WITH_KNOTS ( 'NONE', 3,
 ( #15253, #8876, #668, #10592, #4064, #11961, #18438, #20335, #5562, #10700 ),
 .UNSPECIFIED., .F., .F.,
 ( 4, 2, 2, 2, 4 ),
 ( 0.000000000000000000, 0.0001322853537232420470, 0.0002645707074464840941, 0.0003968560611697261411, 0.0005291414148929681881 ),
 .UNSPECIFIED. ) ;
#10200=CARTESIAN_POINT ( 'NONE',  ( 8.385679600361122255, 39.92613824206362949, 77.69330938776616335 ) ) ;
#10203=FACE_OUTER_BOUND ( 'NONE', #11516, .T. ) ;
#10204=CARTESIAN_POINT ( 'NONE',  ( -7.202537930885374529, 41.41097462079392955, 78.61536821129558916 ) ) ;
#10206=VERTEX_POINT ( 'NONE', #1361 ) ;
#10207=AXIS2_PLACEMENT_3D ( 'NONE', #18959, #20647, #5978 ) ;
#10209=CARTESIAN_POINT ( 'NONE',  ( 6.470644262523409296, 49.79467064229719853, 78.73390793106847241 ) ) ;
#10212=CARTESIAN_POINT ( 'NONE',  ( 8.887668352622405621, 41.43063037816333605, 75.36022115247205022 ) ) ;
#10213=CARTESIAN_POINT ( 'NONE',  ( -2.985824661004252700, 51.57396771150768444, 78.81127817498905586 ) ) ;
#10214=CARTESIAN_POINT ( 'NONE',  ( 8.362036131964948993, 41.75873031979976702, 77.44666563814885762 ) ) ;
#10217=FACE_OUTER_BOUND ( 'NONE', #5243, .T. ) ;
#10219=CARTESIAN_POINT ( 'NONE',  ( 8.119551934336415755, 43.80226376792169418, 75.45433879953087342 ) ) ;
#10222=VECTOR ( 'NONE', #9386, 1000.000000000000000 ) ;
#10224=ORIENTED_EDGE ( 'NONE', *, *, #6633, .T. ) ;
#10225=CARTESIAN_POINT ( 'NONE',  ( 0.5705749803268341802, 52.35434406645455141, 75.97198585835440099 ) ) ;
#10226=VERTEX_POINT ( 'NONE', #931 ) ;
#10227=CARTESIAN_POINT ( 'NONE',  ( 5.363562441227258226, 50.78054159302179471, 77.28832336276830972 ) ) ;
#10228=DIRECTION ( 'NONE',  ( 1.540237394707284220E-16, 1.793354297423764243E-16, -1.000000000000000000 ) ) ;
#10229=CARTESIAN_POINT ( 'NONE',  ( -4.392776879941215462, 37.60686397218470489, 78.93508260432024315 ) ) ;
#10232=CARTESIAN_POINT ( 'NONE',  ( -4.766817752550178255, 37.12851695549264974, 75.97348137399042400 ) ) ;
#10234=CARTESIAN_POINT ( 'NONE',  ( 5.540944419992344550, 50.64230199400775945, 78.19629421043239859 ) ) ;
#10238=CARTESIAN_POINT ( 'NONE',  ( 9.092498755203211047, 42.04452008889646208, 79.47377622490290605 ) ) ;
#10244=CARTESIAN_POINT ( 'NONE',  ( 1.652727357819364640, 35.35299279957455809, 75.45433879953087342 ) ) ;
#10246=CARTESIAN_POINT ( 'NONE',  ( -7.203585122226456861, 41.42633110391964379, 78.75487387812985673 ) ) ;
#10247=EDGE_CURVE ( 'NONE', #17173, #15408, #11597, .T. ) ;
#10249=B_SPLINE_SURFACE_WITH_KNOTS ( 'NONE', 3, 1, ( 
 ( #18056, #6346 ),
 ( #79, #11162 ),
 ( #13167, #19326 ),
 ( #11271, #1682 ),
 ( #3175, #17630 ),
 ( #8164, #14858 ),
 ( #9678, #6663 ),
 ( #9883, #180 ),
 ( #6247, #11475 ),
 ( #6560, #3067 ),
 ( #1794, #21016 ) ),
 .UNSPECIFIED., .F., .F., .F.,
 ( 4, 1, 1, 1, 1, 1, 1, 1, 4 ),
 ( 2, 2 ),
 ( 0.000000000000000000, 0.1088348533325064621, 0.2165694074861221896, 0.3273827587112763671, 0.4434819477562966239, 0.5673092549448471855, 0.7000542417988985244, 0.8441436218123770097, 1.000000000000000000 ),
 ( 0.000000000000000000, 1.000000000000000000 ),
 .UNSPECIFIED. ) ;
#10252=EDGE_LOOP ( 'NONE', ( #17838, #7965, #569, #8046, #14431, #6377, #2264, #8367, #14635, #7841, #13743, #9150, #13556, #2473, #11869, #14748, #7151, #691, #10492, #16789, #2567, #9390, #11555, #8981 ) ) ;
#10259=ORIENTED_EDGE ( 'NONE', *, *, #12611, .F. ) ;
#10260=LINE ( 'NONE', #16735, #11004 ) ;
#10263=CARTESIAN_POINT ( 'NONE',  ( -3.778837258911088792, 51.90462289030131160, 79.34012906335151172 ) ) ;
#10265=CARTESIAN_POINT ( 'NONE',  ( 0.3504751631991869787, 52.35607954813841758, 78.76353264627590534 ) ) ;
#10266=ORIENTED_EDGE ( 'NONE', *, *, #2365, .T. ) ;
#10269=CARTESIAN_POINT ( 'NONE',  ( -3.243516849062964891, 36.87779780655007045, 77.90799200028293114 ) ) ;
#10270=CARTESIAN_POINT ( 'NONE',  ( -7.736834117765939212, 41.07628627713002345, 76.72474157890661672 ) ) ;
#10271=EDGE_CURVE ( 'NONE', #12203, #10073, #13635, .T. ) ;
#10272=CARTESIAN_POINT ( 'NONE',  ( -4.163054115940463262, 37.43240098938879612, 77.00485536016182664 ) ) ;
#10273=CARTESIAN_POINT ( 'NONE',  ( 6.921466148593897749, 50.37568168049836714, 78.61296362383696135 ) ) ;
#10274=VECTOR ( 'NONE', #13133, 1000.000000000000000 ) ;
#10277=ORIENTED_EDGE ( 'NONE', *, *, #19848, .T. ) ;
#10279=B_SPLINE_CURVE_WITH_KNOTS ( 'NONE', 3,
 ( #12736, #9346, #7845, #2738, #6134, #14328, #20806, #18805, #15729, #19119, #1147, #2941, #7525, #13904, #926, #10743 ),
 .UNSPECIFIED., .F., .F.,
 ( 4, 2, 2, 2, 2, 2, 2, 4 ),
 ( 0.000000000000000000, 0.0002950570430945601377, 0.0005901140861891202754, 0.0008851711292836804672, 0.001180228172378240551, 0.001770342258567334046, 0.002065399301661875915, 0.002360456344756417784 ),
 .UNSPECIFIED. ) ;
#10280=ORIENTED_EDGE ( 'NONE', *, *, #3782, .F. ) ;
#10284=CARTESIAN_POINT ( 'NONE',  ( -7.474360244459849589, 42.69441725426494827, 76.61471288230795551 ) ) ;
#10288=VERTEX_POINT ( 'NONE', #6658 ) ;
#10289=VECTOR ( 'NONE', #10085, 1000.000000000000000 ) ;
#10291=LINE ( 'NONE', #14640, #16637 ) ;
#10292=VECTOR ( 'NONE', #13511, 1000.000000000000000 ) ;
#10294=CARTESIAN_POINT ( 'NONE',  ( -4.147124323215474639, 37.44553550079235293, 78.31852111096432623 ) ) ;
#10296=EDGE_LOOP ( 'NONE', ( #10951, #13827, #19745, #10002 ) ) ;
#10301=CARTESIAN_POINT ( 'NONE',  ( 5.859131993956401274, 51.16038512709904040, 75.36137945677606353 ) ) ;
#10303=ADVANCED_FACE ( 'NONE', ( #6240 ), #4849, .F. ) ;
#10304=AXIS2_PLACEMENT_3D ( 'NONE', #8635, #3924, #2337 ) ;
#10307=VERTEX_POINT ( 'NONE', #14436 ) ;
#10309=DIRECTION ( 'NONE',  ( -0.3165065846431826535, -0.9485903129789527988, 0.000000000000000000 ) ) ;
#10310=ORIENTED_EDGE ( 'NONE', *, *, #11997, .T. ) ;
#10311=CARTESIAN_POINT ( 'NONE',  ( -4.523565618882782857, 37.69517167404197266, 75.36122732895108811 ) ) ;
#10315=EDGE_LOOP ( 'NONE', ( #4344, #20408, #15930, #13192 ) ) ;
#10316=EDGE_CURVE ( 'NONE', #8610, #2109, #14338, .T. ) ;
#10317=CARTESIAN_POINT ( 'NONE',  ( 6.448646529778700121, 49.81091948135299674, 78.84682786933051091 ) ) ;
#10319=EDGE_CURVE ( 'NONE', #9753, #10288, #18421, .T. ) ;
#10320=CARTESIAN_POINT ( 'NONE',  ( -3.607485548685017029, 36.27216495724725576, 77.44024473021482891 ) ) ;
#10321=CARTESIAN_POINT ( 'NONE',  ( -0.1389469955404790957, 52.97235366542109603, 75.45826338387253429 ) ) ;
#10323=FACE_OUTER_BOUND ( 'NONE', #20662, .T. ) ;
#10324=CARTESIAN_POINT ( 'NONE',  ( 4.540095451430588902, 52.13470428702989068, 76.74217282813371810 ) ) ;
#10325=FACE_OUTER_BOUND ( 'NONE', #14183, .T. ) ;
#10327=CARTESIAN_POINT ( 'NONE',  ( 8.794665453373390562, 41.15189478912013499, 76.14505377247542128 ) ) ;
#10329=CARTESIAN_POINT ( 'NONE',  ( 4.098701607150998072, 51.53591119238402740, 76.47586842453881673 ) ) ;
#10330=CARTESIAN_POINT ( 'NONE',  ( 5.180932498246527018, 37.42231731781541271, 77.73906448345020692 ) ) ;
#10332=CARTESIAN_POINT ( 'NONE',  ( 8.352500096663396434, 41.72785666267516547, 76.03373457610489083 ) ) ;
#10336=ORIENTED_EDGE ( 'NONE', *, *, #4422, .T. ) ;
#10339=EDGE_CURVE ( 'NONE', #20669, #11820, #12743, .T. ) ;
#10340=DIRECTION ( 'NONE',  ( -1.540237394707284467E-16, -1.793354297423764243E-16, 1.000000000000000000 ) ) ;
#10345=CARTESIAN_POINT ( 'NONE',  ( -0.9504375969237850441, 51.37401713635502887, 77.77566232894263010 ) ) ;
#10346=VERTEX_POINT ( 'NONE', #8158 ) ;
#10348=B_SPLINE_CURVE_WITH_KNOTS ( 'NONE', 3,
 ( #16357, #18050, #19534, #3473, #74, #17736, #3057, #9564, #19219, #4636 ),
 .UNSPECIFIED., .F., .F.,
 ( 4, 2, 2, 2, 4 ),
 ( 0.000000000000000000, 0.0001230208117932171999, 0.0002460416235864343998, 0.0003690624353796515726, 0.0004920832471728687997 ),
 .UNSPECIFIED. ) ;
#10349=CARTESIAN_POINT ( 'NONE',  ( 8.872773925109784798, 41.38599083402314704, 79.54845644658969661 ) ) ;
#10350=CARTESIAN_POINT ( 'NONE',  ( 5.453344025566023490, 40.65105419805430387, 72.45433879953087342 ) ) ;
#10352=ORIENTED_EDGE ( 'NONE', *, *, #12787, .F. ) ;
#10356=CARTESIAN_POINT ( 'NONE',  ( -8.192078482032012943, 42.93655631659661509, 75.45433879953087342 ) ) ;
#10358=CARTESIAN_POINT ( 'NONE',  ( 1.965820793441009240, 52.94144253664489241, 77.13040333250513925 ) ) ;
#10359=CARTESIAN_POINT ( 'NONE',  ( -3.584565806390786591, 36.25523506687804343, 78.05869123030269918 ) ) ;
#10361=B_SPLINE_CURVE_WITH_KNOTS ( 'NONE', 3,
 ( #13181, #19340, #3383, #4971 ),
 .UNSPECIFIED., .F., .F.,
 ( 4, 4 ),
 ( 2.201117333616983738E-17, 0.002523081261280070431 ),
 .UNSPECIFIED. ) ;
#10362=CARTESIAN_POINT ( 'NONE',  ( 0.3279640439667353413, 52.35988168082470651, 72.45433879953087342 ) ) ;
#10363=ORIENTED_EDGE ( 'NONE', *, *, #7748, .F. ) ;
#10364=CARTESIAN_POINT ( 'NONE',  ( -1.769308508470985419, 51.40850462968639079, 72.45432679953087529 ) ) ;
#10366=PLANE ( 'NONE',  #14274 ) ;
#10369=CARTESIAN_POINT ( 'NONE',  ( 6.880132251722071324, 48.33664052787082710, 72.45433879953087342 ) ) ;
#10371=CARTESIAN_POINT ( 'NONE',  ( -3.512376142844359173, 52.09502624807847582, 79.07098488719154261 ) ) ;
#10372=CARTESIAN_POINT ( 'NONE',  ( 0.8304091259513172174, 52.95680132091538894, 77.54407394899503458 ) ) ;
#10373=CARTESIAN_POINT ( 'NONE',  ( 0.8496841725525090538, 52.96357321910183913, 76.36683753262285279 ) ) ;
#10378=ORIENTED_EDGE ( 'NONE', *, *, #17215, .T. ) ;
#10380=CARTESIAN_POINT ( 'NONE',  ( 8.872773925109784798, 41.38599083402314704, 79.54845644658969661 ) ) ;
#10381=DIRECTION ( 'NONE',  ( -1.540237394707284220E-16, -1.793354297423764243E-16, 1.000000000000000000 ) ) ;
#10383=CARTESIAN_POINT ( 'NONE',  ( 5.467491823421675612, 37.62122069371999800, 76.05323035213213245 ) ) ;
#10385=DIRECTION ( 'NONE',  ( 0.02533578529877749883, 0.9996789974703350623, 1.831801750099157041E-16 ) ) ;
#10386=EDGE_CURVE ( 'NONE', #4065, #13955, #10348, .T. ) ;
#10387=ORIENTED_EDGE ( 'NONE', *, *, #12369, .F. ) ;
#10388=CARTESIAN_POINT ( 'NONE',  ( 8.788342534296722519, 41.13294459952883386, 78.64407474691132904 ) ) ;
#10389=ORIENTED_EDGE ( 'NONE', *, *, #7380, .F. ) ;
#10393=CARTESIAN_POINT ( 'NONE',  ( -8.102959993061887189, 42.23164920826034319, 76.93555611204594413 ) ) ;
#10394=ORIENTED_EDGE ( 'NONE', *, *, #191, .T. ) ;
#10396=DIRECTION ( 'NONE',  ( -1.540237394707284467E-16, -1.793354297423764243E-16, 1.000000000000000000 ) ) ;
#10398=PLANE ( 'NONE',  #10510 ) ;
#10399=LINE ( 'NONE', #7175, #8139 ) ;
#10401=LINE ( 'NONE', #10618, #20388 ) ;
#10403=EDGE_CURVE ( 'NONE', #18369, #2200, #7100, .T. ) ;
#10405=CARTESIAN_POINT ( 'NONE',  ( -4.783040473602117260, 51.18705603930939674, 76.11505395997643575 ) ) ;
#10406=CYLINDRICAL_SURFACE ( 'NONE', #19026, 6.200000000000000178 ) ;
#10408=CARTESIAN_POINT ( 'NONE',  ( -4.735411308350331083, 37.10531828029095891, 75.97251605650340878 ) ) ;
#10410=CARTESIAN_POINT ( 'NONE',  ( -4.454500421143473332, 37.64505674804929924, 79.54845644658969661 ) ) ;
#10412=ORIENTED_EDGE ( 'NONE', *, *, #8155, .T. ) ;
#10414=CARTESIAN_POINT ( 'NONE',  ( 0.8535366408858915399, 52.96430285769372404, 75.36710396340995999 ) ) ;
#10417=DIRECTION ( 'NONE',  ( 1.540237394707284220E-16, 1.793354297423764243E-16, -1.000000000000000000 ) ) ;
#10418=CARTESIAN_POINT ( 'NONE',  ( 8.527988662190095326, 48.03182059810101379, 79.44551527011911674 ) ) ;
#10421=CARTESIAN_POINT ( 'NONE',  ( 2.108290839596759003, 51.34989793853182505, 77.84551527011910821 ) ) ;
#10425=FACE_OUTER_BOUND ( 'NONE', #2543, .T. ) ;
#10426=CARTESIAN_POINT ( 'NONE',  ( 8.550070540977731781, 40.41882831985841307, 75.56834740413086138 ) ) ;
#10428=CARTESIAN_POINT ( 'NONE',  ( -3.104272635537439928, 51.51688312651948820, 79.08698131281367694 ) ) ;
#10429=EDGE_CURVE ( 'NONE', #18295, #7860, #410, .T. ) ;
#10433=CARTESIAN_POINT ( 'NONE',  ( 8.225112643453085681, 41.36496456502055707, 76.07953452682116335 ) ) ;
#10436=CARTESIAN_POINT ( 'NONE',  ( 5.197017349930873387, 50.72462959604935406, 75.36146177662637058 ) ) ;
#10437=ADVANCED_FACE ( 'NONE', ( #11777 ), #9203, .T. ) ;
#10440=CARTESIAN_POINT ( 'NONE',  ( 8.365153831044532140, 41.76897630594757516, 76.08825944838494593 ) ) ;
#10441=CARTESIAN_POINT ( 'NONE',  ( 0.3298136261391984014, 52.35624255821358020, 76.26461983994238381 ) ) ;
#10443=CYLINDRICAL_SURFACE ( 'NONE', #8820, 8.199999999999995737 ) ;
#10444=CARTESIAN_POINT ( 'NONE',  ( 5.753005855668248181, 51.23877623043087937, 78.93669174070734584 ) ) ;
#10445=CARTESIAN_POINT ( 'NONE',  ( 8.385679600361122255, 39.92613824206362949, 77.69330938776616335 ) ) ;
#10447=CARTESIAN_POINT ( 'NONE',  ( 2.643026689701002407, 51.46641972551267941, 75.45433879953087342 ) ) ;
#10449=DIRECTION ( 'NONE',  ( -0.3165065846431827090, -0.9485903129789529098, 0.000000000000000000 ) ) ;
#10452=ORIENTED_EDGE ( 'NONE', *, *, #18480, .T. ) ;
#10453=CARTESIAN_POINT ( 'NONE',  ( 8.886583547266173611, 41.42737914769194418, 79.54795956895829079 ) ) ;
#10454=LINE ( 'NONE', #20622, #2647 ) ;
#10455=EDGE_CURVE ( 'NONE', #3218, #15454, #5219, .T. ) ;
#10456=CARTESIAN_POINT ( 'NONE',  ( -2.939085670389444793, 51.59587639763223166, 72.45433879953087342 ) ) ;
#10457=VERTEX_POINT ( 'NONE', #6108 ) ;
#10460=CARTESIAN_POINT ( 'NONE',  ( 0.3821786226492926430, 35.36301154328572949, 76.86610350541323555 ) ) ;
#10463=CARTESIAN_POINT ( 'NONE',  ( -0.6028239774188565159, 52.89035653119623959, 79.22266899401112994 ) ) ;
#10464=CARTESIAN_POINT ( 'NONE',  ( -7.576204955092350701, 47.69026255563115768, 78.31886496287775401 ) ) ;
#10466=CARTESIAN_POINT ( 'NONE',  ( -3.279987361312213690, 36.94427024389478476, 77.85659439586764563 ) ) ;
#10467=DIRECTION ( 'NONE',  ( -0.5813877811927011807, 0.8136266022444372803, 5.636455622144619183E-17 ) ) ;
#10469=CARTESIAN_POINT ( 'NONE',  ( 5.568913169576547695, 50.62012213993821064, 77.10005730845655592 ) ) ;
#10471=CARTESIAN_POINT ( 'NONE',  ( -4.391572913631113906, 50.71986899290229900, 78.89490084226201816 ) ) ;
#10473=ORIENTED_EDGE ( 'NONE', *, *, #14818, .T. ) ;
#10476=CARTESIAN_POINT ( 'NONE',  ( -2.970231456936518910, 51.56264740916601852, 78.78030711080756987 ) ) ;
#10477=CARTESIAN_POINT ( 'NONE',  ( 1.658154530501164237, 36.04125148601230677, 72.45433879953085921 ) ) ;
#10478=FACE_OUTER_BOUND ( 'NONE', #1317, .T. ) ;
#10479=CARTESIAN_POINT ( 'NONE',  ( 0.3906990944827833934, 52.35576236765771796, 78.86056079792015794 ) ) ;
#10480=ORIENTED_EDGE ( 'NONE', *, *, #12099, .T. ) ;
#10482=CIRCLE ( 'NONE', #936, 8.199999999999995737 ) ;
#10483=ORIENTED_EDGE ( 'NONE', *, *, #17243, .T. ) ;
#10486=CYLINDRICAL_SURFACE ( 'NONE', #11830, 8.799999999999995381 ) ;
#10491=CARTESIAN_POINT ( 'NONE',  ( -5.679243918435851413, 37.80248940946449210, 75.65168154244369703 ) ) ;
#10492=ORIENTED_EDGE ( 'NONE', *, *, #19223, .F. ) ;
#10493=CARTESIAN_POINT ( 'NONE',  ( 4.133950555568060459, 51.52399475064406431, 77.16541282331252205 ) ) ;
#10495=ORIENTED_EDGE ( 'NONE', *, *, #2583, .T. ) ;
#10501=CARTESIAN_POINT ( 'NONE',  ( 0.3896696312604364665, 52.96120322344530962, 77.46089148198416297 ) ) ;
#10503=CARTESIAN_POINT ( 'NONE',  ( -4.618682869335207108, 51.30449996580257022, 78.93596273702843291 ) ) ;
#10506=CARTESIAN_POINT ( 'NONE',  ( 1.419815960288714596, 52.31341683702156331, 79.43674840306717044 ) ) ;
#10510=AXIS2_PLACEMENT_3D ( 'NONE', #9104, #15592, #16868 ) ;
#10511=CARTESIAN_POINT ( 'NONE',  ( -4.530495696546473994, 37.70859131435868505, 76.21310604893328389 ) ) ;
#10513=CARTESIAN_POINT ( 'NONE',  ( -3.105924918850441863, 36.80844641393417760, 78.65049157520557799 ) ) ;
#10515=VERTEX_POINT ( 'NONE', #6007 ) ;
#10516=ADVANCED_FACE ( 'NONE', ( #17499, #10728 ), #13997, .F. ) ;
#10517=DIRECTION ( 'NONE',  ( 0.3165065846431827645, 0.9485903129789529098, 0.000000000000000000 ) ) ;
#10521=CARTESIAN_POINT ( 'NONE',  ( -7.203525358565210368, 41.41373112547281465, 78.69802495076405080 ) ) ;
#10523=VECTOR ( 'NONE', #17413, 1000.000000000000227 ) ;
#10524=ORIENTED_EDGE ( 'NONE', *, *, #17672, .T. ) ;
#10528=DIRECTION ( 'NONE',  ( -0.3165065846431928120, -0.9485903129789495791, -2.188653791613883869E-16 ) ) ;
#10531=CARTESIAN_POINT ( 'NONE',  ( 4.125939684684055919, 51.51579152172704568, 77.12434737327507150 ) ) ;
#10533=LINE ( 'NONE', #832, #1152 ) ;
#10534=CARTESIAN_POINT ( 'NONE',  ( 8.787842894572216679, 41.13144714757795128, 76.38644048143638088 ) ) ;
#10538=ADVANCED_FACE ( 'NONE', ( #17290 ), #10927, .F. ) ;
#10539=CARTESIAN_POINT ( 'NONE',  ( -7.368313902600233334, 41.94587499716005397, 78.71972396713441356 ) ) ;
#10540=VERTEX_POINT ( 'NONE', #14303 ) ;
#10541=CARTESIAN_POINT ( 'NONE',  ( 8.924621998940734713, 41.54138280047497744, 78.88894238123772595 ) ) ;
#10542=ADVANCED_FACE ( 'NONE', ( #19400 ), #10741, .T. ) ;
#10543=ADVANCED_FACE ( 'NONE', ( #11339, #14619 ), #3334, .T. ) ;
#10545=ORIENTED_EDGE ( 'NONE', *, *, #5873, .T. ) ;
#10549=CARTESIAN_POINT ( 'NONE',  ( -3.387980870927748800, 52.18391455498849751, 78.68920376838389075 ) ) ;
#10551=DIRECTION ( 'NONE',  ( 1.540237394707284220E-16, 1.793354297423764243E-16, -1.000000000000000000 ) ) ;
#10552=CARTESIAN_POINT ( 'NONE',  ( -6.989009964201624570, 47.26660036502315876, 78.95058778273427436 ) ) ;
#10553=CARTESIAN_POINT ( 'NONE',  ( 8.648170029844118645, 43.06315486489794608, 77.06316232894263862 ) ) ;
#10555=DIRECTION ( 'NONE',  ( -0.9485903129789527988, 0.3165065846431829311, -8.934458285744989980E-17 ) ) ;
#10557=VERTEX_POINT ( 'NONE', #348 ) ;
#10559=CARTESIAN_POINT ( 'NONE',  ( 8.584650940598146818, 42.88688602177342091, 79.09515810002898206 ) ) ;
#10560=DIRECTION ( 'NONE',  ( 1.540237394707284220E-16, 1.793354297423764243E-16, -1.000000000000000000 ) ) ;
#10562=CARTESIAN_POINT ( 'NONE',  ( 5.934652055452926511, 51.10460149980519873, 77.05868164888072158 ) ) ;
#10563=B_SPLINE_SURFACE_WITH_KNOTS ( 'NONE', 3, 1, ( 
 ( #9057, #14046 ),
 ( #9164, #9376 ),
 ( #12764, #15544 ),
 ( #7562, #12668 ),
 ( #19149, #20836 ),
 ( #15859, #14246 ),
 ( #20529, #6056 ),
 ( #1273, #4560 ),
 ( #962, #6364 ),
 ( #16485, #3390 ),
 ( #9695, #11604 ) ),
 .UNSPECIFIED., .F., .F., .F.,
 ( 4, 1, 1, 1, 1, 1, 1, 1, 4 ),
 ( 2, 2 ),
 ( 0.000000000000000000, 0.1077815449370134182, 0.2006545494464173907, 0.2847368448845932765, 0.3681045469499393263, 0.4695596479522798350, 0.6076740370479670750, 0.7836404280850621795, 1.000000000000000000 ),
 ( 0.000000000000000000, 1.000000000000000000 ),
 .UNSPECIFIED. ) ;
#10565=VECTOR ( 'NONE', #19913, 1000.000000000000000 ) ;
#10569=CARTESIAN_POINT ( 'NONE',  ( -5.889261015154382051, 37.95762057880577345, 79.03330530165142420 ) ) ;
#10570=VECTOR ( 'NONE', #10107, 1000.000000000000000 ) ;
#10571=EDGE_CURVE ( 'NONE', #18616, #10028, #3966, .T. ) ;
#10572=CARTESIAN_POINT ( 'NONE',  ( 6.721999984869559519, 37.77659228945417880, 75.79056106475293575 ) ) ;
#10573=ORIENTED_EDGE ( 'NONE', *, *, #3883, .F. ) ;
#10574=ADVANCED_FACE ( 'NONE', ( #7043 ), #6938, .T. ) ;
#10575=FACE_OUTER_BOUND ( 'NONE', #430, .T. ) ;
#10576=EDGE_LOOP ( 'NONE', ( #4965, #11035, #10670, #9786, #3796, #8484, #3786, #4597 ) ) ;
#10577=VECTOR ( 'NONE', #17873, 1000.000000000000000 ) ;
#10578=CARTESIAN_POINT ( 'NONE',  ( -4.446085291674333639, 50.68091644337815893, 78.65631888207801126 ) ) ;
#10579=EDGE_CURVE ( 'NONE', #2608, #16492, #11835, .T. ) ;
#10581=ORIENTED_EDGE ( 'NONE', *, *, #4303, .T. ) ;
#10583=EDGE_CURVE ( 'NONE', #19292, #10724, #15188, .T. ) ;
#10584=ADVANCED_FACE ( 'NONE', ( #8554 ), #18329, .F. ) ;
#10586=DIRECTION ( 'NONE',  ( -0.3219511000281078394, 0.002538702742701116205, -0.9467528949937651372 ) ) ;
#10588=CARTESIAN_POINT ( 'NONE',  ( 0.4974180460467604870, 52.36224188547572567, 77.38972066725763455 ) ) ;
#10589=CARTESIAN_POINT ( 'NONE',  ( -4.189188114579794231, 36.70184521026505564, 79.48068319027247242 ) ) ;
#10590=EDGE_LOOP ( 'NONE', ( #17075, #2417, #18693, #318 ) ) ;
#10592=CARTESIAN_POINT ( 'NONE',  ( 8.245414686166476770, 41.40667145630854407, 77.48117334564075520 ) ) ;
#10595=CARTESIAN_POINT ( 'NONE',  ( 4.629792079547915939, 52.06844900104020013, 77.37197156638603701 ) ) ;
#10596=CARTESIAN_POINT ( 'NONE',  ( 6.912263059922415742, 50.38247963137696672, 77.24227907682649175 ) ) ;
#10598=CARTESIAN_POINT ( 'NONE',  ( 6.266852414816192152, 50.85921847619028568, 79.48482414599367019 ) ) ;
#10599=LINE ( 'NONE', #5665, #13533 ) ;
#10601=CARTESIAN_POINT ( 'NONE',  ( -4.948764291328625831, 37.26291353443464516, 75.36972643424059015 ) ) ;
#10603=CARTESIAN_POINT ( 'NONE',  ( 8.837344731589771740, 41.27980729345753730, 78.92656146296575059 ) ) ;
#10604=VECTOR ( 'NONE', #11524, 1000.000000000000114 ) ;
#10605=ORIENTED_EDGE ( 'NONE', *, *, #354, .T. ) ;
#10606=CARTESIAN_POINT ( 'NONE',  ( -4.383473025373059606, 51.47257230871590394, 78.45066232894264147 ) ) ;
#10613=CARTESIAN_POINT ( 'NONE',  ( 0.5221537403065013017, 44.16218137147968292, 76.96022115247204454 ) ) ;
#10614=VERTEX_POINT ( 'NONE', #10380 ) ;
#10618=CARTESIAN_POINT ( 'NONE',  ( 1.652727357819364418, 35.35299279957455099, 76.16022115247204738 ) ) ;
#10619=CIRCLE ( 'NONE', #9933, 8.199999999999995737 ) ;
#10620=ORIENTED_EDGE ( 'NONE', *, *, #9540, .F. ) ;
#10622=PLANE ( 'NONE',  #5778 ) ;
#10626=CARTESIAN_POINT ( 'NONE',  ( -4.448275204524981596, 37.64785834894585292, 75.98775578934684916 ) ) ;
#10627=CARTESIAN_POINT ( 'NONE',  ( 5.254713546219920595, 50.85372921038054983, 78.82175487302160377 ) ) ;
#10629=EDGE_CURVE ( 'NONE', #5410, #3669, #13542, .T. ) ;
#10630=VERTEX_POINT ( 'NONE', #5450 ) ;
#10631=LINE ( 'NONE', #17100, #15968 ) ;
#10632=ORIENTED_EDGE ( 'NONE', *, *, #9923, .F. ) ;
#10637=VECTOR ( 'NONE', #17365, 1000.000000000000114 ) ;
#10639=CARTESIAN_POINT ( 'NONE',  ( 6.632598449108662031, 50.58905661380737939, 79.28554042632779897 ) ) ;
#10642=DIRECTION ( 'NONE',  ( 0.8043570849667761591, -0.5941461771851692664, 1.733862608106489734E-17 ) ) ;
#10643=CARTESIAN_POINT ( 'NONE',  ( 7.672912595070442876, 40.17111506963394163, 76.58175473889373563 ) ) ;
#10645=CARTESIAN_POINT ( 'NONE',  ( 4.567922609689349045, 52.11414948617044729, 77.12434737327507150 ) ) ;
#10646=CARTESIAN_POINT ( 'NONE',  ( -7.609226043662618899, 43.10354341710602455, 78.64709103647231814 ) ) ;
#10647=DIRECTION ( 'NONE',  ( -0.5941461771851691553, -0.8043570849667760481, -2.357623395011396791E-16 ) ) ;
#10648=CARTESIAN_POINT ( 'NONE',  ( 4.470572738639666532, 36.16780480931087283, 79.45433879953087342 ) ) ;
#10651=CARTESIAN_POINT ( 'NONE',  ( -5.383807009170671343, 49.83799468618045836, 76.28720437108826502 ) ) ;
#10655=CARTESIAN_POINT ( 'NONE',  ( 8.306444873683641816, 41.60874232747575263, 78.93548851266230315 ) ) ;
#10661=LINE ( 'NONE', #17124, #3117 ) ;
#10662=LINE ( 'NONE', #12034, #9285 ) ;
#10665=CARTESIAN_POINT ( 'NONE',  ( 6.880132251722071324, 48.33664052787082710, 75.45433879953087342 ) ) ;
#10666=CARTESIAN_POINT ( 'NONE',  ( 0.3326973149608335456, 52.96014171822455552, 77.76169174070734869 ) ) ;
#10667=CARTESIAN_POINT ( 'NONE',  ( 5.467161035934759994, 36.87993031913157438, 77.68578589458712713 ) ) ;
#10669=ORIENTED_EDGE ( 'NONE', *, *, #9675, .T. ) ;
#10670=ORIENTED_EDGE ( 'NONE', *, *, #2780, .T. ) ;
#10671=CARTESIAN_POINT ( 'NONE',  ( 9.060635047751631532, 41.94902253626816702, 79.49775514261133935 ) ) ;
#10672=CARTESIAN_POINT ( 'NONE',  ( -4.151536175905484072, 36.67403323987894481, 75.43521673441158271 ) ) ;
#10673=CARTESIAN_POINT ( 'NONE',  ( 8.868817592801743643, 41.37413345511091478, 75.97198585835440099 ) ) ;
#10676=CARTESIAN_POINT ( 'NONE',  ( -4.249412910294118717, 50.83092575845958550, 78.93669174070734584 ) ) ;
#10678=CARTESIAN_POINT ( 'NONE',  ( -4.283496025856504019, 47.84326572019833179, 75.45433879953087342 ) ) ;
#10680=DIRECTION ( 'NONE',  ( 1.540237394707284220E-16, 1.793354297423764243E-16, -1.000000000000000000 ) ) ;
#10681=CARTESIAN_POINT ( 'NONE',  ( 0.5221537403065014127, 44.16218137147968292, 76.16022115247204738 ) ) ;
#10683=CARTESIAN_POINT ( 'NONE',  ( 6.136807603568960268, 37.35843523903731977, 75.40772603260481333 ) ) ;
#10684=ORIENTED_EDGE ( 'NONE', *, *, #8192, .T. ) ;
#10685=CARTESIAN_POINT ( 'NONE',  ( 5.394726803408533833, 50.74878659197170094, 77.28963291717792572 ) ) ;
#10686=ORIENTED_EDGE ( 'NONE', *, *, #2970, .T. ) ;
#10687=FACE_OUTER_BOUND ( 'NONE', #8915, .T. ) ;
#10689=( BOUNDED_CURVE ( )  B_SPLINE_CURVE ( 3, ( #1599, #5089, #12600, #17865 ),
 .UNSPECIFIED., .F., .F. ) 
 B_SPLINE_CURVE_WITH_KNOTS ( ( 4, 4 ),
 ( 4.565792013076894307, 4.566698375078894756 ),
 .UNSPECIFIED. ) 
 CURVE ( )  GEOMETRIC_REPRESENTATION_ITEM ( )  RATIONAL_B_SPLINE_CURVE ( ( 1.000000000000000000, 0.9999999315423278023, 0.9999999315423278023, 1.000000000000000000 ) ) 
 REPRESENTATION_ITEM ( '' )  );
#10690=VERTEX_POINT ( 'NONE', #18548 ) ;
#10692=VECTOR ( 'NONE', #20052, 1000.000000000000114 ) ;
#10693=CARTESIAN_POINT ( 'NONE',  ( -0.5881641420295652400, 52.97589590771117685, 75.69129100417544009 ) ) ;
#10694=CARTESIAN_POINT ( 'NONE',  ( -2.990358918575095171, 51.54826506199249536, 78.86270620133520026 ) ) ;
#10696=CARTESIAN_POINT ( 'NONE',  ( 5.273270741223392122, 50.83850129255925054, 77.24912405724838038 ) ) ;
#10697=CARTESIAN_POINT ( 'NONE',  ( -3.096855864432994210, 36.80899838413677827, 78.50831005042292077 ) ) ;
#10698=ORIENTED_EDGE ( 'NONE', *, *, #253, .T. ) ;
#10700=CARTESIAN_POINT ( 'NONE',  ( 8.214799251806553571, 41.32260305165857517, 77.14698585835439815 ) ) ;
#10701=ORIENTED_EDGE ( 'NONE', *, *, #12761, .F. ) ;
#10702=CARTESIAN_POINT ( 'NONE',  ( 5.658108625003792191, 37.01637447524286273, 75.97198585835440099 ) ) ;
#10706=CARTESIAN_POINT ( 'NONE',  ( 6.632598449108662031, 50.58905661380737939, 79.28554042632779897 ) ) ;
#10709=CARTESIAN_POINT ( 'NONE',  ( 6.217311209797515836, 50.06224385580732417, 79.30230994520773891 ) ) ;
#10711=ADVANCED_FACE ( 'NONE', ( #20454 ), #17650, .F. ) ;
#10713=CARTESIAN_POINT ( 'NONE',  ( 4.437233947525204059, 51.36737272290800860, 77.60409055468527129 ) ) ;
#10714=EDGE_CURVE ( 'NONE', #17824, #5907, #13863, .T. ) ;
#10715=ORIENTED_EDGE ( 'NONE', *, *, #2952, .F. ) ;
#10718=CARTESIAN_POINT ( 'NONE',  ( -7.302678038849692577, 42.15150420378952845, 77.34580771017452605 ) ) ;
#10721=FACE_BOUND ( 'NONE', #8141, .T. ) ;
#10723=CARTESIAN_POINT ( 'NONE',  ( -4.705661087595403025, 51.24234851550965431, 78.91934866582661812 ) ) ;
#10724=VERTEX_POINT ( 'NONE', #4067 ) ;
#10725=LINE ( 'NONE', #4296, #2719 ) ;
#10726=CARTESIAN_POINT ( 'NONE',  ( 0.7513193414822582072, 52.35291871808690445, 78.87878230117789258 ) ) ;
#10728=FACE_BOUND ( 'NONE', #9699, .T. ) ;
#10729=CARTESIAN_POINT ( 'NONE',  ( 2.927603783594689979, 51.37146775011972011, 72.45433879953087342 ) ) ;
#10731=CARTESIAN_POINT ( 'NONE',  ( 5.581823371501742237, 36.96186382607169207, 75.98067903659783440 ) ) ;
#10733=CARTESIAN_POINT ( 'NONE',  ( 5.455409717288331350, 36.87153325707006957, 76.14053225265315916 ) ) ;
#10734=DIRECTION ( 'NONE',  ( 0.3164953060534052010, 0.9485565103298893019, -0.008442035118619106368 ) ) ;
#10736=CARTESIAN_POINT ( 'NONE',  ( 1.702985681980708321, 52.20476652859439071, 75.60954117182248524 ) ) ;
#10738=DIRECTION ( 'NONE',  ( -0.3165065846431826535, -0.9485903129789529098, -2.188653791613874008E-16 ) ) ;
#10739=CARTESIAN_POINT ( 'NONE',  ( 0.3869604771732107484, 52.35579184508003436, 77.46088296688223807 ) ) ;
#10741=B_SPLINE_SURFACE_WITH_KNOTS ( 'NONE', 3, 1, ( 
 ( #6624, #6214 ),
 ( #144, #6412 ),
 ( #17810, #17597 ),
 ( #4817, #9639 ),
 ( #11543, #13128 ),
 ( #1757, #19603 ),
 ( #20780, #6523 ),
 ( #8237, #5025 ),
 ( #8024, #12714 ),
 ( #17705, #14724 ),
 ( #18020, #12921 ),
 ( #3135, #3441 ),
 ( #11127, #17911 ),
 ( #11234, #1857 ),
 ( #12810, #19293 ),
 ( #9954, #19192 ),
 ( #45, #4706 ),
 ( #16219, #4607 ),
 ( #20879, #16438 ) ),
 .UNSPECIFIED., .F., .F., .F.,
 ( 4, 1, 1, 1, 1, 1, 1, 1, 1, 1, 1, 1, 1, 1, 1, 1, 4 ),
 ( 2, 2 ),
 ( 0.000000000000000000, 0.07819787255609964016, 0.1515336364311310191, 0.2187066978088008651, 0.2814522326392254747, 0.3385163222030129759, 0.3915958516965070690, 0.4406923075239814191, 0.4864642379862412769, 0.5323932679607442653, 0.5831133966729620255, 0.6391356099194271945, 0.6992555458516984679, 0.7657124642625251498, 0.8379597225178306852, 0.9162365097749198828, 1.000000000000000000 ),
 ( 0.000000000000000000, 1.000000000000000000 ),
 .UNSPECIFIED. ) ;
#10743=CARTESIAN_POINT ( 'NONE',  ( -4.303670962001103106, 50.79176777958974753, 75.36022115247205022 ) ) ;
#10744=ORIENTED_EDGE ( 'NONE', *, *, #15451, .T. ) ;
#10746=CARTESIAN_POINT ( 'NONE',  ( -3.566438244846301231, 38.23101125920473464, 76.53375056423675460 ) ) ;
#10747=CARTESIAN_POINT ( 'NONE',  ( 8.401796425420881675, 39.97444138920005230, 76.12035193564865665 ) ) ;
#10749=CARTESIAN_POINT ( 'NONE',  ( -7.645086356741528810, 40.78432135352825583, 79.43600262374511090 ) ) ;
#10750=CARTESIAN_POINT ( 'NONE',  ( -7.611066721457015127, 43.11777894428342961, 78.46404369028466874 ) ) ;
#10751=CARTESIAN_POINT ( 'NONE',  ( -5.004817973257478236, 39.29348442311233214, 78.18375056423674607 ) ) ;
#10753=DIRECTION ( 'NONE',  ( -0.9485903129789527988, 0.3165065846431829311, -8.934458285744989980E-17 ) ) ;
#10758=PLANE ( 'NONE',  #8145 ) ;
#10760=CARTESIAN_POINT ( 'NONE',  ( -3.355600405723123902, 52.20705244989922988, 78.36353918055804968 ) ) ;
#10762=EDGE_CURVE ( 'NONE', #18313, #13475, #4178, .T. ) ;
#10763=CARTESIAN_POINT ( 'NONE',  ( 5.748274343403733333, 51.24227120794373747, 77.94845644658968808 ) ) ;
#10764=CARTESIAN_POINT ( 'NONE',  ( -7.203937208853350427, 41.84628966447687759, 79.54737348031042643 ) ) ;
#10765=CARTESIAN_POINT ( 'NONE',  ( 2.484494565094232499, 50.04344131194918788, 82.45433879953087342 ) ) ;
#10767=LINE ( 'NONE', #7444, #8032 ) ;
#10769=CARTESIAN_POINT ( 'NONE',  ( 8.936058775400656629, 41.57565954506093675, 76.08336210994360727 ) ) ;
#10770=CARTESIAN_POINT ( 'NONE',  ( 5.939900590116411472, 51.10072461867315496, 76.90580938776616904 ) ) ;
#10774=B_SPLINE_CURVE_WITH_KNOTS ( 'NONE', 3,
 ( #11541, #1537, #14407, #6307, #18018, #3233, #14617, #6520, #15123, #532, #19291, #7013 ),
 .UNSPECIFIED., .F., .F.,
 ( 4, 2, 2, 2, 2, 4 ),
 ( 0.000000000000000000, 0.0002162886299158511697, 0.0004325772598317023394, 0.0006488658897475535091, 0.0007570102047054918333, 0.0008651545196634303743 ),
 .UNSPECIFIED. ) ;
#10775=CARTESIAN_POINT ( 'NONE',  ( -0.9387578428071298164, 52.84007946907634334, 78.24704469840057186 ) ) ;
#10777=CARTESIAN_POINT ( 'NONE',  ( -7.085676915393174902, 47.03388510223538077, 78.01104965316210382 ) ) ;
#10778=CARTESIAN_POINT ( 'NONE',  ( -5.472271698804210160, 38.58561386426530504, 78.92638042842689572 ) ) ;
#10779=DIRECTION ( 'NONE',  ( 0.9539696396349547358, -0.2999031954727301441, 9.315070279690498823E-17 ) ) ;
#10781=EDGE_CURVE ( 'NONE', #19846, #9686, #17764, .T. ) ;
#10782=CARTESIAN_POINT ( 'NONE',  ( 5.389492195292208798, 36.82443100924615464, 78.79551527011911105 ) ) ;
#10783=ORIENTED_EDGE ( 'NONE', *, *, #18070, .F. ) ;
#10787=VERTEX_POINT ( 'NONE', #17266 ) ;
#10789=CARTESIAN_POINT ( 'NONE',  ( -0.9369684686848965827, 52.97864635801455790, 77.04772206183797323 ) ) ;
#10793=CARTESIAN_POINT ( 'NONE',  ( 0.8448630204163343205, 52.35216834387308182, 76.36683753262285279 ) ) ;
#10794=CARTESIAN_POINT ( 'NONE',  ( 3.212180877488374886, 51.27651577472676081, 75.45433879953087342 ) ) ;
#10797=ORIENTED_EDGE ( 'NONE', *, *, #12820, .T. ) ;
#10799=LINE ( 'NONE', #4485, #3326 ) ;
#10800=CARTESIAN_POINT ( 'NONE',  ( -6.792737292293178797, 47.86790251333490431, 78.78375056423675460 ) ) ;
#10801=DIRECTION ( 'NONE',  ( -0.9534635866061451637, -0.3015081906286224411, -2.009271279954815058E-16 ) ) ;
#10807=ADVANCED_FACE ( 'NONE', ( #9086 ), #19348, .F. ) ;
#10808=EDGE_CURVE ( 'NONE', #17046, #279, #16918, .T. ) ;
#10812=CARTESIAN_POINT ( 'NONE',  ( 5.008928291858447679, 51.78839635354462700, 75.50506468444432073 ) ) ;
#10815=CARTESIAN_POINT ( 'NONE',  ( -5.171864905379679023, 50.90921633613218944, 79.44348587025405095 ) ) ;
#10817=VERTEX_POINT ( 'NONE', #12283 ) ;
#10818=VECTOR ( 'NONE', #12436, 1000.000000000000000 ) ;
#10819=CARTESIAN_POINT ( 'NONE',  ( 4.521197205061672442, 36.20397919953602184, 75.90366482745062626 ) ) ;
#10821=EDGE_CURVE ( 'NONE', #14218, #14373, #1597, .T. ) ;
#10825=AXIS2_PLACEMENT_3D ( 'NONE', #9761, #16248, #8263 ) ;
#10826=VERTEX_POINT ( 'NONE', #3191 ) ;
#10831=CARTESIAN_POINT ( 'NONE',  ( 5.228508048761829841, 37.45631306436156649, 75.98067903659783440 ) ) ;
#10832=CARTESIAN_POINT ( 'NONE',  ( 5.644533139590786064, 37.00667393039697828, 75.97264893529829521 ) ) ;
#10833=VECTOR ( 'NONE', #16348, 1000.000000000000000 ) ;
#10834=PLANE ( 'NONE',  #12989 ) ;
#10836=CARTESIAN_POINT ( 'NONE',  ( 0.7278995231378414532, 52.96529355253956339, 75.36169494263242541 ) ) ;
#10837=ORIENTED_EDGE ( 'NONE', *, *, #20250, .F. ) ;
#10838=CARTESIAN_POINT ( 'NONE',  ( 6.467647404187965243, 50.71089930605690910, 75.49932683761802821 ) ) ;
#10839=ADVANCED_FACE ( 'NONE', ( #9696 ), #19456, .F. ) ;
#10840=CARTESIAN_POINT ( 'NONE',  ( -0.001710212166300070519, 52.34625406315150542, 75.41767803229005551 ) ) ;
#10843=CARTESIAN_POINT ( 'NONE',  ( -4.151536175905484072, 36.67403323987894481, 75.43521673441158271 ) ) ;
#10844=EDGE_CURVE ( 'NONE', #2871, #18295, #8295, .T. ) ;
#10845=CARTESIAN_POINT ( 'NONE',  ( 5.807634474669838731, 51.19842427014940967, 79.54761434581399726 ) ) ;
#10847=CARTESIAN_POINT ( 'NONE',  ( 5.706854332355044690, 51.27286650160559134, 79.54768974400036541 ) ) ;
#10849=CARTESIAN_POINT ( 'NONE',  ( 8.392716226808454749, 39.94722745792154939, 76.30598982719874357 ) ) ;
#10850=CIRCLE ( 'NONE', #977, 8.199999999999995737 ) ;
#10853=CARTESIAN_POINT ( 'NONE',  ( -4.853788242550845844, 37.19275855307111556, 77.90854597583356167 ) ) ;
#10855=CARTESIAN_POINT ( 'NONE',  ( -4.588881395441816835, 37.74767372618060080, 79.54736998457485697 ) ) ;
#10857=FACE_OUTER_BOUND ( 'NONE', #19120, .T. ) ;
#10860=CARTESIAN_POINT ( 'NONE',  ( -5.667418469993653396, 43.80274312437727247, 82.45433879953087342 ) ) ;
#10861=CARTESIAN_POINT ( 'NONE',  ( 8.951691408152598228, 41.62251153713423690, 78.44085888008430629 ) ) ;
#10862=CARTESIAN_POINT ( 'NONE',  ( -0.9369880318669705499, 52.97987177264234049, 77.93056416558285093 ) ) ;
#10863=CARTESIAN_POINT ( 'NONE',  ( 0.3821786226492927541, 35.36301154328572949, 76.16022115247204738 ) ) ;
#10864=DIRECTION ( 'NONE',  ( 1.540237394707284220E-16, 1.793354297423764243E-16, -1.000000000000000000 ) ) ;
#10867=CARTESIAN_POINT ( 'NONE',  ( -8.170692237619920917, 42.45118346540571963, 79.33973788556694728 ) ) ;
#10868=CARTESIAN_POINT ( 'NONE',  ( 5.500237024828340537, 36.90356520980568433, 77.71779572520892998 ) ) ;
#10873=CARTESIAN_POINT ( 'NONE',  ( 0.3281727876805012878, 52.35988662561128137, 78.59782856811732188 ) ) ;
#10875=VECTOR ( 'NONE', #10586, 1000.000000000000227 ) ;
#10880=AXIS2_PLACEMENT_3D ( 'NONE', #13825, #7112, #10555 ) ;
#10882=CARTESIAN_POINT ( 'NONE',  ( 0.7879266358239551682, 52.35788869271873125, 78.84197803560836348 ) ) ;
#10883=ORIENTED_EDGE ( 'NONE', *, *, #4669, .F. ) ;
#10884=CARTESIAN_POINT ( 'NONE',  ( 5.936990147225109204, 51.10287444559717329, 77.01219674908871582 ) ) ;
#10885=AXIS2_PLACEMENT_3D ( 'NONE', #19230, #19139, #13070 ) ;
#10886=VERTEX_POINT ( 'NONE', #5444 ) ;
#10889=VERTEX_POINT ( 'NONE', #774 ) ;
#10895=CARTESIAN_POINT ( 'NONE',  ( 0.5221537403065008576, 44.16218137147968292, 80.45433879953087342 ) ) ;
#10896=CARTESIAN_POINT ( 'NONE',  ( 0.7248365744723396231, 52.96455768829495270, 75.99814205791308552 ) ) ;
#10897=CARTESIAN_POINT ( 'NONE',  ( 0.3821786226492926430, 35.36301154328572949, 76.86610350541323555 ) ) ;
#10898=ORIENTED_EDGE ( 'NONE', *, *, #8373, .T. ) ;
#10899=CARTESIAN_POINT ( 'NONE',  ( 0.5221537403065010796, 44.16218137147968292, 78.25433879953088478 ) ) ;
#10903=AXIS2_PLACEMENT_3D ( 'NONE', #14209, #17720, #1553 ) ;
#10907=CARTESIAN_POINT ( 'NONE',  ( 5.383107995780706645, 37.55798503218719020, 78.33046556645599878 ) ) ;
#10908=AXIS2_PLACEMENT_3D ( 'NONE', #19979, #16814, #3923 ) ;
#10909=ORIENTED_EDGE ( 'NONE', *, *, #2098, .F. ) ;
#10910=CARTESIAN_POINT ( 'NONE',  ( 8.246890682022526065, 41.41102172004362814, 76.01662778496600481 ) ) ;
#10912=CARTESIAN_POINT ( 'NONE',  ( -2.915357068909699478, 51.60185863777040538, 76.59793576264409865 ) ) ;
#10913=ADVANCED_FACE ( 'NONE', ( #8976 ), #20726, .T. ) ;
#10915=LINE ( 'NONE', #9519, #19328 ) ;
#10917=CARTESIAN_POINT ( 'NONE',  ( -5.048916887735209080, 50.07712348856472317, 79.26884812577799266 ) ) ;
#10920=CARTESIAN_POINT ( 'NONE',  ( -4.157944255866825145, 37.43340257241605684, 78.67445481091525039 ) ) ;
#10921=CARTESIAN_POINT ( 'NONE',  ( -4.244931195431495219, 50.82465379583177878, 78.93669174070734584 ) ) ;
#10924=CARTESIAN_POINT ( 'NONE',  ( -5.917125461193805336, 40.64525615903904310, 76.16022115247204738 ) ) ;
#10925=DIRECTION ( 'NONE',  ( -0.9534635866061452747, -0.3015081906286225522, -2.009271279954815797E-16 ) ) ;
#10926=VERTEX_POINT ( 'NONE', #3955 ) ;
#10927=PLANE ( 'NONE',  #909 ) ;
#10930=CARTESIAN_POINT ( 'NONE',  ( 5.074636438210348821, 37.34636204506070811, 76.67247627436783830 ) ) ;
#10933=CARTESIAN_POINT ( 'NONE',  ( -7.567930892892213102, 42.78490342736719754, 76.47044134360902490 ) ) ;
#10935=CARTESIAN_POINT ( 'NONE',  ( 2.118098838249972804, 52.81625338523218716, 77.70152060498777757 ) ) ;
#10936=ORIENTED_EDGE ( 'NONE', *, *, #13739, .F. ) ;
#10938=CARTESIAN_POINT ( 'NONE',  ( 5.494509650718089055, 37.64638807017929167, 77.47236191065434241 ) ) ;
#10940=CARTESIAN_POINT ( 'NONE',  ( -3.173569252698743348, 51.48240278743190146, 75.75534724892666816 ) ) ;
#10941=VERTEX_POINT ( 'NONE', #20121 ) ;
#10944=CARTESIAN_POINT ( 'NONE',  ( -3.096437231170314330, 36.81950709836767999, 76.12177974158937843 ) ) ;
#10945=CARTESIAN_POINT ( 'NONE',  ( 5.898472913175941024, 51.13132557482045826, 79.54598470662274678 ) ) ;
#10949=CARTESIAN_POINT ( 'NONE',  ( -7.723582874747324745, 47.23591325229828186, 77.58227997600145898 ) ) ;
#10951=ORIENTED_EDGE ( 'NONE', *, *, #9829, .F. ) ;
#10952=DIRECTION ( 'NONE',  ( -0.007885122365285377952, -0.9999689119394085113, -1.805443505845558427E-16 ) ) ;
#10953=CARTESIAN_POINT ( 'NONE',  ( -6.856111849776215017, 40.77524371008118464, 79.32598559883581402 ) ) ;
#10957=EDGE_CURVE ( 'NONE', #15270, #5478, #566, .T. ) ;
#10958=ADVANCED_FACE ( 'NONE', ( #10478 ), #17514, .F. ) ;
#10959=CARTESIAN_POINT ( 'NONE',  ( 5.655950003444441876, 37.76811099897118851, 78.37198585835440667 ) ) ;
#10963=LINE ( 'NONE', #1258, #2698 ) ;
#10968=CARTESIAN_POINT ( 'NONE',  ( 8.458367304687495647, 40.14398790315176058, 79.09910503406773330 ) ) ;
#10969=DIRECTION ( 'NONE',  ( -0.5941461771851693774, -0.8043570849667760481, -2.357623395011396791E-16 ) ) ;
#10970=ADVANCED_FACE ( 'NONE', ( #19368, #4479 ), #9395, .T. ) ;
#10974=CARTESIAN_POINT ( 'NONE',  ( 5.304793302263875354, 37.51082371353274425, 75.97198585835440099 ) ) ;
#10975=EDGE_LOOP ( 'NONE', ( #5887, #11094, #5960, #17051 ) ) ;
#10978=CARTESIAN_POINT ( 'NONE',  ( -4.032917313034308116, 50.98063674598317618, 76.36012575652569012 ) ) ;
#10979=CARTESIAN_POINT ( 'NONE',  ( 6.832223124813663340, 50.44160190723654580, 77.98033120372964788 ) ) ;
#10980=CIRCLE ( 'NONE', #13328, 8.199999999999995737 ) ;
#10983=LINE ( 'NONE', #3087, #20648 ) ;
#10984=CARTESIAN_POINT ( 'NONE',  ( 5.347338439526899023, 50.79239070589999727, 75.97314036218482158 ) ) ;
#10986=ADVANCED_FACE ( 'NONE', ( #2795 ), #15676, .T. ) ;
#10992=ORIENTED_EDGE ( 'NONE', *, *, #18444, .F. ) ;
#10996=DIRECTION ( 'NONE',  ( -1.540237394707284220E-16, -1.793354297423764243E-16, 1.000000000000000000 ) ) ;
#10998=CARTESIAN_POINT ( 'NONE',  ( 5.755371611800503828, 51.23702874167446453, 77.28963291717792572 ) ) ;
#11000=CARTESIAN_POINT ( 'NONE',  ( 0.8127483387853863261, 52.35242157994007783, 76.07424718102974737 ) ) ;
#11001=CARTESIAN_POINT ( 'NONE',  ( -3.632788261743048253, 37.20487005735590458, 79.44037905412795908 ) ) ;
#11003=CARTESIAN_POINT ( 'NONE',  ( 5.769916034762062829, 37.09626795672559041, 77.71701144737939160 ) ) ;
#11004=VECTOR ( 'NONE', #339, 1000.000000000000000 ) ;
#11005=ORIENTED_EDGE ( 'NONE', *, *, #20294, .T. ) ;
#11010=CARTESIAN_POINT ( 'NONE',  ( -7.357289765694363659, 41.91101321416308423, 78.82529883526802905 ) ) ;
#11015=CARTESIAN_POINT ( 'NONE',  ( -3.416741549526295163, 52.16336322705762996, 76.06019729239972094 ) ) ;
#11017=CARTESIAN_POINT ( 'NONE',  ( -7.108943275890691638, 41.53885404143057514, 78.28419725522122974 ) ) ;
#11020=CARTESIAN_POINT ( 'NONE',  ( -5.093619678490177272, 50.04518051096484754, 79.23104009678212378 ) ) ;
#11022=CARTESIAN_POINT ( 'NONE',  ( 6.761578195034432248, 37.80487342938723572, 78.00072712051441215 ) ) ;
#11023=CARTESIAN_POINT ( 'NONE',  ( -4.578222290571132724, 51.33341161403104280, 78.93596775356181183 ) ) ;
#11024=ORIENTED_EDGE ( 'NONE', *, *, #3532, .F. ) ;
#11025=DIRECTION ( 'NONE',  ( 1.540237394707284220E-16, 1.793354297423764243E-16, -1.000000000000000000 ) ) ;
#11027=ORIENTED_EDGE ( 'NONE', *, *, #16773, .F. ) ;
#11032=CARTESIAN_POINT ( 'NONE',  ( -3.652148518534826138, 36.30515569394113129, 77.93013364623398331 ) ) ;
#11033=CARTESIAN_POINT ( 'NONE',  ( 8.788905609664558582, 41.13463217212708400, 76.28640183395299346 ) ) ;
#11034=CARTESIAN_POINT ( 'NONE',  ( -3.457680572327287649, 37.08634300271093309, 77.67016408458685817 ) ) ;
#11035=ORIENTED_EDGE ( 'NONE', *, *, #8944, .T. ) ;
#11036=CARTESIAN_POINT ( 'NONE',  ( 2.114701336805660414, 52.20152096667261787, 78.26636343789274974 ) ) ;
#11037=CARTESIAN_POINT ( 'NONE',  ( 0.5221537403065010796, 44.16218137147968292, 78.13669174070733447 ) ) ;
#11038=ORIENTED_EDGE ( 'NONE', *, *, #2339, .T. ) ;
#11043=ORIENTED_EDGE ( 'NONE', *, *, #17021, .F. ) ;
#11044=EDGE_LOOP ( 'NONE', ( #20239, #19785, #13826, #3778 ) ) ;
#11046=CARTESIAN_POINT ( 'NONE',  ( -3.274807807204083154, 36.95126225767872796, 75.71473766112499959 ) ) ;
#11047=CARTESIAN_POINT ( 'NONE',  ( 8.333090968688148692, 41.66583349331221342, 78.92761653162175151 ) ) ;
#11049=ORIENTED_EDGE ( 'NONE', *, *, #11554, .F. ) ;
#11050=CARTESIAN_POINT ( 'NONE',  ( 6.545534159973747990, 50.65336749702785113, 77.68963291717794561 ) ) ;
#11054=CARTESIAN_POINT ( 'NONE',  ( 6.499036340715795390, 49.77623430136497262, 76.16185523003329649 ) ) ;
#11055=CARTESIAN_POINT ( 'NONE',  ( -7.121200219685121624, 41.61353638602459171, 79.54638463348854316 ) ) ;
#11056=CARTESIAN_POINT ( 'NONE',  ( -5.474757466566057218, 38.56948656142584753, 78.95744879387162030 ) ) ;
#11059=ADVANCED_FACE ( 'NONE', ( #8314 ), #13417, .F. ) ;
#11060=CARTESIAN_POINT ( 'NONE',  ( -5.838428831739582492, 50.43291415881836315, 76.76022115247205591 ) ) ;
#11063=CARTESIAN_POINT ( 'NONE',  ( 8.644901377098815232, 43.03925179711409754, 75.45433879953088763 ) ) ;
#11064=CARTESIAN_POINT ( 'NONE',  ( -0.1926216938105645149, 52.97400217050763160, 79.43762534667510522 ) ) ;
#11065=EDGE_LOOP ( 'NONE', ( #8573, #6042, #1561, #19061, #8780, #10378, #20848, #2068, #2670, #362, #12449, #3504, #1101 ) ) ;
#11066=CARTESIAN_POINT ( 'NONE',  ( -4.176781812633367785, 37.44206058802408421, 76.15041543488503351 ) ) ;
#11067=DIRECTION ( 'NONE',  ( 0.3165065846431829311, 0.9485903129789527988, 2.188653791613874255E-16 ) ) ;
#11069=CARTESIAN_POINT ( 'NONE',  ( -7.320717484398829633, 46.55579181444844750, 79.45433879953087342 ) ) ;
#11071=EDGE_CURVE ( 'NONE', #8686, #1769, #2030, .T. ) ;
#11073=EDGE_CURVE ( 'NONE', #17248, #17173, #20709, .T. ) ;
#11074=ORIENTED_EDGE ( 'NONE', *, *, #6101, .T. ) ;
#11075=PRODUCT_DEFINITION ( 'UNKNOWN', '', #5461, #14852 ) ;
#11077=CARTESIAN_POINT ( 'NONE',  ( -3.874372605692205873, 36.46930367539203388, 79.33401574558745040 ) ) ;
#11082=CARTESIAN_POINT ( 'NONE',  ( 8.869748494521283888, 41.37692342661967615, 77.52492703482499792 ) ) ;
#11083=CARTESIAN_POINT ( 'NONE',  ( 6.489427164124363046, 49.76997852774753994, 77.12327887040382279 ) ) ;
#11084=LINE ( 'NONE', #16073, #6722 ) ;
#11085=CARTESIAN_POINT ( 'NONE',  ( 5.245347708343344628, 50.86538805717837874, 76.02658503615866437 ) ) ;
#11086=VERTEX_POINT ( 'NONE', #6489 ) ;
#11089=CARTESIAN_POINT ( 'NONE',  ( -3.055718635266669647, 36.78391400955043622, 76.62933879953087057 ) ) ;
#11090=ORIENTED_EDGE ( 'NONE', *, *, #5472, .T. ) ;
#11092=EDGE_CURVE ( 'NONE', #4079, #12581, #925, .T. ) ;
#11094=ORIENTED_EDGE ( 'NONE', *, *, #7976, .F. ) ;
#11095=DIRECTION ( 'NONE',  ( -1.540237394707283727E-16, -1.793354297423763257E-16, 1.000000000000000000 ) ) ;
#11096=CARTESIAN_POINT ( 'NONE',  ( -0.8472276979131061481, 52.97793871905674479, 76.01337353251631157 ) ) ;
#11097=DIRECTION ( 'NONE',  ( -0.5941461771851691553, -0.8043570849667760481, -2.357623395011396791E-16 ) ) ;
#11099=CARTESIAN_POINT ( 'NONE',  ( 0.8431453059911918624, 52.96362478046774669, 76.16511824318942558 ) ) ;
#11100=EDGE_CURVE ( 'NONE', #8246, #13387, #2185, .T. ) ;
#11102=ORIENTED_EDGE ( 'NONE', *, *, #2390, .F. ) ;
#11103=DIRECTION ( 'NONE',  ( -1.540237394707284220E-16, -1.793354297423764243E-16, 1.000000000000000000 ) ) ;
#11104=VERTEX_POINT ( 'NONE', #20096 ) ;
#11105=DIRECTION ( 'NONE',  ( -0.009567942452863074584, 0.9999542261909885044, 1.778535306010356147E-16 ) ) ;
#11107=CARTESIAN_POINT ( 'NONE',  ( 0.5186725038864670179, 52.36221944467538947, 75.97427063642290079 ) ) ;
#11108=B_SPLINE_CURVE_WITH_KNOTS ( 'NONE', 3,
 ( #20432, #7344, #4250, #5749, #17037, #13735, #17240, #13836, #8957, #20535, #13950, #20315, #2563, #966, #12258 ),
 .UNSPECIFIED., .F., .F.,
 ( 4, 1, 1, 1, 1, 1, 1, 1, 1, 1, 1, 1, 4 ),
 ( 0.000000000000000000, 0.1267531625455885769, 0.2402085644777646467, 0.3404273024139109483, 0.4286057740769950719, 0.5026654758471001960, 0.5652545264784208934, 0.6141369997546152204, 0.6524264903941315863, 0.7200380101346053330, 0.7961149349448265466, 0.8886173437222998350, 0.9999999999999998890 ),
 .UNSPECIFIED. ) ;
#11110=CARTESIAN_POINT ( 'NONE',  ( -7.876934599565286632, 41.52403546573567183, 78.93589458924091673 ) ) ;
#11113=VERTEX_POINT ( 'NONE', #15437 ) ;
#11115=CARTESIAN_POINT ( 'NONE',  ( -3.013002030064880987, 51.53208512353911175, 75.97742918362793318 ) ) ;
#11117=CARTESIAN_POINT ( 'NONE',  ( -7.090928860711239068, 41.48188680325438327, 78.43135113490271237 ) ) ;
#11119=CARTESIAN_POINT ( 'NONE',  ( -5.838428831739585156, 50.43291415881836315, 78.10580938776615767 ) ) ;
#11120=CARTESIAN_POINT ( 'NONE',  ( 6.539349088566551949, 37.64607664623218142, 78.24541959536460922 ) ) ;
#11126=ORIENTED_EDGE ( 'NONE', *, *, #9829, .T. ) ;
#11127=CARTESIAN_POINT ( 'NONE',  ( 4.751063331615088536, 51.97887081224218520, 77.86982703766624070 ) ) ;
#11129=LINE ( 'NONE', #3141, #19035 ) ;
#11131=AXIS2_PLACEMENT_3D ( 'NONE', #13654, #2059, #18227 ) ;
#11132=B_SPLINE_CURVE_WITH_KNOTS ( 'NONE', 3,
 ( #16855, #11759, #5458, #14832, #2273, #6740, #7160, #13662, #13350, #8455, #249, #6319, #13141, #20990, #8140, #2204, #20271, #16991, #12209, #18692, #2528, #15185, #601, #13583, #13900, #20385, #20064 ),
 .UNSPECIFIED., .F., .F.,
 ( 4, 1, 1, 1, 1, 1, 1, 1, 1, 1, 1, 1, 1, 1, 1, 1, 1, 1, 1, 1, 1, 1, 1, 1, 4 ),
 ( 0.000000000000000000, 0.04692756115915790172, 0.09175764483083305445, 0.1348320239538815524, 0.1755606184341063081, 0.2149124488236470176, 0.2520401868719510108, 0.2875439711136699161, 0.3211732624427411364, 0.3845494416143411254, 0.4434775415870848558, 0.4991878644837567380, 0.5522905917841786083, 0.6030460594100006677, 0.6509449284921694501, 0.6968976034913704209, 0.7406443924834601455, 0.7634319837341128068, 0.7890572409307390345, 0.8171397283500007047, 0.8480511511928767732, 0.8815178987434894031, 0.9182285974223420855, 0.9576130192529551666, 1.000000000000000000 ),
 .UNSPECIFIED. ) ;
#11133=CARTESIAN_POINT ( 'NONE',  ( 5.075898477934015496, 37.34726385244101721, 76.52220546472133833 ) ) ;
#11134=CARTESIAN_POINT ( 'NONE',  ( 8.207311740369052089, 47.02196222218739763, 75.43669174070734584 ) ) ;
#11135=CARTESIAN_POINT ( 'NONE',  ( -3.053961058146955398, 36.78813166039994798, 76.77671532909576513 ) ) ;
#11137=CARTESIAN_POINT ( 'NONE',  ( 2.089542904467925677, 52.95439430598839436, 78.73916595950259989 ) ) ;
#11138=VERTEX_POINT ( 'NONE', #2456 ) ;
#11139=CARTESIAN_POINT ( 'NONE',  ( -8.190409139795066906, 42.92474528817020740, 76.06610350541322418 ) ) ;
#11140=DIRECTION ( 'NONE',  ( 0.3165065846431827645, 0.9485903129789529098, 0.000000000000000000 ) ) ;
#11141=CARTESIAN_POINT ( 'NONE',  ( 9.263154249150899133, 42.55598543044034443, 79.20437336408532758 ) ) ;
#11142=CARTESIAN_POINT ( 'NONE',  ( 8.097263698133225773, 41.42615553683592111, 79.54516904849367620 ) ) ;
#11143=VERTEX_POINT ( 'NONE', #7338 ) ;
#11145=ORIENTED_EDGE ( 'NONE', *, *, #13409, .F. ) ;
#11147=CARTESIAN_POINT ( 'NONE',  ( -3.560029042603979565, 37.16194369485645410, 75.49480657079904233 ) ) ;
#11148=CARTESIAN_POINT ( 'NONE',  ( -4.718161399584269056, 37.09257646755418847, 75.97198585835440099 ) ) ;
#11150=ORIENTED_EDGE ( 'NONE', *, *, #13298, .F. ) ;
#11151=CARTESIAN_POINT ( 'NONE',  ( -4.686954935604244810, 37.06952550968518523, 77.27854074750605662 ) ) ;
#11152=CARTESIAN_POINT ( 'NONE',  ( 8.791848479292760032, 41.14345213909496835, 77.32915800260404637 ) ) ;
#11155=CARTESIAN_POINT ( 'NONE',  ( 8.550006361060139781, 45.88717064157471270, 78.74480812004853192 ) ) ;
#11162=CARTESIAN_POINT ( 'NONE',  ( 0.3498111802063197939, 52.96792241217284669, 77.07502437766733294 ) ) ;
#11163=B_SPLINE_CURVE_WITH_KNOTS ( 'NONE', 3,
 ( #4116, #16896, #12332, #4224, #5715, #1049, #830, #20073, #8814, #2430, #17114, #12021, #10646, #10750, #14023, #18814 ),
 .UNSPECIFIED., .F., .F.,
 ( 4, 2, 2, 2, 2, 2, 2, 4 ),
 ( 0.000000000000000000, 0.0002724318156510209619, 0.0005448636313020419238, 0.001089727262604055225, 0.001362159078255057105, 0.001634590893906058984, 0.001907022709557060864, 0.002179454525208062744 ),
 .UNSPECIFIED. ) ;
#11164=CARTESIAN_POINT ( 'NONE',  ( 0.5221537403065019678, 44.16218137147968292, 72.45433879953087342 ) ) ;
#11165=CARTESIAN_POINT ( 'NONE',  ( -0.9143118842621357212, 52.21725223193028853, 78.68934297065942474 ) ) ;
#11169=CARTESIAN_POINT ( 'NONE',  ( 0.6854345734903630749, 52.36071088544267127, 75.98019728166023867 ) ) ;
#11170=CARTESIAN_POINT ( 'NONE',  ( 1.328797878535935784, 52.92566332880988966, 79.46664029610046498 ) ) ;
#11175=CARTESIAN_POINT ( 'NONE',  ( 9.317552545512265638, 42.71902057559893962, 75.91044101036179370 ) ) ;
#11176=CARTESIAN_POINT ( 'NONE',  ( 2.337612517491833852, 49.93701999136722947, 72.45433879953087342 ) ) ;
#11177=CARTESIAN_POINT ( 'NONE',  ( 6.873747143562635387, 50.41092978727617435, 78.08828162113617566 ) ) ;
#11179=ADVANCED_FACE ( 'NONE', ( #20202 ), #9092, .F. ) ;
#11180=DIRECTION ( 'NONE',  ( -1.540237394707283727E-16, -1.793354297423763257E-16, 1.000000000000000000 ) ) ;
#11181=DIRECTION ( 'NONE',  ( 0.3014524538335020543, -0.9532873293559830374, -0.01922721423134257299 ) ) ;
#11182=CARTESIAN_POINT ( 'NONE',  ( 6.295211134694258526, 49.91343808518868741, 77.55733179791843668 ) ) ;
#11184=ADVANCED_FACE ( 'NONE', ( #17028 ), #18298, .T. ) ;
#11185=VECTOR ( 'NONE', #10801, 1000.000000000000114 ) ;
#11186=CARTESIAN_POINT ( 'NONE',  ( -4.877143884790711148, 38.14601692126417731, 79.49842882144521639 ) ) ;
#11187=CARTESIAN_POINT ( 'NONE',  ( 0.7560837815594079192, 52.35885938535841433, 78.87528329032154772 ) ) ;
#11189=CARTESIAN_POINT ( 'NONE',  ( -3.156842967632347730, 36.83372846983282045, 77.40205577532607606 ) ) ;
#11191=DIRECTION ( 'NONE',  ( 0.9485903129789495791, -0.3165065846431930341, 8.934458285744763183E-17 ) ) ;
#11192=CARTESIAN_POINT ( 'NONE',  ( 8.848467398349676216, 41.31314263134580500, 75.36050707951255845 ) ) ;
#11195=CARTESIAN_POINT ( 'NONE',  ( 6.882736312352589536, 37.89144858414100270, 76.69330938776616335 ) ) ;
#11196=CARTESIAN_POINT ( 'NONE',  ( 8.985665979147935190, 41.72433548171385098, 78.13399373581940210 ) ) ;
#11198=DIRECTION ( 'NONE',  ( -0.5813877811927011807, 0.8136266022444372803, 5.636455622144619183E-17 ) ) ;
#11200=CARTESIAN_POINT ( 'NONE',  ( 5.544276951911417228, 50.64433212932689088, 72.45433879953087342 ) ) ;
#11201=AXIS2_PLACEMENT_3D ( 'NONE', #18714, #2649, #7215 ) ;
#11204=EDGE_CURVE ( 'NONE', #17246, #5430, #2139, .T. ) ;
#11207=CARTESIAN_POINT ( 'NONE',  ( -7.367656984315425817, 48.05973018190410073, 78.78375056423675460 ) ) ;
#11210=FACE_OUTER_BOUND ( 'NONE', #2840, .T. ) ;
#11212=ORIENTED_EDGE ( 'NONE', *, *, #13910, .F. ) ;
#11214=CARTESIAN_POINT ( 'NONE',  ( 4.890314246961300348, 51.87601177044496836, 77.76130678786321937 ) ) ;
#11217=VECTOR ( 'NONE', #15067, 1000.000000000000000 ) ;
#11218=CARTESIAN_POINT ( 'NONE',  ( -3.448085832972781262, 52.14096574969422448, 75.97742918362793318 ) ) ;
#11221=CARTESIAN_POINT ( 'NONE',  ( -7.789419058798823237, 41.24013430743122655, 78.49688471925094291 ) ) ;
#11222=VERTEX_POINT ( 'NONE', #11933 ) ;
#11223=CARTESIAN_POINT ( 'NONE',  ( 1.369964938772391561, 52.31939965602356324, 76.79052535208408869 ) ) ;
#11224=CARTESIAN_POINT ( 'NONE',  ( 5.202885763635528349, 50.89499265101085967, 76.90580938776616904 ) ) ;
#11225=CARTESIAN_POINT ( 'NONE',  ( 4.643940233704298315, 36.29168687389493897, 75.71841013695411959 ) ) ;
#11228=ORIENTED_EDGE ( 'NONE', *, *, #19507, .F. ) ;
#11229=VECTOR ( 'NONE', #1437, 1000.000000000000227 ) ;
#11230=CARTESIAN_POINT ( 'NONE',  ( 6.691294758883309157, 37.75465145915448062, 79.45433879953087342 ) ) ;
#11231=VECTOR ( 'NONE', #9207, 1000.000000000000114 ) ;
#11232=FACE_OUTER_BOUND ( 'NONE', #7191, .T. ) ;
#11233=VERTEX_POINT ( 'NONE', #18410 ) ;
#11234=CARTESIAN_POINT ( 'NONE',  ( 4.791956560326987358, 51.94866463147243962, 77.83360891957636341 ) ) ;
#11237=CARTESIAN_POINT ( 'NONE',  ( 5.848951923618479931, 37.15274410921379911, 77.37492703482499223 ) ) ;
#11242=CARTESIAN_POINT ( 'NONE',  ( 5.889143815203415677, 51.13821660369377753, 76.04053158567903381 ) ) ;
#11244=EDGE_CURVE ( 'NONE', #18543, #19191, #3829, .T. ) ;
#11245=CARTESIAN_POINT ( 'NONE',  ( 2.111809426605781859, 52.81745860575872342, 77.55799709713352286 ) ) ;
#11247=ORIENTED_EDGE ( 'NONE', *, *, #6604, .F. ) ;
#11248=PLANE ( 'NONE',  #10903 ) ;
#11249=CARTESIAN_POINT ( 'NONE',  ( -5.835824771109036746, 39.98772221508849611, 75.45433879953087342 ) ) ;
#11251=B_SPLINE_SURFACE_WITH_KNOTS ( 'NONE', 3, 1, ( 
 ( #2387, #7050 ),
 ( #18449, #15376 ),
 ( #7491, #8674 ),
 ( #10603, #13551 ),
 ( #16958, #684 ),
 ( #20029, #20463 ),
 ( #790, #12179 ),
 ( #15155, #7271 ),
 ( #5460, #18772 ),
 ( #7163, #568 ),
 ( #20136, #5571 ),
 ( #10388, #4187 ),
 ( #13766, #2499 ),
 ( #8991, #16857 ),
 ( #890, #12394 ) ),
 .UNSPECIFIED., .F., .F., .F.,
 ( 4, 1, 1, 1, 1, 1, 1, 1, 1, 1, 1, 1, 4 ),
 ( 2, 2 ),
 ( 0.000000000000000000, 0.07527217715292475186, 0.1459465445934834404, 0.2117756949130734923, 0.2766029815265222958, 0.3381147468631120478, 0.3951637252042238257, 0.4534551218168583753, 0.5124046679576552688, 0.5890284689491043224, 0.6947781202056673155, 0.8321371544603952675, 0.9999999999999998890 ),
 ( 0.000000000000000000, 1.000000000000000000 ),
 .UNSPECIFIED. ) ;
#11252=CARTESIAN_POINT ( 'NONE',  ( 7.928945443998646425, 40.92169505128364904, 79.45050910333212357 ) ) ;
#11254=CARTESIAN_POINT ( 'NONE',  ( 5.709672981839667649, 51.27078447877342882, 77.95044976498417100 ) ) ;
#11256=CIRCLE ( 'NONE', #17688, 6.200000000000000178 ) ;
#11257=CARTESIAN_POINT ( 'NONE',  ( -7.896563877726270775, 41.59953023782934878, 78.92964143347573724 ) ) ;
#11258=DIRECTION ( 'NONE',  ( 1.540237394707284220E-16, 1.793354297423764243E-16, -1.000000000000000000 ) ) ;
#11259=CARTESIAN_POINT ( 'NONE',  ( -6.721143750142749340, 40.31838871648160705, 78.26846280200385308 ) ) ;
#11260=EDGE_LOOP ( 'NONE', ( #19999, #11422, #6325, #6644 ) ) ;
#11261=CARTESIAN_POINT ( 'NONE',  ( -4.159002695544564254, 37.45430957594182786, 77.01245883157920957 ) ) ;
#11262=CARTESIAN_POINT ( 'NONE',  ( -6.920047200808406629, 40.71838479833773050, 79.30581651637976393 ) ) ;
#11266=CARTESIAN_POINT ( 'NONE',  ( 5.457062992516449107, 50.71104673348453673, 78.93032258866925588 ) ) ;
#11267=CARTESIAN_POINT ( 'NONE',  ( 6.375360725391126415, 38.41906761359206968, 75.91875917877068503 ) ) ;
#11269=EDGE_CURVE ( 'NONE', #19301, #11113, #12041, .T. ) ;
#11270=CARTESIAN_POINT ( 'NONE',  ( -2.939085670389443905, 51.59587639763223166, 72.45433879953087342 ) ) ;
#11271=CARTESIAN_POINT ( 'NONE',  ( 0.4452092196042181649, 52.34431542127848047, 76.95466777776533718 ) ) ;
#11276=CARTESIAN_POINT ( 'NONE',  ( 9.351996896326966180, 42.82225248009945773, 76.45750776978282204 ) ) ;
#11277=CARTESIAN_POINT ( 'NONE',  ( 0.8438208634514194895, 52.35586981924091532, 76.28587743965509560 ) ) ;
#11280=ORIENTED_EDGE ( 'NONE', *, *, #18743, .T. ) ;
#11282=EDGE_CURVE ( 'NONE', #6129, #15829, #10454, .T. ) ;
#11284=CARTESIAN_POINT ( 'NONE',  ( -4.463792963332828378, 40.72925446781975722, 72.45432679953087529 ) ) ;
#11285=CARTESIAN_POINT ( 'NONE',  ( 6.903329084842819263, 50.38907879888579089, 78.20944795639196911 ) ) ;
#11287=CARTESIAN_POINT ( 'NONE',  ( -3.147842262194972207, 36.82924344237826375, 75.96820239334293490 ) ) ;
#11289=FACE_OUTER_BOUND ( 'NONE', #11380, .T. ) ;
#11290=DIRECTION ( 'NONE',  ( -0.007885122365275663500, -0.9999689119394085113, -1.805443505845543142E-16 ) ) ;
#11291=CARTESIAN_POINT ( 'NONE',  ( 0.3201111382462866750, 51.36399839264385037, 77.76169174070734869 ) ) ;
#11293=EDGE_CURVE ( 'NONE', #20036, #2288, #14837, .T. ) ;
#11297=ORIENTED_EDGE ( 'NONE', *, *, #10316, .F. ) ;
#11299=CARTESIAN_POINT ( 'NONE',  ( 5.831313177393474767, 37.14014010695713353, 78.35708441643889444 ) ) ;
#11303=CARTESIAN_POINT ( 'NONE',  ( 9.054037327392332912, 41.92924874979977545, 78.13567616980381558 ) ) ;
#11304=VERTEX_POINT ( 'NONE', #7661 ) ;
#11305=CARTESIAN_POINT ( 'NONE',  ( -0.4710197511697722383, 52.21577876075154734, 75.60318094692254931 ) ) ;
#11306=CARTESIAN_POINT ( 'NONE',  ( 0.07355455234133151388, 52.20946254203077075, 79.50648293536016809 ) ) ;
#11307=CARTESIAN_POINT ( 'NONE',  ( 2.246318977524931260, 38.35943151540528362, 72.45433879953087342 ) ) ;
#11309=CARTESIAN_POINT ( 'NONE',  ( 8.869748494521283888, 41.37692342661967615, 77.52492703482499792 ) ) ;
#11311=CARTESIAN_POINT ( 'NONE',  ( 8.374986225289852371, 41.81414519758808979, 76.31823237213514233 ) ) ;
#11312=EDGE_LOOP ( 'NONE', ( #15078, #16937, #4863, #4032, #19702, #14946, #4291, #9520, #15619, #9367, #9448, #11435 ) ) ;
#11315=CARTESIAN_POINT ( 'NONE',  ( -4.211488180634966660, 48.16625856408043660, 80.45433879953087342 ) ) ;
#11318=CARTESIAN_POINT ( 'NONE',  ( -4.792503378000012582, 37.91763016944491227, 77.33669174070733732 ) ) ;
#11319=ORIENTED_EDGE ( 'NONE', *, *, #1680, .F. ) ;
#11320=CARTESIAN_POINT ( 'NONE',  ( 5.211422077973618450, 50.88905158406131335, 77.07967726685606635 ) ) ;
#11323=LINE ( 'NONE', #12907, #18746 ) ;
#11325=ORIENTED_EDGE ( 'NONE', *, *, #20402, .F. ) ;
#11326=EDGE_CURVE ( 'NONE', #26, #3490, #6206, .T. ) ;
#11328=EDGE_CURVE ( 'NONE', #5035, #17146, #20723, .T. ) ;
#11329=CARTESIAN_POINT ( 'NONE',  ( -4.859530362865108977, 37.19700002604054134, 79.54807357191100436 ) ) ;
#11332=FACE_OUTER_BOUND ( 'NONE', #18567, .T. ) ;
#11334=DIRECTION ( 'NONE',  ( 1.540237394707283727E-16, 1.793354297423763257E-16, -1.000000000000000000 ) ) ;
#11336=FACE_OUTER_BOUND ( 'NONE', #18351, .T. ) ;
#11337=DIRECTION ( 'NONE',  ( 0.3015081906286223301, -0.9534635866061452747, -1.245503830460468587E-16 ) ) ;
#11339=FACE_OUTER_BOUND ( 'NONE', #11312, .T. ) ;
#11341=EDGE_CURVE ( 'NONE', #16624, #8340, #2967, .T. ) ;
#11343=CARTESIAN_POINT ( 'NONE',  ( -5.782670150369643380, 50.47275727106970322, 76.07566230427023868 ) ) ;
#11345=LINE ( 'NONE', #13240, #13715 ) ;
#11349=EDGE_LOOP ( 'NONE', ( #16403, #18668, #6275, #5046 ) ) ;
#11350=CARTESIAN_POINT ( 'NONE',  ( 1.937197196555007661, 52.84783582409303193, 77.09277561753447117 ) ) ;
#11353=CARTESIAN_POINT ( 'NONE',  ( -7.783793320189392517, 41.25506035324961829, 78.45492795665607844 ) ) ;
#11357=CARTESIAN_POINT ( 'NONE',  ( 5.605612954821764582, 51.34764942893797013, 78.13212606300182017 ) ) ;
#11358=CARTESIAN_POINT ( 'NONE',  ( -7.762578640187608237, 47.15103685007025547, 79.11815246340434271 ) ) ;
#11360=DIRECTION ( 'NONE',  ( -0.3165065846431824870, -0.9485903129789529098, 0.000000000000000000 ) ) ;
#11361=CARTESIAN_POINT ( 'NONE',  ( 8.378637954445377289, 41.81363803720061867, 78.41904468188381827 ) ) ;
#11363=ORIENTED_EDGE ( 'NONE', *, *, #17674, .T. ) ;
#11364=FACE_OUTER_BOUND ( 'NONE', #16957, .T. ) ;
#11366=CARTESIAN_POINT ( 'NONE',  ( 8.869748494521283888, 41.37692342661967615, 77.52492703482499792 ) ) ;
#11369=EDGE_LOOP ( 'NONE', ( #19188, #16166, #11930, #5226, #10141, #19430, #19695 ) ) ;
#11370=DIRECTION ( 'NONE',  ( 0.9999689119394086223, -0.007885122365275665235, 1.526048693634353392E-16 ) ) ;
#11372=CARTESIAN_POINT ( 'NONE',  ( -5.507377839757669591, 38.60475994759722340, 78.70824393732894464 ) ) ;
#11373=ADVANCED_FACE ( 'NONE', ( #7974 ), #4241, .T. ) ;
#11374=CARTESIAN_POINT ( 'NONE',  ( -5.754662135367683895, 50.49277077315122142, 75.98690818113186651 ) ) ;
#11375=CARTESIAN_POINT ( 'NONE',  ( -4.532425740520046986, 37.70530639010522833, 76.20224062571769252 ) ) ;
#11376=B_SPLINE_CURVE_WITH_KNOTS ( 'NONE', 3,
 ( #12354, #958, #15540, #20831, #15760, #20722, #7660, #1175, #14138, #9371, #4455, #2556 ),
 .UNSPECIFIED., .F., .F.,
 ( 4, 2, 2, 2, 2, 4 ),
 ( 0.000000000000000000, 7.773291567551462685E-05, 0.0001554658313510292537, 0.0003109316627020570437, 0.0004663974940530848609, 0.0006218633254041125696 ),
 .UNSPECIFIED. ) ;
#11377=DIRECTION ( 'NONE',  ( 0.3165065846431826535, 0.9485903129789529098, 2.188653791613874008E-16 ) ) ;
#11378=CARTESIAN_POINT ( 'NONE',  ( 4.432284427945813121, 36.14044538431356557, 77.43080938776617472 ) ) ;
#11379=CARTESIAN_POINT ( 'NONE',  ( 8.436128353966983795, 40.07733635702963682, 79.00897045670630803 ) ) ;
#11380=EDGE_LOOP ( 'NONE', ( #906, #20567, #16500, #19970 ) ) ;
#11382=PLANE ( 'NONE',  #18749 ) ;
#11383=CARTESIAN_POINT ( 'NONE',  ( 0.5867509473165513079, 52.35421642379875351, 77.38375056423674891 ) ) ;
#11385=ORIENTED_EDGE ( 'NONE', *, *, #5029, .F. ) ;
#11386=EDGE_LOOP ( 'NONE', ( #1304, #12794, #16788, #15799 ) ) ;
#11388=FACE_OUTER_BOUND ( 'NONE', #5493, .T. ) ;
#11394=DIRECTION ( 'NONE',  ( 0.3165065846431826535, 0.9485903129789529098, 2.188653791613874008E-16 ) ) ;
#11395=CARTESIAN_POINT ( 'NONE',  ( -3.860974883312077832, 38.44857360937989199, 79.54845644658969661 ) ) ;
#11400=ADVANCED_FACE ( 'NONE', ( #13080 ), #6466, .T. ) ;
#11401=VERTEX_POINT ( 'NONE', #14460 ) ;
#11402=DIRECTION ( 'NONE',  ( 0.007885122365275663500, 0.9999689119394085113, 1.805443505845543142E-16 ) ) ;
#11403=CARTESIAN_POINT ( 'NONE',  ( 5.242046259730475555, 50.86759873786404285, 78.66925348396956963 ) ) ;
#11404=CARTESIAN_POINT ( 'NONE',  ( 8.907015937602837496, 41.48861631773759484, 77.50814924735175282 ) ) ;
#11405=CARTESIAN_POINT ( 'NONE',  ( 9.333517871656532350, 42.76686967087471913, 77.60952670463396430 ) ) ;
#11407=CARTESIAN_POINT ( 'NONE',  ( 6.268485860042931179, 37.45252770006494103, 75.44618574453703275 ) ) ;
#11408=CARTESIAN_POINT ( 'NONE',  ( 0.4030602640235012579, 52.96930499935337622, 79.54130260543404063 ) ) ;
#11409=CARTESIAN_POINT ( 'NONE',  ( 8.095534471974675128, 41.01620876067410393, 79.49089192870339105 ) ) ;
#11410=CARTESIAN_POINT ( 'NONE',  ( 4.178324861372344934, 51.50200996931119590, 75.94208404623037723 ) ) ;
#11411=FACE_OUTER_BOUND ( 'NONE', #3854, .T. ) ;
#11413=CARTESIAN_POINT ( 'NONE',  ( 0.3201111382462865640, 51.36399839264385037, 78.50066232894263862 ) ) ;
#11417=CARTESIAN_POINT ( 'NONE',  ( -3.532917577324402369, 36.21708460058427193, 78.46683879953087626 ) ) ;
#11419=EDGE_CURVE ( 'NONE', #13402, #585, #10004, .T. ) ;
#11421=CARTESIAN_POINT ( 'NONE',  ( 5.622879012935364962, 37.74899935393362682, 78.37107466246847309 ) ) ;
#11422=ORIENTED_EDGE ( 'NONE', *, *, #11204, .T. ) ;
#11423=CARTESIAN_POINT ( 'NONE',  ( -4.519095118814111522, 36.94553422482819371, 76.36459416792565946 ) ) ;
#11425=CARTESIAN_POINT ( 'NONE',  ( -7.723582874747324745, 47.23591325229828186, 77.58227997600145898 ) ) ;
#11429=CARTESIAN_POINT ( 'NONE',  ( 1.979752811602338181, 52.23166353794246675, 77.14917161731061412 ) ) ;
#11431=CARTESIAN_POINT ( 'NONE',  ( 5.913630530257057316, 51.12012925366870064, 76.09715583564816654 ) ) ;
#11433=CARTESIAN_POINT ( 'NONE',  ( -3.349688636638950889, 52.21127678364309332, 78.10580938776615767 ) ) ;
#11435=ORIENTED_EDGE ( 'NONE', *, *, #20141, .F. ) ;
#11436=CARTESIAN_POINT ( 'NONE',  ( -4.448383556050954368, 51.42618962001968441, 76.01002907825849775 ) ) ;
#11440=CARTESIAN_POINT ( 'NONE',  ( -7.555311451759470387, 40.50225460051125026, 77.45762758118813451 ) ) ;
#11441=CARTESIAN_POINT ( 'NONE',  ( -4.355629557941309571, 50.57269264884984494, 75.36324311589748959 ) ) ;
#11444=ADVANCED_FACE ( 'NONE', ( #8073 ), #4758, .T. ) ;
#11449=VECTOR ( 'NONE', #4866, 1000.000000000000000 ) ;
#11450=CARTESIAN_POINT ( 'NONE',  ( 5.468950880928916014, 50.69396025583560572, 75.98827401121828018 ) ) ;
#11453=VERTEX_POINT ( 'NONE', #12861 ) ;
#11454=CARTESIAN_POINT ( 'NONE',  ( -7.919272757704022503, 41.67135357887591596, 77.69952636542143409 ) ) ;
#11457=LINE ( 'NONE', #19205, #19101 ) ;
#11458=ORIENTED_EDGE ( 'NONE', *, *, #487, .T. ) ;
#11459=B_SPLINE_CURVE_WITH_KNOTS ( 'NONE', 3,
 ( #1230, #7515, #912, #18995, #7401, #4307, #4208, #6114, #13890, #10733, #20375, #9117, #2618, #15606, #5919, #12416, #18895, #10832, #17296 ),
 .UNSPECIFIED., .F., .F.,
 ( 4, 1, 1, 1, 1, 1, 1, 1, 1, 1, 1, 1, 1, 1, 1, 1, 4 ),
 ( 0.000000000000000000, 0.1068357064626556524, 0.2062857352809531475, 0.2975635024103033266, 0.3806658168942347320, 0.4556695234475648948, 0.5225582867794639208, 0.5822950421180911329, 0.6340416422721021350, 0.6795378779249960921, 0.7218021178892558565, 0.7627433693661896941, 0.8042009657065650741, 0.8472253578321278233, 0.8932235139329930407, 0.9440217631200717996, 0.9999999999999998890 ),
 .UNSPECIFIED. ) ;
#11460=PLANE ( 'NONE',  #3735 ) ;
#11461=CARTESIAN_POINT ( 'NONE',  ( -4.756616962678589466, 37.12098204292738757, 75.36046818803191627 ) ) ;
#11464=DIRECTION ( 'NONE',  ( 1.540237394707284220E-16, 1.793354297423764243E-16, -1.000000000000000000 ) ) ;
#11467=VERTEX_POINT ( 'NONE', #6574 ) ;
#11469=CARTESIAN_POINT ( 'NONE',  ( -4.238691248938474487, 37.51317230028318050, 77.97288938838477179 ) ) ;
#11471=CARTESIAN_POINT ( 'NONE',  ( 5.520808673089612206, 50.66245348763631284, 78.85200372869584839 ) ) ;
#11472=CARTESIAN_POINT ( 'NONE',  ( 1.925877929012052903, 52.84973764076755032, 75.80025412519856332 ) ) ;
#11474=CARTESIAN_POINT ( 'NONE',  ( 6.375754489315274220, 49.85394395361436892, 75.81347835631012799 ) ) ;
#11475=CARTESIAN_POINT ( 'NONE',  ( 0.9565776152847129676, 52.96313783584191270, 76.77464780632124075 ) ) ;
#11476=ADVANCED_FACE ( 'NONE', ( #8392 ), #7487, .T. ) ;
#11477=CARTESIAN_POINT ( 'NONE',  ( 4.766132218518882802, 37.29877637478772812, 75.41205140984322952 ) ) ;
#11478=B_SPLINE_CURVE_WITH_KNOTS ( 'NONE', 3,
 ( #7999, #14591, #119, #9927, #12888, #5210, #8419, #216, #18200, #19790, #3620, #1730, #17, #6492, #13001 ),
 .UNSPECIFIED., .F., .F.,
 ( 4, 1, 1, 1, 1, 1, 1, 1, 1, 1, 1, 1, 4 ),
 ( 0.000000000000000000, 0.1142047618744220089, 0.2098279651953024738, 0.2930641324527410441, 0.3714084400245239448, 0.4142179382887971051, 0.4671782061414135323, 0.5290873093409070860, 0.6015893617863945497, 0.6852532414128420513, 0.7789222961280750646, 0.8837899115430479791, 1.000000000000000000 ),
 .UNSPECIFIED. ) ;
#11479=CARTESIAN_POINT ( 'NONE',  ( 7.675798357370772429, 40.16299717330817742, 77.69330938776616335 ) ) ;
#11480=AXIS2_PLACEMENT_3D ( 'NONE', #11284, #16481, #14666 ) ;
#11482=CARTESIAN_POINT ( 'NONE',  ( -4.244920859621176490, 37.49018728506336373, 76.00056232034928883 ) ) ;
#11483=CARTESIAN_POINT ( 'NONE',  ( 9.353328126263708242, 42.82624226067153472, 76.54645538997905874 ) ) ;
#11484=EDGE_CURVE ( 'NONE', #2608, #559, #5389, .T. ) ;
#11485=CARTESIAN_POINT ( 'NONE',  ( 0.5221537403065014127, 44.16218137147968292, 76.16022115247204738 ) ) ;
#11486=CARTESIAN_POINT ( 'NONE',  ( 2.002611129390325484, 52.83679921599847518, 78.99455554248785916 ) ) ;
#11489=VERTEX_POINT ( 'NONE', #13592 ) ;
#11491=ORIENTED_EDGE ( 'NONE', *, *, #9785, .T. ) ;
#11495=CARTESIAN_POINT ( 'NONE',  ( 8.328612408207245466, 41.65204230202461133, 77.51978620826790234 ) ) ;
#11497=CARTESIAN_POINT ( 'NONE',  ( -5.510796958474739604, 38.60848837797752964, 76.73301527011911105 ) ) ;
#11499=CARTESIAN_POINT ( 'NONE',  ( 6.238653020734597376, 49.95521528567088154, 77.60602934391619101 ) ) ;
#11501=DIRECTION ( 'NONE',  ( -1.540237394707284220E-16, -1.793354297423764243E-16, 1.000000000000000000 ) ) ;
#11503=VERTEX_POINT ( 'NONE', #11908 ) ;
#11504=DIRECTION ( 'NONE',  ( -1.540237394707284467E-16, -1.793354297423764243E-16, 1.000000000000000000 ) ) ;
#11506=CARTESIAN_POINT ( 'NONE',  ( -5.827090762987216621, 50.44101592763561115, 78.49957729094111869 ) ) ;
#11507=EDGE_CURVE ( 'NONE', #6991, #264, #1389, .T. ) ;
#11508=FACE_OUTER_BOUND ( 'NONE', #4268, .T. ) ;
#11510=LINE ( 'NONE', #14787, #13902 ) ;
#11512=CARTESIAN_POINT ( 'NONE',  ( 6.837774032321189743, 37.85932018500469809, 76.05683950549904182 ) ) ;
#11513=CARTESIAN_POINT ( 'NONE',  ( 7.680900363438858847, 40.16312786850421190, 78.17527862778651127 ) ) ;
#11516=EDGE_LOOP ( 'NONE', ( #20916, #3098, #16762, #18726 ) ) ;
#11517=LINE ( 'NONE', #11413, #12821 ) ;
#11518=CIRCLE ( 'NONE', #10165, 8.799999999999997158 ) ;
#11521=CARTESIAN_POINT ( 'NONE',  ( 0.4682140828567994961, 52.36204277483403757, 75.98649299885811104 ) ) ;
#11522=CARTESIAN_POINT ( 'NONE',  ( -3.533008836142939035, 36.21715200979739535, 78.43912781517941823 ) ) ;
#11523=EDGE_CURVE ( 'NONE', #5069, #18148, #17578, .T. ) ;
#11524=DIRECTION ( 'NONE',  ( 0.5800177190770223756, 0.8146038580541393737, 2.354238310054622780E-16 ) ) ;
#11525=ORIENTED_EDGE ( 'NONE', *, *, #13907, .F. ) ;
#11533=CARTESIAN_POINT ( 'NONE',  ( 8.244331251587055931, 41.40382638133797144, 77.92171669569661674 ) ) ;
#11534=CARTESIAN_POINT ( 'NONE',  ( -5.889261015154378498, 37.95762057880577345, 79.03330530165142420 ) ) ;
#11539=PLANE ( 'NONE',  #4076 ) ;
#11540=EDGE_CURVE ( 'NONE', #9657, #3218, #15386, .T. ) ;
#11541=CARTESIAN_POINT ( 'NONE',  ( 1.083001295814570053, 52.34297901104275041, 76.77198585835439815 ) ) ;
#11542=ORIENTED_EDGE ( 'NONE', *, *, #18306, .T. ) ;
#11543=CARTESIAN_POINT ( 'NONE',  ( 4.588242150565980282, 52.09914025984591746, 78.23954818826248925 ) ) ;
#11548=ADVANCED_FACE ( 'NONE', ( #20072 ), #16895, .F. ) ;
#11550=CARTESIAN_POINT ( 'NONE',  ( 5.835344820533724608, 37.14302097153727544, 76.09175310361966638 ) ) ;
#11552=CARTESIAN_POINT ( 'NONE',  ( 5.552985721865087321, 50.63188710396593706, 76.09715583564816654 ) ) ;
#11553=AXIS2_PLACEMENT_3D ( 'NONE', #13445, #19917, #5341 ) ;
#11554=EDGE_CURVE ( 'NONE', #5907, #8246, #722, .T. ) ;
#11555=ORIENTED_EDGE ( 'NONE', *, *, #324, .F. ) ;
#11559=ORIENTED_EDGE ( 'NONE', *, *, #19670, .F. ) ;
#11560=DIRECTION ( 'NONE',  ( 0.9539696396349525154, -0.2999031954727372495, 9.315070279690337353E-17 ) ) ;
#11561=CARTESIAN_POINT ( 'NONE',  ( 9.350990972312333227, 42.81923766201297354, 78.59572304307680213 ) ) ;
#11562=AXIS2_PLACEMENT_3D ( 'NONE', #6659, #19840, #2089 ) ;
#11563=EDGE_LOOP ( 'NONE', ( #19354, #13642, #11809, #15874, #11126, #1628, #717, #6155, #5257, #12124, #1512, #20213 ) ) ;
#11564=VECTOR ( 'NONE', #11638, 1000.000000000000114 ) ;
#11565=CARTESIAN_POINT ( 'NONE',  ( -5.728661668566968679, 37.83899231081794312, 75.70067668752250256 ) ) ;
#11566=ORIENTED_EDGE ( 'NONE', *, *, #11714, .T. ) ;
#11570=EDGE_LOOP ( 'NONE', ( #3291, #14282, #18057, #20406 ) ) ;
#11571=CARTESIAN_POINT ( 'NONE',  ( 0.6135278437555422570, 52.96173443653181323, 77.38466869867853859 ) ) ;
#11572=CARTESIAN_POINT ( 'NONE',  ( -4.428896237227788468, 37.65366906320820561, 77.91201545794896788 ) ) ;
#11575=ORIENTED_EDGE ( 'NONE', *, *, #8959, .F. ) ;
#11576=CARTESIAN_POINT ( 'NONE',  ( -4.798777446476682584, 51.17581097466058537, 76.24916814194597237 ) ) ;
#11578=LINE ( 'NONE', #18052, #2379 ) ;
#11581=CARTESIAN_POINT ( 'NONE',  ( -4.530198942227657177, 37.70355750481248691, 76.15642697799287930 ) ) ;
#11584=ORIENTED_EDGE ( 'NONE', *, *, #20785, .F. ) ;
#11585=CARTESIAN_POINT ( 'NONE',  ( 4.600886763243814848, 37.18069802247041622, 75.46362501775257670 ) ) ;
#11586=VECTOR ( 'NONE', #19361, 1000.000000000000227 ) ;
#11588=DIRECTION ( 'NONE',  ( 0.3165065846431828200, 0.9485903129789527988, 0.000000000000000000 ) ) ;
#11591=CARTESIAN_POINT ( 'NONE',  ( 2.118765075475726345, 52.81613201993158668, 78.36533242353944217 ) ) ;
#11594=PLANE ( 'NONE',  #6558 ) ;
#11595=ORIENTED_EDGE ( 'NONE', *, *, #20911, .T. ) ;
#11596=EDGE_CURVE ( 'NONE', #19492, #16873, #12218, .T. ) ;
#11597=B_SPLINE_CURVE_WITH_KNOTS ( 'NONE', 3,
 ( #5712, #18812, #6141, #18912, #9353, #12531, #13912, #14224, #4324, #7532, #15838, #11054, #1250, #1155, #17321, #7742 ),
 .UNSPECIFIED., .F., .F.,
 ( 4, 2, 2, 2, 2, 2, 2, 4 ),
 ( 0.000000000000000000, 0.0005762146036707721389, 0.0008643219055061592384, 0.001152429207341546229, 0.001440536509176933329, 0.001728643811012320428, 0.002016751112847707528, 0.002304858414683094627 ),
 .UNSPECIFIED. ) ;
#11598=CARTESIAN_POINT ( 'NONE',  ( 7.680445814051256370, 40.16232446084477914, 76.89670332066808101 ) ) ;
#11599=CARTESIAN_POINT ( 'NONE',  ( 4.461908506452709311, 51.26762488673620055, 77.64500276804245971 ) ) ;
#11601=CARTESIAN_POINT ( 'NONE',  ( -0.9143671159618040889, 52.84414119167043822, 76.25586683505548535 ) ) ;
#11603=B_SPLINE_SURFACE_WITH_KNOTS ( 'NONE', 3, 1, ( 
 ( #716, #7198 ),
 ( #823, #15089 ),
 ( #2206, #12014 ),
 ( #13700, #10209 ),
 ( #8706, #10317 ),
 ( #3798, #11794 ),
 ( #18269, #16791 ),
 ( #15189, #20175 ),
 ( #5605, #3688 ),
 ( #10639, #20274 ),
 ( #4004, #15512 ),
 ( #2423, #13798 ),
 ( #6884, #5704 ),
 ( #17106, #9447 ),
 ( #14217, #4531 ),
 ( #20694, #1039 ),
 ( #10945, #15933 ),
 ( #10845, #12524 ),
 ( #4318, #4628 ) ),
 .UNSPECIFIED., .F., .F., .F.,
 ( 4, 1, 1, 1, 1, 1, 1, 1, 1, 1, 1, 1, 1, 1, 1, 1, 4 ),
 ( 2, 2 ),
 ( 0.000000000000000000, 0.06302581646095750667, 0.1222495429959427476, 0.1789669701231155763, 0.2332877456213924006, 0.2860909212508800925, 0.3384954837963008445, 0.3911857795644178570, 0.4453574251251987137, 0.5015394511440722791, 0.5602660668541803446, 0.6223358252984214634, 0.6886061413240012197, 0.7590929558684775813, 0.8342439359547982880, 0.9143471077142913961, 1.000000000000000000 ),
 ( 0.000000000000000000, 1.000000000000000000 ),
 .UNSPECIFIED. ) ;
#11604=CARTESIAN_POINT ( 'NONE',  ( 5.239313537742215310, 50.86510457629285042, 78.30875056423674607 ) ) ;
#11606=CARTESIAN_POINT ( 'NONE',  ( -3.054046897975729813, 36.78819506682361151, 76.51650556680409920 ) ) ;
#11607=CARTESIAN_POINT ( 'NONE',  ( -4.533682039091601723, 37.71094493724306318, 76.26481528174605273 ) ) ;
#11611=ORIENTED_EDGE ( 'NONE', *, *, #2074, .T. ) ;
#11612=CARTESIAN_POINT ( 'NONE',  ( 0.4858785009097955077, 52.96635066793365354, 75.98243536310876323 ) ) ;
#11615=CARTESIAN_POINT ( 'NONE',  ( 2.035123479059382401, 36.10296785094196537, 72.45433879953085921 ) ) ;
#11616=CARTESIAN_POINT ( 'NONE',  ( -4.893796645199854467, 37.22231114847117084, 78.64904841171450300 ) ) ;
#11617=CARTESIAN_POINT ( 'NONE',  ( -7.079975527142585712, 43.92211762787398044, 72.45432679953087529 ) ) ;
#11618=CARTESIAN_POINT ( 'NONE',  ( 9.178784097065811665, 42.30312273229867515, 78.05372954401303787 ) ) ;
#11621=CARTESIAN_POINT ( 'NONE',  ( 0.6035869791250174643, 52.96772377251001984, 79.54835876252475657 ) ) ;
#11622=CARTESIAN_POINT ( 'NONE',  ( 6.604417847172709521, 37.69257239881283539, 78.19824744938543404 ) ) ;
#11623=CARTESIAN_POINT ( 'NONE',  ( 4.214696258237026427, 51.48399209946829558, 75.85240097884792476 ) ) ;
#11626=CARTESIAN_POINT ( 'NONE',  ( 8.951667845840693971, 41.62244091939069790, 76.38301527011910252 ) ) ;
#11627=CARTESIAN_POINT ( 'NONE',  ( -3.349688636638950889, 52.21127678364309332, 76.69845644658968808 ) ) ;
#11628=VERTEX_POINT ( 'NONE', #15518 ) ;
#11630=ADVANCED_FACE ( 'NONE', ( #20505 ), #14280, .F. ) ;
#11631=CARTESIAN_POINT ( 'NONE',  ( -7.870013012521086537, 41.50220630618382245, 78.93669174070734584 ) ) ;
#11633=VECTOR ( 'NONE', #14839, 1000.000000000000000 ) ;
#11634=CARTESIAN_POINT ( 'NONE',  ( 8.598743959472566090, 42.74347214292002661, 79.23761354080345143 ) ) ;
#11636=CARTESIAN_POINT ( 'NONE',  ( -4.211488180634966660, 48.16625856408043660, 82.45433879953087342 ) ) ;
#11638=DIRECTION ( 'NONE',  ( 0.007885122365275663500, 0.9999689119394085113, 1.805443505845543142E-16 ) ) ;
#11640=DIRECTION ( 'NONE',  ( 1.540237394707284220E-16, 1.793354297423764243E-16, -1.000000000000000000 ) ) ;
#11643=CARTESIAN_POINT ( 'NONE',  ( -3.566438244846302119, 38.23101125920473464, 78.58080938776616620 ) ) ;
#11646=CARTESIAN_POINT ( 'NONE',  ( 0.3552956088218497954, 52.96739482532228749, 78.76353264627590534 ) ) ;
#11647=ORIENTED_EDGE ( 'NONE', *, *, #9548, .F. ) ;
#11648=CARTESIAN_POINT ( 'NONE',  ( -4.412197277429617870, 51.45204700985827628, 76.06958028623719770 ) ) ;
#11649=VECTOR ( 'NONE', #9989, 1000.000000000000000 ) ;
#11650=ORIENTED_EDGE ( 'NONE', *, *, #9928, .T. ) ;
#11651=CARTESIAN_POINT ( 'NONE',  ( 1.652727357819363974, 35.35299279957455099, 79.45433879953087342 ) ) ;
#11652=CARTESIAN_POINT ( 'NONE',  ( -6.841199144977723634, 40.72807414154878103, 77.45762758118813451 ) ) ;
#11654=CARTESIAN_POINT ( 'NONE',  ( -4.535389824330220421, 37.70745443760639404, 77.32412050424863992 ) ) ;
#11657=CARTESIAN_POINT ( 'NONE',  ( 5.454420194094963037, 37.61774161224509072, 76.04105433551922033 ) ) ;
#11659=ORIENTED_EDGE ( 'NONE', *, *, #17628, .F. ) ;
#11660=DIRECTION ( 'NONE',  ( 0.3165065846431827645, 0.9485903129789529098, 0.000000000000000000 ) ) ;
#11662=EDGE_CURVE ( 'NONE', #15850, #6157, #17889, .T. ) ;
#11664=VECTOR ( 'NONE', #14637, 1000.000000000000000 ) ;
#11668=ORIENTED_EDGE ( 'NONE', *, *, #7930, .F. ) ;
#11670=CARTESIAN_POINT ( 'NONE',  ( -5.231921090767167826, 38.40807655202139870, 75.65168154244369703 ) ) ;
#11672=EDGE_LOOP ( 'NONE', ( #4594, #686, #19755, #6388 ) ) ;
#11673=CARTESIAN_POINT ( 'NONE',  ( 5.649834628789608182, 51.31498465973561451, 78.90029747732744170 ) ) ;
#11676=ORIENTED_EDGE ( 'NONE', *, *, #8058, .F. ) ;
#11677=CARTESIAN_POINT ( 'NONE',  ( -4.717426356068906479, 37.09203352051870439, 77.92182307551118470 ) ) ;
#11678=EDGE_LOOP ( 'NONE', ( #8738, #4420, #9546, #5373 ) ) ;
#11684=CARTESIAN_POINT ( 'NONE',  ( -7.202537930885374529, 41.41097462079392955, 78.61536821129558916 ) ) ;
#11686=CARTESIAN_POINT ( 'NONE',  ( 4.556677822976353376, 36.22933235006951946, 75.83703142516586126 ) ) ;
#11688=EDGE_CURVE ( 'NONE', #11453, #11104, #7743, .T. ) ;
#11690=FACE_OUTER_BOUND ( 'NONE', #19675, .T. ) ;
#11691=FACE_OUTER_BOUND ( 'NONE', #5910, .T. ) ;
#11692=B_SPLINE_CURVE_WITH_KNOTS ( 'NONE', 3,
 ( #1830, #15225, #5208, #6810, #14894, #16504, #13316, #20097, #8417, #19788, #18099, #3520 ),
 .UNSPECIFIED., .F., .F.,
 ( 4, 2, 2, 2, 2, 4 ),
 ( 0.000000000000000000, 0.0001692975960979477246, 0.0003385951921958954493, 0.0004232439902448494572, 0.0005078927882938035192, 0.0006771903843916710942 ),
 .UNSPECIFIED. ) ;
#11697=VECTOR ( 'NONE', #5510, 1000.000000000000227 ) ;
#11700=CARTESIAN_POINT ( 'NONE',  ( -3.673304938980978651, 36.32078308949211731, 77.52205638859560111 ) ) ;
#11705=CARTESIAN_POINT ( 'NONE',  ( 0.6810009142495576651, 52.96482701376152136, 77.39848739855237625 ) ) ;
#11713=CARTESIAN_POINT ( 'NONE',  ( 5.316416202095706645, 37.50973464508803801, 75.36022115247205022 ) ) ;
#11714=EDGE_CURVE ( 'NONE', #10035, #9413, #5159, .T. ) ;
#11715=ADVANCED_FACE ( 'NONE', ( #3168 ), #3267, .F. ) ;
#11716=ORIENTED_EDGE ( 'NONE', *, *, #12241, .T. ) ;
#11717=CARTESIAN_POINT ( 'NONE',  ( 8.934486310075088866, 41.57094676672487310, 78.86350455626283917 ) ) ;
#11718=CARTESIAN_POINT ( 'NONE',  ( 8.579938887586086693, 42.63956115774173838, 75.59610358210291281 ) ) ;
#11719=FACE_OUTER_BOUND ( 'NONE', #17177, .T. ) ;
#11722=CARTESIAN_POINT ( 'NONE',  ( 5.785641543149844246, 51.21466956273390991, 77.95070864408322109 ) ) ;
#11723=ORIENTED_EDGE ( 'NONE', *, *, #7433, .F. ) ;
#11724=CARTESIAN_POINT ( 'NONE',  ( 6.388813065772197319, 37.53850911581889704, 78.31663032931759005 ) ) ;
#11726=CARTESIAN_POINT ( 'NONE',  ( 2.527576913102089762, 36.82540565608437078, 72.45433879953085921 ) ) ;
#11729=CARTESIAN_POINT ( 'NONE',  ( 8.373523562223194716, 41.80976150358770838, 76.25788209700408515 ) ) ;
#11730=CARTESIAN_POINT ( 'NONE',  ( -4.559776018715441026, 36.97558356685869541, 78.86760481232144571 ) ) ;
#11731=ORIENTED_EDGE ( 'NONE', *, *, #11244, .T. ) ;
#11733=CARTESIAN_POINT ( 'NONE',  ( -7.247910519723778755, 41.56650193107834923, 78.91953837536544825 ) ) ;
#11735=CARTESIAN_POINT ( 'NONE',  ( 8.951667845840693971, 41.62244091939069790, 77.14698585835439815 ) ) ;
#11736=ORIENTED_EDGE ( 'NONE', *, *, #17243, .F. ) ;
#11740=DIRECTION ( 'NONE',  ( 1.540237394707284467E-16, 1.793354297423764243E-16, -1.000000000000000000 ) ) ;
#11743=ORIENTED_EDGE ( 'NONE', *, *, #6245, .T. ) ;
#11744=LINE ( 'NONE', #18952, #3838 ) ;
#11745=DIRECTION ( 'NONE',  ( -0.5941461771851691553, -0.8043570849667760481, -2.357623395011396791E-16 ) ) ;
#11748=CARTESIAN_POINT ( 'NONE',  ( 0.3721289191693305520, 52.35590880031470817, 78.82913797267801215 ) ) ;
#11749=ORIENTED_EDGE ( 'NONE', *, *, #9410, .T. ) ;
#11750=CARTESIAN_POINT ( 'NONE',  ( -4.044210365576157429, 50.96808155198777968, 76.14127734336351239 ) ) ;
#11751=ORIENTED_EDGE ( 'NONE', *, *, #15451, .F. ) ;
#11752=CARTESIAN_POINT ( 'NONE',  ( -3.154068805640487749, 36.83224912750022639, 78.04613744265782316 ) ) ;
#11754=EDGE_CURVE ( 'NONE', #13741, #15505, #13077, .T. ) ;
#11755=CARTESIAN_POINT ( 'NONE',  ( -4.160049236649933313, 37.43039271674265933, 76.90921114709620099 ) ) ;
#11758=CARTESIAN_POINT ( 'NONE',  ( 5.847829093480187979, 37.15194177590640834, 76.49330797698027595 ) ) ;
#11759=CARTESIAN_POINT ( 'NONE',  ( -4.621776214648809500, 51.30228957449607208, 75.36056307228784590 ) ) ;
#11760=ORIENTED_EDGE ( 'NONE', *, *, #17036, .F. ) ;
#11761=CARTESIAN_POINT ( 'NONE',  ( 1.205864535894263900, 52.96136243468175309, 79.49721971971477785 ) ) ;
#11762=CARTESIAN_POINT ( 'NONE',  ( 5.450944860649778789, 36.86834283398499679, 78.16244716952144245 ) ) ;
#11764=DIRECTION ( 'NONE',  ( 0.5941461771841298756, 0.8043570849675437673, -3.462188797834771445E-14 ) ) ;
#11765=DIRECTION ( 'NONE',  ( -0.02533578529877045238, -0.9996789974703352843, -1.831801750099146688E-16 ) ) ;
#11767=B_SPLINE_SURFACE_WITH_KNOTS ( 'NONE', 3, 1, ( 
 ( #15804, #12402 ),
 ( #18779, #14184 ),
 ( #12494, #4194 ),
 ( #18881, #4289 ),
 ( #20664, #13773 ),
 ( #10815, #20246 ),
 ( #17281, #2706 ),
 ( #9213, #14089 ),
 ( #6098, #18980 ),
 ( #2814, #4392 ),
 ( #12603, #10917 ),
 ( #17387, #11020 ),
 ( #17490, #15902 ),
 ( #18010, #9414 ),
 ( #13119, #12704 ),
 ( #6513, #12910 ),
 ( #6300, #12800 ),
 ( #3015, #1322 ),
 ( #3124, #7807 ),
 ( #9728, #9521 ),
 ( #19182, #17587 ),
 ( #6613, #4595 ),
 ( #20768, #14608 ),
 ( #16209, #6202 ),
 ( #4908, #9626 ),
 ( #6403, #13019 ),
 ( #11119, #9830 ) ),
 .UNSPECIFIED., .F., .F., .F.,
 ( 4, 1, 1, 1, 1, 1, 1, 1, 1, 1, 1, 1, 1, 1, 1, 1, 1, 1, 1, 1, 1, 1, 1, 1, 4 ),
 ( 2, 2 ),
 ( 0.000000000000000000, 0.08415130211954198469, 0.1639620550106605512, 0.2403084560778752377, 0.3136616503690570767, 0.3487238096526073527, 0.3821668720153286181, 0.4136737894986983743, 0.4437099131648768457, 0.4722505124987256275, 0.4989577201472497614, 0.5245780966751731889, 0.5489676856186370690, 0.5954867311152326481, 0.6405007172309487018, 0.6844907576478919120, 0.7283883565803446203, 0.7516682776372889396, 0.7779555554382332483, 0.8073737814008299374, 0.8396655338036946858, 0.8751296329422569853, 0.9135058715745314473, 0.9551265033309996877, 1.000000000000000000 ),
 ( 0.000000000000000000, 1.000000000000000000 ),
 .UNSPECIFIED. ) ;
#11768=VERTEX_POINT ( 'NONE', #9875 ) ;
#11769=CARTESIAN_POINT ( 'NONE',  ( -4.608840676074902554, 37.94783214889832124, 75.38158877174898009 ) ) ;
#11771=CARTESIAN_POINT ( 'NONE',  ( 6.012275498921958672, 37.26944915646792822, 78.37198585835440667 ) ) ;
#11772=LINE ( 'NONE', #6650, #1003 ) ;
#11773=EDGE_LOOP ( 'NONE', ( #20539, #19319, #574, #18170 ) ) ;
#11774=CARTESIAN_POINT ( 'NONE',  ( -4.155425753337090633, 37.45166743282118915, 78.17872471894986575 ) ) ;
#11776=EDGE_LOOP ( 'NONE', ( #9286, #3147, #3362, #16905 ) ) ;
#11777=FACE_OUTER_BOUND ( 'NONE', #9397, .T. ) ;
#11778=CARTESIAN_POINT ( 'NONE',  ( 0.6888015158513324243, 52.96107022024632727, 75.36125108926063376 ) ) ;
#11779=VECTOR ( 'NONE', #14480, 1000.000000000000000 ) ;
#11781=CARTESIAN_POINT ( 'NONE',  ( 5.553908412425695218, 50.63686217341278706, 77.18328619514350919 ) ) ;
#11782=CARTESIAN_POINT ( 'NONE',  ( -7.880212061628153464, 41.54679441531448703, 76.16022115247204738 ) ) ;
#11783=ORIENTED_EDGE ( 'NONE', *, *, #11282, .F. ) ;
#11784=ORIENTED_EDGE ( 'NONE', *, *, #5425, .T. ) ;
#11785=CARTESIAN_POINT ( 'NONE',  ( 4.449581223279069242, 37.07258062326099690, 75.53067132529541539 ) ) ;
#11786=CARTESIAN_POINT ( 'NONE',  ( 7.690906676071723069, 40.20827776290879285, 78.77723610448765612 ) ) ;
#11787=ORIENTED_EDGE ( 'NONE', *, *, #2977, .T. ) ;
#11792=ORIENTED_EDGE ( 'NONE', *, *, #16808, .T. ) ;
#11794=CARTESIAN_POINT ( 'NONE',  ( 6.416710426036811299, 49.83450939472239583, 78.95155228521747404 ) ) ;
#11795=ORIENTED_EDGE ( 'NONE', *, *, #13883, .F. ) ;
#11796=CARTESIAN_POINT ( 'NONE',  ( 5.552491339591165698, 50.63796333333529986, 76.08571115608103241 ) ) ;
#11797=CARTESIAN_POINT ( 'NONE',  ( 7.962360810970000813, 41.03860973493735997, 75.42295143068700725 ) ) ;
#11798=CARTESIAN_POINT ( 'NONE',  ( -4.032264951078913029, 50.98107207184723677, 78.45066232894264147 ) ) ;
#11799=DIRECTION ( 'NONE',  ( 0.3165065846431827645, 0.9485903129789529098, 0.000000000000000000 ) ) ;
#11800=EDGE_CURVE ( 'NONE', #14895, #15118, #5058, .T. ) ;
#11802=CARTESIAN_POINT ( 'NONE',  ( 8.801580714196775901, 41.17262026450377022, 76.07953452682116335 ) ) ;
#11807=CARTESIAN_POINT ( 'NONE',  ( -7.370301013496298737, 41.95215886586026954, 78.67381781145438424 ) ) ;
#11808=LINE ( 'NONE', #305, #1057 ) ;
#11809=ORIENTED_EDGE ( 'NONE', *, *, #5232, .T. ) ;
#11810=DIRECTION ( 'NONE',  ( 0.3165065846431827645, 0.9485903129789529098, 0.000000000000000000 ) ) ;
#11817=LINE ( 'NONE', #13722, #8596 ) ;
#11820=VERTEX_POINT ( 'NONE', #1843 ) ;
#11821=VECTOR ( 'NONE', #18703, 1000.000000000000114 ) ;
#11822=CARTESIAN_POINT ( 'NONE',  ( 8.265572330772934961, 41.46143766428760813, 79.54654421141340492 ) ) ;
#11823=CARTESIAN_POINT ( 'NONE',  ( -4.716387082485073989, 37.09126585098686490, 75.36022115247205022 ) ) ;
#11826=EDGE_CURVE ( 'NONE', #10614, #11899, #7025, .T. ) ;
#11827=CARTESIAN_POINT ( 'NONE',  ( 5.755371611800503828, 51.23702874167446453, 77.28963291717792572 ) ) ;
#11828=CARTESIAN_POINT ( 'NONE',  ( -4.689916854477826469, 37.07171335984372718, 78.93589701864812014 ) ) ;
#11830=AXIS2_PLACEMENT_3D ( 'NONE', #12172, #17063, #17164 ) ;
#11831=CARTESIAN_POINT ( 'NONE',  ( 1.994229309409025097, 52.20255399867006929, 77.17808573571203112 ) ) ;
#11834=CARTESIAN_POINT ( 'NONE',  ( -3.716800330428160049, 36.35291138305289849, 77.85659439586764563 ) ) ;
#11835=B_SPLINE_CURVE_WITH_KNOTS ( 'NONE', 3,
 ( #19815, #10158, #16640, #5237, #10269, #11752, #19915, #11852, #2377, #3548 ),
 .UNSPECIFIED., .F., .F.,
 ( 4, 2, 2, 2, 4 ),
 ( 0.000000000000000000, 0.0002565823024332847865, 0.0005131646048665695729, 0.0007697469072998543594, 0.001026329209733139146 ),
 .UNSPECIFIED. ) ;
#11836=CARTESIAN_POINT ( 'NONE',  ( -8.189734885440142165, 42.91998662985088941, 78.64696458830286474 ) ) ;
#11838=DIRECTION ( 'NONE',  ( -1.540237394707284220E-16, -1.793354297423764243E-16, 1.000000000000000000 ) ) ;
#11840=CARTESIAN_POINT ( 'NONE',  ( -7.720485820677993161, 47.24421020474736110, 77.98042076123601873 ) ) ;
#11842=ORIENTED_EDGE ( 'NONE', *, *, #12121, .F. ) ;
#11844=VECTOR ( 'NONE', #15273, 1000.000000000000000 ) ;
#11846=CARTESIAN_POINT ( 'NONE',  ( -4.092737432821778931, 51.68032131864361389, 79.48422614141084352 ) ) ;
#11850=CARTESIAN_POINT ( 'NONE',  ( 5.241460166982748525, 50.86801069014953924, 78.30875056423674607 ) ) ;
#11851=ORIENTED_EDGE ( 'NONE', *, *, #20141, .T. ) ;
#11852=CARTESIAN_POINT ( 'NONE',  ( -3.103229033235510581, 36.80712667557776285, 78.29630717499995285 ) ) ;
#11854=CARTESIAN_POINT ( 'NONE',  ( -6.756808310619874192, 40.46120382059411469, 77.87635769503857830 ) ) ;
#11855=CARTESIAN_POINT ( 'NONE',  ( -7.294472080575377326, 41.68420623513899415, 78.93669174070734584 ) ) ;
#11856=CARTESIAN_POINT ( 'NONE',  ( -7.674265136008432187, 40.95548271059750078, 76.88066623382401588 ) ) ;
#11858=CARTESIAN_POINT ( 'NONE',  ( 5.843112203128086435, 37.14857125875717969, 76.21413800766271152 ) ) ;
#11861=EDGE_CURVE ( 'NONE', #1174, #19686, #19131, .T. ) ;
#11864=CARTESIAN_POINT ( 'NONE',  ( 5.518796429342951448, 36.91682708076865538, 78.21801395346943764 ) ) ;
#11869=ORIENTED_EDGE ( 'NONE', *, *, #5062, .F. ) ;
#11870=CARTESIAN_POINT ( 'NONE',  ( 8.793292705229012185, 41.14778057584590698, 77.83369646723784285 ) ) ;
#11874=CARTESIAN_POINT ( 'NONE',  ( 1.087740465381641375, 52.94398708878058102, 76.77198585835439815 ) ) ;
#11875=ORIENTED_EDGE ( 'NONE', *, *, #1581, .T. ) ;
#11876=CARTESIAN_POINT ( 'NONE',  ( -4.681776609547218193, 37.06570048882251456, 77.92992558049613194 ) ) ;
#11879=VERTEX_POINT ( 'NONE', #5222 ) ;
#11880=CARTESIAN_POINT ( 'NONE',  ( 0.7328066911292444585, 52.35949871758720775, 77.42541623458531319 ) ) ;
#11881=CARTESIAN_POINT ( 'NONE',  ( 2.112743662072855688, 52.81725452181535019, 76.30775568555031896 ) ) ;
#11885=EDGE_CURVE ( 'NONE', #8267, #13025, #16518, .T. ) ;
#11886=CARTESIAN_POINT ( 'NONE',  ( 6.645808250425207397, 50.57929906569810896, 75.61685692759286326 ) ) ;
#11888=VECTOR ( 'NONE', #8150, 1000.000000000000000 ) ;
#11889=B_SPLINE_CURVE_WITH_KNOTS ( 'NONE', 3,
 ( #3275, #6351, #9888, #11066, #12655, #17536, #6457, #11482, #9466, #1373, #7861, #16369 ),
 .UNSPECIFIED., .F., .F.,
 ( 4, 2, 2, 2, 2, 4 ),
 ( 0.000000000000000000, 0.0003548653088398171624, 0.0004435816360497409462, 0.0005322979632596647843, 0.0006210142904695885140, 0.0007097306176795123520 ),
 .UNSPECIFIED. ) ;
#11893=CARTESIAN_POINT ( 'NONE',  ( 0.5221537403065005245, 44.16218137147968292, 82.45433879953087342 ) ) ;
#11895=ORIENTED_EDGE ( 'NONE', *, *, #16156, .T. ) ;
#11897=CARTESIAN_POINT ( 'NONE',  ( 0.3403435922581479200, 52.35615943634957858, 77.57937361552639288 ) ) ;
#11898=CARTESIAN_POINT ( 'NONE',  ( -6.709328582052544121, 40.29621921162755172, 72.45433879953085921 ) ) ;
#11899=VERTEX_POINT ( 'NONE', #3842 ) ;
#11901=VECTOR ( 'NONE', #19189, 1000.000000000000227 ) ;
#11902=VECTOR ( 'NONE', #7959, 1000.000000000000227 ) ;
#11903=DIRECTION ( 'NONE',  ( -0.9534635866061451637, -0.3015081906286224411, -2.009271279954815058E-16 ) ) ;
#11905=CARTESIAN_POINT ( 'NONE',  ( 5.459413332645724815, 50.70932733642038670, 75.97917348163453255 ) ) ;
#11906=CARTESIAN_POINT ( 'NONE',  ( 0.3908531827224452360, 52.96817599631071261, 75.36353278631986541 ) ) ;
#11907=PLANE ( 'NONE',  #3282 ) ;
#11908=CARTESIAN_POINT ( 'NONE',  ( 5.076572431691917409, 37.34329067111212197, 76.70433879953087342 ) ) ;
#11911=VECTOR ( 'NONE', #20909, 1000.000000000000000 ) ;
#11912=CARTESIAN_POINT ( 'NONE',  ( 0.8500593474157197571, 52.96349392588599869, 77.74134350746754762 ) ) ;
#11913=VECTOR ( 'NONE', #9437, 1000.000000000000000 ) ;
#11915=PLANE ( 'NONE',  #19043 ) ;
#11916=B_SPLINE_CURVE_WITH_KNOTS ( 'NONE', 3,
 ( #20368, #5804, #20157, #1017, #2613, #9113, #15600, #5587, #12092, #15814, #18891, #9640 ),
 .UNSPECIFIED., .F., .F.,
 ( 4, 2, 2, 2, 2, 4 ),
 ( 0.000000000000000000, 0.0004479885639438729037, 0.0005599857049298308026, 0.0006719828459157885930, 0.0007839799869017464919, 0.0008959771278877043908 ),
 .UNSPECIFIED. ) ;
#11918=VECTOR ( 'NONE', #19930, 999.9999999999998863 ) ;
#11920=CARTESIAN_POINT ( 'NONE',  ( 0.4126924915616977940, 52.96692776651367751, 76.01942718764288998 ) ) ;
#11922=CARTESIAN_POINT ( 'NONE',  ( 5.327820932109281316, 50.80650718277960465, 77.28232693284115840 ) ) ;
#11923=DIRECTION ( 'NONE',  ( -0.5941461771851691553, -0.8043570849667760481, -2.357623395011396791E-16 ) ) ;
#11924=CARTESIAN_POINT ( 'NONE',  ( -4.895465483855350186, 37.22354385236106822, 78.55727908454632313 ) ) ;
#11926=ADVANCED_FACE ( 'NONE', ( #16622 ), #8540, .T. ) ;
#11927=CARTESIAN_POINT ( 'NONE',  ( -4.517625420443597939, 36.94444861784495515, 76.85096240152589075 ) ) ;
#11928=FACE_OUTER_BOUND ( 'NONE', #5221, .T. ) ;
#11930=ORIENTED_EDGE ( 'NONE', *, *, #16493, .T. ) ;
#11931=EDGE_LOOP ( 'NONE', ( #21002, #7270, #7998, #7258 ) ) ;
#11932=CARTESIAN_POINT ( 'NONE',  ( 6.403524027200472091, 49.87623753264638538, 77.45731366823912367 ) ) ;
#11933=CARTESIAN_POINT ( 'NONE',  ( -7.949137504989498559, 41.77948864320536160, 78.13669174070733447 ) ) ;
#11934=CARTESIAN_POINT ( 'NONE',  ( -4.166541536208259622, 37.43491202974078647, 78.74462879972740836 ) ) ;
#11942=CARTESIAN_POINT ( 'NONE',  ( -7.816556923607321572, 41.33316136529717966, 78.89406302991613984 ) ) ;
#11945=DIRECTION ( 'NONE',  ( 0.5813877811927012917, -0.8136266022444372803, -5.636455622144620416E-17 ) ) ;
#11946=ORIENTED_EDGE ( 'NONE', *, *, #2246, .T. ) ;
#11949=AXIS2_PLACEMENT_3D ( 'NONE', #13634, #226, #19997 ) ;
#11950=CARTESIAN_POINT ( 'NONE',  ( -4.804325902087982492, 51.17184625142267151, 78.52518475144754007 ) ) ;
#11951=VECTOR ( 'NONE', #10467, 1000.000000000000227 ) ;
#11954=CARTESIAN_POINT ( 'NONE',  ( 6.705715917364262424, 48.58072850854415492, 75.45433879953087342 ) ) ;
#11955=CARTESIAN_POINT ( 'NONE',  ( -2.055347584452832166, 51.31805217249780782, 72.45433879953087342 ) ) ;
#11957=CARTESIAN_POINT ( 'NONE',  ( 5.581406744796362673, 50.61539444998253856, 76.38301527011910252 ) ) ;
#11958=CARTESIAN_POINT ( 'NONE',  ( 5.223270137239985011, 50.87543472457460325, 77.16202479023476712 ) ) ;
#11960=ORIENTED_EDGE ( 'NONE', *, *, #19710, .T. ) ;
#11961=CARTESIAN_POINT ( 'NONE',  ( 8.221632462510044093, 41.34112525087960677, 77.36736982993747347 ) ) ;
#11962=EDGE_CURVE ( 'NONE', #492, #3468, #8429, .T. ) ;
#11963=ORIENTED_EDGE ( 'NONE', *, *, #11688, .F. ) ;
#11965=CARTESIAN_POINT ( 'NONE',  ( 6.569564547327074955, 50.63561721789299952, 77.67636243622263237 ) ) ;
#11968=VECTOR ( 'NONE', #10385, 1000.000000000000114 ) ;
#11975=ORIENTED_EDGE ( 'NONE', *, *, #4153, .T. ) ;
#11976=LINE ( 'NONE', #18876, #11231 ) ;
#11980=CARTESIAN_POINT ( 'NONE',  ( -7.332176014465951575, 42.24478606644824907, 77.21863129581211638 ) ) ;
#11981=ORIENTED_EDGE ( 'NONE', *, *, #15762, .T. ) ;
#11982=LINE ( 'NONE', #2182, #7842 ) ;
#11983=FACE_BOUND ( 'NONE', #11369, .T. ) ;
#11985=VECTOR ( 'NONE', #14651, 1000.000000000000114 ) ;
#11986=DIRECTION ( 'NONE',  ( -0.5941461771851693774, -0.8043570849667760481, -2.357623395011396791E-16 ) ) ;
#11991=EDGE_CURVE ( 'NONE', #7324, #20830, #8750, .T. ) ;
#11993=DIRECTION ( 'NONE',  ( -0.9485903129789527988, 0.3165065846431829311, -8.934458285744989980E-17 ) ) ;
#11996=DIRECTION ( 'NONE',  ( 0.9485903129789529098, -0.3165065846431826535, 8.934458285744997376E-17 ) ) ;
#11997=EDGE_CURVE ( 'NONE', #8922, #20886, #3424, .T. ) ;
#12000=CARTESIAN_POINT ( 'NONE',  ( -4.481786250374327985, 37.67261160860749669, 76.00936707281648808 ) ) ;
#12002=VECTOR ( 'NONE', #15903, 1000.000000000000114 ) ;
#12003=CARTESIAN_POINT ( 'NONE',  ( -3.853146778511270742, 37.22459720243209347, 79.49239465720451392 ) ) ;
#12007=CARTESIAN_POINT ( 'NONE',  ( -4.895593109503407980, 37.22363812428621088, 78.53742703482498655 ) ) ;
#12008=ORIENTED_EDGE ( 'NONE', *, *, #1803, .F. ) ;
#12010=CARTESIAN_POINT ( 'NONE',  ( 0.4298316049500268132, 52.96680757607156664, 77.42486900944150818 ) ) ;
#12011=DIRECTION ( 'NONE',  ( 1.540237394707284220E-16, 1.793354297423764243E-16, -1.000000000000000000 ) ) ;
#12013=EDGE_CURVE ( 'NONE', #1879, #5410, #17147, .T. ) ;
#12014=CARTESIAN_POINT ( 'NONE',  ( 6.484653179477954943, 49.78432281965648087, 78.61296362383696135 ) ) ;
#12015=VERTEX_POINT ( 'NONE', #5965 ) ;
#12016=CARTESIAN_POINT ( 'NONE',  ( 5.579938407236030073, 50.61660530761176346, 76.19612812024240611 ) ) ;
#12018=VECTOR ( 'NONE', #3899, 1000.000000000000227 ) ;
#12019=CARTESIAN_POINT ( 'NONE',  ( 9.115819689944924420, 42.11441440976988559, 75.45386443748748206 ) ) ;
#12020=CARTESIAN_POINT ( 'NONE',  ( 4.555266191169155654, 52.12349827269967761, 77.01204236660041147 ) ) ;
#12021=CARTESIAN_POINT ( 'NONE',  ( -7.607912653626056176, 43.09321218401766629, 78.73993707373800532 ) ) ;
#12023=CARTESIAN_POINT ( 'NONE',  ( 0.7555763647120519177, 52.35288517333821545, 77.43909148762901395 ) ) ;
#12024=DIRECTION ( 'NONE',  ( -0.9534635866061452747, -0.3015081906286225522, -2.009271279954815797E-16 ) ) ;
#12025=CARTESIAN_POINT ( 'NONE',  ( 4.097390034816025484, 51.53687999803451447, 76.58963291717793709 ) ) ;
#12027=CARTESIAN_POINT ( 'NONE',  ( -7.373282680283180568, 41.96158783262483638, 78.50654468188380974 ) ) ;
#12029=CARTESIAN_POINT ( 'NONE',  ( -4.517072128342570991, 36.94403992325788977, 76.53375056423675460 ) ) ;
#12032=CARTESIAN_POINT ( 'NONE',  ( -4.579686653871014812, 36.99029075099881680, 76.02016401025396419 ) ) ;
#12034=CARTESIAN_POINT ( 'NONE',  ( 5.327803506469481754, 40.48109702276099853, 75.45433879953087342 ) ) ;
#12036=CARTESIAN_POINT ( 'NONE',  ( -4.871646723878168217, 37.20594989384409956, 76.06675994099744287 ) ) ;
#12038=DIRECTION ( 'NONE',  ( -0.3165065846431827645, -0.9485903129789529098, 0.000000000000000000 ) ) ;
#12039=VERTEX_POINT ( 'NONE', #12153 ) ;
#12040=CARTESIAN_POINT ( 'NONE',  ( 9.244427017087200937, 42.49985872791199881, 79.25343573416346032 ) ) ;
#12041=LINE ( 'NONE', #2239, #16902 ) ;
#12044=CARTESIAN_POINT ( 'NONE',  ( 5.770850603891227060, 51.22559503374887413, 77.28904345712264501 ) ) ;
#12048=CARTESIAN_POINT ( 'NONE',  ( 1.417490718652078652, 52.94576632079922263, 76.80858772049349170 ) ) ;
#12051=CARTESIAN_POINT ( 'NONE',  ( -8.156636136238528678, 42.70560223241731990, 79.14287594667040082 ) ) ;
#12053=CARTESIAN_POINT ( 'NONE',  ( 5.439084145646494228, 50.71602161008325282, 77.28794373216803137 ) ) ;
#12055=DIRECTION ( 'NONE',  ( 0.3165065846431826535, 0.9485903129789529098, 2.188653791613874008E-16 ) ) ;
#12057=ORIENTED_EDGE ( 'NONE', *, *, #16399, .T. ) ;
#12059=CARTESIAN_POINT ( 'NONE',  ( -4.539611090124166637, 51.36100176422416297, 79.54777180229389444 ) ) ;
#12061=CARTESIAN_POINT ( 'NONE',  ( 0.3481951245351748159, 52.36035653588419336, 77.54150877948023890 ) ) ;
#12062=CARTESIAN_POINT ( 'NONE',  ( 0.3607744984173847924, 52.35599833409515469, 78.79918605040184332 ) ) ;
#12063=ORIENTED_EDGE ( 'NONE', *, *, #20431, .F. ) ;
#12064=DIRECTION ( 'NONE',  ( 0.3165065846431828200, 0.9485903129789527988, 0.000000000000000000 ) ) ;
#12066=CARTESIAN_POINT ( 'NONE',  ( 6.488291687484917247, 49.78758830262064095, 78.40346922251953288 ) ) ;
#12070=CARTESIAN_POINT ( 'NONE',  ( -7.497325726272184632, 40.53822013297730820, 77.43474300570518665 ) ) ;
#12073=ORIENTED_EDGE ( 'NONE', *, *, #6746, .F. ) ;
#12074=CARTESIAN_POINT ( 'NONE',  ( 4.120959222841843683, 51.53026784114320691, 77.04928664276771144 ) ) ;
#12075=ORIENTED_EDGE ( 'NONE', *, *, #11662, .T. ) ;
#12076=CARTESIAN_POINT ( 'NONE',  ( -4.157721234522135489, 51.63388627315737267, 75.40660817806873695 ) ) ;
#12077=EDGE_CURVE ( 'NONE', #18429, #4049, #2411, .T. ) ;
#12080=VERTEX_POINT ( 'NONE', #4162 ) ;
#12084=DIRECTION ( 'NONE',  ( 0.007885122365275663500, 0.9999689119394085113, 1.805443505845543142E-16 ) ) ;
#12086=ADVANCED_FACE ( 'NONE', ( #10575 ), #15656, .T. ) ;
#12087=ORIENTED_EDGE ( 'NONE', *, *, #19263, .T. ) ;
#12090=ORIENTED_EDGE ( 'NONE', *, *, #19646, .T. ) ;
#12091=CARTESIAN_POINT ( 'NONE',  ( 0.8440319792177738423, 52.35586314820839249, 77.67431863760063493 ) ) ;
#12092=CARTESIAN_POINT ( 'NONE',  ( 5.190347370342537126, 37.42057832489953739, 75.99789977449030687 ) ) ;
#12093=EDGE_CURVE ( 'NONE', #13846, #3162, #2774, .T. ) ;
#12096=CARTESIAN_POINT ( 'NONE',  ( -4.501113814897558463, 37.68688810195902050, 76.03818239474222196 ) ) ;
#12097=CARTESIAN_POINT ( 'NONE',  ( 0.3326973149608338787, 52.96014171822455552, 78.50066232894263862 ) ) ;
#12099=EDGE_CURVE ( 'NONE', #4049, #4681, #16285, .T. ) ;
#12101=EDGE_LOOP ( 'NONE', ( #1350, #13179, #7302, #2965, #5585, #9399 ) ) ;
#12102=ADVANCED_FACE ( 'NONE', ( #15973 ), #9802, .T. ) ;
#12103=CARTESIAN_POINT ( 'NONE',  ( 2.114015745586784512, 52.20152540548682651, 76.39978148915828626 ) ) ;
#12106=CARTESIAN_POINT ( 'NONE',  ( 0.4760101966287402786, 52.96644344090527312, 77.40025757944940210 ) ) ;
#12108=VERTEX_POINT ( 'NONE', #17555 ) ;
#12111=CARTESIAN_POINT ( 'NONE',  ( -3.899663497332586104, 36.48798503826752437, 77.67016408458685817 ) ) ;
#12112=LINE ( 'NONE', #20393, #5765 ) ;
#12114=CARTESIAN_POINT ( 'NONE',  ( -7.324458055672637968, 41.78044449906338542, 78.92964119392561884 ) ) ;
#12117=B_SPLINE_SURFACE_WITH_KNOTS ( 'NONE', 3, 1, ( 
 ( #17531, #9460 ),
 ( #15945, #7856 ),
 ( #10301, #16466 ),
 ( #1887, #19842 ),
 ( #6662, #13274 ),
 ( #2093, #1987 ),
 ( #8374, #13165 ),
 ( #19742, #10191 ),
 ( #16673, #5162 ),
 ( #19539, #16361 ),
 ( #8274, #18158 ),
 ( #488, #1791 ),
 ( #11886, #3578 ),
 ( #14963, #10083 ),
 ( #8594, #15074 ),
 ( #14757, #14649 ),
 ( #13065, #11474 ),
 ( #16565, #6868 ),
 ( #5081, #291 ),
 ( #6784, #13288 ),
 ( #19964, #8397 ),
 ( #298, #8082 ),
 ( #19152, #12278 ),
 ( #7876, #17866 ),
 ( #6265, #9795 ),
 ( #20731, #16074 ),
 ( #1497, #12869 ) ),
 .UNSPECIFIED., .F., .F., .F.,
 ( 4, 1, 1, 1, 1, 1, 1, 1, 1, 1, 1, 1, 1, 1, 1, 1, 1, 1, 1, 1, 1, 1, 1, 1, 4 ),
 ( 2, 2 ),
 ( 0.000000000000000000, 0.05959187408140657199, 0.1157444014141101180, 0.1691701821137891193, 0.2193251454534784761, 0.2669475916912845692, 0.3117751794269221777, 0.3541065092364359956, 0.3940487965473342680, 0.4318372767115636890, 0.4680493653760790518, 0.5025338411669280081, 0.5356117844586580912, 0.5674765898557931898, 0.5983444621881826020, 0.6284125990791417093, 0.6580179645932986432, 0.6886630208720043722, 0.7222707808379922323, 0.7592609375352028511, 0.7993858191113136780, 0.8438632570080943918, 0.8918964550480946718, 0.9439126001412549982, 1.000000000000000000 ),
 ( 0.000000000000000000, 1.000000000000000000 ),
 .UNSPECIFIED. ) ;
#12118=CARTESIAN_POINT ( 'NONE',  ( 0.8299508218102534807, 52.96365248900040967, 77.55588632845071118 ) ) ;
#12120=CARTESIAN_POINT ( 'NONE',  ( -4.158578283022523969, 37.42937009194850617, 78.58080938776616620 ) ) ;
#12121=EDGE_CURVE ( 'NONE', #8117, #19239, #20844, .T. ) ;
#12124=ORIENTED_EDGE ( 'NONE', *, *, #12237, .T. ) ;
#12127=EDGE_CURVE ( 'NONE', #5907, #2608, #4685, .T. ) ;
#12129=ORIENTED_EDGE ( 'NONE', *, *, #6187, .F. ) ;
#12130=DIRECTION ( 'NONE',  ( 0.3165065846431827645, 0.9485903129789529098, 0.000000000000000000 ) ) ;
#12132=CARTESIAN_POINT ( 'NONE',  ( 8.386782761808312614, 39.92944448690413140, 78.16120960217517677 ) ) ;
#12134=CARTESIAN_POINT ( 'NONE',  ( -4.895069120933021267, 37.22325107503680641, 76.32271929704664615 ) ) ;
#12135=CARTESIAN_POINT ( 'NONE',  ( -6.788816072239765020, 47.86659415929654671, 78.78375056423675460 ) ) ;
#12137=CARTESIAN_POINT ( 'NONE',  ( 5.894623494294806143, 51.13416898548390321, 78.12411320240556734 ) ) ;
#12138=ORIENTED_EDGE ( 'NONE', *, *, #11484, .F. ) ;
#12140=CARTESIAN_POINT ( 'NONE',  ( 8.467255801511027968, 42.53504534252056857, 79.38025142445083304 ) ) ;
#12141=CARTESIAN_POINT ( 'NONE',  ( -6.753843712027886248, 40.38066566033639759, 72.45433879953085921 ) ) ;
#12142=CARTESIAN_POINT ( 'NONE',  ( 4.470572738639666532, 36.16780480931087283, 79.45433879953087342 ) ) ;
#12144=CARTESIAN_POINT ( 'NONE',  ( 5.562547263452509938, 51.37946032036057886, 77.00567114208729436 ) ) ;
#12145=AXIS2_PLACEMENT_3D ( 'NONE', #6280, #14481, #14161 ) ;
#12146=CARTESIAN_POINT ( 'NONE',  ( 8.316956916703102110, 42.08459004996775121, 78.13669174070733447 ) ) ;
#12148=CARTESIAN_POINT ( 'NONE',  ( 0.1681371321675577124, 52.95815348057784888, 79.53018714708582593 ) ) ;
#12149=CARTESIAN_POINT ( 'NONE',  ( -7.062866454872595234, 47.10224949948419493, 78.22140724958771330 ) ) ;
#12150=EDGE_CURVE ( 'NONE', #18554, #6620, #2148, .T. ) ;
#12153=CARTESIAN_POINT ( 'NONE',  ( 6.691294758883309157, 37.75465145915448062, 79.45433879953087342 ) ) ;
#12155=VECTOR ( 'NONE', #5284, 1000.000000000000227 ) ;
#12156=CARTESIAN_POINT ( 'NONE',  ( -4.451219113684727446, 50.67724800213075298, 78.47639829077699858 ) ) ;
#12161=CARTESIAN_POINT ( 'NONE',  ( -3.491755833756905236, 51.18998518371629558, 79.42193487995672285 ) ) ;
#12162=CARTESIAN_POINT ( 'NONE',  ( 0.8384463289470892589, 52.95649690220134431, 77.58758240811609141 ) ) ;
#12164=CARTESIAN_POINT ( 'NONE',  ( -3.110947477468488209, 36.81940729104130128, 78.70659543854199569 ) ) ;
#12166=FACE_OUTER_BOUND ( 'NONE', #11773, .T. ) ;
#12169=EDGE_CURVE ( 'NONE', #10787, #13741, #6688, .T. ) ;
#12172=CARTESIAN_POINT ( 'NONE',  ( 0.5221537403065019678, 44.16218137147968292, 72.45433879953087342 ) ) ;
#12174=CARTESIAN_POINT ( 'NONE',  ( 6.923174433796239313, 50.37441983903331533, 78.52964612251847143 ) ) ;
#12177=CARTESIAN_POINT ( 'NONE',  ( 5.404201196092212278, 50.75047497752489534, 79.54845644658969661 ) ) ;
#12178=ORIENTED_EDGE ( 'NONE', *, *, #16781, .T. ) ;
#12179=CARTESIAN_POINT ( 'NONE',  ( 8.228415462672815650, 41.37506577911731398, 78.86399424569901839 ) ) ;
#12181=ORIENTED_EDGE ( 'NONE', *, *, #14421, .T. ) ;
#12182=CARTESIAN_POINT ( 'NONE',  ( -4.037464293073704802, 50.80004189835040762, 75.36471306604558151 ) ) ;
#12184=EDGE_LOOP ( 'NONE', ( #17550, #5876, #19314 ) ) ;
#12187=CARTESIAN_POINT ( 'NONE',  ( 4.470572738639666532, 36.16780480931087283, 79.45433879953087342 ) ) ;
#12188=CARTESIAN_POINT ( 'NONE',  ( -6.792737292293178797, 47.86790251333490431, 78.32492703482499508 ) ) ;
#12189=CARTESIAN_POINT ( 'NONE',  ( 6.880132251722071324, 48.33664052787082710, 72.45432679953087529 ) ) ;
#12190=EDGE_LOOP ( 'NONE', ( #8467, #2500, #12075, #878 ) ) ;
#12193=ORIENTED_EDGE ( 'NONE', *, *, #9750, .T. ) ;
#12194=CARTESIAN_POINT ( 'NONE',  ( -4.309867278466398055, 50.78806163760442161, 79.54633918777975055 ) ) ;
#12195=FACE_OUTER_BOUND ( 'NONE', #7796, .T. ) ;
#12196=CARTESIAN_POINT ( 'NONE',  ( 9.176231272041631470, 45.98187388689780164, 75.44992703482499508 ) ) ;
#12199=CARTESIAN_POINT ( 'NONE',  ( -4.517232838915925974, 37.69879457568749359, 76.09452555557021469 ) ) ;
#12200=ADVANCED_FACE ( 'NONE', ( #11508 ), #7837, .F. ) ;
#12201=CARTESIAN_POINT ( 'NONE',  ( 5.614631715549363022, 51.34098763368633911, 78.82175487302160377 ) ) ;
#12202=CARTESIAN_POINT ( 'NONE',  ( -7.506717439198443920, 42.46581745002679753, 76.87606454720180693 ) ) ;
#12203=VERTEX_POINT ( 'NONE', #18400 ) ;
#12204=CARTESIAN_POINT ( 'NONE',  ( 1.637918093877997361, 52.95811772167194675, 75.56770918405875648 ) ) ;
#12206=CARTESIAN_POINT ( 'NONE',  ( -0.8970780467398890012, 52.23845657948073296, 78.77588839903116025 ) ) ;
#12209=CARTESIAN_POINT ( 'NONE',  ( -3.396200966244447450, 52.17804077583208766, 76.13050287850805375 ) ) ;
#12210=ORIENTED_EDGE ( 'NONE', *, *, #15507, .T. ) ;
#12211=AXIS2_PLACEMENT_3D ( 'NONE', #10153, #6516, #9946 ) ;
#12212=FACE_OUTER_BOUND ( 'NONE', #10078, .T. ) ;
#12213=ORIENTED_EDGE ( 'NONE', *, *, #12241, .F. ) ;
#12214=CARTESIAN_POINT ( 'NONE',  ( 4.905034931190686009, 51.86513819399005598, 79.33697856897433098 ) ) ;
#12217=CARTESIAN_POINT ( 'NONE',  ( 5.451303755781102822, 37.60902651911217731, 77.68277620389109472 ) ) ;
#12218=LINE ( 'NONE', #13705, #11821 ) ;
#12227=AXIS2_PLACEMENT_3D ( 'NONE', #1060, #7435, #4232 ) ;
#12229=CARTESIAN_POINT ( 'NONE',  ( 8.941920682866751235, 41.59322805360929465, 78.83412695248559032 ) ) ;
#12231=ORIENTED_EDGE ( 'NONE', *, *, #17431, .T. ) ;
#12232=LINE ( 'NONE', #9363, #4400 ) ;
#12233=AXIS2_PLACEMENT_3D ( 'NONE', #14928, #6940, #13346 ) ;
#12234=CARTESIAN_POINT ( 'NONE',  ( 0.5221537403065019678, 44.16218137147968292, 72.45433879953087342 ) ) ;
#12235=CARTESIAN_POINT ( 'NONE',  ( -3.512376142844359173, 52.09502624807847582, 79.07098488719154261 ) ) ;
#12237=EDGE_CURVE ( 'NONE', #2058, #5122, #5947, .T. ) ;
#12238=CARTESIAN_POINT ( 'NONE',  ( -4.883901707777988932, 37.21500215679002821, 76.12782976279942204 ) ) ;
#12239=CARTESIAN_POINT ( 'NONE',  ( -7.195832550073633094, 46.64673995458454669, 79.32924967153994089 ) ) ;
#12240=CARTESIAN_POINT ( 'NONE',  ( 5.631785411401764918, 36.99756487055721976, 77.76022115247205591 ) ) ;
#12241=EDGE_CURVE ( 'NONE', #585, #19492, #8406, .T. ) ;
#12242=CARTESIAN_POINT ( 'NONE',  ( -5.661408436751226070, 39.74363423441516829, 72.45432679953087529 ) ) ;
#12243=AXIS2_PLACEMENT_3D ( 'NONE', #19322, #14340, #14545 ) ;
#12245=VERTEX_POINT ( 'NONE', #5299 ) ;
#12247=CARTESIAN_POINT ( 'NONE',  ( 8.608186895778700887, 42.95742477254270852, 78.97126489842982267 ) ) ;
#12248=CARTESIAN_POINT ( 'NONE',  ( -4.320790804570143528, 36.79905481608121676, 75.39293290059653430 ) ) ;
#12250=CARTESIAN_POINT ( 'NONE',  ( 8.949991632966883159, 41.61741720307092152, 76.25788209700408515 ) ) ;
#12251=CARTESIAN_POINT ( 'NONE',  ( 5.916041096196198446, 51.11834866571297908, 77.16780247135808679 ) ) ;
#12253=B_SPLINE_SURFACE_WITH_KNOTS ( 'NONE', 3, 1, ( 
 ( #11366, #14220 ),
 ( #6137, #12640 ),
 ( #19122, #9561 ),
 ( #3164, #12837 ),
 ( #12527, #4631 ),
 ( #1246, #21004 ),
 ( #19316, #9450 ),
 ( #11152, #7739 ),
 ( #6439, #15936 ),
 ( #4732, #9666 ),
 ( #12948, #19428 ) ),
 .UNSPECIFIED., .F., .F., .F.,
 ( 4, 1, 1, 1, 1, 1, 1, 1, 4 ),
 ( 2, 2 ),
 ( 0.000000000000000000, 0.1182921183292337947, 0.2229146666077276573, 0.3191072744444787279, 0.4123240778398947204, 0.5160602913484956256, 0.6446607815519475038, 0.8056994663548258107, 1.000000000000000000 ),
 ( 0.000000000000000000, 1.000000000000000000 ),
 .UNSPECIFIED. ) ;
#12254=DIRECTION ( 'NONE',  ( -0.9534635866061452747, -0.3015081906286225522, -2.009271279954815797E-16 ) ) ;
#12256=CARTESIAN_POINT ( 'NONE',  ( 8.396447191880023198, 42.32282744744201608, 78.11626675975762168 ) ) ;
#12258=CARTESIAN_POINT ( 'NONE',  ( -4.592862224480081856, 51.32295045326188898, 75.97198585835440099 ) ) ;
#12259=CARTESIAN_POINT ( 'NONE',  ( -7.088565933990943257, 47.02522653022194987, 77.78596583901244799 ) ) ;
#12262=CARTESIAN_POINT ( 'NONE',  ( 6.386300776676741897, 37.53671392601205525, 75.49608936836499140 ) ) ;
#12263=EDGE_LOOP ( 'NONE', ( #13449, #11491, #18488, #12210 ) ) ;
#12264=CARTESIAN_POINT ( 'NONE',  ( 2.115041367457930033, 52.20598078514408513, 76.48963291717792856 ) ) ;
#12267=CARTESIAN_POINT ( 'NONE',  ( -4.744888236371026302, 51.21431823119217341, 78.89490084226201816 ) ) ;
#12271=CARTESIAN_POINT ( 'NONE',  ( -5.004817973257478236, 39.29348442311233214, 78.18375056423674607 ) ) ;
#12272=CARTESIAN_POINT ( 'NONE',  ( -3.077292339936458454, 51.48614562192336308, 79.07098488719154261 ) ) ;
#12276=FACE_OUTER_BOUND ( 'NONE', #8673, .T. ) ;
#12278=CARTESIAN_POINT ( 'NONE',  ( 6.504942014150000951, 49.75851833300988858, 76.28194508213313441 ) ) ;
#12279=DIRECTION ( 'NONE',  ( -1.540237394707283727E-16, -1.793354297423763257E-16, 1.000000000000000000 ) ) ;
#12283=CARTESIAN_POINT ( 'NONE',  ( -4.517072128342571880, 36.94403992325788977, 78.34992703482498655 ) ) ;
#12284=DIRECTION ( 'NONE',  ( 0.003108166696664913138, -0.009828999206266906055, -0.9999468636254573717 ) ) ;
#12285=CARTESIAN_POINT ( 'NONE',  ( -0.9436870690626146807, 52.23009998296728895, 77.77566232894263010 ) ) ;
#12286=CARTESIAN_POINT ( 'NONE',  ( -7.302117543854899750, 40.13466614431609258, 78.26848339007013067 ) ) ;
#12287=DIRECTION ( 'NONE',  ( -0.9485903129789527988, 0.3165065846431829311, -8.934458285744989980E-17 ) ) ;
#12289=CARTESIAN_POINT ( 'NONE',  ( 6.055018060417216574, 50.21607566361303299, 79.42942117149121373 ) ) ;
#12290=EDGE_LOOP ( 'NONE', ( #20655, #13363, #6781, #14097 ) ) ;
#12291=CARTESIAN_POINT ( 'NONE',  ( 4.527140486693829402, 51.31778872522085777, 77.65249324435147571 ) ) ;
#12292=AXIS2_PLACEMENT_3D ( 'NONE', #12565, #20843, #6270 ) ;
#12294=EDGE_LOOP ( 'NONE', ( #9554, #16946, #14113, #10483 ) ) ;
#12295=CARTESIAN_POINT ( 'NONE',  ( -4.621776214648809500, 51.30228957449607208, 75.36056307228784590 ) ) ;
#12297=CARTESIAN_POINT ( 'NONE',  ( -7.955322860971263843, 41.76477423154450008, 77.57193099691271243 ) ) ;
#12298=EDGE_LOOP ( 'NONE', ( #1249, #8232, #16519, #4309, #6636 ) ) ;
#12303=ORIENTED_EDGE ( 'NONE', *, *, #5839, .F. ) ;
#12305=CARTESIAN_POINT ( 'NONE',  ( 0.6748029067580463281, 52.96487981809853096, 78.92081865479288183 ) ) ;
#12306=VECTOR ( 'NONE', #18614, 1000.000000000000114 ) ;
#12307=VERTEX_POINT ( 'NONE', #15213 ) ;
#12308=CARTESIAN_POINT ( 'NONE',  ( -5.073584210444301412, 50.15674762947981691, 79.28952735418165787 ) ) ;
#12310=VECTOR ( 'NONE', #17537, 1000.000000000000114 ) ;
#12312=CARTESIAN_POINT ( 'NONE',  ( -3.899559394394517486, 36.48790814162070006, 77.72081520951157074 ) ) ;
#12313=CARTESIAN_POINT ( 'NONE',  ( 5.753005855668248181, 51.23877623043087937, 78.93669174070734584 ) ) ;
#12314=EDGE_CURVE ( 'NONE', #20066, #10307, #10662, .T. ) ;
#12316=ORIENTED_EDGE ( 'NONE', *, *, #20131, .F. ) ;
#12317=CARTESIAN_POINT ( 'NONE',  ( 1.193698689701933713, 52.96162055492719389, 75.41083127720757773 ) ) ;
#12318=ORIENTED_EDGE ( 'NONE', *, *, #6498, .F. ) ;
#12323=VECTOR ( 'NONE', #16922, 1000.000000000000000 ) ;
#12324=ORIENTED_EDGE ( 'NONE', *, *, #16156, .F. ) ;
#12327=CARTESIAN_POINT ( 'NONE',  ( 5.166781194794222820, 50.75778176762062799, 79.54621928524807117 ) ) ;
#12330=CARTESIAN_POINT ( 'NONE',  ( -4.517387068041351483, 36.94427255652684039, 78.31852111096432623 ) ) ;
#12331=CARTESIAN_POINT ( 'NONE',  ( -7.426618516485039123, 40.09345743339805068, 78.72343487459158951 ) ) ;
#12332=CARTESIAN_POINT ( 'NONE',  ( -7.366006458923896716, 41.92050534979284038, 79.54485830165070581 ) ) ;
#12333=LINE ( 'NONE', #4012, #11697 ) ;
#12334=DIRECTION ( 'NONE',  ( 0.5941461771851692664, 0.8043570849667761591, 2.357623395011396791E-16 ) ) ;
#12335=VECTOR ( 'NONE', #693, 1000.000000000000114 ) ;
#12336=CARTESIAN_POINT ( 'NONE',  ( -5.403345028831681773, 49.82403353266325041, 76.76022115247205591 ) ) ;
#12337=CARTESIAN_POINT ( 'NONE',  ( 4.891544444475510289, 50.95027012611001993, 75.39573407869305299 ) ) ;
#12341=EDGE_CURVE ( 'NONE', #14974, #6003, #16618, .T. ) ;
#12342=CARTESIAN_POINT ( 'NONE',  ( -7.337607140633251923, 40.20406537192692298, 78.93275508898662451 ) ) ;
#12343=CARTESIAN_POINT ( 'NONE',  ( 8.385679600361122255, 39.92613824206362949, 77.69330938776616335 ) ) ;
#12346=CARTESIAN_POINT ( 'NONE',  ( -4.428870440144692999, 50.69880833818904620, 78.82590693216131683 ) ) ;
#12348=VECTOR ( 'NONE', #6828, 1000.000000000000227 ) ;
#12350=CARTESIAN_POINT ( 'NONE',  ( -7.708574807372626125, 47.31288976295603277, 79.02985774836469091 ) ) ;
#12351=CARTESIAN_POINT ( 'NONE',  ( 5.619997200715287633, 36.98914144679460492, 77.75986257808632729 ) ) ;
#12353=EDGE_CURVE ( 'NONE', #9638, #5209, #9771, .T. ) ;
#12354=CARTESIAN_POINT ( 'NONE',  ( 8.296628936784257391, 41.55497301399228149, 78.93669174070734584 ) ) ;
#12355=CARTESIAN_POINT ( 'NONE',  ( -4.244029479098209379, 50.83477438462418974, 75.97198585835440099 ) ) ;
#12358=CARTESIAN_POINT ( 'NONE',  ( -2.073200253767597090, 36.38374080505226971, 72.45433879953087342 ) ) ;
#12361=EDGE_CURVE ( 'NONE', #4917, #10614, #4910, .T. ) ;
#12362=EDGE_CURVE ( 'NONE', #11879, #10061, #12546, .T. ) ;
#12363=EDGE_CURVE ( 'NONE', #5674, #9005, #2901, .T. ) ;
#12364=CARTESIAN_POINT ( 'NONE',  ( -0.9376789570059210766, 52.84025085569253122, 78.01128938824629699 ) ) ;
#12365=CARTESIAN_POINT ( 'NONE',  ( -6.937748720045943784, 47.47723528808076310, 78.31886496287775401 ) ) ;
#12366=DIRECTION ( 'NONE',  ( 1.540237394707284220E-16, 1.793354297423764243E-16, -1.000000000000000000 ) ) ;
#12369=EDGE_CURVE ( 'NONE', #19774, #10630, #4450, .T. ) ;
#12370=CARTESIAN_POINT ( 'NONE',  ( 5.939883047636084434, 51.10073757659671401, 76.92469047792664583 ) ) ;
#12374=ORIENTED_EDGE ( 'NONE', *, *, #13471, .F. ) ;
#12376=CIRCLE ( 'NONE', #3863, 8.800000000000000711 ) ;
#12377=CARTESIAN_POINT ( 'NONE',  ( -0.8532138448282817755, 52.21879250163868846, 76.01337353251631157 ) ) ;
#12380=DIRECTION ( 'NONE',  ( -0.3165065846431825980, -0.9485903129789527988, 0.000000000000000000 ) ) ;
#12381=CARTESIAN_POINT ( 'NONE',  ( -3.681032862722698695, 36.32649139546035855, 79.10742496273583413 ) ) ;
#12382=VERTEX_POINT ( 'NONE', #11069 ) ;
#12383=CARTESIAN_POINT ( 'NONE',  ( 8.305956354856951052, 41.60725829672735898, 75.97389479739716478 ) ) ;
#12385=CARTESIAN_POINT ( 'NONE',  ( -3.055718635266669647, 36.78391400955043622, 76.62933879953087057 ) ) ;
#12386=CARTESIAN_POINT ( 'NONE',  ( 3.961507247562194411, 36.71833509068318335, 72.45433879953087342 ) ) ;
#12391=CARTESIAN_POINT ( 'NONE',  ( -6.374721436948748376, 46.24015083227975964, 79.45433879953087342 ) ) ;
#12392=EDGE_LOOP ( 'NONE', ( #3754, #17521, #20199, #9443 ) ) ;
#12393=EDGE_CURVE ( 'NONE', #15079, #3682, #3903, .T. ) ;
#12394=CARTESIAN_POINT ( 'NONE',  ( 8.211300288254456348, 41.32377051561905290, 78.45948585835439815 ) ) ;
#12396=EDGE_LOOP ( 'NONE', ( #182, #6291, #3023, #2812 ) ) ;
#12399=CARTESIAN_POINT ( 'NONE',  ( 4.881482038019723468, 51.88253576740703465, 75.58280986828056314 ) ) ;
#12400=ORIENTED_EDGE ( 'NONE', *, *, #19903, .T. ) ;
#12402=CARTESIAN_POINT ( 'NONE',  ( -4.139151435122498945, 50.72720857236262759, 79.54845644658969661 ) ) ;
#12404=CARTESIAN_POINT ( 'NONE',  ( 4.884665026186969961, 36.46369999710588417, 75.53067132529541539 ) ) ;
#12405=CARTESIAN_POINT ( 'NONE',  ( -4.802657821332910082, 51.17303820085790278, 78.59458524649963351 ) ) ;
#12406=ADVANCED_FACE ( 'NONE', ( #10203 ), #8382, .T. ) ;
#12408=CARTESIAN_POINT ( 'NONE',  ( 1.602182432222049702, 52.29126342916185166, 79.36024077264127641 ) ) ;
#12411=CARTESIAN_POINT ( 'NONE',  ( -5.405834154369066447, 49.82777573959609185, 78.20908272895746904 ) ) ;
#12415=CARTESIAN_POINT ( 'NONE',  ( 5.521494261397323022, 36.91875485278077207, 76.01263398532663018 ) ) ;
#12416=CARTESIAN_POINT ( 'NONE',  ( 5.581823371501742237, 36.96186382607169207, 75.98067903659783440 ) ) ;
#12418=ORIENTED_EDGE ( 'NONE', *, *, #13422, .F. ) ;
#12419=CARTESIAN_POINT ( 'NONE',  ( 0.9669959323506999160, 52.21057007825091745, 75.37848164766056414 ) ) ;
#12420=ORIENTED_EDGE ( 'NONE', *, *, #3216, .F. ) ;
#12421=CARTESIAN_POINT ( 'NONE',  ( 0.5221537403065008576, 44.16218137147968292, 80.45433879953087342 ) ) ;
#12422=CARTESIAN_POINT ( 'NONE',  ( 0.3528405447447653387, 52.36129150091981899, 75.36602869171218799 ) ) ;
#12424=B_SPLINE_SURFACE_WITH_KNOTS ( 'NONE', 3, 1, ( 
 ( #7890, #20851 ),
 ( #6279, #12780 ),
 ( #20446, #19261 ),
 ( #4675, #9604 ),
 ( #18853, #13314 ),
 ( #11724, #9809 ),
 ( #17779, #3206 ),
 ( #6380, #5205 ),
 ( #11622, #19572 ),
 ( #9921, #4781 ),
 ( #19471, #6699 ),
 ( #18196, #8415 ),
 ( #12885, #3302 ),
 ( #9708, #16187 ),
 ( #1613, #14892 ),
 ( #8204, #18096 ),
 ( #3518, #3411 ),
 ( #13203, #8097 ),
 ( #315, #16293 ) ),
 .UNSPECIFIED., .F., .F., .F.,
 ( 4, 1, 1, 1, 1, 1, 1, 1, 1, 1, 1, 1, 1, 1, 1, 1, 4 ),
 ( 2, 2 ),
 ( 0.000000000000000000, 0.07116601901339190961, 0.1384582187113551910, 0.2014355002094309066, 0.2607329607935783833, 0.3172301401005571675, 0.3704881719161017273, 0.4221645193212664182, 0.4717967126376631515, 0.5218096718684601676, 0.5745631757277218643, 0.6310618342314253670, 0.6925022631777019155, 0.7595319055140381526, 0.8328598856178031085, 0.9128843800434378597, 0.9999999999999998890 ),
 ( 0.000000000000000000, 1.000000000000000000 ),
 .UNSPECIFIED. ) ;
#12427=ORIENTED_EDGE ( 'NONE', *, *, #14164, .F. ) ;
#12428=CARTESIAN_POINT ( 'NONE',  ( 4.283022132325689846, 51.41057898707959595, 79.11209812681292419 ) ) ;
#12429=DIRECTION ( 'NONE',  ( 1.540237394707284220E-16, 1.793354297423764243E-16, -1.000000000000000000 ) ) ;
#12430=CARTESIAN_POINT ( 'NONE',  ( 7.680282685949594068, 40.19320369954859729, 76.21925085218815354 ) ) ;
#12431=ORIENTED_EDGE ( 'NONE', *, *, #4099, .F. ) ;
#12433=CARTESIAN_POINT ( 'NONE',  ( -6.891583108293479754, 40.88741496916635754, 79.38495514127318131 ) ) ;
#12436=DIRECTION ( 'NONE',  ( -0.5941461771851693774, -0.8043570849667760481, -2.357623395011396791E-16 ) ) ;
#12437=CARTESIAN_POINT ( 'NONE',  ( 4.776132423410367700, 51.96035328397762498, 75.67068799376596644 ) ) ;
#12443=DIRECTION ( 'NONE',  ( -0.3165065846431825980, -0.9485903129789527988, 0.000000000000000000 ) ) ;
#12444=CARTESIAN_POINT ( 'NONE',  ( -3.850375455727051310, 51.85350431403718119, 79.38294305353919356 ) ) ;
#12446=CARTESIAN_POINT ( 'NONE',  ( -8.311663145292943256, 42.89697774700320565, 78.43041451606663372 ) ) ;
#12447=CARTESIAN_POINT ( 'NONE',  ( 8.628576132315311398, 42.92643779739703547, 77.76019013650333989 ) ) ;
#12448=EDGE_CURVE ( 'NONE', #12841, #374, #8282, .T. ) ;
#12449=ORIENTED_EDGE ( 'NONE', *, *, #20534, .T. ) ;
#12451=CARTESIAN_POINT ( 'NONE',  ( -4.637383097126852149, 37.03290878947740339, 79.54612747205591461 ) ) ;
#12452=CARTESIAN_POINT ( 'NONE',  ( 8.909863635552733641, 41.49715104914803021, 76.00786757613292366 ) ) ;
#12453=CARTESIAN_POINT ( 'NONE',  ( 0.3295378388929664504, 52.35996878549973133, 78.69601710400918648 ) ) ;
#12454=DIRECTION ( 'NONE',  ( -1.540237394707284467E-16, -1.793354297423764243E-16, 1.000000000000000000 ) ) ;
#12455=CARTESIAN_POINT ( 'NONE',  ( -4.038468682635965479, 50.97692532282305677, 78.66485665160126928 ) ) ;
#12458=EDGE_CURVE ( 'NONE', #5674, #4858, #1690, .T. ) ;
#12459=VERTEX_POINT ( 'NONE', #85 ) ;
#12460=CARTESIAN_POINT ( 'NONE',  ( -5.508129029085064410, 38.61210022972240097, 78.53742703482498655 ) ) ;
#12461=CARTESIAN_POINT ( 'NONE',  ( 0.6309698074632331677, 52.36148849043851072, 78.93320637710581877 ) ) ;
#12462=CARTESIAN_POINT ( 'NONE',  ( 5.895605937740185709, 51.13344329408603528, 78.75475733230618403 ) ) ;
#12463=CARTESIAN_POINT ( 'NONE',  ( 0.9542774672681346715, 52.35128066847121886, 75.37609433907658740 ) ) ;
#12465=B_SPLINE_CURVE_WITH_KNOTS ( 'NONE', 3,
 ( #2410, #8911, #15075, #707, #15400, #5591, #3579, #13572, #3991, #12097 ),
 .UNSPECIFIED., .F., .F.,
 ( 4, 2, 2, 2, 4 ),
 ( 0.000000000000000000, 0.0001454258534705730479, 0.0002181387802058595718, 0.0002908517069411460957, 0.0005817034138821733629 ),
 .UNSPECIFIED. ) ;
#12466=ORIENTED_EDGE ( 'NONE', *, *, #18293, .T. ) ;
#12467=LINE ( 'NONE', #6066, #15658 ) ;
#12469=ORIENTED_EDGE ( 'NONE', *, *, #1186, .T. ) ;
#12470=CARTESIAN_POINT ( 'NONE',  ( 6.691294758883309157, 37.75465145915448062, 78.79551527011911105 ) ) ;
#12471=CARTESIAN_POINT ( 'NONE',  ( 0.5221537403065015237, 44.16218137147968292, 75.45433879953088763 ) ) ;
#12473=CARTESIAN_POINT ( 'NONE',  ( 8.263696488377984650, 41.51540230796872066, 78.01079203130994699 ) ) ;
#12474=DIRECTION ( 'NONE',  ( 1.540237394707284220E-16, 1.793354297423764243E-16, -1.000000000000000000 ) ) ;
#12476=CARTESIAN_POINT ( 'NONE',  ( -3.736319852780225048, 36.36732966792004618, 79.18890841331918296 ) ) ;
#12477=EDGE_LOOP ( 'NONE', ( #10363, #17357, #5646, #11458 ) ) ;
#12478=LINE ( 'NONE', #2993, #17667 ) ;
#12480=CARTESIAN_POINT ( 'NONE',  ( 6.208852450660900857, 50.07003620731933324, 77.72233382526972889 ) ) ;
#12481=CARTESIAN_POINT ( 'NONE',  ( 4.567922609689349045, 52.11414948617044729, 77.12434737327507150 ) ) ;
#12487=VERTEX_POINT ( 'NONE', #10092 ) ;
#12488=ORIENTED_EDGE ( 'NONE', *, *, #8700, .F. ) ;
#12489=CARTESIAN_POINT ( 'NONE',  ( -3.566438244846301231, 38.23101125920473464, 76.81463291717793140 ) ) ;
#12491=CARTESIAN_POINT ( 'NONE',  ( 4.634072907867718527, 52.06528692560263494, 75.88092117868445996 ) ) ;
#12494=CARTESIAN_POINT ( 'NONE',  ( -4.740836738068939127, 51.21721328354402658, 79.54427050475041483 ) ) ;
#12496=VERTEX_POINT ( 'NONE', #3278 ) ;
#12498=CARTESIAN_POINT ( 'NONE',  ( 4.393996117251955269, 36.11308595931626542, 76.73963291717792856 ) ) ;
#12503=CARTESIAN_POINT ( 'NONE',  ( 0.6699824260347926330, 52.35356008955702123, 78.92081865479288183 ) ) ;
#12504=VECTOR ( 'NONE', #4320, 1000.000000000000227 ) ;
#12505=EDGE_LOOP ( 'NONE', ( #15988, #19932, #7686, #5976 ) ) ;
#12511=CARTESIAN_POINT ( 'NONE',  ( 5.074465183246153366, 37.34623967253333632, 76.70433879953087342 ) ) ;
#12512=CARTESIAN_POINT ( 'NONE',  ( 5.677877744449962627, 51.29427033984291029, 78.92241520643889885 ) ) ;
#12513=AXIS2_PLACEMENT_3D ( 'NONE', #3393, #8297, #11290 ) ;
#12514=CARTESIAN_POINT ( 'NONE',  ( -3.513222121926658392, 37.12736930804990010, 77.68963291717793140 ) ) ;
#12516=CARTESIAN_POINT ( 'NONE',  ( 1.374762211169257897, 52.92186301335429732, 76.79053302980838680 ) ) ;
#12518=CARTESIAN_POINT ( 'NONE',  ( 6.780993214391527246, 50.47944337839869888, 75.76076839092205262 ) ) ;
#12519=CARTESIAN_POINT ( 'NONE',  ( -0.9307445186194918119, 52.23244111531224831, 76.43472685704757907 ) ) ;
#12521=ORIENTED_EDGE ( 'NONE', *, *, #17925, .T. ) ;
#12523=CARTESIAN_POINT ( 'NONE',  ( -4.238909561394200942, 37.66340538711140340, 75.36060488990274564 ) ) ;
#12524=CARTESIAN_POINT ( 'NONE',  ( 5.370821505553895925, 50.60706540930752340, 79.54761434581399726 ) ) ;
#12526=CARTESIAN_POINT ( 'NONE',  ( 5.270041363239100995, 50.68150764076370507, 79.54768974400036541 ) ) ;
#12527=CARTESIAN_POINT ( 'NONE',  ( 8.818545868716455516, 41.22346590884859552, 77.48357784852399277 ) ) ;
#12529=VECTOR ( 'NONE', #3849, 1000.000000000000114 ) ;
#12530=ORIENTED_EDGE ( 'NONE', *, *, #5873, .F. ) ;
#12531=CARTESIAN_POINT ( 'NONE',  ( 6.120570592859386316, 50.15433377453709340, 75.51955991867161799 ) ) ;
#12540=CARTESIAN_POINT ( 'NONE',  ( -7.382281811460246423, 40.29405236905069643, 79.07682695550360563 ) ) ;
#12541=CARTESIAN_POINT ( 'NONE',  ( 8.951736416449948663, 41.62264642985666541, 78.48252796260671005 ) ) ;
#12543=CARTESIAN_POINT ( 'NONE',  ( -0.9304578138521076847, 52.97982027947340100, 78.32762347114741885 ) ) ;
#12545=DIRECTION ( 'NONE',  ( 0.9485903129789527988, -0.3165065846431829311, 8.934458285744989980E-17 ) ) ;
#12546=LINE ( 'NONE', #17336, #4834 ) ;
#12547=( NAMED_UNIT ( * ) PLANE_ANGLE_UNIT ( ) SI_UNIT ( $, .RADIAN. ) );
#12549=CARTESIAN_POINT ( 'NONE',  ( -7.294099066665586051, 42.13140977396874831, 79.52797380487967871 ) ) ;
#12550=CARTESIAN_POINT ( 'NONE',  ( 5.341647780419348734, 37.53715857429408231, 75.97340568087561508 ) ) ;
#12555=CARTESIAN_POINT ( 'NONE',  ( 8.947628219434415442, 41.61033390278195299, 77.32525259820312158 ) ) ;
#12556=AXIS2_PLACEMENT_3D ( 'NONE', #20962, #15798, #19384 ) ;
#12557=CARTESIAN_POINT ( 'NONE',  ( -4.056262464355276265, 50.96498501010217552, 78.79673532154967575 ) ) ;
#12558=CARTESIAN_POINT ( 'NONE',  ( 5.398882651910504649, 50.75441279359508684, 77.28963291717792572 ) ) ;
#12559=VECTOR ( 'NONE', #4746, 1000.000000000000114 ) ;
#12561=ORIENTED_EDGE ( 'NONE', *, *, #13418, .T. ) ;
#12562=CARTESIAN_POINT ( 'NONE',  ( -5.953540064417265576, 38.00510092317821176, 78.67637590524894620 ) ) ;
#12563=EDGE_CURVE ( 'NONE', #11086, #6021, #19950, .T. ) ;
#12564=VECTOR ( 'NONE', #14519, 1000.000000000000000 ) ;
#12565=CARTESIAN_POINT ( 'NONE',  ( 0.5221537403065015237, 44.16218137147968292, 75.45433879953088763 ) ) ;
#12566=CARTESIAN_POINT ( 'NONE',  ( 5.590052860727733552, 36.96774431777176062, 78.26671861549210973 ) ) ;
#12567=AXIS2_PLACEMENT_3D ( 'NONE', #1227, #12811, #6310 ) ;
#12568=VECTOR ( 'NONE', #6197, 1000.000000000000227 ) ;
#12569=EDGE_LOOP ( 'NONE', ( #1376, #14906, #2097, #12324 ) ) ;
#12573=CARTESIAN_POINT ( 'NONE',  ( -5.405939962049822967, 49.82766502745145232, 78.10580938776615767 ) ) ;
#12577=CARTESIAN_POINT ( 'NONE',  ( 5.760694563098077481, 51.23309689197249384, 79.54845644658969661 ) ) ;
#12578=FACE_OUTER_BOUND ( 'NONE', #18571, .T. ) ;
#12579=CARTESIAN_POINT ( 'NONE',  ( 0.6297410054736833906, 52.96530755180469896, 75.97323462179006981 ) ) ;
#12580=CARTESIAN_POINT ( 'NONE',  ( -3.547760446584435012, 36.22804843019940790, 78.70659543854199569 ) ) ;
#12581=VERTEX_POINT ( 'NONE', #16371 ) ;
#12582=DIRECTION ( 'NONE',  ( -0.3165065846431825980, -0.9485903129789530208, 0.000000000000000000 ) ) ;
#12584=VERTEX_POINT ( 'NONE', #1996 ) ;
#12586=AXIS2_PLACEMENT_3D ( 'NONE', #7645, #15420, #835 ) ;
#12589=CARTESIAN_POINT ( 'NONE',  ( 5.427780505986065762, 36.85179043424346190, 77.43080938776617472 ) ) ;
#12591=CARTESIAN_POINT ( 'NONE',  ( -7.286377378278460881, 41.68676597530894412, 78.93669174070734584 ) ) ;
#12592=B_SPLINE_SURFACE_WITH_KNOTS ( 'NONE', 3, 1, ( 
 ( #999, #687 ),
 ( #12295, #20240 ),
 ( #2600, #2502 ),
 ( #9096, #12182 ),
 ( #8777, #8993 ),
 ( #7166, #15266 ),
 ( #20140, #5573 ),
 ( #12076, #3970 ),
 ( #17382, #19279 ),
 ( #20865, #6399 ),
 ( #9409, #17486 ),
 ( #7906, #14395 ),
 ( #12796, #17582 ),
 ( #19086, #7702 ),
 ( #15898, #12598 ),
 ( #4495, #1212 ),
 ( #11218, #11115 ),
 ( #11015, #6091 ),
 ( #19177, #1318 ),
 ( #18976, #15800 ),
 ( #4387, #17797 ),
 ( #4692, #7801 ),
 ( #17692, #2912 ),
 ( #3011, #2809 ),
 ( #3221, #10912 ),
 ( #14288, #20764 ),
 ( #12700, #16205 ) ),
 .UNSPECIFIED., .F., .F., .F.,
 ( 4, 1, 1, 1, 1, 1, 1, 1, 1, 1, 1, 1, 1, 1, 1, 1, 1, 1, 1, 1, 1, 1, 1, 1, 4 ),
 ( 2, 2 ),
 ( 0.000000000000000000, 0.04692756115915790172, 0.09175764483083305445, 0.1348320239538815524, 0.1755606184341063081, 0.2149124488236470176, 0.2520401868719510108, 0.2875439711136699161, 0.3211732624427411364, 0.3845494416143411254, 0.4434775415870848558, 0.4991878644837567380, 0.5522905917841786083, 0.6030460594100006677, 0.6509449284921694501, 0.6968976034913704209, 0.7406443924834601455, 0.7634319837341128068, 0.7890572409307390345, 0.8171397283500007047, 0.8480511511928767732, 0.8815178987434894031, 0.9182285974223420855, 0.9576130192529551666, 1.000000000000000000 ),
 ( 0.000000000000000000, 1.000000000000000000 ),
 .UNSPECIFIED. ) ;
#12593=CIRCLE ( 'NONE', #3409, 8.800000000000000711 ) ;
#12598=CARTESIAN_POINT ( 'NONE',  ( -3.119948039661358585, 51.45566542062479698, 75.79042024895623797 ) ) ;
#12600=CARTESIAN_POINT ( 'NONE',  ( 8.617049974001410817, 45.47086815721986142, 79.23054824294796106 ) ) ;
#12601=CARTESIAN_POINT ( 'NONE',  ( 8.787829143201870252, 41.13140593384865440, 77.80727997600146750 ) ) ;
#12603=CARTESIAN_POINT ( 'NONE',  ( -5.484081776600456593, 50.68611759094706315, 79.26884812577799266 ) ) ;
#12604=LINE ( 'NONE', #7607, #17429 ) ;
#12605=CARTESIAN_POINT ( 'NONE',  ( 4.425132644269478277, 36.13533498154198043, 76.25036098622081226 ) ) ;
#12606=EDGE_CURVE ( 'NONE', #16873, #2184, #5530, .T. ) ;
#12607=CARTESIAN_POINT ( 'NONE',  ( 5.228185313790076449, 50.87180408165244927, 76.07177712439327877 ) ) ;
#12610=CARTESIAN_POINT ( 'NONE',  ( 0.8172236777486411308, 52.96375677797878012, 78.79200666326234170 ) ) ;
#12611=EDGE_CURVE ( 'NONE', #2112, #13012, #3777, .T. ) ;
#12614=DIRECTION ( 'NONE',  ( 0.3165065846431826535, 0.9485903129789529098, 2.188653791613874008E-16 ) ) ;
#12616=CARTESIAN_POINT ( 'NONE',  ( 5.144371138689071365, 37.39619190887245992, 76.03636210503219672 ) ) ;
#12617=CARTESIAN_POINT ( 'NONE',  ( 5.599463258324014703, 51.35219196201597214, 78.62371398036725623 ) ) ;
#12618=ADVANCED_FACE ( 'NONE', ( #6974 ), #5642, .F. ) ;
#12620=CARTESIAN_POINT ( 'NONE',  ( -3.752498811055299477, 36.37928041266965806, 77.59103917682324436 ) ) ;
#12622=ORIENTED_EDGE ( 'NONE', *, *, #13819, .F. ) ;
#12623=CARTESIAN_POINT ( 'NONE',  ( 1.830036527069967445, 52.86461688513685431, 76.99776405956157532 ) ) ;
#12627=CARTESIAN_POINT ( 'NONE',  ( 5.631785411401764918, 36.99756487055721976, 77.76022115247205591 ) ) ;
#12634=CARTESIAN_POINT ( 'NONE',  ( -4.546230963980876005, 36.96557838055436207, 76.09208750614521932 ) ) ;
#12635=DIRECTION ( 'NONE',  ( -0.5941461771851783702, -0.8043570849667693867, -2.357623395011398763E-16 ) ) ;
#12636=VECTOR ( 'NONE', #13718, 1000.000000000000000 ) ;
#12637=ORIENTED_EDGE ( 'NONE', *, *, #7938, .T. ) ;
#12638=ADVANCED_FACE ( 'NONE', ( #3896 ), #7080, .T. ) ;
#12639=CARTESIAN_POINT ( 'NONE',  ( 4.154601481547989472, 51.50543814870972881, 78.70655549710109256 ) ) ;
#12640=CARTESIAN_POINT ( 'NONE',  ( 8.286663948227678489, 41.54943773017198794, 77.52392363563762956 ) ) ;
#12644=CARTESIAN_POINT ( 'NONE',  ( -7.176555495732481305, 41.78858715306228078, 79.54845644658969661 ) ) ;
#12645=CARTESIAN_POINT ( 'NONE',  ( 6.243933501899546101, 38.28785586627228099, 75.68656110871486931 ) ) ;
#12647=DIRECTION ( 'NONE',  ( 0.000000000000000000, 0.000000000000000000, 1.000000000000000000 ) ) ;
#12648=FACE_OUTER_BOUND ( 'NONE', #7552, .T. ) ;
#12651=EDGE_CURVE ( 'NONE', #12841, #17122, #8216, .T. ) ;
#12652=DIRECTION ( 'NONE',  ( -1.540237394707284467E-16, -1.793354297423764243E-16, 1.000000000000000000 ) ) ;
#12655=CARTESIAN_POINT ( 'NONE',  ( -4.180832706968435453, 37.44488997341807845, 76.12122195298280758 ) ) ;
#12658=CARTESIAN_POINT ( 'NONE',  ( 5.563409226749892689, 51.37882362279480475, 76.27120023672567584 ) ) ;
#12659=CARTESIAN_POINT ( 'NONE',  ( 8.661599634585138929, 45.15687757339797059, 72.45433879953087342 ) ) ;
#12662=VECTOR ( 'NONE', #20164, 1000.000000000000000 ) ;
#12664=DIRECTION ( 'NONE',  ( -0.009567942452870459302, 0.9999542261909885044, 1.778535306010345054E-16 ) ) ;
#12665=CARTESIAN_POINT ( 'NONE',  ( 5.077125919649112085, 37.34365979239193933, 77.51217538217308345 ) ) ;
#12666=VECTOR ( 'NONE', #18436, 1000.000000000000000 ) ;
#12667=CARTESIAN_POINT ( 'NONE',  ( 0.3744753729714065948, 52.36086421975554828, 78.83587839956341270 ) ) ;
#12668=CARTESIAN_POINT ( 'NONE',  ( 5.315345751398379726, 50.80894264282942885, 77.96371040190514634 ) ) ;
#12669=CARTESIAN_POINT ( 'NONE',  ( -6.709328582052544121, 40.29621921162754461, 72.45433879953085921 ) ) ;
#12673=CARTESIAN_POINT ( 'NONE',  ( 8.787829143201872029, 41.13140593384864729, 78.45948585835439815 ) ) ;
#12675=CARTESIAN_POINT ( 'NONE',  ( -5.435385416347992660, 50.72091422709593189, 79.30596685730465367 ) ) ;
#12676=CARTESIAN_POINT ( 'NONE',  ( 5.275347668770276499, 50.84403652138585272, 78.87333753819284254 ) ) ;
#12677=ORIENTED_EDGE ( 'NONE', *, *, #11540, .T. ) ;
#12681=CARTESIAN_POINT ( 'NONE',  ( 5.541571994271107471, 50.64183843016825648, 78.67852979887695142 ) ) ;
#12682=CARTESIAN_POINT ( 'NONE',  ( -0.9184319840176534688, 52.97850019102069297, 76.32609705745309725 ) ) ;
#12685=CARTESIAN_POINT ( 'NONE',  ( 0.7882770238055200052, 52.35261454525205238, 76.04568394904065087 ) ) ;
#12686=CARTESIAN_POINT ( 'NONE',  ( -1.376885767552595619, 38.47063949360596524, 82.45433879953087342 ) ) ;
#12688=CARTESIAN_POINT ( 'NONE',  ( 8.873269659708348911, 41.38747658206386149, 75.97261045075327957 ) ) ;
#12689=VECTOR ( 'NONE', #8971, 1000.000000000000227 ) ;
#12690=ORIENTED_EDGE ( 'NONE', *, *, #16049, .T. ) ;
#12692=DIRECTION ( 'NONE',  ( 1.540237394707284220E-16, 1.793354297423764243E-16, -1.000000000000000000 ) ) ;
#12693=CARTESIAN_POINT ( 'NONE',  ( 0.3501649423846716624, 52.36039128232832240, 76.08536861688374131 ) ) ;
#12694=CARTESIAN_POINT ( 'NONE',  ( 5.835344820533724608, 37.14302097153727544, 76.09175310361966638 ) ) ;
#12697=CARTESIAN_POINT ( 'NONE',  ( 4.791956560326987358, 51.94866463147243962, 77.83360891957636341 ) ) ;
#12699=VECTOR ( 'NONE', #12692, 1000.000000000000000 ) ;
#12700=CARTESIAN_POINT ( 'NONE',  ( -3.349688636638950889, 52.21127678364309332, 76.69845644658968808 ) ) ;
#12702=CARTESIAN_POINT ( 'NONE',  ( 4.561823949912076515, 52.11865432047892455, 76.17419329630023128 ) ) ;
#12704=CARTESIAN_POINT ( 'NONE',  ( -5.233355322855509861, 49.94533053554986424, 79.06611278947218580 ) ) ;
#12705=CARTESIAN_POINT ( 'NONE',  ( 8.889576793745449734, 46.88836537034026719, 78.73595644658969661 ) ) ;
#12706=CARTESIAN_POINT ( 'NONE',  ( -4.156427319950603660, 37.43228207296065335, 78.58080938776616620 ) ) ;
#12707=CARTESIAN_POINT ( 'NONE',  ( -4.405821937837398394, 51.45660259411479132, 78.79092181577959764 ) ) ;
#12714=CARTESIAN_POINT ( 'NONE',  ( 4.203679381925226721, 51.46918628067947310, 78.02172882224894579 ) ) ;
#12716=LINE ( 'NONE', #11237, #20027 ) ;
#12718=CARTESIAN_POINT ( 'NONE',  ( 5.081160855019016154, 37.35102415443803636, 76.36627918048426977 ) ) ;
#12720=CARTESIAN_POINT ( 'NONE',  ( -3.067799679179274541, 36.79835369230286091, 77.03801799112748938 ) ) ;
#12721=ADVANCED_FACE ( 'NONE', ( #2419 ), #2625, .F. ) ;
#12722=ORIENTED_EDGE ( 'NONE', *, *, #7, .F. ) ;
#12723=CARTESIAN_POINT ( 'NONE',  ( -7.125180600693382438, 47.12171300294919973, 78.21942560846048309 ) ) ;
#12724=ORIENTED_EDGE ( 'NONE', *, *, #14818, .F. ) ;
#12725=B_SPLINE_CURVE_WITH_KNOTS ( 'NONE', 3,
 ( #1845, #8329, #1937, #6716, #19699, #4904, #13223, #16732, #3320, #5011, #19802, #6508, #11840, #2047, #9825, #11425 ),
 .UNSPECIFIED., .F., .F.,
 ( 4, 2, 2, 2, 2, 2, 2, 4 ),
 ( 0.000000000000000000, 0.0003384078081585416482, 0.0005076117122378233414, 0.0006768156163171051972, 0.0007614175683567383189, 0.0008460195203963712237, 0.001015223424475636925, 0.001353631232634169845 ),
 .UNSPECIFIED. ) ;
#12727=CARTESIAN_POINT ( 'NONE',  ( -7.077609990433002096, 44.22210830145579763, 75.45433879953087342 ) ) ;
#12728=CARTESIAN_POINT ( 'NONE',  ( 8.953205446347402230, 41.62704920565285249, 79.54154676390322720 ) ) ;
#12730=CARTESIAN_POINT ( 'NONE',  ( -8.310158986959008232, 42.88687749725123410, 76.06610350541322418 ) ) ;
#12732=DIRECTION ( 'NONE',  ( -0.3165065846431826535, -0.9485903129789527988, 0.000000000000000000 ) ) ;
#12734=CARTESIAN_POINT ( 'NONE',  ( -3.607357127890974180, 36.27207009797979254, 75.89423958357750166 ) ) ;
#12735=DIRECTION ( 'NONE',  ( -0.9539696396349525154, 0.2999031954727373050, -9.315070279690336121E-17 ) ) ;
#12736=CARTESIAN_POINT ( 'NONE',  ( -5.405939962049822078, 49.82766502745145942, 76.76022115247205591 ) ) ;
#12737=EDGE_LOOP ( 'NONE', ( #20950, #6350, #10094, #6757 ) ) ;
#12738=CARTESIAN_POINT ( 'NONE',  ( -4.545392591669653370, 36.96495910869975177, 77.09144163344554102 ) ) ;
#12739=EDGE_CURVE ( 'NONE', #1868, #13402, #2526, .T. ) ;
#12740=CARTESIAN_POINT ( 'NONE',  ( 0.5221537403065010796, 44.16218137147968292, 78.25433879953088478 ) ) ;
#12743=LINE ( 'NONE', #9766, #1248 ) ;
#12745=CARTESIAN_POINT ( 'NONE',  ( 5.706391565287319168, 37.80821467551069048, 75.39252012644811884 ) ) ;
#12748=CARTESIAN_POINT ( 'NONE',  ( -5.799282478806809138, 50.46088670938467402, 76.15119298917683466 ) ) ;
#12749=DIRECTION ( 'NONE',  ( 0.3895766659341561300, -0.003071955182676040438, 0.9209889165733659011 ) ) ;
#12751=CARTESIAN_POINT ( 'NONE',  ( -0.2786462761171127345, 52.21223977499909807, 79.40856224512604911 ) ) ;
#12752=DIRECTION ( 'NONE',  ( -1.540237394707284220E-16, -1.793354297423764243E-16, 1.000000000000000000 ) ) ;
#12753=PLANE ( 'NONE',  #3467 ) ;
#12754=CARTESIAN_POINT ( 'NONE',  ( 5.694198211105373275, 51.28221506855305734, 75.97344461144770378 ) ) ;
#12755=CARTESIAN_POINT ( 'NONE',  ( 6.108721190857805183, 50.06200863618597197, 77.68963291717794561 ) ) ;
#12756=ORIENTED_EDGE ( 'NONE', *, *, #4617, .T. ) ;
#12758=EDGE_CURVE ( 'NONE', #5281, #15280, #16714, .T. ) ;
#12760=CARTESIAN_POINT ( 'NONE',  ( -4.199287694144524963, 50.86673310655319113, 75.97336489801017478 ) ) ;
#12761=EDGE_CURVE ( 'NONE', #4049, #8055, #16204, .T. ) ;
#12762=CARTESIAN_POINT ( 'NONE',  ( -4.831226022076290150, 37.17609274966823563, 78.89646723195187406 ) ) ;
#12763=B_SPLINE_SURFACE_WITH_KNOTS ( 'NONE', 3, 1, ( 
 ( #710, #18580 ),
 ( #13693, #18798 ),
 ( #3996, #10836 ),
 ( #5922, #10414 ),
 ( #12419, #20490 ),
 ( #5597, #2621 ),
 ( #16882, #12317 ),
 ( #13894, #18898 ),
 ( #2416, #16983 ),
 ( #15610, #917 ),
 ( #1026, #7406 ),
 ( #4310, #12204 ),
 ( #10736, #20059 ),
 ( #817, #17199 ),
 ( #7518, #14006 ),
 ( #20378, #18477 ),
 ( #18684, #8914 ),
 ( #3893, #8800 ),
 ( #2303, #17301 ),
 ( #15292, #5696 ),
 ( #2726, #9231 ),
 ( #15404, #4102 ),
 ( #7301, #15504 ),
 ( #7190, #15718 ),
 ( #12103, #20167 ),
 ( #1137, #9019 ),
 ( #7625, #20266 ) ),
 .UNSPECIFIED., .F., .F., .F.,
 ( 4, 1, 1, 1, 1, 1, 1, 1, 1, 1, 1, 1, 1, 1, 1, 1, 1, 1, 1, 1, 1, 1, 1, 1, 4 ),
 ( 2, 2 ),
 ( 0.000000000000000000, 0.06065359464870424822, 0.1186516444374059315, 0.1737719091481386702, 0.2263851634537537849, 0.2765697945827291226, 0.3242346565764495647, 0.3697019794926615921, 0.4132083501371872081, 0.4544918499020897396, 0.4940385985015171566, 0.5318644461502587406, 0.5683353705239246878, 0.6034301395582813976, 0.6379278300831724424, 0.6713730032816831450, 0.7045442076430231682, 0.7379120707191915152, 0.7717275693920926383, 0.8063464942012584791, 0.8421824305429153057, 0.8795242022246468894, 0.9178549694745260501, 0.9579765912138670236, 1.000000000000000000 ),
 ( 0.000000000000000000, 1.000000000000000000 ),
 .UNSPECIFIED. ) ;
#12764=CARTESIAN_POINT ( 'NONE',  ( 5.709672981839667649, 51.27078447877342882, 77.95044976498417100 ) ) ;
#12765=CARTESIAN_POINT ( 'NONE',  ( 6.786106954071964736, 50.47566606489075980, 77.50555814853646552 ) ) ;
#12767=DIRECTION ( 'NONE',  ( 0.007885122365275663500, 0.9999689119394085113, 1.805443505845543142E-16 ) ) ;
#12769=ADVANCED_FACE ( 'NONE', ( #19111 ), #6985, .T. ) ;
#12770=ORIENTED_EDGE ( 'NONE', *, *, #3312, .T. ) ;
#12771=CARTESIAN_POINT ( 'NONE',  ( -5.356359482101716196, 38.49999417901607757, 79.21211992218960063 ) ) ;
#12772=FACE_OUTER_BOUND ( 'NONE', #19948, .T. ) ;
#12774=ORIENTED_EDGE ( 'NONE', *, *, #14712, .F. ) ;
#12778=CARTESIAN_POINT ( 'NONE',  ( -0.5941502889447408675, 52.21674969029312052, 75.69129100417544009 ) ) ;
#12779=CARTESIAN_POINT ( 'NONE',  ( 8.292258355465955688, 41.60100403556243975, 78.05744560429982926 ) ) ;
#12780=CARTESIAN_POINT ( 'NONE',  ( 5.611902828867023629, 37.90313308730407726, 78.37121987722640881 ) ) ;
#12781=CARTESIAN_POINT ( 'NONE',  ( 0.8409237682492959332, 52.96364229810927071, 76.13704228601427815 ) ) ;
#12783=ORIENTED_EDGE ( 'NONE', *, *, #1153, .F. ) ;
#12786=LINE ( 'NONE', #7896, #4008 ) ;
#12787=EDGE_CURVE ( 'NONE', #374, #16250, #6226, .T. ) ;
#12791=CARTESIAN_POINT ( 'NONE',  ( -6.427915807670530945, 42.26053564693651055, 78.13669174070733447 ) ) ;
#12794=ORIENTED_EDGE ( 'NONE', *, *, #494, .F. ) ;
#12796=CARTESIAN_POINT ( 'NONE',  ( -3.704223681964030845, 51.95793902061026870, 75.61719165653033770 ) ) ;
#12798=CARTESIAN_POINT ( 'NONE',  ( -7.785180019746818836, 41.22672913468994693, 78.61536821129558916 ) ) ;
#12800=CARTESIAN_POINT ( 'NONE',  ( -5.326399992380450144, 49.87884422129010886, 78.87652712212219797 ) ) ;
#12801=CARTESIAN_POINT ( 'NONE',  ( 8.951667845840693971, 41.62244091939069790, 78.41904468188381827 ) ) ;
#12802=CARTESIAN_POINT ( 'NONE',  ( -4.199131210323472807, 37.46382571656145899, 78.86760481232144571 ) ) ;
#12804=CARTESIAN_POINT ( 'NONE',  ( 5.200841308562122123, 50.89200199683061498, 76.36928804473561172 ) ) ;
#12810=CARTESIAN_POINT ( 'NONE',  ( 4.837856207073459203, 51.91476041137136832, 77.79664654212120922 ) ) ;
#12811=DIRECTION ( 'NONE',  ( -1.540237394707284220E-16, -1.793354297423764243E-16, 1.000000000000000000 ) ) ;
#12812=CARTESIAN_POINT ( 'NONE',  ( -5.831867965436852153, 50.43760231366965030, 76.45423404125398292 ) ) ;
#12817=CARTESIAN_POINT ( 'NONE',  ( 5.560944854430392326, 50.62600801335337053, 76.13071926429850578 ) ) ;
#12818=VERTEX_POINT ( 'NONE', #11249 ) ;
#12819=CARTESIAN_POINT ( 'NONE',  ( -7.143058794816434798, 47.07503762047384299, 78.14998754261981162 ) ) ;
#12820=EDGE_CURVE ( 'NONE', #11113, #16604, #14109, .T. ) ;
#12821=VECTOR ( 'NONE', #17991, 1000.000000000000114 ) ;
#12823=CARTESIAN_POINT ( 'NONE',  ( -7.852872584391570321, 41.45951414001282842, 78.01861101995372394 ) ) ;
#12824=CARTESIAN_POINT ( 'NONE',  ( 5.448219197780140632, 37.61331060731148312, 77.67950998295866327 ) ) ;
#12826=LINE ( 'NONE', #4526, #14583 ) ;
#12827=ORIENTED_EDGE ( 'NONE', *, *, #7724, .F. ) ;
#12828=CARTESIAN_POINT ( 'NONE',  ( 8.530649028577993676, 48.02340768410154936, 78.56977997600147035 ) ) ;
#12831=CARTESIAN_POINT ( 'NONE',  ( -3.196673508984729128, 36.89354759902561653, 75.82994300095940332 ) ) ;
#12832=CARTESIAN_POINT ( 'NONE',  ( -4.161402579748598285, 37.43595709695774332, 76.29203488853940485 ) ) ;
#12834=ORIENTED_EDGE ( 'NONE', *, *, #11554, .T. ) ;
#12835=CARTESIAN_POINT ( 'NONE',  ( -4.585830261548859532, 37.76958990528607529, 77.32892190166411694 ) ) ;
#12837=CARTESIAN_POINT ( 'NONE',  ( 8.256691324932248222, 41.45960787672780157, 77.50846324053436831 ) ) ;
#12841=VERTEX_POINT ( 'NONE', #3251 ) ;
#12842=CARTESIAN_POINT ( 'NONE',  ( 8.317158657711994252, 46.70735294479731436, 78.73595644658969661 ) ) ;
#12844=CARTESIAN_POINT ( 'NONE',  ( -5.427705199025447236, 38.51945526935772790, 79.11457076817336542 ) ) ;
#12849=CARTESIAN_POINT ( 'NONE',  ( 8.788263343888127466, 41.13270726085054463, 77.24417474779077963 ) ) ;
#12851=CARTESIAN_POINT ( 'NONE',  ( -0.7161872237684476783, 52.97813067712484525, 79.09854784679095019 ) ) ;
#12854=CARTESIAN_POINT ( 'NONE',  ( 9.348773431696422165, 42.81259155210894107, 76.30013550906805619 ) ) ;
#12855=CARTESIAN_POINT ( 'NONE',  ( 0.8409531834210948187, 52.35598196211776667, 76.19861658564380491 ) ) ;
#12860=CARTESIAN_POINT ( 'NONE',  ( 9.348773431696422165, 42.81259155210894107, 76.30013550906805619 ) ) ;
#12861=CARTESIAN_POINT ( 'NONE',  ( -1.483269432489140005, 51.49895708687498086, 72.45433879953087342 ) ) ;
#12863=CARTESIAN_POINT ( 'NONE',  ( 4.480833922618288945, 51.34373684881791178, 79.31790653140825498 ) ) ;
#12865=CARTESIAN_POINT ( 'NONE',  ( -4.598246518171406727, 51.31910303412164609, 78.93669174070734584 ) ) ;
#12867=CARTESIAN_POINT ( 'NONE',  ( 6.386126596379389397, 49.84628249594006633, 77.45110917081549928 ) ) ;
#12868=CARTESIAN_POINT ( 'NONE',  ( 5.665287683258889651, 37.02150436742986273, 75.36022115247205022 ) ) ;
#12869=CARTESIAN_POINT ( 'NONE',  ( 6.519924314245371555, 49.74745151145329203, 76.63889762306028786 ) ) ;
#12874=LINE ( 'NONE', #18188, #14309 ) ;
#12876=CARTESIAN_POINT ( 'NONE',  ( 5.257910441395027945, 50.85640482246301275, 78.82166709644059210 ) ) ;
#12880=CARTESIAN_POINT ( 'NONE',  ( 8.810541937945364666, 41.19947762056773399, 75.36738766396204880 ) ) ;
#12881=ORIENTED_EDGE ( 'NONE', *, *, #8497, .F. ) ;
#12882=AXIS2_PLACEMENT_3D ( 'NONE', #3223, #13117, #19701 ) ;
#12883=CARTESIAN_POINT ( 'NONE',  ( 6.447652509444688818, 38.50032921029611543, 76.69330938776616335 ) ) ;
#12884=LINE ( 'NONE', #1918, #6070 ) ;
#12885=CARTESIAN_POINT ( 'NONE',  ( 6.799065290779627624, 37.83166033551658103, 77.90902863000688683 ) ) ;
#12887=ORIENTED_EDGE ( 'NONE', *, *, #6356, .F. ) ;
#12888=CARTESIAN_POINT ( 'NONE',  ( -4.451527680475927617, 51.42394294381934117, 78.89116106075270807 ) ) ;
#12893=B_SPLINE_CURVE_WITH_KNOTS ( 'NONE', 3,
 ( #16810, #16705, #7217, #1627, #12032, #4902, #3705, #419, #8111, #3219, #6504, #11423, #9721, #13717, #18505 ),
 .UNSPECIFIED., .F., .F.,
 ( 4, 1, 1, 1, 1, 1, 1, 1, 1, 1, 1, 1, 4 ),
 ( 0.000000000000000000, 0.09897586389363323411, 0.1834007553115765132, 0.2562582723958196640, 0.3272804813821422187, 0.3687296102942994591, 0.4216358900696890455, 0.4870080516106923274, 0.5645314195351998077, 0.6541098812875514312, 0.7570203673134348055, 0.8723000540617986687, 1.000000000000000000 ),
 .UNSPECIFIED. ) ;
#12895=CARTESIAN_POINT ( 'NONE',  ( 0.3411207544655743829, 52.36018373693247696, 76.11020748613105980 ) ) ;
#12898=CIRCLE ( 'NONE', #9176, 8.800000000000000711 ) ;
#12899=B_SPLINE_CURVE_WITH_KNOTS ( 'NONE', 3,
 ( #17888, #6600, #7898, #20755, #6189, #12895, #12693, #19377, #19171, #9716, #11521, #11107, #14386, #1621 ),
 .UNSPECIFIED., .F., .F.,
 ( 4, 2, 2, 2, 2, 2, 4 ),
 ( 0.000000000000000000, 0.0001566768555925129511, 0.0003133537111850259022, 0.0003916921389812823913, 0.0004700305667775389346, 0.0005483689945737954237, 0.0006267074223700516960 ),
 .UNSPECIFIED. ) ;
#12900=ORIENTED_EDGE ( 'NONE', *, *, #13272, .T. ) ;
#12901=DIRECTION ( 'NONE',  ( 0.9534635866061492715, 0.3015081906286096181, 2.009271279954798787E-16 ) ) ;
#12903=VECTOR ( 'NONE', #17059, 1000.000000000000000 ) ;
#12906=EDGE_CURVE ( 'NONE', #17907, #14373, #18143, .T. ) ;
#12907=CARTESIAN_POINT ( 'NONE',  ( 2.527576913102088874, 36.82540565608437078, 72.45432679953087529 ) ) ;
#12910=CARTESIAN_POINT ( 'NONE',  ( -5.286500981006134303, 49.90735459402215213, 78.97495844722888592 ) ) ;
#12911=CARTESIAN_POINT ( 'NONE',  ( -5.606854386412797098, 37.74901817818727778, 79.39214668191834789 ) ) ;
#12912=CARTESIAN_POINT ( 'NONE',  ( -4.661432690376161148, 37.05067325523394572, 78.93441095796421791 ) ) ;
#12913=CARTESIAN_POINT ( 'NONE',  ( 5.600448134661695221, 51.35146447353857013, 76.04240903267428564 ) ) ;
#12916=VECTOR ( 'NONE', #3524, 1000.000000000000114 ) ;
#12918=VECTOR ( 'NONE', #446, 1000.000000000000000 ) ;
#12919=PLANE ( 'NONE',  #4852 ) ;
#12920=ORIENTED_EDGE ( 'NONE', *, *, #10583, .F. ) ;
#12921=CARTESIAN_POINT ( 'NONE',  ( 4.248944230316001658, 51.43575096055252516, 77.94290914044947272 ) ) ;
#12923=CARTESIAN_POINT ( 'NONE',  ( 0.6357006819926122043, 52.96147595994789015, 78.93320643228391020 ) ) ;
#12928=CARTESIAN_POINT ( 'NONE',  ( 5.266681877975375237, 37.48359068508447933, 77.75986257808632729 ) ) ;
#12930=ORIENTED_EDGE ( 'NONE', *, *, #2356, .T. ) ;
#12931=CARTESIAN_POINT ( 'NONE',  ( 2.002786569115004855, 52.95507841157613171, 78.99734963310253022 ) ) ;
#12937=B_SPLINE_SURFACE_WITH_KNOTS ( 'NONE', 3, 1, ( 
 ( #17620, #7848 ),
 ( #4846, #20809 ),
 ( #16044, #3263 ),
 ( #9762, #8154 ),
 ( #3572, #5363 ),
 ( #13157, #171 ),
 ( #11572, #8264 ),
 ( #19838, #5258 ),
 ( #10077, #11677 ),
 ( #375, #11876 ),
 ( #18356, #3776 ),
 ( #11469, #1784 ),
 ( #13464, #9979 ),
 ( #3470, #72 ),
 ( #14644, #18047 ),
 ( #11774, #8369 ),
 ( #481, #18250 ),
 ( #10294, #14750 ),
 ( #6551, #16460 ) ),
 .UNSPECIFIED., .F., .F., .F.,
 ( 4, 1, 1, 1, 1, 1, 1, 1, 1, 1, 1, 1, 1, 1, 1, 1, 4 ),
 ( 2, 2 ),
 ( 0.000000000000000000, 0.1026547437176949656, 0.1953110930976798554, 0.2773242249590897601, 0.3493914542831295655, 0.4108068724308638342, 0.4622887491528899773, 0.5032980238437735343, 0.5345418472720404601, 0.5847168530758872773, 0.6322731508218554231, 0.6775315938118185999, 0.7246750034944897667, 0.7779009386454487363, 0.8408031781967141294, 0.9146367246678260843, 1.000000000000000000 ),
 ( 0.000000000000000000, 1.000000000000000000 ),
 .UNSPECIFIED. ) ;
#12938=CARTESIAN_POINT ( 'NONE',  ( 8.744145067270602922, 41.00048198701652780, 79.52393066155629242 ) ) ;
#12940=CARTESIAN_POINT ( 'NONE',  ( 5.939900590116411472, 51.10072461867315496, 76.90580938776616904 ) ) ;
#12941=CARTESIAN_POINT ( 'NONE',  ( -7.184859864745180680, 41.78596111121809997, 79.54845644658969661 ) ) ;
#12943=VECTOR ( 'NONE', #8626, 1000.000000000000000 ) ;
#12944=CARTESIAN_POINT ( 'NONE',  ( 5.677877744449962627, 51.29427033984291029, 78.92241520643889885 ) ) ;
#12945=LINE ( 'NONE', #15932, #11888 ) ;
#12948=CARTESIAN_POINT ( 'NONE',  ( 8.787829143201870252, 41.13140593384865440, 77.14698585835439815 ) ) ;
#12950=VERTEX_POINT ( 'NONE', #9857 ) ;
#12951=CARTESIAN_POINT ( 'NONE',  ( -4.804516487068378083, 51.17171006637344277, 76.41659450085566618 ) ) ;
#12953=EDGE_CURVE ( 'NONE', #10926, #4092, #9751, .T. ) ;
#12955=CARTESIAN_POINT ( 'NONE',  ( -5.644616003178662744, 50.57140571016744701, 75.79002994479621691 ) ) ;
#12956=CARTESIAN_POINT ( 'NONE',  ( 8.951667845840693971, 41.62244091939069790, 76.38301527011910252 ) ) ;
#12958=CARTESIAN_POINT ( 'NONE',  ( 8.648170029844118645, 43.06315486489794608, 76.74257409364851412 ) ) ;
#12959=ORIENTED_EDGE ( 'NONE', *, *, #8592, .F. ) ;
#12962=CARTESIAN_POINT ( 'NONE',  ( 8.317158657711994252, 46.70735294479731436, 78.73595644658969661 ) ) ;
#12968=ORIENTED_EDGE ( 'NONE', *, *, #14367, .T. ) ;
#12969=CARTESIAN_POINT ( 'NONE',  ( 7.680032241523796266, 40.16158449578585277, 77.13595644658970230 ) ) ;
#12970=CARTESIAN_POINT ( 'NONE',  ( 1.652727357819364640, 35.35299279957455809, 75.45433879953087342 ) ) ;
#12971=CARTESIAN_POINT ( 'NONE',  ( -4.895593109503408868, 37.22363812428621088, 78.53742703482498655 ) ) ;
#12975=LINE ( 'NONE', #19455, #5002 ) ;
#12976=EDGE_CURVE ( 'NONE', #7376, #6491, #20993, .T. ) ;
#12977=CARTESIAN_POINT ( 'NONE',  ( -5.968382836370074607, 47.45797339585421071, 78.32492703482499508 ) ) ;
#12979=LINE ( 'NONE', #11395, #20054 ) ;
#12984=LINE ( 'NONE', #4877, #6130 ) ;
#12987=CARTESIAN_POINT ( 'NONE',  ( 8.946998292058729874, 41.60844597047518789, 78.80177617112552468 ) ) ;
#12988=CARTESIAN_POINT ( 'NONE',  ( -3.219615297498348738, 36.86557920496366592, 77.48809274675903680 ) ) ;
#12989=AXIS2_PLACEMENT_3D ( 'NONE', #7298, #6014, #10734 ) ;
#12990=CIRCLE ( 'NONE', #3479, 8.199999999999995737 ) ;
#12991=CARTESIAN_POINT ( 'NONE',  ( 8.874399228141724549, 41.39086197031718228, 75.36031793586835192 ) ) ;
#12993=CARTESIAN_POINT ( 'NONE',  ( 5.951216973768841179, 38.14559455216716799, 75.49608936836499140 ) ) ;
#12994=CARTESIAN_POINT ( 'NONE',  ( 0.1818310095788190917, 52.97104947332776703, 79.52116152017964623 ) ) ;
#12996=CARTESIAN_POINT ( 'NONE',  ( -3.496029822981026491, 36.18983710238020279, 76.51650556680409920 ) ) ;
#12997=DIRECTION ( 'NONE',  ( -0.3165065846431827645, -0.9485903129789529098, 0.000000000000000000 ) ) ;
#12999=VERTEX_POINT ( 'NONE', #9969 ) ;
#13000=EDGE_CURVE ( 'NONE', #19814, #9748, #8142, .T. ) ;
#13001=CARTESIAN_POINT ( 'NONE',  ( -4.383473025373059606, 51.47257230871590394, 78.45066232894264147 ) ) ;
#13007=CARTESIAN_POINT ( 'NONE',  ( 5.844285037446443454, 37.14940932322087264, 76.26708001093082601 ) ) ;
#13009=CARTESIAN_POINT ( 'NONE',  ( -5.950833756536985319, 38.00310188256379007, 76.46818962967083166 ) ) ;
#13011=CARTESIAN_POINT ( 'NONE',  ( 0.8377421044266867289, 51.35991668224300355, 78.52566232894263010 ) ) ;
#13012=VERTEX_POINT ( 'NONE', #17693 ) ;
#13015=CARTESIAN_POINT ( 'NONE',  ( 2.927603783594689091, 51.37146775011972011, 75.45433879953087342 ) ) ;
#13018=VERTEX_POINT ( 'NONE', #4905 ) ;
#13019=CARTESIAN_POINT ( 'NONE',  ( -5.403220070277449771, 49.82395140618747575, 78.14282209630749776 ) ) ;
#13024=FACE_OUTER_BOUND ( 'NONE', #1124, .T. ) ;
#13025=VERTEX_POINT ( 'NONE', #8223 ) ;
#13026=DIRECTION ( 'NONE',  ( -0.5813877811927010697, 0.8136266022444373913, 5.636455622144621648E-17 ) ) ;
#13030=EDGE_CURVE ( 'NONE', #19237, #10307, #11323, .T. ) ;
#13031=CARTESIAN_POINT ( 'NONE',  ( -7.093231395208066559, 41.52507926682920214, 76.45513158819304067 ) ) ;
#13032=CARTESIAN_POINT ( 'NONE',  ( -4.790713360849209401, 51.18157327500495768, 75.36324311589748959 ) ) ;
#13037=FACE_OUTER_BOUND ( 'NONE', #19525, .T. ) ;
#13040=CARTESIAN_POINT ( 'NONE',  ( -3.522017727535928344, 36.20903332061824642, 77.14704031750767399 ) ) ;
#13041=ORIENTED_EDGE ( 'NONE', *, *, #18102, .F. ) ;
#13045=FACE_OUTER_BOUND ( 'NONE', #14590, .T. ) ;
#13047=CARTESIAN_POINT ( 'NONE',  ( 8.887668352622405621, 41.43063037816333605, 75.36022115247205022 ) ) ;
#13048=VERTEX_POINT ( 'NONE', #1846 ) ;
#13053=DIRECTION ( 'NONE',  ( -0.5941461771851693774, -0.8043570849667760481, -2.357623395011396791E-16 ) ) ;
#13056=CARTESIAN_POINT ( 'NONE',  ( -4.316692190778365301, 37.57078845395070488, 77.27854074750605662 ) ) ;
#13060=ORIENTED_EDGE ( 'NONE', *, *, #12121, .T. ) ;
#13061=DIRECTION ( 'NONE',  ( -0.007885122365275663500, -0.9999689119394085113, -1.805443505845543142E-16 ) ) ;
#13065=CARTESIAN_POINT ( 'NONE',  ( 6.817737414320570899, 50.45230191805777054, 75.81347835631012799 ) ) ;
#13066=LINE ( 'NONE', #9569, #11649 ) ;
#13067=CARTESIAN_POINT ( 'NONE',  ( 0.5221537403065015237, 44.16218137147968292, 75.45433879953088763 ) ) ;
#13068=CARTESIAN_POINT ( 'NONE',  ( 8.479137094719348511, 40.20623628148813111, 79.16795596456493911 ) ) ;
#13069=ORIENTED_EDGE ( 'NONE', *, *, #1917, .F. ) ;
#13070=DIRECTION ( 'NONE',  ( -0.3165065846431827090, -0.9485903129789527988, 0.000000000000000000 ) ) ;
#13071=CARTESIAN_POINT ( 'NONE',  ( 8.587085583998218752, 42.89418280249433479, 75.81656704941096336 ) ) ;
#13073=CARTESIAN_POINT ( 'NONE',  ( 2.075677826575113016, 52.82397334471521333, 78.80921410649150971 ) ) ;
#13076=EDGE_LOOP ( 'NONE', ( #15956, #11525, #7812, #14889 ) ) ;
#13077=B_SPLINE_CURVE_WITH_KNOTS ( 'NONE', 3,
 ( #14647, #1883, #11266, #174, #11471, #3364, #13161, #17737 ),
 .UNSPECIFIED., .F., .F.,
 ( 4, 2, 2, 4 ),
 ( 0.000000000000000000, 0.0001105466857480712239, 0.0002210933714961424478, 0.0004421867429922453222 ),
 .UNSPECIFIED. ) ;
#13079=CARTESIAN_POINT ( 'NONE',  ( 7.698155637638221194, 40.19417714920118812, 76.18042117906708199 ) ) ;
#13080=FACE_OUTER_BOUND ( 'NONE', #8310, .T. ) ;
#13082=CARTESIAN_POINT ( 'NONE',  ( -1.047061061252479108, 36.11373028406117669, 75.45433879953087342 ) ) ;
#13084=CARTESIAN_POINT ( 'NONE',  ( 8.614432416951936844, 42.97614299570737018, 77.68070116889359156 ) ) ;
#13090=CARTESIAN_POINT ( 'NONE',  ( -3.539401246598059991, 43.09270903039240608, 82.45433879953087342 ) ) ;
#13091=CARTESIAN_POINT ( 'NONE',  ( 8.647984279038439581, 43.06178145482667219, 76.54298940512656202 ) ) ;
#13093=LINE ( 'NONE', #11617, #10577 ) ;
#13094=PLANE ( 'NONE',  #18992 ) ;
#13097=EDGE_CURVE ( 'NONE', #14733, #14867, #7192, .T. ) ;
#13098=CARTESIAN_POINT ( 'NONE',  ( 6.859321636172213132, 37.87471731380851026, 76.18799845131768222 ) ) ;
#13099=FACE_OUTER_BOUND ( 'NONE', #13672, .T. ) ;
#13100=CARTESIAN_POINT ( 'NONE',  ( 8.224838919204344734, 41.34743166599955089, 79.54253259009090016 ) ) ;
#13102=CARTESIAN_POINT ( 'NONE',  ( 5.389492195292208798, 36.82443100924615464, 78.09625056423675460 ) ) ;
#13105=EDGE_CURVE ( 'NONE', #9723, #14881, #10619, .T. ) ;
#13106=ORIENTED_EDGE ( 'NONE', *, *, #11540, .F. ) ;
#13108=CARTESIAN_POINT ( 'NONE',  ( 1.338678443490884273, 52.94638778455286143, 76.79234737414994072 ) ) ;
#13109=CARTESIAN_POINT ( 'NONE',  ( -3.096104608208455566, 36.80844346142616530, 78.46683879953087626 ) ) ;
#13110=CARTESIAN_POINT ( 'NONE',  ( -7.373158828693091138, 41.96119617500171728, 78.52713215918005574 ) ) ;
#13111=B_SPLINE_SURFACE_WITH_KNOTS ( 'NONE', 3, 1, ( 
 ( #17716, #9745 ),
 ( #15918, #18028 ),
 ( #1765, #16227 ),
 ( #5034, #13136 ),
 ( #9542, #19407 ),
 ( #9430, #1652 ),
 ( #19612, #12817 ),
 ( #9647, #11552 ),
 ( #8134, #1339 ),
 ( #11242, #20789 ),
 ( #6531, #4926 ),
 ( #3032, #11450 ),
 ( #17919, #3342 ),
 ( #9848, #14311 ),
 ( #7933, #14415 ) ),
 .UNSPECIFIED., .F., .F., .F.,
 ( 4, 1, 1, 1, 1, 1, 1, 1, 1, 1, 1, 1, 4 ),
 ( 2, 2 ),
 ( 0.000000000000000000, 0.1124872259413081665, 0.2145177594606929306, 0.3061691560909166610, 0.3877635431594634863, 0.4596729905988826692, 0.5233009716387192478, 0.5766443983521717387, 0.6225226080321302202, 0.7076769590374641927, 0.7964950891574525960, 0.8912003305064800651, 1.000000000000000000 ),
 ( 0.000000000000000000, 1.000000000000000000 ),
 .UNSPECIFIED. ) ;
#13112=CARTESIAN_POINT ( 'NONE',  ( 8.648042534604279297, 43.06221218663710459, 78.51015103835841558 ) ) ;
#13114=ORIENTED_EDGE ( 'NONE', *, *, #18211, .F. ) ;
#13117=DIRECTION ( 'NONE',  ( 1.540237394707284220E-16, 1.793354297423764243E-16, -1.000000000000000000 ) ) ;
#13118=ORIENTED_EDGE ( 'NONE', *, *, #1680, .T. ) ;
#13119=CARTESIAN_POINT ( 'NONE',  ( -5.668520211720758262, 50.55432463793220421, 79.06611278947218580 ) ) ;
#13120=DIRECTION ( 'NONE',  ( -1.540237394707284220E-16, -1.793354297423764243E-16, 1.000000000000000000 ) ) ;
#13122=DIRECTION ( 'NONE',  ( -0.3165065846431824870, -0.9485903129789529098, 0.000000000000000000 ) ) ;
#13123=CARTESIAN_POINT ( 'NONE',  ( 5.076982970477778245, 37.34803879110698688, 77.55899030588862786 ) ) ;
#13126=CARTESIAN_POINT ( 'NONE',  ( 0.8503869109451517305, 52.96349527369733323, 78.52566232894263010 ) ) ;
#13128=CARTESIAN_POINT ( 'NONE',  ( 4.151429181450037476, 51.50778139900403119, 78.23954818826248925 ) ) ;
#13129=CARTESIAN_POINT ( 'NONE',  ( -7.445240191484915115, 40.15417470793909871, 78.06261470525505786 ) ) ;
#13130=CARTESIAN_POINT ( 'NONE',  ( -4.217603907031332255, 50.67132072554849742, 75.36022115247205022 ) ) ;
#13133=DIRECTION ( 'NONE',  ( -1.540237394707284467E-16, -1.793354297423764243E-16, 1.000000000000000000 ) ) ;
#13136=CARTESIAN_POINT ( 'NONE',  ( 5.576569238758990465, 50.61446691003841636, 76.26580079864017137 ) ) ;
#13138=CARTESIAN_POINT ( 'NONE',  ( 1.647117196182025678, 52.95788299529235843, 79.33873778842219338 ) ) ;
#13139=CARTESIAN_POINT ( 'NONE',  ( 5.160332980892567534, 37.41848089432694024, 78.21801395346943764 ) ) ;
#13141=CARTESIAN_POINT ( 'NONE',  ( -3.704223681964030845, 51.95793902061026870, 75.61719165653033770 ) ) ;
#13143=DIRECTION ( 'NONE',  ( 0.5813877811927011807, -0.8136266022444372803, -5.636455622144619183E-17 ) ) ;
#13152=CARTESIAN_POINT ( 'NONE',  ( -4.156427319950602772, 37.43228207296065335, 76.53375056423675460 ) ) ;
#13153=EDGE_CURVE ( 'NONE', #2164, #5281, #7873, .T. ) ;
#13155=ORIENTED_EDGE ( 'NONE', *, *, #13105, .F. ) ;
#13156=CARTESIAN_POINT ( 'NONE',  ( -4.730130202819499807, 37.10141734037124905, 77.29630340639747033 ) ) ;
#13157=CARTESIAN_POINT ( 'NONE',  ( -4.483525497724968112, 37.69402149733662810, 77.90854597583356167 ) ) ;
#13160=ORIENTED_EDGE ( 'NONE', *, *, #19238, .T. ) ;
#13161=CARTESIAN_POINT ( 'NONE',  ( 5.543801380518728728, 50.64470058390610774, 78.66695423199873005 ) ) ;
#13162=DIRECTION ( 'NONE',  ( 1.540237394707284220E-16, 1.793354297423764243E-16, -1.000000000000000000 ) ) ;
#13165=CARTESIAN_POINT ( 'NONE',  ( 5.799744778572546444, 50.27941912385354328, 75.41423045364997790 ) ) ;
#13166=CARTESIAN_POINT ( 'NONE',  ( -4.398409473784897550, 37.60244433931075747, 75.97311671873485750 ) ) ;
#13167=CARTESIAN_POINT ( 'NONE',  ( 0.3788305629195590774, 52.34483884138099796, 77.02254451525793399 ) ) ;
#13168=CARTESIAN_POINT ( 'NONE',  ( 5.036257573895150053, 37.49179806381912528, 75.36841521003546518 ) ) ;
#13169=VECTOR ( 'NONE', #7203, 1000.000000000000227 ) ;
#13170=ORIENTED_EDGE ( 'NONE', *, *, #16378, .T. ) ;
#13171=CARTESIAN_POINT ( 'NONE',  ( -5.119673272240743422, 38.21139563191785982, 75.53183897749521236 ) ) ;
#13174=CARTESIAN_POINT ( 'NONE',  ( 1.136649954779953786, 52.94122945111733003, 79.51059422203249483 ) ) ;
#13175=VERTEX_POINT ( 'NONE', #740 ) ;
#13176=ORIENTED_EDGE ( 'NONE', *, *, #6063, .F. ) ;
#13177=EDGE_CURVE ( 'NONE', #8069, #19924, #1173, .T. ) ;
#13179=ORIENTED_EDGE ( 'NONE', *, *, #10429, .F. ) ;
#13180=AXIS2_PLACEMENT_3D ( 'NONE', #10648, #2749, #7422 ) ;
#13181=CARTESIAN_POINT ( 'NONE',  ( -4.211488180634966660, 48.16625856408043660, 78.25433879953088478 ) ) ;
#13182=CARTESIAN_POINT ( 'NONE',  ( 4.531118403667150574, 51.21650232360861565, 77.67439681936272677 ) ) ;
#13183=DIRECTION ( 'NONE',  ( 1.540237394707284220E-16, 1.793354297423764243E-16, -1.000000000000000000 ) ) ;
#13189=CARTESIAN_POINT ( 'NONE',  ( -3.053409417734729736, 36.78772418584885884, 76.59109406773794149 ) ) ;
#13190=FACE_OUTER_BOUND ( 'NONE', #19668, .T. ) ;
#13192=ORIENTED_EDGE ( 'NONE', *, *, #14780, .F. ) ;
#13193=DIRECTION ( 'NONE',  ( -0.5941461771851693774, -0.8043570849667760481, -2.357623395011396791E-16 ) ) ;
#13195=ORIENTED_EDGE ( 'NONE', *, *, #3244, .T. ) ;
#13196=LINE ( 'NONE', #19669, #13304 ) ;
#13197=CARTESIAN_POINT ( 'NONE',  ( -4.533151836807888913, 37.71055329817392732, 78.64904841171450300 ) ) ;
#13198=CARTESIAN_POINT ( 'NONE',  ( 8.300051067836092145, 41.58955977690143158, 77.52397343602532942 ) ) ;
#13199=CARTESIAN_POINT ( 'NONE',  ( 8.435567168294131335, 40.07565444796716747, 75.89798363837520867 ) ) ;
#13200=ORIENTED_EDGE ( 'NONE', *, *, #13357, .F. ) ;
#13201=CARTESIAN_POINT ( 'NONE',  ( 6.055654410823096079, 38.22022172098753146, 75.55565825109377442 ) ) ;
#13202=CARTESIAN_POINT ( 'NONE',  ( 4.577225057937401864, 52.10727814237509392, 78.46169174070733732 ) ) ;
#13203=CARTESIAN_POINT ( 'NONE',  ( 6.882043956598291601, 37.89095385206773869, 77.31245045813156480 ) ) ;
#13205=CARTESIAN_POINT ( 'NONE',  ( -4.171956714443219916, 37.43867258617596860, 78.78605677924578288 ) ) ;
#13206=EDGE_LOOP ( 'NONE', ( #14041, #12690, #20323, #9797 ) ) ;
#13213=EDGE_CURVE ( 'NONE', #10206, #9230, #3010, .T. ) ;
#13214=CARTESIAN_POINT ( 'NONE',  ( 1.920580872171021358, 52.20313474366393081, 77.08393542551461053 ) ) ;
#13215=CARTESIAN_POINT ( 'NONE',  ( -3.096372156315136959, 36.80864108843506699, 78.38559710128819802 ) ) ;
#13216=B_SPLINE_CURVE_WITH_KNOTS ( 'NONE', 3,
 ( #5133, #13237, #5239, #11654, #3649, #8344, #18131, #1759, #8241, #16535, #18022, #10272, #11755, #3551 ),
 .UNSPECIFIED., .F., .F.,
 ( 4, 2, 2, 2, 2, 2, 4 ),
 ( 8.673617379884035472E-19, 0.0002848466061852771079, 0.0004272699092779162311, 0.0005696932123705553000, 0.0007121165154631944232, 0.0008545398185558335464, 0.001139386424741116888 ),
 .UNSPECIFIED. ) ;
#13217=CARTESIAN_POINT ( 'NONE',  ( 6.012275498921958672, 37.26944915646792822, 78.37198585835440667 ) ) ;
#13221=ADVANCED_FACE ( 'NONE', ( #7442 ), #18928, .T. ) ;
#13223=CARTESIAN_POINT ( 'NONE',  ( -7.669666148856070897, 47.37719010417367116, 78.26793921993403558 ) ) ;
#13226=VERTEX_POINT ( 'NONE', #7225 ) ;
#13227=CARTESIAN_POINT ( 'NONE',  ( 8.848467398349676216, 41.31314263134580500, 75.36050707951255845 ) ) ;
#13229=LINE ( 'NONE', #5231, #8128 ) ;
#13230=CARTESIAN_POINT ( 'NONE',  ( 0.3280703116875920977, 52.35625621862651258, 78.56344688395670062 ) ) ;
#13232=CARTESIAN_POINT ( 'NONE',  ( -4.058881954689706362, 50.95759777156840187, 76.06958028623719770 ) ) ;
#13233=ORIENTED_EDGE ( 'NONE', *, *, #985, .F. ) ;
#13235=CARTESIAN_POINT ( 'NONE',  ( -7.428404849043024782, 40.10093606804371547, 78.24455606223649795 ) ) ;
#13237=CARTESIAN_POINT ( 'NONE',  ( -4.720151432595600660, 37.85605236037169874, 77.33560970407651780 ) ) ;
#13239=EDGE_CURVE ( 'NONE', #5416, #11467, #198, .T. ) ;
#13240=CARTESIAN_POINT ( 'NONE',  ( 5.453344025566022601, 40.65105419805430387, 75.45433879953087342 ) ) ;
#13242=CARTESIAN_POINT ( 'NONE',  ( -7.086630388250130252, 47.03102748359589214, 77.94747975791852923 ) ) ;
#13243=AXIS2_PLACEMENT_3D ( 'NONE', #19542, #17848, #20711 ) ;
#13244=VECTOR ( 'NONE', #18333, 999.9999999999998863 ) ;
#13246=VERTEX_POINT ( 'NONE', #15330 ) ;
#13248=CARTESIAN_POINT ( 'NONE',  ( 5.666494898543479763, 37.02236699927324537, 78.30432351818811298 ) ) ;
#13251=EDGE_CURVE ( 'NONE', #14909, #19757, #20197, .T. ) ;
#13255=CARTESIAN_POINT ( 'NONE',  ( -8.264604465707931169, 42.74281979478013938, 76.25640820822667365 ) ) ;
#13256=ORIENTED_EDGE ( 'NONE', *, *, #8084, .T. ) ;
#13257=VECTOR ( 'NONE', #20685, 1000.000000000000227 ) ;
#13258=CARTESIAN_POINT ( 'NONE',  ( -5.281338840898281539, 38.44457945337485683, 75.70067668752250256 ) ) ;
#13261=CARTESIAN_POINT ( 'NONE',  ( 6.489847418355314979, 49.78593742637539776, 78.48669174070734300 ) ) ;
#13264=ORIENTED_EDGE ( 'NONE', *, *, #5198, .T. ) ;
#13265=DIRECTION ( 'NONE',  ( 1.540237394707284220E-16, 1.793354297423764243E-16, -1.000000000000000000 ) ) ;
#13267=ORIENTED_EDGE ( 'NONE', *, *, #15246, .F. ) ;
#13269=CARTESIAN_POINT ( 'NONE',  ( -7.313565574299385474, 41.74526126053015673, 79.54845644658969661 ) ) ;
#13271=ADVANCED_FACE ( 'NONE', ( #9369 ), #18208, .T. ) ;
#13272=EDGE_CURVE ( 'NONE', #11820, #2058, #1862, .T. ) ;
#13274=CARTESIAN_POINT ( 'NONE',  ( 5.620183367589484114, 50.41205390497189143, 75.37891144279687694 ) ) ;
#13275=CARTESIAN_POINT ( 'NONE',  ( -3.696676068499483048, 37.12873482127974256, 79.45447414167722400 ) ) ;
#13277=CARTESIAN_POINT ( 'NONE',  ( 4.425132644269478277, 36.13533498154198043, 76.25036098622081226 ) ) ;
#13278=CARTESIAN_POINT ( 'NONE',  ( 8.386004485381512552, 39.92711194308005673, 78.01856368782078732 ) ) ;
#13281=CARTESIAN_POINT ( 'NONE',  ( 9.162426004170315608, 42.25409649015283975, 75.50722976489458915 ) ) ;
#13282=DIRECTION ( 'NONE',  ( 1.540237394707284220E-16, 1.793354297423764243E-16, -1.000000000000000000 ) ) ;
#13284=ORIENTED_EDGE ( 'NONE', *, *, #654, .F. ) ;
#13285=CARTESIAN_POINT ( 'NONE',  ( 5.791714832554497150, 51.21018346849771063, 78.93490712750880789 ) ) ;
#13288=CARTESIAN_POINT ( 'NONE',  ( 6.456868491357829143, 49.79402830777683420, 76.00796742194241062 ) ) ;
#13289=CARTESIAN_POINT ( 'NONE',  ( 9.340212240349364592, 42.78693311852996572, 76.09591779779900378 ) ) ;
#13291=DIRECTION ( 'NONE',  ( -0.9485903129789527988, 0.3165065846431829311, -8.934458285744989980E-17 ) ) ;
#13293=LINE ( 'NONE', #19865, #5212 ) ;
#13294=B_SPLINE_SURFACE_WITH_KNOTS ( 'NONE', 3, 1, ( 
 ( #16448, #10064 ),
 ( #18139, #1768 ),
 ( #11762, #14939 ),
 ( #11864, #13139 ),
 ( #16546, #1867 ),
 ( #13248, #8458 ),
 ( #18237, #16649 ),
 ( #2071, #467 ),
 ( #14705, #17507 ),
 ( #9434, #11421 ),
 ( #13217, #13428 ) ),
 .UNSPECIFIED., .F., .F., .F.,
 ( 4, 1, 1, 1, 1, 1, 1, 1, 4 ),
 ( 2, 2 ),
 ( 0.000000000000000000, 0.1208544691022559597, 0.2402546218586821825, 0.3598696579477268509, 0.4809300011950208842, 0.6037041574249993880, 0.7308714335393303729, 0.8631644367168944676, 0.9999999999999998890 ),
 ( 0.000000000000000000, 1.000000000000000000 ),
 .UNSPECIFIED. ) ;
#13296=PLANE ( 'NONE',  #5766 ) ;
#13297=CARTESIAN_POINT ( 'NONE',  ( 4.694131320935415630, 52.02092419516998234, 75.77039595153209461 ) ) ;
#13298=EDGE_CURVE ( 'NONE', #682, #14937, #19591, .T. ) ;
#13301=ORIENTED_EDGE ( 'NONE', *, *, #6580, .T. ) ;
#13303=CARTESIAN_POINT ( 'NONE',  ( 4.080804472568812180, 36.77439181754974840, 75.94166117767865387 ) ) ;
#13304=VECTOR ( 'NONE', #19776, 999.9999999999998863 ) ;
#13306=CARTESIAN_POINT ( 'NONE',  ( -4.525718010196823293, 37.70506222990913869, 78.74088963820604192 ) ) ;
#13308=DIRECTION ( 'NONE',  ( -1.540237394707284220E-16, -1.793354297423764243E-16, 1.000000000000000000 ) ) ;
#13310=EDGE_CURVE ( 'NONE', #20868, #6298, #8348, .T. ) ;
#13311=CARTESIAN_POINT ( 'NONE',  ( 9.353817388681445522, 42.82770861117572281, 78.41904468188381827 ) ) ;
#13314=CARTESIAN_POINT ( 'NONE',  ( 5.868769507328080337, 38.08668061124301829, 78.34126521887253602 ) ) ;
#13315=DIRECTION ( 'NONE',  ( 0.3165065846431827645, 0.9485903129789529098, 0.000000000000000000 ) ) ;
#13316=CARTESIAN_POINT ( 'NONE',  ( 0.8456863967494556711, 52.95623207773213181, 76.19861728079081331 ) ) ;
#13318=VECTOR ( 'NONE', #5071, 1000.000000000000114 ) ;
#13319=LINE ( 'NONE', #8101, #19942 ) ;
#13321=ORIENTED_EDGE ( 'NONE', *, *, #20016, .F. ) ;
#13323=CARTESIAN_POINT ( 'NONE',  ( 2.114319545972857650, 52.20160704302087140, 77.78911287202200242 ) ) ;
#13325=AXIS2_PLACEMENT_3D ( 'NONE', #18368, #593, #5267 ) ;
#13326=CARTESIAN_POINT ( 'NONE',  ( 8.332139447377956643, 41.66172086508280614, 79.54742650360671519 ) ) ;
#13328=AXIS2_PLACEMENT_3D ( 'NONE', #4890, #8099, #12997 ) ;
#13330=VERTEX_POINT ( 'NONE', #14830 ) ;
#13331=DIRECTION ( 'NONE',  ( -0.9485903129789529098, 0.3165065846431826535, -8.934458285744997376E-17 ) ) ;
#13334=CARTESIAN_POINT ( 'NONE',  ( 2.421193248165596668, 49.85372324935340060, 80.45433879953087342 ) ) ;
#13335=CARTESIAN_POINT ( 'NONE',  ( 8.133552201135486825, 41.55168119144260430, 75.36050707951255845 ) ) ;
#13337=CARTESIAN_POINT ( 'NONE',  ( -4.398802922602397913, 51.46161812541917868, 78.75145056212190298 ) ) ;
#13338=CARTESIAN_POINT ( 'NONE',  ( 0.3769493647919933688, 52.96722407749858519, 78.82913797267801215 ) ) ;
#13340=CARTESIAN_POINT ( 'NONE',  ( -4.239546901740170348, 50.82850121497202167, 75.97198585835440099 ) ) ;
#13342=VERTEX_POINT ( 'NONE', #15153 ) ;
#13343=CARTESIAN_POINT ( 'NONE',  ( 0.5221537403065015237, 44.16218137147968292, 75.45433879953087342 ) ) ;
#13345=AXIS2_PLACEMENT_3D ( 'NONE', #19452, #4868, #16797 ) ;
#13346=DIRECTION ( 'NONE',  ( -0.9485903129789527988, 0.3165065846431829311, -8.934458285744989980E-17 ) ) ;
#13349=CARTESIAN_POINT ( 'NONE',  ( 5.488638308869484561, 37.64219262425781665, 76.17246542145134924 ) ) ;
#13350=CARTESIAN_POINT ( 'NONE',  ( -4.089052737068717747, 51.68295426732343856, 75.42336258079946276 ) ) ;
#13351=VERTEX_POINT ( 'NONE', #14729 ) ;
#13352=DIRECTION ( 'NONE',  ( 1.540237394707284220E-16, 1.793354297423764243E-16, -1.000000000000000000 ) ) ;
#13357=EDGE_CURVE ( 'NONE', #4192, #158, #150, .T. ) ;
#13358=DIRECTION ( 'NONE',  ( 1.540237394707284220E-16, 1.793354297423764243E-16, -1.000000000000000000 ) ) ;
#13360=ORIENTED_EDGE ( 'NONE', *, *, #7398, .F. ) ;
#13361=CARTESIAN_POINT ( 'NONE',  ( 8.879174460483845621, 41.40517364458161609, 78.05744560429982926 ) ) ;
#13362=CARTESIAN_POINT ( 'NONE',  ( -4.716387082485078430, 37.09126585098686490, 75.36022115247205022 ) ) ;
#13363=ORIENTED_EDGE ( 'NONE', *, *, #16254, .F. ) ;
#13365=CARTESIAN_POINT ( 'NONE',  ( 0.3326973149608341562, 52.96014171822455552, 76.44919174070734869 ) ) ;
#13367=DIRECTION ( 'NONE',  ( -0.8043570849667761591, 0.5941461771851692664, -1.733862608106489734E-17 ) ) ;
#13372=VECTOR ( 'NONE', #3739, 1000.000000000000000 ) ;
#13376=FACE_OUTER_BOUND ( 'NONE', #8499, .T. ) ;
#13378=ORIENTED_EDGE ( 'NONE', *, *, #14969, .F. ) ;
#13379=CARTESIAN_POINT ( 'NONE',  ( 5.116981105040771638, 36.62970456142029008, 75.43572969368668168 ) ) ;
#13380=EDGE_CURVE ( 'NONE', #12382, #13012, #18655, .T. ) ;
#13381=CARTESIAN_POINT ( 'NONE',  ( 7.682243507100542601, 40.18231369592098190, 78.58253683706189463 ) ) ;
#13383=DIRECTION ( 'NONE',  ( -0.3165065846431827090, -0.9485903129789527988, 0.000000000000000000 ) ) ;
#13386=EDGE_CURVE ( 'NONE', #4079, #16470, #17376, .T. ) ;
#13387=VERTEX_POINT ( 'NONE', #8989 ) ;
#13390=DIRECTION ( 'NONE',  ( 0.007885122365275663500, 0.9999689119394085113, 1.805443505845543142E-16 ) ) ;
#13392=CARTESIAN_POINT ( 'NONE',  ( -2.083470957239373256, 47.45622447009557021, 82.45433879953087342 ) ) ;
#13394=CARTESIAN_POINT ( 'NONE',  ( -2.919077339881743782, 51.60516013878824992, 78.30927351043679607 ) ) ;
#13396=CARTESIAN_POINT ( 'NONE',  ( -0.9228510475973594751, 52.84273317725999419, 76.37557405286315770 ) ) ;
#13398=CARTESIAN_POINT ( 'NONE',  ( 0.8503868799515119647, 52.96349134317159013, 77.76169174070734869 ) ) ;
#13402=VERTEX_POINT ( 'NONE', #8772 ) ;
#13403=CARTESIAN_POINT ( 'NONE',  ( 4.252632704766235783, 36.85940042850018017, 75.70221307569202907 ) ) ;
#13404=ORIENTED_EDGE ( 'NONE', *, *, #1901, .F. ) ;
#13407=CARTESIAN_POINT ( 'NONE',  ( 0.3821786226492928651, 35.36301154328572949, 75.45433879953087342 ) ) ;
#13409=EDGE_CURVE ( 'NONE', #8044, #8009, #6552, .T. ) ;
#13410=LINE ( 'NONE', #3609, #13946 ) ;
#13412=ADVANCED_BREP_SHAPE_REPRESENTATION ( '', ( #18516, #18366 ), #19057 ) ;
#13414=CARTESIAN_POINT ( 'NONE',  ( 5.202885763635528349, 50.89499265101085967, 76.39036821129558064 ) ) ;
#13416=CARTESIAN_POINT ( 'NONE',  ( 8.625916568955123154, 43.01056172780193521, 78.83313045764568017 ) ) ;
#13417=PLANE ( 'NONE',  #17897 ) ;
#13418=EDGE_CURVE ( 'NONE', #3669, #16858, #20235, .T. ) ;
#13422=EDGE_CURVE ( 'NONE', #13387, #8823, #1742, .T. ) ;
#13425=ADVANCED_FACE ( 'NONE', ( #7794 ), #15796, .F. ) ;
#13426=CARTESIAN_POINT ( 'NONE',  ( 2.120831115265152444, 52.94022022329007626, 77.84551527011910821 ) ) ;
#13428=CARTESIAN_POINT ( 'NONE',  ( 5.653812050471574757, 37.77110297002621309, 78.37198585835440667 ) ) ;
#13429=ORIENTED_EDGE ( 'NONE', *, *, #13589, .F. ) ;
#13432=CARTESIAN_POINT ( 'NONE',  ( -4.895593109503407092, 37.22363812428621088, 77.05433879953086773 ) ) ;
#13435=CARTESIAN_POINT ( 'NONE',  ( 8.344059103522193155, 41.69997857441280331, 78.09649493259128405 ) ) ;
#13437=DIRECTION ( 'NONE',  ( -1.540237394707283727E-16, -1.793354297423763257E-16, 1.000000000000000000 ) ) ;
#13438=EDGE_CURVE ( 'NONE', #14937, #18369, #1279, .T. ) ;
#13440=EDGE_LOOP ( 'NONE', ( #16340, #2839, #2819, #1360 ) ) ;
#13441=DIRECTION ( 'NONE',  ( -0.3181025035074024898, 0.9480563259966799938, 1.210247515173824561E-16 ) ) ;
#13443=DIRECTION ( 'NONE',  ( -1.540237394707284220E-16, -1.793354297423764243E-16, 1.000000000000000000 ) ) ;
#13444=CARTESIAN_POINT ( 'NONE',  ( -6.882752284265650111, 40.85947821762912469, 77.28168744664917256 ) ) ;
#13445=CARTESIAN_POINT ( 'NONE',  ( 5.508100443945853186, 47.59510827513957310, 72.45432679953087529 ) ) ;
#13446=CARTESIAN_POINT ( 'NONE',  ( -7.782479702508445563, 41.24717501159041433, 76.51864607170344357 ) ) ;
#13449=ORIENTED_EDGE ( 'NONE', *, *, #16378, .F. ) ;
#13450=CARTESIAN_POINT ( 'NONE',  ( 0.5221537403065010796, 44.16218137147968292, 78.41904468188380406 ) ) ;
#13451=DIRECTION ( 'NONE',  ( -1.540237394707284220E-16, -1.793354297423764243E-16, 1.000000000000000000 ) ) ;
#13452=EDGE_LOOP ( 'NONE', ( #18214, #4894, #12521, #17105 ) ) ;
#13453=LINE ( 'NONE', #5353, #17660 ) ;
#13457=EDGE_LOOP ( 'NONE', ( #13842, #14642, #16130, #4539 ) ) ;
#13459=CARTESIAN_POINT ( 'NONE',  ( -5.868264228364995283, 37.94211109820661676, 75.91870325888974946 ) ) ;
#13461=CARTESIAN_POINT ( 'NONE',  ( -1.376885767552596063, 38.47063949360596524, 82.45433879953087342 ) ) ;
#13462=CARTESIAN_POINT ( 'NONE',  ( 0.4199111084294616658, 52.96161903445963759, 76.98462281259935480 ) ) ;
#13463=ORIENTED_EDGE ( 'NONE', *, *, #6872, .T. ) ;
#13464=CARTESIAN_POINT ( 'NONE',  ( -4.208505828092586221, 37.49087554584724558, 78.00876120161012750 ) ) ;
#13466=ORIENTED_EDGE ( 'NONE', *, *, #7667, .F. ) ;
#13467=CARTESIAN_POINT ( 'NONE',  ( -4.649709362898930998, 51.28232956945436882, 75.97399450257033493 ) ) ;
#13470=CARTESIAN_POINT ( 'NONE',  ( 8.207311740369052089, 47.02196222218739763, 75.43669174070734584 ) ) ;
#13471=EDGE_CURVE ( 'NONE', #9413, #9222, #2804, .T. ) ;
#13473=ORIENTED_EDGE ( 'NONE', *, *, #16686, .F. ) ;
#13474=CYLINDRICAL_SURFACE ( 'NONE', #16975, 6.000000000000002665 ) ;
#13475=VERTEX_POINT ( 'NONE', #11318 ) ;
#13481=VECTOR ( 'NONE', #18197, 1000.000000000000000 ) ;
#13484=CARTESIAN_POINT ( 'NONE',  ( -3.955205046931956403, 36.52901134360649138, 77.68963291717793140 ) ) ;
#13485=CARTESIAN_POINT ( 'NONE',  ( 8.621533274486752774, 40.63300666569625008, 75.47105533938442079 ) ) ;
#13488=CARTESIAN_POINT ( 'NONE',  ( -4.225462782839600528, 50.84799750334796187, 79.54845644658969661 ) ) ;
#13489=CARTESIAN_POINT ( 'NONE',  ( 0.3575591894758495259, 52.96144190202271318, 75.36602842597199015 ) ) ;
#13491=CARTESIAN_POINT ( 'NONE',  ( 8.292349522058055200, 41.56647775562769453, 75.97198585835440099 ) ) ;
#13495=VECTOR ( 'NONE', #21010, 1000.000000000000114 ) ;
#13496=FACE_OUTER_BOUND ( 'NONE', #16657, .T. ) ;
#13497=ORIENTED_EDGE ( 'NONE', *, *, #8342, .F. ) ;
#13498=CARTESIAN_POINT ( 'NONE',  ( 0.3616762838632459620, 52.96733004806014122, 76.07436980028356288 ) ) ;
#13501=CARTESIAN_POINT ( 'NONE',  ( -4.889784912074390810, 37.21934784281386044, 78.69750623079058016 ) ) ;
#13506=CARTESIAN_POINT ( 'NONE',  ( 5.459965721645525960, 50.70211769645560906, 77.96367690144739981 ) ) ;
#13508=VECTOR ( 'NONE', #825, 1000.000000000000000 ) ;
#13509=CARTESIAN_POINT ( 'NONE',  ( 8.953205446347402230, 41.62704920565285249, 79.54154676390322720 ) ) ;
#13511=DIRECTION ( 'NONE',  ( 1.540237394707284220E-16, 1.793354297423764243E-16, -1.000000000000000000 ) ) ;
#13512=ORIENTED_EDGE ( 'NONE', *, *, #20609, .T. ) ;
#13517=EDGE_CURVE ( 'NONE', #13475, #14379, #17482, .T. ) ;
#13519=CARTESIAN_POINT ( 'NONE',  ( 2.050865772649529628, 52.20210739934316990, 77.29915700192239569 ) ) ;
#13520=ADVANCED_FACE ( 'NONE', ( #14278 ), #7695, .F. ) ;
#13526=EDGE_CURVE ( 'NONE', #20602, #14974, #19173, .T. ) ;
#13527=ORIENTED_EDGE ( 'NONE', *, *, #14201, .F. ) ;
#13528=DIRECTION ( 'NONE',  ( -0.3165065846431826535, -0.9485903129789529098, -2.188653791613874008E-16 ) ) ;
#13530=ADVANCED_FACE ( 'NONE', ( #11210 ), #18560, .F. ) ;
#13533=VECTOR ( 'NONE', #19078, 1000.000000000000000 ) ;
#13534=CARTESIAN_POINT ( 'NONE',  ( -3.944959226007137776, 38.51060946023304865, 78.53742703482498655 ) ) ;
#13535=CARTESIAN_POINT ( 'NONE',  ( -3.448881463449838591, 52.14039722128521959, 78.93778436892569061 ) ) ;
#13537=CARTESIAN_POINT ( 'NONE',  ( 5.244536171700299398, 50.85972636156689219, 77.21343514867072599 ) ) ;
#13538=CARTESIAN_POINT ( 'NONE',  ( 0.3361279572737660426, 52.96754596929898184, 78.62228161321135644 ) ) ;
#13541=EDGE_LOOP ( 'NONE', ( #3831, #18111, #16792, #12622 ) ) ;
#13542=LINE ( 'NONE', #16849, #15877 ) ;
#13543=CARTESIAN_POINT ( 'NONE',  ( 6.737194059699555204, 50.51179604963209613, 77.55733179791843668 ) ) ;
#13545=PLANE ( 'NONE',  #1651 ) ;
#13547=CARTESIAN_POINT ( 'NONE',  ( 5.845446004764687231, 37.15023890796076245, 76.33129752952908120 ) ) ;
#13548=VECTOR ( 'NONE', #20946, 1000.000000000000000 ) ;
#13549=ORIENTED_EDGE ( 'NONE', *, *, #16424, .T. ) ;
#13550=EDGE_CURVE ( 'NONE', #4385, #15280, #20080, .T. ) ;
#13551=CARTESIAN_POINT ( 'NONE',  ( 8.260815876642354283, 41.47217187522794291, 78.92656146296575059 ) ) ;
#13552=EDGE_LOOP ( 'NONE', ( #2573, #6320, #1686, #7147 ) ) ;
#13553=DIRECTION ( 'NONE',  ( -0.007885122365285377952, -0.9999689119394085113, -1.805443505845558427E-16 ) ) ;
#13556=ORIENTED_EDGE ( 'NONE', *, *, #4933, .T. ) ;
#13561=CARTESIAN_POINT ( 'NONE',  ( -4.804325902087982492, 51.17184625142267151, 78.52518475144754007 ) ) ;
#13562=EDGE_LOOP ( 'NONE', ( #13429, #15823, #9242, #20380 ) ) ;
#13563=LINE ( 'NONE', #18463, #7123 ) ;
#13566=ORIENTED_EDGE ( 'NONE', *, *, #1286, .T. ) ;
#13567=CARTESIAN_POINT ( 'NONE',  ( 0.6306725468420852909, 52.36149037339925627, 77.38615272760776520 ) ) ;
#13571=CARTESIAN_POINT ( 'NONE',  ( -4.842431058766297980, 37.18436945890473311, 76.00936707281648808 ) ) ;
#13572=CARTESIAN_POINT ( 'NONE',  ( 0.3342709565510947334, 52.96022202444907379, 78.69601584788405546 ) ) ;
#13573=VECTOR ( 'NONE', #12735, 1000.000000000000000 ) ;
#13577=CARTESIAN_POINT ( 'NONE',  ( 3.959183846440533117, 36.72216061236609619, 76.69403369658814995 ) ) ;
#13579=VERTEX_POINT ( 'NONE', #5517 ) ;
#13581=CARTESIAN_POINT ( 'NONE',  ( 0.3332767407100286627, 52.96756894666060589, 77.72734411258261389 ) ) ;
#13583=CARTESIAN_POINT ( 'NONE',  ( -3.353456363966241138, 52.20858450364031000, 76.50206692849373269 ) ) ;
#13589=EDGE_CURVE ( 'NONE', #12459, #11489, #9587, .T. ) ;
#13590=PLANE ( 'NONE',  #21026 ) ;
#13592=CARTESIAN_POINT ( 'NONE',  ( 8.378637954445377289, 41.81363803720061867, 76.38301527011910252 ) ) ;
#13593=CARTESIAN_POINT ( 'NONE',  ( 7.680032241523795378, 40.16158449578585277, 77.69330938776616335 ) ) ;
#13594=DIRECTION ( 'NONE',  ( 0.8043570849667761591, -0.5941461771851692664, 1.733862608106489734E-17 ) ) ;
#13595=AXIS2_PLACEMENT_3D ( 'NONE', #6704, #1331, #20781 ) ;
#13596=CARTESIAN_POINT ( 'NONE',  ( 0.6366586698427276758, 52.96517666865470630, 77.38563349023446847 ) ) ;
#13598=B_SPLINE_CURVE_WITH_KNOTS ( 'NONE', 3,
 ( #11361, #4530, #3160, #6330, #16245, #1666, #17829, #3259, #9446, #11047, #20693, #1460 ),
 .UNSPECIFIED., .F., .F.,
 ( 4, 2, 2, 2, 2, 4 ),
 ( 0.000000000000000000, 0.0001730768718649229035, 0.0003461537437298458069, 0.0004326921796623278043, 0.0005192306155948099100, 0.0006923074874598105508 ),
 .UNSPECIFIED. ) ;
#13599=CARTESIAN_POINT ( 'NONE',  ( -4.032264951078912141, 50.98107207184723677, 76.47051527011910821 ) ) ;
#13603=CARTESIAN_POINT ( 'NONE',  ( -7.951966518800452022, 41.76130995793021583, 78.71972396713441356 ) ) ;
#13605=CARTESIAN_POINT ( 'NONE',  ( 0.3568559529620515813, 52.35602931952836059, 76.07436980028356288 ) ) ;
#13606=ORIENTED_EDGE ( 'NONE', *, *, #4564, .T. ) ;
#13607=DIRECTION ( 'NONE',  ( 0.5813877811927011807, -0.8136266022444372803, -5.636455622144619183E-17 ) ) ;
#13613=CARTESIAN_POINT ( 'NONE',  ( -7.474077239038335208, 48.01569385150226310, 78.79824701870994375 ) ) ;
#13614=ADVANCED_FACE ( 'NONE', ( #13496 ), #4017, .T. ) ;
#13616=B_SPLINE_CURVE_WITH_KNOTS ( 'NONE', 3,
 ( #19753, #3685, #16886, #20172, #20063, #16576, #15298, #10521, #18169, #10204 ),
 .UNSPECIFIED., .F., .F.,
 ( 4, 2, 2, 2, 4 ),
 ( 0.000000000000000000, 0.0001230216279879512049, 0.0002460432559759024099, 0.0003690648839638536148, 0.0004920865119518048197 ),
 .UNSPECIFIED. ) ;
#13617=ORIENTED_EDGE ( 'NONE', *, *, #12169, .T. ) ;
#13619=CARTESIAN_POINT ( 'NONE',  ( 8.176702304275824673, 41.66423807893649212, 79.54795956895829079 ) ) ;
#13622=VERTEX_POINT ( 'NONE', #730 ) ;
#13628=CARTESIAN_POINT ( 'NONE',  ( -7.850119897725965856, 41.43929802982232502, 78.93401657524854897 ) ) ;
#13630=CARTESIAN_POINT ( 'NONE',  ( -7.640244526827991045, 47.49833189654476939, 78.29855163726114142 ) ) ;
#13632=CARTESIAN_POINT ( 'NONE',  ( 6.872381782841294751, 37.88404961645574076, 76.32925572521180868 ) ) ;
#13634=CARTESIAN_POINT ( 'NONE',  ( 0.5221537403065019678, 44.16218137147968292, 72.45433879953087342 ) ) ;
#13635=B_SPLINE_CURVE_WITH_KNOTS ( 'NONE', 3,
 ( #9453, #15939, #7851, #20280, #2744, #12217, #15735, #20395, #5826, #17212 ),
 .UNSPECIFIED., .F., .F.,
 ( 4, 2, 2, 2, 4 ),
 ( 0.000000000000000000, 0.0001356155976497246129, 0.0002712311952994492258, 0.0004068467929491738659, 0.0005424623905988984517 ),
 .UNSPECIFIED. ) ;
#13636=VERTEX_POINT ( 'NONE', #15422 ) ;
#13638=CARTESIAN_POINT ( 'NONE',  ( -4.302529968709936981, 50.78349582127268746, 78.93463708245236887 ) ) ;
#13639=AXIS2_PLACEMENT_3D ( 'NONE', #12234, #10228, #3920 ) ;
#13642=ORIENTED_EDGE ( 'NONE', *, *, #17552, .T. ) ;
#13644=CARTESIAN_POINT ( 'NONE',  ( 2.091368541865482822, 52.21063245889818916, 75.45433879953088763 ) ) ;
#13646=DIRECTION ( 'NONE',  ( 1.540237394707284220E-16, 1.793354297423764243E-16, -1.000000000000000000 ) ) ;
#13647=CARTESIAN_POINT ( 'NONE',  ( -5.769203958596529347, 48.43638519259696551, 72.45433879953087342 ) ) ;
#13649=CARTESIAN_POINT ( 'NONE',  ( 0.8436899295658937259, 52.35217759412554983, 76.26682227151283655 ) ) ;
#13650=CARTESIAN_POINT ( 'NONE',  ( 0.3313075116511031704, 52.35623069211510483, 78.62228161321135644 ) ) ;
#13652=CARTESIAN_POINT ( 'NONE',  ( 0.5221537403065019678, 44.16218137147968292, 72.45433879953087342 ) ) ;
#13654=CARTESIAN_POINT ( 'NONE',  ( 0.5221537403065009686, 44.16218137147968292, 79.45433879953087342 ) ) ;
#13655=CARTESIAN_POINT ( 'NONE',  ( -7.131166555022944387, 41.64504215559904310, 76.30903472146037814 ) ) ;
#13657=CARTESIAN_POINT ( 'NONE',  ( -7.355728065240099589, 40.24014096896499382, 77.93115699112124162 ) ) ;
#13660=CARTESIAN_POINT ( 'NONE',  ( -5.841826873769421447, 37.92258288932846710, 75.85972562479176418 ) ) ;
#13662=CARTESIAN_POINT ( 'NONE',  ( -4.157721234522135489, 51.63388627315737267, 75.40660817806873695 ) ) ;
#13671=CARTESIAN_POINT ( 'NONE',  ( 0.3340858135836293763, 52.96017298819928243, 77.67332619259997273 ) ) ;
#13672=EDGE_LOOP ( 'NONE', ( #14323, #865, #9177, #20144 ) ) ;
#13675=DIRECTION ( 'NONE',  ( 0.007885122365278605591, 0.9999689119394085113, 1.805443505845548073E-16 ) ) ;
#13677=VECTOR ( 'NONE', #3617, 1000.000000000000000 ) ;
#13679=CARTESIAN_POINT ( 'NONE',  ( -3.055718635266669647, 36.78391400955043622, 76.62933879953087057 ) ) ;
#13683=EDGE_CURVE ( 'NONE', #20489, #10089, #20188, .T. ) ;
#13686=CARTESIAN_POINT ( 'NONE',  ( -4.861758623289528458, 37.19864595225625692, 76.03818239474222196 ) ) ;
#13687=DIRECTION ( 'NONE',  ( -1.540237394707284220E-16, -1.793354297423764243E-16, 1.000000000000000000 ) ) ;
#13689=DIRECTION ( 'NONE',  ( -0.2999031954727373050, -0.9539696396349525154, -2.172727669310459771E-16 ) ) ;
#13693=CARTESIAN_POINT ( 'NONE',  ( 0.6361344075657290320, 52.21317904296746093, 75.36071969156348871 ) ) ;
#13696=CARTESIAN_POINT ( 'NONE',  ( 0.4711897470839793711, 52.35512766633201664, 77.40025757944940210 ) ) ;
#13700=CARTESIAN_POINT ( 'NONE',  ( 6.907457231639352102, 50.38602950313908480, 78.73390793106847241 ) ) ;
#13704=CARTESIAN_POINT ( 'NONE',  ( 9.009194133669925719, 41.79485085341455886, 75.38196330830126612 ) ) ;
#13705=CARTESIAN_POINT ( 'NONE',  ( 0.3821786226492927541, 35.36301154328572949, 76.16022115247204738 ) ) ;
#13709=CARTESIAN_POINT ( 'NONE',  ( 0.8188518330924889899, 52.96374000860539155, 77.51877209028926075 ) ) ;
#13711=CARTESIAN_POINT ( 'NONE',  ( 5.750640099535992533, 51.24052371918730842, 75.36022115247205022 ) ) ;
#13714=CARTESIAN_POINT ( 'NONE',  ( 8.374959273921817271, 41.81408433146208381, 78.54183882225588320 ) ) ;
#13715=VECTOR ( 'NONE', #1861, 1000.000000000000000 ) ;
#13716=ORIENTED_EDGE ( 'NONE', *, *, #18701, .F. ) ;
#13717=CARTESIAN_POINT ( 'NONE',  ( -4.517176205512259735, 36.94411680087065974, 76.50360254650976799 ) ) ;
#13718=DIRECTION ( 'NONE',  ( -1.540237394707284467E-16, -1.793354297423764243E-16, 1.000000000000000000 ) ) ;
#13719=CARTESIAN_POINT ( 'NONE',  ( -4.471346911670678992, 51.40978084683593607, 79.54642512701808243 ) ) ;
#13721=CARTESIAN_POINT ( 'NONE',  ( -5.018595066975969132, 37.31449471545010965, 77.33253961758860839 ) ) ;
#13722=CARTESIAN_POINT ( 'NONE',  ( -5.389245695702297390, 49.84508174962770255, 72.45433879953087342 ) ) ;
#13724=EDGE_CURVE ( 'NONE', #8370, #20695, #4547, .T. ) ;
#13725=CARTESIAN_POINT ( 'NONE',  ( 5.534705324965363715, 50.64691056217811393, 78.12411320240556734 ) ) ;
#13728=CARTESIAN_POINT ( 'NONE',  ( 6.224138097561578320, 50.05597543161009355, 77.64680307551286376 ) ) ;
#13729=CARTESIAN_POINT ( 'NONE',  ( -4.509672285278093717, 36.93857395727003023, 75.36838243422435824 ) ) ;
#13732=CARTESIAN_POINT ( 'NONE',  ( -6.782631326057146026, 43.38225751353197523, 78.28007409364852265 ) ) ;
#13733=DIRECTION ( 'NONE',  ( 1.540237394707284220E-16, 1.793354297423764243E-16, -1.000000000000000000 ) ) ;
#13735=CARTESIAN_POINT ( 'NONE',  ( -4.392497846706504561, 51.46612350181082007, 76.19049300047602458 ) ) ;
#13736=CARTESIAN_POINT ( 'NONE',  ( -3.545047478496396565, 36.22604446995779170, 78.23707788297487298 ) ) ;
#13737=CARTESIAN_POINT ( 'NONE',  ( -7.724133150439582707, 47.24691236978577535, 78.01104965316210382 ) ) ;
#13739=EDGE_CURVE ( 'NONE', #4812, #11233, #18918, .T. ) ;
#13741=VERTEX_POINT ( 'NONE', #20819 ) ;
#13742=CARTESIAN_POINT ( 'NONE',  ( 1.973315136850091855, 52.23284655848411973, 75.87673665581081650 ) ) ;
#13743=ORIENTED_EDGE ( 'NONE', *, *, #2976, .F. ) ;
#13749=EDGE_CURVE ( 'NONE', #11138, #8211, #14229, .T. ) ;
#13750=CARTESIAN_POINT ( 'NONE',  ( -2.928118925487932067, 51.59273948230099904, 78.48078762820125576 ) ) ;
#13752=CARTESIAN_POINT ( 'NONE',  ( 0.5424873107736979394, 52.36227596382597227, 77.38586826841044797 ) ) ;
#13755=FACE_OUTER_BOUND ( 'NONE', #10576, .T. ) ;
#13756=ORIENTED_EDGE ( 'NONE', *, *, #8497, .T. ) ;
#13757=CARTESIAN_POINT ( 'NONE',  ( 4.903891431458001549, 51.86598285117960216, 77.64500276804245971 ) ) ;
#13758=CARTESIAN_POINT ( 'NONE',  ( 6.786106954071964736, 50.47566606489075980, 77.50555814853646552 ) ) ;
#13760=CARTESIAN_POINT ( 'NONE',  ( 6.811311454328823345, 50.45704851585021800, 79.04700635913849283 ) ) ;
#13763=CARTESIAN_POINT ( 'NONE',  ( 5.547036553094518929, 37.68180603056410405, 78.36773547936199691 ) ) ;
#13764=B_SPLINE_SURFACE_WITH_KNOTS ( 'NONE', 3, 1, ( 
 ( #16601, #16182 ),
 ( #3513, #308 ),
 ( #18190, #2022 ),
 ( #19882, #6908 ),
 ( #19466, #6482 ),
 ( #8519, #15004 ),
 ( #17979, #6586 ),
 ( #11404, #424 ),
 ( #4883, #5302 ),
 ( #16398, #13198 ),
 ( #9703, #3404 ) ),
 .UNSPECIFIED., .F., .F., .F.,
 ( 4, 1, 1, 1, 1, 1, 1, 1, 4 ),
 ( 2, 2 ),
 ( 0.000000000000000000, 0.1891742793480645779, 0.3478164846204494509, 0.4767017694705349973, 0.5812052966572537338, 0.6755649002106222101, 0.7721207368275812000, 0.8786749842102796748, 1.000000000000000000 ),
 ( 0.000000000000000000, 1.000000000000000000 ),
 .UNSPECIFIED. ) ;
#13765=ORIENTED_EDGE ( 'NONE', *, *, #2105, .T. ) ;
#13766=CARTESIAN_POINT ( 'NONE',  ( 8.788011242024287739, 41.13195169557157271, 78.55826321071354812 ) ) ;
#13767=( BOUNDED_CURVE ( )  B_SPLINE_CURVE ( 3, ( #15843, #4444, #6344, #19025 ),
 .UNSPECIFIED., .F., .F. ) 
 B_SPLINE_CURVE_WITH_KNOTS ( ( 4, 4 ),
 ( 1.425105721489102084, 1.727008346339851785 ),
 .UNSPECIFIED. ) 
 CURVE ( )  GEOMETRIC_REPRESENTATION_ITEM ( )  RATIONAL_B_SPLINE_CURVE ( ( 1.000000000000000000, 0.9924189787924448947, 0.9924189787924448947, 1.000000000000000000 ) ) 
 REPRESENTATION_ITEM ( '' )  );
#13768=ORIENTED_EDGE ( 'NONE', *, *, #10271, .F. ) ;
#13773=CARTESIAN_POINT ( 'NONE',  ( -4.617530944194691678, 50.38537608977133431, 79.48628414162533318 ) ) ;
#13778=CARTESIAN_POINT ( 'NONE',  ( 2.096812674726597603, 52.20958845481697352, 78.66304280023771867 ) ) ;
#13780=EDGE_LOOP ( 'NONE', ( #14186, #14741, #3714, #3539 ) ) ;
#13781=CARTESIAN_POINT ( 'NONE',  ( -4.225462782839600528, 50.84799750334796187, 79.54845644658969661 ) ) ;
#13784=CARTESIAN_POINT ( 'NONE',  ( -6.613032277150674432, 45.52591812603678534, 79.45433879953087342 ) ) ;
#13787=LINE ( 'NONE', #20376, #6856 ) ;
#13789=ORIENTED_EDGE ( 'NONE', *, *, #4402, .F. ) ;
#13790=LINE ( 'NONE', #12007, #7453 ) ;
#13792=CARTESIAN_POINT ( 'NONE',  ( 5.859131993956401274, 51.16038512709904040, 75.36137945677606353 ) ) ;
#13794=DIRECTION ( 'NONE',  ( 0.007885122365275663500, 0.9999689119394085113, 1.805443505845543142E-16 ) ) ;
#13796=EDGE_CURVE ( 'NONE', #6021, #14506, #15689, .T. ) ;
#13798=CARTESIAN_POINT ( 'NONE',  ( 6.030765343457317407, 50.11959148040762102, 79.40187404227555135 ) ) ;
#13799=ORIENTED_EDGE ( 'NONE', *, *, #1731, .F. ) ;
#13803=CARTESIAN_POINT ( 'NONE',  ( 8.121917471046002035, 44.10225444150351137, 72.45432679953087529 ) ) ;
#13808=CARTESIAN_POINT ( 'NONE',  ( 8.849350546267242379, 41.31578948168061061, 75.97436175383765544 ) ) ;
#13809=CARTESIAN_POINT ( 'NONE',  ( -5.283659240720997019, 50.82933219714914230, 75.48294376282896678 ) ) ;
#13810=CARTESIAN_POINT ( 'NONE',  ( 4.717386066067114747, 51.07891390471289128, 75.44114465464750197 ) ) ;
#13814=CARTESIAN_POINT ( 'NONE',  ( 8.912702722122396892, 41.50565997170561161, 78.91042349786003740 ) ) ;
#13816=ORIENTED_EDGE ( 'NONE', *, *, #5988, .F. ) ;
#13817=CARTESIAN_POINT ( 'NONE',  ( -7.367656984315424928, 48.05973018190410073, 72.45433879953087342 ) ) ;
#13818=LINE ( 'NONE', #15212, #18083 ) ;
#13819=EDGE_CURVE ( 'NONE', #17272, #8211, #14389, .T. ) ;
#13820=CARTESIAN_POINT ( 'NONE',  ( -3.477340361660131496, 52.12006153457090818, 79.00686454089694166 ) ) ;
#13824=CARTESIAN_POINT ( 'NONE',  ( 8.571241826522742357, 42.59017791465015534, 78.02841696848460629 ) ) ;
#13825=CARTESIAN_POINT ( 'NONE',  ( 8.951667845840693971, 41.62244091939069790, 76.38301527011910252 ) ) ;
#13826=ORIENTED_EDGE ( 'NONE', *, *, #2173, .T. ) ;
#13827=ORIENTED_EDGE ( 'NONE', *, *, #3619, .F. ) ;
#13829=CARTESIAN_POINT ( 'NONE',  ( 6.291655274237696993, 49.98965726174421320, 77.59820540376455256 ) ) ;
#13834=CARTESIAN_POINT ( 'NONE',  ( 9.178784097065811665, 42.30312273229867515, 78.05372954401303787 ) ) ;
#13836=CARTESIAN_POINT ( 'NONE',  ( -4.404666252920439895, 51.45742840424412634, 76.10127045261064893 ) ) ;
#13837=CARTESIAN_POINT ( 'NONE',  ( -7.727295065384001127, 47.23743591010920539, 77.61879955032603107 ) ) ;
#13838=CARTESIAN_POINT ( 'NONE',  ( -5.954796862783082290, 38.00602926950411842, 78.58503192925951453 ) ) ;
#13839=CARTESIAN_POINT ( 'NONE',  ( -8.191933259318233240, 42.93552377858928537, 78.37203949479768994 ) ) ;
#13840=EDGE_LOOP ( 'NONE', ( #6694, #14321, #12318, #15041, #12213, #1694, #16107, #20689, #16728, #2311, #13527 ) ) ;
#13841=CARTESIAN_POINT ( 'NONE',  ( 5.894741035747108171, 51.13408216234794423, 77.22227766523002401 ) ) ;
#13842=ORIENTED_EDGE ( 'NONE', *, *, #16514, .F. ) ;
#13843=AXIS2_PLACEMENT_3D ( 'NONE', #14437, #4850, #19321 ) ;
#13844=CARTESIAN_POINT ( 'NONE',  ( -4.804644443005473775, 51.17161863374555963, 78.45066232894264147 ) ) ;
#13846=VERTEX_POINT ( 'NONE', #4230 ) ;
#13849=CARTESIAN_POINT ( 'NONE',  ( -2.915674812773581426, 51.60163158963862173, 78.23748737924660190 ) ) ;
#13851=CARTESIAN_POINT ( 'NONE',  ( 5.710003222748535556, 51.27054054311695808, 77.28795170149270177 ) ) ;
#13853=ORIENTED_EDGE ( 'NONE', *, *, #3280, .F. ) ;
#13854=CARTESIAN_POINT ( 'NONE',  ( 1.652727357819364418, 35.35299279957455099, 76.86610350541323555 ) ) ;
#13856=VECTOR ( 'NONE', #10026, 1000.000000000000000 ) ;
#13857=ORIENTED_EDGE ( 'NONE', *, *, #11341, .F. ) ;
#13858=CARTESIAN_POINT ( 'NONE',  ( -0.8071739151948656987, 40.17810205696807913, 82.45433879953087342 ) ) ;
#13862=CARTESIAN_POINT ( 'NONE',  ( 0.5221537403065015237, 44.16218137147968292, 75.45433879953088763 ) ) ;
#13863=B_SPLINE_CURVE_WITH_KNOTS ( 'NONE', 3,
 ( #5888, #5662, #988, #7478, #18763, #5981, #20930, #16071, #11287, #3085, #9585, #12385 ),
 .UNSPECIFIED., .F., .F.,
 ( 4, 2, 2, 2, 2, 4 ),
 ( 0.000000000000000000, 0.0005742104900236383314, 0.001148420980047276663, 0.001435526225059106887, 0.001722631470070937545, 0.002296841960094558530 ),
 .UNSPECIFIED. ) ;
#13865=CARTESIAN_POINT ( 'NONE',  ( -6.782631326057146026, 43.38225751353197523, 78.13669174070733447 ) ) ;
#13866=ORIENTED_EDGE ( 'NONE', *, *, #16583, .F. ) ;
#13867=CARTESIAN_POINT ( 'NONE',  ( 4.311926990668543347, 51.43403001777136296, 77.50896141901741032 ) ) ;
#13870=LINE ( 'NONE', #10606, #3066 ) ;
#13872=CARTESIAN_POINT ( 'NONE',  ( -7.275583942264174375, 42.06582416155776372, 77.46376836651262465 ) ) ;
#13875=DIRECTION ( 'NONE',  ( 0.9480563259966822143, 0.3181025035073955509, 2.030702297275135124E-16 ) ) ;
#13877=ORIENTED_EDGE ( 'NONE', *, *, #17837, .T. ) ;
#13880=ORIENTED_EDGE ( 'NONE', *, *, #12150, .F. ) ;
#13881=FACE_BOUND ( 'NONE', #16238, .T. ) ;
#13882=CARTESIAN_POINT ( 'NONE',  ( 0.7561398222055120133, 52.96423844662842129, 78.87878230117789258 ) ) ;
#13883=EDGE_CURVE ( 'NONE', #16412, #10206, #7649, .T. ) ;
#13889=CARTESIAN_POINT ( 'NONE',  ( 5.427780505986066650, 36.85179043424346190, 76.70433879953087342 ) ) ;
#13890=CARTESIAN_POINT ( 'NONE',  ( 5.449567083428624947, 36.86735832482640518, 76.18683980367092090 ) ) ;
#13891=DIRECTION ( 'NONE',  ( 1.540237394707284220E-16, 1.793354297423764243E-16, -1.000000000000000000 ) ) ;
#13894=CARTESIAN_POINT ( 'NONE',  ( 1.288664704385863669, 52.20803360176820007, 75.43490186719157009 ) ) ;
#13897=CARTESIAN_POINT ( 'NONE',  ( 6.645808250425207397, 50.57929906569810896, 75.61685692759286326 ) ) ;
#13900=CARTESIAN_POINT ( 'NONE',  ( -3.350440871817599753, 52.21073926392551812, 76.59793576264409865 ) ) ;
#13902=VECTOR ( 'NONE', #19782, 1000.000000000000114 ) ;
#13903=ADVANCED_FACE ( 'NONE', ( #17744 ), #10249, .F. ) ;
#13904=CARTESIAN_POINT ( 'NONE',  ( -4.461854692652708287, 50.67442117498146104, 75.36473603976158131 ) ) ;
#13906=PLANE ( 'NONE',  #15910 ) ;
#13907=EDGE_CURVE ( 'NONE', #5223, #11489, #19640, .T. ) ;
#13908=DIRECTION ( 'NONE',  ( 1.540237394707284220E-16, 1.793354297423764243E-16, -1.000000000000000000 ) ) ;
#13909=CARTESIAN_POINT ( 'NONE',  ( 7.686881228206692285, 40.21297994929685160, 76.12035193564865665 ) ) ;
#13910=EDGE_CURVE ( 'NONE', #10028, #2112, #13066, .T. ) ;
#13911=AXIS2_PLACEMENT_3D ( 'NONE', #826, #929, #3902 ) ;
#13912=CARTESIAN_POINT ( 'NONE',  ( 6.184266552044742404, 50.09404646486822088, 75.56305138714441227 ) ) ;
#13916=DIRECTION ( 'NONE',  ( -1.540237394707284220E-16, -1.793354297423764243E-16, 1.000000000000000000 ) ) ;
#13918=CARTESIAN_POINT ( 'NONE',  ( -5.134411146083727395, 50.01620383897704869, 75.69846806870741318 ) ) ;
#13919=CARTESIAN_POINT ( 'NONE',  ( 5.531249400824703955, 51.40257879072892422, 75.36789977960694387 ) ) ;
#13920=EDGE_CURVE ( 'NONE', #6135, #12999, #5065, .T. ) ;
#13922=AXIS2_PLACEMENT_3D ( 'NONE', #10863, #15642, #14034 ) ;
#13923=CARTESIAN_POINT ( 'NONE',  ( -4.257991192395801150, 43.33247370687232092, 79.04308574771191331 ) ) ;
#13925=CARTESIAN_POINT ( 'NONE',  ( 8.865792162213244509, 41.36506604770743678, 78.93669174070734584 ) ) ;
#13927=DIRECTION ( 'NONE',  ( -1.540237394707284220E-16, -1.793354297423764243E-16, 1.000000000000000000 ) ) ;
#13932=CARTESIAN_POINT ( 'NONE',  ( -4.861758623289527570, 37.19864595225625692, 76.03818239474222196 ) ) ;
#13933=CARTESIAN_POINT ( 'NONE',  ( -7.606686202760679194, 43.11990846545297273, 78.43041451606663372 ) ) ;
#13934=CARTESIAN_POINT ( 'NONE',  ( 8.638503602126267111, 42.99341659656273862, 77.63357130927565208 ) ) ;
#13937=VERTEX_POINT ( 'NONE', #19226 ) ;
#13939=CARTESIAN_POINT ( 'NONE',  ( -4.385124331863694991, 37.59250281884201428, 78.93547643519214319 ) ) ;
#13941=ADVANCED_FACE ( 'NONE', ( #17847 ), #4957, .T. ) ;
#13942=CARTESIAN_POINT ( 'NONE',  ( 8.896031707678503153, 41.45569588382780779, 75.98771331677210128 ) ) ;
#13943=CARTESIAN_POINT ( 'NONE',  ( 5.929557977968517690, 51.10836428964097422, 77.10005730845655592 ) ) ;
#13944=B_SPLINE_SURFACE_WITH_KNOTS ( 'NONE', 3, 1, ( 
 ( #10349, #853 ),
 ( #10453, #13619 ),
 ( #15333, #20095 ),
 ( #13509, #15119 ),
 ( #16820, #8639 ),
 ( #19986, #7117 ),
 ( #10671, #3717 ),
 ( #10238, #5307 ),
 ( #5413, #2138 ),
 ( #6913, #431 ),
 ( #15223, #12140 ),
 ( #2238, #16919 ),
 ( #5533, #18619 ),
 ( #12040, #15436 ),
 ( #2343, #746 ),
 ( #4033, #8948 ),
 ( #7230, #10559 ),
 ( #7337, #20307 ),
 ( #5737, #12247 ),
 ( #18729, #4142 ),
 ( #2029, #13416 ),
 ( #19887, #2769 ),
 ( #15652, #17447 ),
 ( #14357, #9270 ),
 ( #20421, #2966 ),
 ( #1067, #17541 ),
 ( #14241, #2872 ) ),
 .UNSPECIFIED., .F., .F., .F.,
 ( 4, 1, 1, 1, 1, 1, 1, 1, 1, 1, 1, 1, 1, 1, 1, 1, 1, 1, 1, 1, 1, 1, 1, 1, 4 ),
 ( 2, 2 ),
 ( 0.000000000000000000, 0.06037445285962812075, 0.1180910611743953287, 0.1732658017268006723, 0.2259310541736886668, 0.2758310469819637567, 0.3235430165773793276, 0.3690552752481174870, 0.4126046436208182233, 0.4542408720228611196, 0.4938267050212239995, 0.5316899362873784840, 0.5681969051958857264, 0.6035856803598054210, 0.6378784996589128564, 0.6713567270158068423, 0.7043713979572046036, 0.7376082755227613141, 0.7714571943499641815, 0.8061103333465380327, 0.8420729482554840661, 0.8794516251380997129, 0.9177737848194706949, 0.9579350591099196066, 1.000000000000000000 ),
 ( 0.000000000000000000, 1.000000000000000000 ),
 .UNSPECIFIED. ) ;
#13945=CARTESIAN_POINT ( 'NONE',  ( 8.951218635964366399, 41.62109460889399770, 77.24172240072661566 ) ) ;
#13946=VECTOR ( 'NONE', #10119, 1000.000000000000000 ) ;
#13947=CARTESIAN_POINT ( 'NONE',  ( 9.201306621205869618, 42.37062416594873326, 78.02362291919803283 ) ) ;
#13950=CARTESIAN_POINT ( 'NONE',  ( -4.448383556050954368, 51.42618962001968441, 76.01002907825849775 ) ) ;
#13951=ADVANCED_FACE ( 'NONE', ( #1578 ), #1888, .T. ) ;
#13952=CARTESIAN_POINT ( 'NONE',  ( -7.484880448772741168, 47.96396789458968613, 78.32492703482499508 ) ) ;
#13954=CARTESIAN_POINT ( 'NONE',  ( 5.722750437672663892, 37.06256514788822898, 75.36130176902827316 ) ) ;
#13955=VERTEX_POINT ( 'NONE', #1476 ) ;
#13956=EDGE_CURVE ( 'NONE', #3254, #19301, #9362, .T. ) ;
#13958=ORIENTED_EDGE ( 'NONE', *, *, #14500, .F. ) ;
#13963=LINE ( 'NONE', #978, #8793 ) ;
#13964=CARTESIAN_POINT ( 'NONE',  ( -4.181418169567056253, 51.61695331097443784, 79.50772166908967620 ) ) ;
#13965=DIRECTION ( 'NONE',  ( 0.5954989751681698529, -0.8033560671169786005, -5.234922652618075161E-17 ) ) ;
#13967=CARTESIAN_POINT ( 'NONE',  ( -4.473072018670162464, 36.91153881467540288, 79.53329352641277694 ) ) ;
#13968=ORIENTED_EDGE ( 'NONE', *, *, #15102, .F. ) ;
#13969=DIRECTION ( 'NONE',  ( -0.9485903129789527988, 0.3165065846431829311, -8.934458285744989980E-17 ) ) ;
#13972=CARTESIAN_POINT ( 'NONE',  ( -5.004817973257477348, 39.29348442311233214, 77.05433879953086773 ) ) ;
#13973=CARTESIAN_POINT ( 'NONE',  ( -5.835824771109036746, 39.98772221508849611, 72.45433879953085921 ) ) ;
#13976=CARTESIAN_POINT ( 'NONE',  ( 5.841953631609400510, 37.14774338596793513, 76.17246542145134924 ) ) ;
#13977=CARTESIAN_POINT ( 'NONE',  ( 5.437844490049829282, 37.59859269650263514, 78.34743064351589226 ) ) ;
#13978=B_SPLINE_CURVE_WITH_KNOTS ( 'NONE', 3,
 ( #21031, #7870, #9788, #8180, #4759, #10979, #11177, #11285, #17543, #6467, #14359 ),
 .UNSPECIFIED., .F., .F.,
 ( 4, 1, 1, 1, 1, 1, 1, 1, 4 ),
 ( 0.000000000000000000, 0.1230989878275519644, 0.2403818709996815850, 0.3547287725962395277, 0.4701889909135318901, 0.5896219003167558759, 0.7153806559642975627, 0.8522030906580475573, 1.000000000000000000 ),
 .UNSPECIFIED. ) ;
#13979=EDGE_LOOP ( 'NONE', ( #9129, #7023, #17735, #16449 ) ) ;
#13980=CARTESIAN_POINT ( 'NONE',  ( -0.3916064810627546966, 36.00492801184311986, 78.58487462435995496 ) ) ;
#13982=VERTEX_POINT ( 'NONE', #19437 ) ;
#13983=LINE ( 'NONE', #17076, #14616 ) ;
#13985=CARTESIAN_POINT ( 'NONE',  ( -7.795419580117447289, 41.25910984028834605, 78.43135113490271237 ) ) ;
#13986=VERTEX_POINT ( 'NONE', #4855 ) ;
#13989=FACE_BOUND ( 'NONE', #18128, .T. ) ;
#13990=CARTESIAN_POINT ( 'NONE',  ( 5.035970566151715566, 36.57181739631530348, 75.46362501775257670 ) ) ;
#13991=CARTESIAN_POINT ( 'NONE',  ( 3.099655065065782367, 37.00631057046152961, 75.45433879953087342 ) ) ;
#13992=VERTEX_POINT ( 'NONE', #3270 ) ;
#13993=CARTESIAN_POINT ( 'NONE',  ( 1.034831540439702158, 52.34672676983775119, 79.52523235054587758 ) ) ;
#13995=AXIS2_PLACEMENT_3D ( 'NONE', #15648, #3925, #5629 ) ;
#13997=PLANE ( 'NONE',  #20259 ) ;
#13998=CARTESIAN_POINT ( 'NONE',  ( -0.2058114043728421494, 41.98042365162810086, 80.45433879953087342 ) ) ;
#13999=VECTOR ( 'NONE', #14037, 1000.000000000000114 ) ;
#14001=CARTESIAN_POINT ( 'NONE',  ( 5.196215417279978155, 37.43323793221333773, 75.99415254657458263 ) ) ;
#14002=CARTESIAN_POINT ( 'NONE',  ( 5.628424039023946612, 51.33079979992434261, 78.86786983087660019 ) ) ;
#14004=ORIENTED_EDGE ( 'NONE', *, *, #529, .F. ) ;
#14006=CARTESIAN_POINT ( 'NONE',  ( 1.832302049357034335, 52.95658493274570588, 75.70482343270806780 ) ) ;
#14008=VECTOR ( 'NONE', #1058, 1000.000000000000000 ) ;
#14009=CARTESIAN_POINT ( 'NONE',  ( -0.7686299002591694407, 52.26036095920864000, 79.04667360578667967 ) ) ;
#14010=CARTESIAN_POINT ( 'NONE',  ( 0.5312634811787118050, 52.96600774845068571, 77.38663191694250543 ) ) ;
#14016=CARTESIAN_POINT ( 'NONE',  ( 5.196643236000038080, 51.64973888592641771, 79.48101422306089603 ) ) ;
#14023=CARTESIAN_POINT ( 'NONE',  ( -7.611239903938034068, 43.11915264683222659, 78.37207201143637292 ) ) ;
#14028=VECTOR ( 'NONE', #13120, 1000.000000000000000 ) ;
#14031=ADVANCED_FACE ( 'NONE', ( #13376 ), #18161, .T. ) ;
#14032=CARTESIAN_POINT ( 'NONE',  ( -7.290527651941959952, 40.11224193202943411, 78.50801527011910252 ) ) ;
#14033=CARTESIAN_POINT ( 'NONE',  ( 8.375193797766709025, 41.81478721430313072, 78.41904468188381827 ) ) ;
#14034=DIRECTION ( 'NONE',  ( -0.3165065846431826535, -0.9485903129789529098, -2.188653791613874008E-16 ) ) ;
#14036=CARTESIAN_POINT ( 'NONE',  ( 8.385768451058924100, 39.92640453324153071, 77.75090705316073070 ) ) ;
#14037=DIRECTION ( 'NONE',  ( -0.9485903129789527988, 0.3165065846431829311, -8.934458285744989980E-17 ) ) ;
#14039=CARTESIAN_POINT ( 'NONE',  ( -7.811913822204808788, 47.00317617979911944, 79.21909685159604919 ) ) ;
#14041=ORIENTED_EDGE ( 'NONE', *, *, #9856, .F. ) ;
#14043=DIRECTION ( 'NONE',  ( 0.9996789974703350623, -0.02533578529877749536, 1.494306935163130398E-16 ) ) ;
#14046=CARTESIAN_POINT ( 'NONE',  ( 5.388356174074294458, 50.75501278463794819, 77.94845644658968808 ) ) ;
#14052=EDGE_CURVE ( 'NONE', #12950, #10787, #6871, .T. ) ;
#14055=EDGE_CURVE ( 'NONE', #11467, #9723, #16676, .T. ) ;
#14056=CARTESIAN_POINT ( 'NONE',  ( 0.5221537403065005245, 44.16218137147968292, 82.45433879953087342 ) ) ;
#14057=EDGE_LOOP ( 'NONE', ( #17171, #18069, #8418, #9326 ) ) ;
#14059=EDGE_CURVE ( 'NONE', #18295, #8403, #19943, .T. ) ;
#14063=EDGE_CURVE ( 'NONE', #19757, #2342, #14356, .T. ) ;
#14065=CARTESIAN_POINT ( 'NONE',  ( -0.9375041090292165480, 52.97865058173552910, 77.15777051809955367 ) ) ;
#14068=DIRECTION ( 'NONE',  ( -0.8146038580541393737, 0.5800177190770224867, -2.145060549591027246E-17 ) ) ;
#14071=ADVANCED_FACE ( 'NONE', ( #708 ), #8912, .T. ) ;
#14073=EDGE_LOOP ( 'NONE', ( #5362, #12181, #4077, #15008, #15678, #15107, #16063, #18969 ) ) ;
#14074=CARTESIAN_POINT ( 'NONE',  ( 6.153536035488349043, 50.12267912296926653, 77.68963291717793140 ) ) ;
#14075=CARTESIAN_POINT ( 'NONE',  ( 4.728442938187240152, 51.99557958566231264, 77.51131257087278925 ) ) ;
#14078=LINE ( 'NONE', #12589, #14222 ) ;
#14080=CARTESIAN_POINT ( 'NONE',  ( -5.338436749040042173, 37.55074888198200256, 75.45005776384208218 ) ) ;
#14082=CARTESIAN_POINT ( 'NONE',  ( 2.927603783594689979, 51.37146775011972011, 72.45432679953087529 ) ) ;
#14083=VERTEX_POINT ( 'NONE', #11782 ) ;
#14087=CARTESIAN_POINT ( 'NONE',  ( 5.750640099535992533, 51.24052371918730842, 75.36022115247205022 ) ) ;
#14088=ORIENTED_EDGE ( 'NONE', *, *, #6710, .T. ) ;
#14089=CARTESIAN_POINT ( 'NONE',  ( -4.888424451833091489, 50.19180550725726420, 79.37256909934775706 ) ) ;
#14092=CARTESIAN_POINT ( 'NONE',  ( 4.442698562174268062, 36.14788694334743013, 76.14998054923410109 ) ) ;
#14094=VERTEX_POINT ( 'NONE', #2196 ) ;
#14095=CARTESIAN_POINT ( 'NONE',  ( -4.574316323987747346, 51.33620267474496757, 79.54845644658969661 ) ) ;
#14096=CARTESIAN_POINT ( 'NONE',  ( 0.6316246594797694236, 52.96522029444659552, 78.93480014378108933 ) ) ;
#14097=ORIENTED_EDGE ( 'NONE', *, *, #11826, .T. ) ;
#14102=CARTESIAN_POINT ( 'NONE',  ( 5.096251760688711663, 37.36180756311627960, 76.18683980367092090 ) ) ;
#14103=CARTESIAN_POINT ( 'NONE',  ( 8.798005484913860030, 41.16190507553456968, 76.10950202369875228 ) ) ;
#14104=CARTESIAN_POINT ( 'NONE',  ( -5.462576778579502523, 43.73439565840071452, 80.45433879953087342 ) ) ;
#14106=CARTESIAN_POINT ( 'NONE',  ( -7.153763766568051352, 47.04667285769743046, 77.69611589407060137 ) ) ;
#14108=CARTESIAN_POINT ( 'NONE',  ( 5.787513446439723985, 51.21328686317854562, 75.36061482756318242 ) ) ;
#14109=LINE ( 'NONE', #17721, #16037 ) ;
#14111=CARTESIAN_POINT ( 'NONE',  ( -3.060074010023764668, 51.53860695331515274, 75.91504661370008478 ) ) ;
#14113=ORIENTED_EDGE ( 'NONE', *, *, #8177, .T. ) ;
#14114=CARTESIAN_POINT ( 'NONE',  ( -4.680892486399498509, 37.06504742266799468, 75.36060488990274564 ) ) ;
#14117=CARTESIAN_POINT ( 'NONE',  ( 5.323881593982133786, 50.64173803113061467, 79.54845644658969661 ) ) ;
#14118=CARTESIAN_POINT ( 'NONE',  ( -7.204754451251679015, 41.41175569818021529, 79.53765352848668613 ) ) ;
#14119=CARTESIAN_POINT ( 'NONE',  ( 8.509969478268430976, 40.29864289095467456, 75.64968528315669971 ) ) ;
#14120=ORIENTED_EDGE ( 'NONE', *, *, #19274, .F. ) ;
#14121=CARTESIAN_POINT ( 'NONE',  ( -4.681776609547195100, 37.06570048882255008, 77.92992558049613194 ) ) ;
#14122=CARTESIAN_POINT ( 'NONE',  ( 5.869592478971509486, 51.15265838819242106, 78.02050120841747116 ) ) ;
#14123=CARTESIAN_POINT ( 'NONE',  ( 5.508100443945853186, 47.59510827513957310, 72.45433879953087342 ) ) ;
#14128=DIRECTION ( 'NONE',  ( -0.9485903129789527988, 0.3165065846431829311, -8.934458285744989980E-17 ) ) ;
#14129=CARTESIAN_POINT ( 'NONE',  ( 8.358012262001102144, 41.76329306163730593, 78.86350455626283917 ) ) ;
#14130=EDGE_CURVE ( 'NONE', #3211, #9657, #7073, .T. ) ;
#14132=FACE_OUTER_BOUND ( 'NONE', #1896, .T. ) ;
#14134=CARTESIAN_POINT ( 'NONE',  ( 5.724311780639353309, 51.25997138778688367, 75.97249762499970416 ) ) ;
#14136=CARTESIAN_POINT ( 'NONE',  ( -7.150534706529382056, 46.78250046532827611, 79.21909685159604919 ) ) ;
#14137=CARTESIAN_POINT ( 'NONE',  ( 8.594421463742152767, 42.71629281084112506, 77.95855867472361922 ) ) ;
#14138=CARTESIAN_POINT ( 'NONE',  ( 8.215612168451047026, 41.32480612096441064, 78.66873573524837582 ) ) ;
#14139=CARTESIAN_POINT ( 'NONE',  ( -3.547760446584432348, 36.22804843019941501, 78.70659543854198148 ) ) ;
#14140=CARTESIAN_POINT ( 'NONE',  ( -6.709328582052545009, 40.29621921162755172, 75.45433879953087342 ) ) ;
#14141=CARTESIAN_POINT ( 'NONE',  ( -7.423951210289297720, 47.94363824867885171, 78.32492703482499508 ) ) ;
#14145=CIRCLE ( 'NONE', #14485, 6.200000000000000178 ) ;
#14146=ORIENTED_EDGE ( 'NONE', *, *, #11754, .T. ) ;
#14149=CARTESIAN_POINT ( 'NONE',  ( -4.901409867458520253, 51.10247360423972651, 79.52300236340988704 ) ) ;
#14151=EDGE_CURVE ( 'NONE', #16492, #271, #14910, .T. ) ;
#14153=DIRECTION ( 'NONE',  ( -0.8043570849667734945, 0.5941461771851728191, -1.733862608106382498E-17 ) ) ;
#14158=VECTOR ( 'NONE', #18861, 1000.000000000000000 ) ;
#14159=CARTESIAN_POINT ( 'NONE',  ( -4.451370124631321090, 50.68173085449596726, 76.23059302469468435 ) ) ;
#14161=DIRECTION ( 'NONE',  ( 0.8136266022444381685, 0.5813877811926999595, 2.295812393977108607E-16 ) ) ;
#14164=EDGE_CURVE ( 'NONE', #3603, #5849, #4992, .T. ) ;
#14166=ORIENTED_EDGE ( 'NONE', *, *, #8222, .T. ) ;
#14167=ADVANCED_FACE ( 'NONE', ( #15819 ), #10834, .T. ) ;
#14173=ADVANCED_FACE ( 'NONE', ( #2724 ), #914, .T. ) ;
#14174=EDGE_CURVE ( 'NONE', #12584, #4385, #18681, .T. ) ;
#14177=DIRECTION ( 'NONE',  ( 1.540237394707284220E-16, 1.793354297423764243E-16, -1.000000000000000000 ) ) ;
#14182=CARTESIAN_POINT ( 'NONE',  ( 5.333527369480803415, 51.54862809055342154, 75.39573407869305299 ) ) ;
#14183=EDGE_LOOP ( 'NONE', ( #19833, #11102, #14695, #995 ) ) ;
#14184=CARTESIAN_POINT ( 'NONE',  ( -4.195629287973702048, 50.68685156650132484, 79.54703672271651271 ) ) ;
#14186=ORIENTED_EDGE ( 'NONE', *, *, #947, .T. ) ;
#14188=CARTESIAN_POINT ( 'NONE',  ( 6.716472115211415961, 37.77264227618470471, 78.07897440853361104 ) ) ;
#14189=FACE_OUTER_BOUND ( 'NONE', #7076, .T. ) ;
#14191=FACE_OUTER_BOUND ( 'NONE', #11260, .T. ) ;
#14193=AXIS2_PLACEMENT_3D ( 'NONE', #4845, #14539, #21003 ) ;
#14194=ORIENTED_EDGE ( 'NONE', *, *, #11328, .F. ) ;
#14195=CARTESIAN_POINT ( 'NONE',  ( -5.388909339631083206, 49.84547635099989549, 78.62002338016745284 ) ) ;
#14200=CARTESIAN_POINT ( 'NONE',  ( 5.168178938657410626, 37.41320409107064648, 76.01263398532663018 ) ) ;
#14201=EDGE_CURVE ( 'NONE', #19914, #11768, #13787, .T. ) ;
#14202=CARTESIAN_POINT ( 'NONE',  ( 5.599886173630381769, 51.35187957151522653, 78.68193220087633222 ) ) ;
#14204=CARTESIAN_POINT ( 'NONE',  ( -3.310515886049998358, 36.97763837711306678, 77.59103917682324436 ) ) ;
#14206=CARTESIAN_POINT ( 'NONE',  ( 2.109887651937126574, 52.20155892434686251, 78.45122513788126639 ) ) ;
#14207=CARTESIAN_POINT ( 'NONE',  ( -3.936224163802637399, 36.51499092983547001, 77.70026928173652436 ) ) ;
#14209=CARTESIAN_POINT ( 'NONE',  ( -1.493738069816088920, 38.45421922485636657, 72.45432679953087529 ) ) ;
#14210=CARTESIAN_POINT ( 'NONE',  ( 5.649998448837412646, 37.01057924028687296, 77.75931883872233641 ) ) ;
#14212=CARTESIAN_POINT ( 'NONE',  ( -4.303670962001103106, 50.79176777958974753, 75.36022115247205022 ) ) ;
#14216=CARTESIAN_POINT ( 'NONE',  ( -4.185586155588906010, 37.45382053025712565, 76.09208750614521932 ) ) ;
#14217=CARTESIAN_POINT ( 'NONE',  ( 6.152864644243832615, 50.94341665060460400, 79.51305506302354331 ) ) ;
#14218=VERTEX_POINT ( 'NONE', #14104 ) ;
#14219=CARTESIAN_POINT ( 'NONE',  ( 8.648170029844118645, 43.06315486489794608, 77.06316232894263862 ) ) ;
#14220=CARTESIAN_POINT ( 'NONE',  ( 8.293280423777593668, 41.56926772713645590, 77.52492703482499792 ) ) ;
#14222=VECTOR ( 'NONE', #5891, 1000.000000000000227 ) ;
#14224=CARTESIAN_POINT ( 'NONE',  ( 6.300200331733075032, 49.98117806904839000, 75.66941908770607483 ) ) ;
#14226=CARTESIAN_POINT ( 'NONE',  ( 6.293245987533939712, 38.33655849317105435, 75.75804681942297236 ) ) ;
#14228=CARTESIAN_POINT ( 'NONE',  ( 5.714504673297025938, 37.81512451739774150, 78.37063972127445766 ) ) ;
#14229=LINE ( 'NONE', #10860, #3133 ) ;
#14230=CARTESIAN_POINT ( 'NONE',  ( 5.132218997419849771, 37.56036858369791531, 75.36140480012781495 ) ) ;
#14232=CARTESIAN_POINT ( 'NONE',  ( -0.9223007646069696364, 52.21731522718776830, 78.60293901857092180 ) ) ;
#14235=CARTESIAN_POINT ( 'NONE',  ( 5.561690527597086486, 51.38009315662554854, 76.32883089164610624 ) ) ;
#14238=CARTESIAN_POINT ( 'NONE',  ( -7.600258659080383339, 43.09958255378303704, 78.69093640348562246 ) ) ;
#14241=CARTESIAN_POINT ( 'NONE',  ( 9.353817388681445522, 42.82770861117572281, 78.41904468188381827 ) ) ;
#14242=CARTESIAN_POINT ( 'NONE',  ( -4.074300354217368358, 50.95281676589303999, 76.03497679752658200 ) ) ;
#14243=CARTESIAN_POINT ( 'NONE',  ( -4.865811501566807529, 37.20163965017977858, 78.83844719616611485 ) ) ;
#14246=CARTESIAN_POINT ( 'NONE',  ( 5.267397447889379691, 50.84436012315604358, 78.02054163389647101 ) ) ;
#14247=CARTESIAN_POINT ( 'NONE',  ( 8.643306328402520222, 43.06267994005154520, 77.22643688620827618 ) ) ;
#14250=CARTESIAN_POINT ( 'NONE',  ( 8.788342534296720743, 41.13294459952883386, 78.64407474691132904 ) ) ;
#14251=VECTOR ( 'NONE', #4924, 1000.000000000000227 ) ;
#14252=CARTESIAN_POINT ( 'NONE',  ( -5.323589340698339001, 50.80079960963960417, 79.37256909934775706 ) ) ;
#14254=CARTESIAN_POINT ( 'NONE',  ( -3.135751968098504427, 36.82324114996664122, 77.34971200965068761 ) ) ;
#14258=LINE ( 'NONE', #2787, #15313 ) ;
#14261=CARTESIAN_POINT ( 'NONE',  ( 5.887048643069795695, 51.13976422295020541, 78.81551702238962775 ) ) ;
#14262=DIRECTION ( 'NONE',  ( -1.540237394707284467E-16, -1.793354297423764243E-16, 1.000000000000000000 ) ) ;
#14263=AXIS2_PLACEMENT_3D ( 'NONE', #1223, #7814, #15810 ) ;
#14264=CARTESIAN_POINT ( 'NONE',  ( 8.825683451842801119, 41.24485769827808213, 77.95380709400741637 ) ) ;
#14266=CARTESIAN_POINT ( 'NONE',  ( 0.8282905380627915148, 52.35229902398692303, 76.10706146582900544 ) ) ;
#14267=DIRECTION ( 'NONE',  ( 0.3165065846431827645, 0.9485903129789529098, 0.000000000000000000 ) ) ;
#14268=EDGE_LOOP ( 'NONE', ( #15923, #13195, #7611, #3333 ) ) ;
#14269=CARTESIAN_POINT ( 'NONE',  ( 5.824017363460040286, 37.13492678543709502, 77.62670008255557264 ) ) ;
#14271=VERTEX_POINT ( 'NONE', #1023 ) ;
#14273=VECTOR ( 'NONE', #4148, 1000.000000000000000 ) ;
#14274=AXIS2_PLACEMENT_3D ( 'NONE', #16836, #15240, #12055 ) ;
#14275=CARTESIAN_POINT ( 'NONE',  ( -7.261358630300751571, 46.74278378791238708, 79.27428047227293462 ) ) ;
#14276=CARTESIAN_POINT ( 'NONE',  ( 0.1927955687583305933, 35.96649868655307358, 78.00552566015733191 ) ) ;
#14277=CARTESIAN_POINT ( 'NONE',  ( 5.760549983993971779, 37.08957531975971023, 75.99604373986946371 ) ) ;
#14278=FACE_OUTER_BOUND ( 'NONE', #10174, .T. ) ;
#14280=B_SPLINE_SURFACE_WITH_KNOTS ( 'NONE', 3, 1, ( 
 ( #12644, #14339 ),
 ( #7641, #19220 ),
 ( #11055, #9454 ),
 ( #2536, #7533 ),
 ( #932, #5936 ),
 ( #20396, #19019 ),
 ( #5827, #10749 ),
 ( #12433, #7852 ),
 ( #10953, #1048 ),
 ( #20813, #4325 ),
 ( #17322, #15626 ),
 ( #9031, #7419 ),
 ( #6142, #2949 ),
 ( #20604, #19126 ),
 ( #2745, #9250 ),
 ( #15736, #12331 ),
 ( #18813, #4440 ),
 ( #4223, #17213 ),
 ( #1156, #6032 ) ),
 .UNSPECIFIED., .F., .F., .F.,
 ( 4, 1, 1, 1, 1, 1, 1, 1, 1, 1, 1, 1, 1, 1, 1, 1, 4 ),
 ( 2, 2 ),
 ( 0.000000000000000000, 0.08922172431123952252, 0.1727371540427279917, 0.2514909308953109934, 0.3251734978287333933, 0.3948954482456704107, 0.4603701760623962747, 0.5227882573036246594, 0.5823557395532832359, 0.6395037089141992759, 0.6939186205323212286, 0.7459813003653354979, 0.7965562351082946524, 0.8464932973566897667, 0.8966162271720948818, 0.9474565856282386456, 1.000000000000000000 ),
 ( 0.000000000000000000, 1.000000000000000000 ),
 .UNSPECIFIED. ) ;
#14282=ORIENTED_EDGE ( 'NONE', *, *, #19324, .T. ) ;
#14283=CARTESIAN_POINT ( 'NONE',  ( 4.661266133293011649, 52.04520038539091331, 77.98100106196224601 ) ) ;
#14286=ADVANCED_FACE ( 'NONE', ( #17298 ), #15344, .F. ) ;
#14287=ORIENTED_EDGE ( 'NONE', *, *, #15241, .T. ) ;
#14288=CARTESIAN_POINT ( 'NONE',  ( -3.349945445540459588, 52.21109327740445138, 76.66413924479479647 ) ) ;
#14290=CARTESIAN_POINT ( 'NONE',  ( -7.084928339392615015, 41.46291127039725666, 78.49688471925094291 ) ) ;
#14291=VERTEX_POINT ( 'NONE', #19514 ) ;
#14292=FACE_OUTER_BOUND ( 'NONE', #1321, .T. ) ;
#14295=CARTESIAN_POINT ( 'NONE',  ( 4.400857426521584514, 36.11798879971178167, 76.47837415541054895 ) ) ;
#14298=ADVANCED_FACE ( 'NONE', ( #17604 ), #13111, .T. ) ;
#14302=ORIENTED_EDGE ( 'NONE', *, *, #206, .F. ) ;
#14303=CARTESIAN_POINT ( 'NONE',  ( 9.271561067608034890, 45.68041113525027441, 79.47125056423675460 ) ) ;
#14304=CARTESIAN_POINT ( 'NONE',  ( -6.782631326057145138, 43.38225751353197523, 75.45433879953087342 ) ) ;
#14305=CARTESIAN_POINT ( 'NONE',  ( 0.8043224091395101416, 52.95766084152177910, 78.82132898185037106 ) ) ;
#14308=CARTESIAN_POINT ( 'NONE',  ( -3.755902984582861759, 36.38179493852598512, 77.82155188814751057 ) ) ;
#14309=VECTOR ( 'NONE', #11402, 1000.000000000000114 ) ;
#14311=CARTESIAN_POINT ( 'NONE',  ( 5.396193866099816105, 50.74770293185853376, 75.97260389846793771 ) ) ;
#14312=ORIENTED_EDGE ( 'NONE', *, *, #1298, .F. ) ;
#14313=CARTESIAN_POINT ( 'NONE',  ( 2.120837336286425678, 52.95414753789260942, 78.20017459567505114 ) ) ;
#14314=LINE ( 'NONE', #20683, #15781 ) ;
#14317=EDGE_CURVE ( 'NONE', #15999, #20602, #11132, .T. ) ;
#14318=CARTESIAN_POINT ( 'NONE',  ( 5.683893922249901642, 37.03479970459495263, 77.75763958275959453 ) ) ;
#14319=CARTESIAN_POINT ( 'NONE',  ( 8.913594855155908547, 41.50833375100289402, 79.54698768757486960 ) ) ;
#14320=CARTESIAN_POINT ( 'NONE',  ( 1.964251312053308718, 36.08998497932209659, 72.45433879953085921 ) ) ;
#14321=ORIENTED_EDGE ( 'NONE', *, *, #13920, .F. ) ;
#14322=CARTESIAN_POINT ( 'NONE',  ( 5.675263920727823042, 51.29620106613522523, 77.96371040190514634 ) ) ;
#14323=ORIENTED_EDGE ( 'NONE', *, *, #1038, .F. ) ;
#14325=CARTESIAN_POINT ( 'NONE',  ( -4.233737104609306634, 36.73475175465707565, 75.41196988111011024 ) ) ;
#14326=CARTESIAN_POINT ( 'NONE',  ( -4.557243880370990041, 36.97371317826440418, 76.05537227506185616 ) ) ;
#14328=CARTESIAN_POINT ( 'NONE',  ( -5.360233167866653048, 49.87514610275245275, 76.07559164877143587 ) ) ;
#14330=ORIENTED_EDGE ( 'NONE', *, *, #2970, .F. ) ;
#14331=CARTESIAN_POINT ( 'NONE',  ( -4.147362675617721095, 37.44571156211047480, 76.85096240152589075 ) ) ;
#14335=EDGE_CURVE ( 'NONE', #8009, #10690, #6277, .T. ) ;
#14338=LINE ( 'NONE', #9874, #19577 ) ;
#14339=CARTESIAN_POINT ( 'NONE',  ( -7.891196933625220566, 41.56260028800092954, 79.54845644658969661 ) ) ;
#14340=DIRECTION ( 'NONE',  ( -0.3165065846431829311, -0.9485903129789527988, -2.188653791613874255E-16 ) ) ;
#14342=B_SPLINE_CURVE_WITH_KNOTS ( 'NONE', 3,
 ( #19494, #20869, #1634, #19283, #4697, #11429, #16108, #20968, #19391, #17902, #3324, #11223, #1747, #8014 ),
 .UNSPECIFIED., .F., .F.,
 ( 4, 2, 2, 2, 2, 2, 4 ),
 ( 0.000000000000000000, 0.0004305053772964893247, 0.0006457580659447340141, 0.0008610107545929786494, 0.001076263443241223718, 0.001291516131889468896, 0.001722021509185946240 ),
 .UNSPECIFIED. ) ;
#14343=CARTESIAN_POINT ( 'NONE',  ( -5.050952507338172914, 50.99561590888721696, 75.40305853716382956 ) ) ;
#14346=CARTESIAN_POINT ( 'NONE',  ( -4.303670962001103106, 50.79176777958974753, 75.36022115247205022 ) ) ;
#14347=VECTOR ( 'NONE', #3640, 1000.000000000000000 ) ;
#14348=CARTESIAN_POINT ( 'NONE',  ( -0.6541186644085422719, 52.97764124372373118, 79.16576412035692556 ) ) ;
#14350=CARTESIAN_POINT ( 'NONE',  ( 0.5221537403065008576, 44.16218137147968292, 80.45433879953087342 ) ) ;
#14356=CIRCLE ( 'NONE', #19436, 6.200000000000000178 ) ;
#14357=CARTESIAN_POINT ( 'NONE',  ( 9.350990972312333227, 42.81923766201297354, 78.59572304307680213 ) ) ;
#14358=CARTESIAN_POINT ( 'NONE',  ( -4.056193511719762945, 50.96503781144581069, 76.08556810432578743 ) ) ;
#14359=CARTESIAN_POINT ( 'NONE',  ( 6.924055141134583202, 50.37376929599953712, 78.48669174070734300 ) ) ;
#14360=VECTOR ( 'NONE', #19864, 1000.000000000000227 ) ;
#14361=LINE ( 'NONE', #2876, #17784 ) ;
#14363=CARTESIAN_POINT ( 'NONE',  ( 8.214799251806553571, 41.32260305165857517, 77.80727997600146750 ) ) ;
#14365=CARTESIAN_POINT ( 'NONE',  ( -4.504974378170068405, 37.87111029862571598, 79.54733240137164785 ) ) ;
#14367=EDGE_CURVE ( 'NONE', #9681, #3298, #96, .T. ) ;
#14370=VERTEX_POINT ( 'NONE', #13082 ) ;
#14371=DIRECTION ( 'NONE',  ( 0.3165065846431827645, 0.9485903129789529098, 0.000000000000000000 ) ) ;
#14373=VERTEX_POINT ( 'NONE', #4974 ) ;
#14374=CARTESIAN_POINT ( 'NONE',  ( -0.9236265496033003730, 52.97854115207936587, 76.40919915166844589 ) ) ;
#14375=CARTESIAN_POINT ( 'NONE',  ( 8.398749874130045256, 41.92016587269467465, 78.13399373581940210 ) ) ;
#14379=VERTEX_POINT ( 'NONE', #9903 ) ;
#14382=ORIENTED_EDGE ( 'NONE', *, *, #20294, .F. ) ;
#14383=CARTESIAN_POINT ( 'NONE',  ( 6.575359255040893913, 44.22010074469034180, 75.45433879953087342 ) ) ;
#14386=CARTESIAN_POINT ( 'NONE',  ( 0.5446115036918264263, 52.36219191590829070, 75.97284715574890868 ) ) ;
#14389=B_SPLINE_CURVE_WITH_KNOTS ( 'NONE', 3,
 ( #7428, #13923, #2755, #5943 ),
 .UNSPECIFIED., .F., .F.,
 ( 4, 4 ),
 ( 0.000000000000000000, 0.002523081261280060890 ),
 .UNSPECIFIED. ) ;
#14391=LINE ( 'NONE', #9310, #6759 ) ;
#14393=ORIENTED_EDGE ( 'NONE', *, *, #10455, .F. ) ;
#14394=AXIS2_PLACEMENT_3D ( 'NONE', #7092, #13594, #7205 ) ;
#14395=CARTESIAN_POINT ( 'NONE',  ( -3.364214957493191438, 51.28112122432482778, 75.54713691134779197 ) ) ;
#14398=CARTESIAN_POINT ( 'NONE',  ( 4.539819439306699955, 52.13490816606735478, 76.55090572632929025 ) ) ;
#14400=DIRECTION ( 'NONE',  ( 0.8043570849667693867, -0.5941461771851783702, 1.733862608106223493E-17 ) ) ;
#14401=CARTESIAN_POINT ( 'NONE',  ( 3.983393151002395438, 36.72848634532710577, 72.45433879953087342 ) ) ;
#14402=CARTESIAN_POINT ( 'NONE',  ( 6.212565296439490403, 37.41256891269643603, 78.35997004935869370 ) ) ;
#14403=CARTESIAN_POINT ( 'NONE',  ( 5.740585635973908474, 51.24795054640212300, 75.97198585835440099 ) ) ;
#14406=CARTESIAN_POINT ( 'NONE',  ( -7.290527651941959952, 40.11224193202943411, 78.50801527011910252 ) ) ;
#14407=CARTESIAN_POINT ( 'NONE',  ( 0.9390242073577395043, 52.35189112169444314, 76.77576052100340576 ) ) ;
#14410=DIRECTION ( 'NONE',  ( -1.540237394707283727E-16, -1.793354297423763257E-16, 1.000000000000000000 ) ) ;
#14411=CARTESIAN_POINT ( 'NONE',  ( -5.838255805151811195, 50.43303779728307745, 76.65235776097600251 ) ) ;
#14415=CARTESIAN_POINT ( 'NONE',  ( 5.379940827581938478, 50.75970839669935941, 75.97198585835440099 ) ) ;
#14418=CARTESIAN_POINT ( 'NONE',  ( 9.176231272041631470, 45.98187388689780164, 75.44992703482499508 ) ) ;
#14421=EDGE_CURVE ( 'NONE', #3162, #8610, #19130, .T. ) ;
#14422=CARTESIAN_POINT ( 'NONE',  ( -0.9276151719557895747, 52.23300467605542252, 76.37477783580860091 ) ) ;
#14423=CARTESIAN_POINT ( 'NONE',  ( 9.353718648869055130, 42.82741268169404947, 78.44945682776121032 ) ) ;
#14424=CARTESIAN_POINT ( 'NONE',  ( 8.638826686988997139, 40.68483612003910110, 79.45050910333212357 ) ) ;
#14427=ORIENTED_EDGE ( 'NONE', *, *, #11991, .T. ) ;
#14428=CARTESIAN_POINT ( 'NONE',  ( -4.074436747594614161, 36.61708299794012333, 75.46341390175899733 ) ) ;
#14429=CARTESIAN_POINT ( 'NONE',  ( -4.532046673723622021, 36.95510101671938941, 76.17409373158149322 ) ) ;
#14431=ORIENTED_EDGE ( 'NONE', *, *, #12758, .T. ) ;
#14432=FACE_OUTER_BOUND ( 'NONE', #3957, .T. ) ;
#14433=CARTESIAN_POINT ( 'NONE',  ( -7.261744020088604756, 41.57725440279298823, 79.54647244615752300 ) ) ;
#14436=CARTESIAN_POINT ( 'NONE',  ( 2.527576913102087985, 36.82540565608436367, 75.45433879953087342 ) ) ;
#14437=CARTESIAN_POINT ( 'NONE',  ( -6.374721436948748376, 46.24015083227975964, 79.45433879953087342 ) ) ;
#14442=EDGE_CURVE ( 'NONE', #19814, #13351, #11817, .T. ) ;
#14443=CARTESIAN_POINT ( 'NONE',  ( -5.825614074793430852, 50.44207111495388318, 76.36675183022860836 ) ) ;
#14445=CARTESIAN_POINT ( 'NONE',  ( 8.833159395675938441, 41.26726357621102181, 77.50846324053436831 ) ) ;
#14448=EDGE_CURVE ( 'NONE', #3841, #4878, #3610, .T. ) ;
#14449=CARTESIAN_POINT ( 'NONE',  ( -0.9426531034333153203, 52.21747571285902012, 78.07640427701528552 ) ) ;
#14450=ORIENTED_EDGE ( 'NONE', *, *, #18602, .T. ) ;
#14451=LINE ( 'NONE', #20917, #20413 ) ;
#14452=CARTESIAN_POINT ( 'NONE',  ( 8.640860003252242905, 43.05534814838419777, 76.37534566197098229 ) ) ;
#14453=CARTESIAN_POINT ( 'NONE',  ( 0.7863323750428190539, 52.35808013066139210, 76.03473341409473107 ) ) ;
#14458=ORIENTED_EDGE ( 'NONE', *, *, #15377, .T. ) ;
#14459=CARTESIAN_POINT ( 'NONE',  ( 9.353817388681445522, 42.82770861117572281, 76.74257409364852833 ) ) ;
#14460=CARTESIAN_POINT ( 'NONE',  ( 8.300594306733913186, 41.56682737740558764, 77.52492703482499792 ) ) ;
#14461=CARTESIAN_POINT ( 'NONE',  ( 5.127341568105101999, 37.37742690587217709, 77.69977153848151374 ) ) ;
#14462=CARTESIAN_POINT ( 'NONE',  ( 4.831344325983889298, 51.13914440238564652, 79.48349463613192256 ) ) ;
#14465=CARTESIAN_POINT ( 'NONE',  ( 6.462739881952892063, 49.81458902753052342, 78.15691020095597707 ) ) ;
#14467=CARTESIAN_POINT ( 'NONE',  ( 9.315603341877332966, 42.71317868864986877, 77.73063109826868811 ) ) ;
#14469=CARTESIAN_POINT ( 'NONE',  ( 5.309312511458522899, 50.81985754494123597, 75.97849039075508415 ) ) ;
#14471=CARTESIAN_POINT ( 'NONE',  ( 8.790412360755954779, 41.13914800073450095, 78.76104738055306598 ) ) ;
#14472=CARTESIAN_POINT ( 'NONE',  ( 0.8261150126163424590, 52.35656485298985530, 78.75698059774664728 ) ) ;
#14473=CARTESIAN_POINT ( 'NONE',  ( 0.5855440626654981884, 51.36190535648659505, 75.36022115247205022 ) ) ;
#14475=CARTESIAN_POINT ( 'NONE',  ( -6.427915807670530945, 42.26053564693651055, 78.50654468188380974 ) ) ;
#14476=CARTESIAN_POINT ( 'NONE',  ( 9.080605399405701661, 42.00887494707089331, 78.12791555553386047 ) ) ;
#14478=CARTESIAN_POINT ( 'NONE',  ( 6.880792506138228681, 37.89005961138749967, 76.49840989696882332 ) ) ;
#14480=DIRECTION ( 'NONE',  ( -1.540237394707284220E-16, -1.793354297423764243E-16, 1.000000000000000000 ) ) ;
#14481=DIRECTION ( 'NONE',  ( -0.5813877811926999595, 0.8136266022444381685, -1.516940570386243703E-15 ) ) ;
#14482=LINE ( 'NONE', #20748, #17412 ) ;
#14485=AXIS2_PLACEMENT_3D ( 'NONE', #10895, #12474, #7683 ) ;
#14486=ORIENTED_EDGE ( 'NONE', *, *, #17656, .F. ) ;
#14489=LINE ( 'NONE', #6496, #14574 ) ;
#14490=CARTESIAN_POINT ( 'NONE',  ( 5.848951923618479931, 37.15274410921379911, 76.58742703482498371 ) ) ;
#14491=CARTESIAN_POINT ( 'NONE',  ( -5.933958468462559921, 37.99063678704128932, 76.24300064276494027 ) ) ;
#14494=ORIENTED_EDGE ( 'NONE', *, *, #17955, .T. ) ;
#14495=AXIS2_PLACEMENT_3D ( 'NONE', #15541, #20308, #636 ) ;
#14496=DIRECTION ( 'NONE',  ( 0.5813877811927011807, -0.8136266022444372803, -5.636455622144619183E-17 ) ) ;
#14498=CARTESIAN_POINT ( 'NONE',  ( 5.389492195292208798, 36.82443100924615464, 78.79551527011911105 ) ) ;
#14500=EDGE_CURVE ( 'NONE', #445, #19138, #5303, .T. ) ;
#14503=CARTESIAN_POINT ( 'NONE',  ( 5.933960187751527116, 51.10511255460609448, 76.21496574784163158 ) ) ;
#14505=CARTESIAN_POINT ( 'NONE',  ( 0.5221537403065015237, 44.16218137147968292, 75.45433879953088763 ) ) ;
#14506=VERTEX_POINT ( 'NONE', #14887 ) ;
#14512=CARTESIAN_POINT ( 'NONE',  ( 2.538045550429134600, 49.87014351810298507, 72.45433879953087342 ) ) ;
#14513=B_SPLINE_CURVE_WITH_KNOTS ( 'NONE', 3,
 ( #1104, #7791, #15575, #14275, #2800, #20754, #990, #20456, #4275, #19269, #9506, #10800 ),
 .UNSPECIFIED., .F., .F.,
 ( 4, 2, 2, 2, 2, 4 ),
 ( 0.000000000000000000, 0.0001995372338163474250, 0.0003990744676326948501, 0.0007981489352653508857, 0.001197223402898007138, 0.001596297870530663174 ),
 .UNSPECIFIED. ) ;
#14519=DIRECTION ( 'NONE',  ( -1.540237394707284220E-16, -1.793354297423764243E-16, 1.000000000000000000 ) ) ;
#14520=CARTESIAN_POINT ( 'NONE',  ( -3.053082554203018439, 36.78748274492485137, 76.62933879953087057 ) ) ;
#14521=ORIENTED_EDGE ( 'NONE', *, *, #8084, .F. ) ;
#14522=CARTESIAN_POINT ( 'NONE',  ( -1.202011496911928434, 49.96493122755408223, 75.45433879953087342 ) ) ;
#14523=CARTESIAN_POINT ( 'NONE',  ( -3.518392077816012709, 37.12037020444837765, 77.68963291717793140 ) ) ;
#14524=CONICAL_SURFACE ( 'NONE', #8424, 6.200000000000020606, 1.047197551196600518 ) ;
#14525=ORIENTED_EDGE ( 'NONE', *, *, #6361, .T. ) ;
#14526=DIRECTION ( 'NONE',  ( -0.3165065846431827645, -0.9485903129789529098, 0.000000000000000000 ) ) ;
#14527=ADVANCED_FACE ( 'NONE', ( #15217 ), #425, .T. ) ;
#14529=DIRECTION ( 'NONE',  ( 0.07958035169224103589, -0.2516580640468327190, -0.9645388465089104191 ) ) ;
#14531=CARTESIAN_POINT ( 'NONE',  ( 5.599756831756513620, 51.35197511114724733, 78.21422674182478829 ) ) ;
#14536=CARTESIAN_POINT ( 'NONE',  ( -4.177068838871750955, 37.44752913149660856, 76.12832907849806929 ) ) ;
#14539=DIRECTION ( 'NONE',  ( 1.540237394707284220E-16, 1.793354297423764243E-16, -1.000000000000000000 ) ) ;
#14540=CARTESIAN_POINT ( 'NONE',  ( -6.830989029115968947, 40.53234436544566677, 79.14164642658485604 ) ) ;
#14542=ORIENTED_EDGE ( 'NONE', *, *, #19825, .T. ) ;
#14543=CARTESIAN_POINT ( 'NONE',  ( -4.788785806866687089, 51.18295063450860738, 76.15325518536063498 ) ) ;
#14545=DIRECTION ( 'NONE',  ( -0.9485903129789527988, 0.3165065846431829311, -8.934458285744989980E-17 ) ) ;
#14550=CARTESIAN_POINT ( 'NONE',  ( 6.100231826182790584, 38.15139326043413348, 78.27625046823177968 ) ) ;
#14552=CARTESIAN_POINT ( 'NONE',  ( 8.791848479292760032, 41.14345213909496835, 77.32915800260404637 ) ) ;
#14553=CARTESIAN_POINT ( 'NONE',  ( 5.427780505986065762, 36.85179043424346190, 77.43080938776617472 ) ) ;
#14554=CARTESIAN_POINT ( 'NONE',  ( -0.9162890130466297967, 52.97970855327192652, 78.60293901857092180 ) ) ;
#14555=ORIENTED_EDGE ( 'NONE', *, *, #6448, .T. ) ;
#14556=DIRECTION ( 'NONE',  ( -0.3165065846431775465, -0.9485903129789546862, 0.000000000000000000 ) ) ;
#14557=CARTESIAN_POINT ( 'NONE',  ( 8.607671302521914924, 42.95587950684349465, 75.91044101036179370 ) ) ;
#14558=ADVANCED_FACE ( 'NONE', ( #11928 ), #19883, .T. ) ;
#14559=CARTESIAN_POINT ( 'NONE',  ( 8.400787919062072007, 39.97141883166423781, 78.77723610448765612 ) ) ;
#14560=ADVANCED_FACE ( 'NONE', ( #522 ), #6819, .F. ) ;
#14563=VERTEX_POINT ( 'NONE', #10666 ) ;
#14564=ORIENTED_EDGE ( 'NONE', *, *, #3974, .F. ) ;
#14565=CARTESIAN_POINT ( 'NONE',  ( 9.240682951717872129, 42.48863752648103542, 75.64289537645213102 ) ) ;
#14566=ADVANCED_FACE ( 'NONE', ( #846 ), #10069, .F. ) ;
#14567=CARTESIAN_POINT ( 'NONE',  ( -4.895465483855352851, 37.22354385236106111, 78.55727908454632313 ) ) ;
#14568=CARTESIAN_POINT ( 'NONE',  ( 4.143017335158133641, 51.51944627275094746, 78.46169174070733732 ) ) ;
#14570=CARTESIAN_POINT ( 'NONE',  ( -1.117719678584870424, 36.12782917792895176, 72.45433879953085921 ) ) ;
#14571=DIRECTION ( 'NONE',  ( -1.540237394707284220E-16, -1.793354297423764243E-16, 1.000000000000000000 ) ) ;
#14572=CARTESIAN_POINT ( 'NONE',  ( 6.949446517235058352, 50.35501370930113296, 76.97234655072247733 ) ) ;
#14574=VECTOR ( 'NONE', #21, 1000.000000000000000 ) ;
#14575=ORIENTED_EDGE ( 'NONE', *, *, #19794, .T. ) ;
#14576=CARTESIAN_POINT ( 'NONE',  ( 8.797946357469051293, 41.16172786683149099, 78.83414475571305502 ) ) ;
#14578=DIRECTION ( 'NONE',  ( 0.007885122365275663500, 0.9999689119394085113, 1.805443505845543142E-16 ) ) ;
#14581=CARTESIAN_POINT ( 'NONE',  ( 9.277577006266444215, 42.59921134847828483, 77.86785210695053649 ) ) ;
#14583=VECTOR ( 'NONE', #20688, 1000.000000000000114 ) ;
#14584=CARTESIAN_POINT ( 'NONE',  ( 0.1922742723289393996, 52.96974186399811657, 75.38460717221940399 ) ) ;
#14585=CARTESIAN_POINT ( 'NONE',  ( 4.676321589340446394, 52.03407952647943091, 79.02133806855546538 ) ) ;
#14586=CARTESIAN_POINT ( 'NONE',  ( 5.076572431691917409, 37.34329067111212197, 77.43080938776617472 ) ) ;
#14587=CARTESIAN_POINT ( 'NONE',  ( 4.611431799778751284, 51.27033221398914975, 75.50754157125952304 ) ) ;
#14588=ADVANCED_FACE ( 'NONE', ( #19419 ), #14634, .F. ) ;
#14590=EDGE_LOOP ( 'NONE', ( #19445, #17309, #3590, #11647 ) ) ;
#14591=CARTESIAN_POINT ( 'NONE',  ( -4.578222290571132724, 51.33341161403104280, 78.93596775356181183 ) ) ;
#14592=EDGE_CURVE ( 'NONE', #9005, #2886, #1663, .T. ) ;
#14593=ORIENTED_EDGE ( 'NONE', *, *, #6995, .F. ) ;
#14596=CARTESIAN_POINT ( 'NONE',  ( 1.173218185867612506, 52.94769249949187895, 76.77301385304936332 ) ) ;
#14601=CARTESIAN_POINT ( 'NONE',  ( 5.241302188025125375, 50.86813933424380707, 77.20515338154341123 ) ) ;
#14608=CARTESIAN_POINT ( 'NONE',  ( -5.397178805542148794, 49.82826827278250903, 78.41225960292398156 ) ) ;
#14610=CARTESIAN_POINT ( 'NONE',  ( 5.787239255393352266, 51.21348939705941206, 75.97375991483075097 ) ) ;
#14611=CARTESIAN_POINT ( 'NONE',  ( 0.5221537403065014127, 44.16218137147968292, 76.48963291717792856 ) ) ;
#14612=DIRECTION ( 'NONE',  ( 0.007885122365275663500, 0.9999689119394085113, 1.805443505845543142E-16 ) ) ;
#14615=DIRECTION ( 'NONE',  ( 0.9480563259966798828, 0.3181025035074024343, 2.030702297275143506E-16 ) ) ;
#14616=VECTOR ( 'NONE', #5672, 1000.000000000000114 ) ;
#14617=CARTESIAN_POINT ( 'NONE',  ( 0.5264284712812515865, 52.36237607488513390, 76.89393222956012153 ) ) ;
#14619=FACE_BOUND ( 'NONE', #6769, .T. ) ;
#14621=CARTESIAN_POINT ( 'NONE',  ( -4.264291154750528889, 50.63795972765758791, 75.36124333316173818 ) ) ;
#14623=AXIS2_PLACEMENT_3D ( 'NONE', #8408, #14683, #16286 ) ;
#14625=CARTESIAN_POINT ( 'NONE',  ( 7.864691922653266332, 47.81281597943210215, 78.56977997600147035 ) ) ;
#14629=B_SPLINE_CURVE_WITH_KNOTS ( 'NONE', 3,
 ( #10022, #1725, #11513, #7995, #20947, #114, #5104, #10126, #19679, #17986, #16502, #16606, #1919, #11409, #6593, #13100, #11822, #18297 ),
 .UNSPECIFIED., .F., .F.,
 ( 4, 2, 2, 2, 2, 2, 2, 2, 4 ),
 ( 0.000000000000000000, 0.0007228893211762224416, 0.0009036116514702782418, 0.001084333981764333934, 0.001445778642352450738, 0.001807223302940567326, 0.002168667963528683913, 0.002530112624116800935, 0.002891557284704917522 ),
 .UNSPECIFIED. ) ;
#14633=CARTESIAN_POINT ( 'NONE',  ( 9.294532183588495755, 42.65002709052886587, 79.09515810002898206 ) ) ;
#14634=B_SPLINE_SURFACE_WITH_KNOTS ( 'NONE', 3, 1, ( 
 ( #4839, #13362 ),
 ( #8362, #11461 ),
 ( #19732, #6752 ),
 ( #5149, #18244 ),
 ( #11769, #5253 ),
 ( #16659, #3665 ),
 ( #14843, #19624 ),
 ( #18040, #6544 ),
 ( #3461, #5358 ),
 ( #16240, #475 ),
 ( #1874, #1776 ),
 ( #8257, #14743 ),
 ( #11670, #17930 ),
 ( #13258, #11565 ),
 ( #10176, #9973 ),
 ( #4939, #17826 ),
 ( #9755, #3353 ),
 ( #18147, #13459 ),
 ( #2080, #63 ),
 ( #164, #1973 ),
 ( #16454, #3566 ),
 ( #8575, #5045 ),
 ( #6647, #9863 ),
 ( #15062, #16346 ),
 ( #6953, #19931 ),
 ( #3256, #10072 ),
 ( #19832, #263 ) ),
 .UNSPECIFIED., .F., .F., .F.,
 ( 4, 1, 1, 1, 1, 1, 1, 1, 1, 1, 1, 1, 1, 1, 1, 1, 1, 1, 1, 1, 1, 1, 1, 1, 4 ),
 ( 2, 2 ),
 ( 0.000000000000000000, 0.06156270711109813193, 0.1195928175617291256, 0.1747495234496604655, 0.2265549029623682431, 0.2754357869405233972, 0.3212504303641821046, 0.3646692690278454108, 0.4055209537250142326, 0.4439801712034092684, 0.4803226396643038298, 0.5144678959723257838, 0.5464657104125147935, 0.5769957197620103617, 0.6058640933454703115, 0.6335754242279014736, 0.6604510950290067850, 0.6887476664015759198, 0.7209157586619387992, 0.7570169132788651112, 0.7970502319830404803, 0.8414026928090143631, 0.8898175437432860324, 0.9426652073923825759, 1.000000000000000000 ),
 ( 0.000000000000000000, 1.000000000000000000 ),
 .UNSPECIFIED. ) ;
#14635=ORIENTED_EDGE ( 'NONE', *, *, #19129, .T. ) ;
#14637=DIRECTION ( 'NONE',  ( -1.540237394707284220E-16, -1.793354297423764243E-16, 1.000000000000000000 ) ) ;
#14638=ORIENTED_EDGE ( 'NONE', *, *, #12362, .F. ) ;
#14639=CARTESIAN_POINT ( 'NONE',  ( 5.713366999337934793, 51.26805585685155364, 78.93442753446957738 ) ) ;
#14640=CARTESIAN_POINT ( 'NONE',  ( 0.3326973149608342673, 52.96014171822455552, 72.45433879953087342 ) ) ;
#14642=ORIENTED_EDGE ( 'NONE', *, *, #10781, .F. ) ;
#14644=CARTESIAN_POINT ( 'NONE',  ( -4.167066744307394544, 37.46026616392322950, 78.11020518223413944 ) ) ;
#14645=ORIENTED_EDGE ( 'NONE', *, *, #12237, .F. ) ;
#14647=CARTESIAN_POINT ( 'NONE',  ( 5.396517835962451493, 50.75616155517602834, 78.93669174070734584 ) ) ;
#14648=CYLINDRICAL_SURFACE ( 'NONE', #7131, 8.199999999999995737 ) ;
#14649=CARTESIAN_POINT ( 'NONE',  ( 6.339010289386230568, 49.88108541395529016, 75.76076839092205262 ) ) ;
#14650=CARTESIAN_POINT ( 'NONE',  ( 0.8503282811412333775, 52.95606000782370870, 77.76169174070734869 ) ) ;
#14651=DIRECTION ( 'NONE',  ( -0.9485903129789527988, 0.3165065846431829311, -8.934458285744989980E-17 ) ) ;
#14653=CARTESIAN_POINT ( 'NONE',  ( 7.894261924073310510, 40.81774634178594141, 79.41216397796385706 ) ) ;
#14654=VERTEX_POINT ( 'NONE', #369 ) ;
#14656=CARTESIAN_POINT ( 'NONE',  ( -5.505078341044295165, 38.60214220976732236, 76.32343661933127521 ) ) ;
#14657=CARTESIAN_POINT ( 'NONE',  ( 9.317552545512265638, 42.71902057559893962, 75.91044101036179370 ) ) ;
#14658=CARTESIAN_POINT ( 'NONE',  ( 0.5915713968613122153, 52.96553219837200999, 77.38375056423674891 ) ) ;
#14659=DIRECTION ( 'NONE',  ( 0.5941461771851693774, 0.8043570849667760481, 2.357623395011396791E-16 ) ) ;
#14663=CARTESIAN_POINT ( 'NONE',  ( 5.826095025493096990, 51.18478820489261949, 78.92065061514911406 ) ) ;
#14666=DIRECTION ( 'NONE',  ( -0.5670994908670485835, 0.8236492988270761595, 6.036271672687166828E-17 ) ) ;
#14667=CARTESIAN_POINT ( 'NONE',  ( -4.721994780338719444, 37.09540803149950250, 78.93613021445058564 ) ) ;
#14669=CARTESIAN_POINT ( 'NONE',  ( -7.077609990433001208, 44.22210830145579763, 72.45433879953085921 ) ) ;
#14673=B_SPLINE_CURVE_WITH_KNOTS ( 'NONE', 3,
 ( #14074, #20555, #12480, #15791, #1493, #8878, #17061, #7980, #14465, #2488, #12066, #18547 ),
 .UNSPECIFIED., .F., .F.,
 ( 4, 2, 2, 2, 2, 4 ),
 ( 0.000000000000000000, 0.0001234850242348347618, 0.0002469700484696695235, 0.0004939400969393640921, 0.0007409101454090586064, 0.0009878801938787531208 ),
 .UNSPECIFIED. ) ;
#14674=CARTESIAN_POINT ( 'NONE',  ( 6.912263059922415742, 50.38247963137696672, 77.24227907682649175 ) ) ;
#14679=CARTESIAN_POINT ( 'NONE',  ( -5.300296504961807820, 38.45858271615729507, 79.28390783734228364 ) ) ;
#14680=CARTESIAN_POINT ( 'NONE',  ( -5.761564881245698544, 50.48783832367244884, 78.87652712212219797 ) ) ;
#14681=CARTESIAN_POINT ( 'NONE',  ( -4.865811501566803088, 37.20163965017978569, 78.83844719616611485 ) ) ;
#14683=DIRECTION ( 'NONE',  ( -0.9999689119394086223, 0.007885122365275665235, -1.526048693634353392E-16 ) ) ;
#14685=CARTESIAN_POINT ( 'NONE',  ( 8.456021123984127641, 40.13695625074483786, 75.80967849220077426 ) ) ;
#14686=VERTEX_POINT ( 'NONE', #15271 ) ;
#14687=ORIENTED_EDGE ( 'NONE', *, *, #6198, .T. ) ;
#14688=CARTESIAN_POINT ( 'NONE',  ( -0.3971402239501222176, 52.97438961391468126, 75.56421855115301867 ) ) ;
#14689=CARTESIAN_POINT ( 'NONE',  ( 0.5221537403065014127, 44.16218137147968292, 76.16022115247204738 ) ) ;
#14690=DIRECTION ( 'NONE',  ( -0.3165065846431824870, -0.9485903129789529098, 0.000000000000000000 ) ) ;
#14693=ORIENTED_EDGE ( 'NONE', *, *, #15324, .F. ) ;
#14695=ORIENTED_EDGE ( 'NONE', *, *, #13030, .F. ) ;
#14699=CARTESIAN_POINT ( 'NONE',  ( 1.332854164384612128, 52.20776918474795281, 76.79234737414994072 ) ) ;
#14703=ADVANCED_FACE ( 'NONE', ( #7501, #5795, #11983, #15590, #13989, #10721 ), #20039, .T. ) ;
#14704=CARTESIAN_POINT ( 'NONE',  ( 8.378637954445377289, 41.81363803720061867, 76.38301527011910252 ) ) ;
#14705=CARTESIAN_POINT ( 'NONE',  ( 5.920503277122149299, 37.20387208676527280, 78.36928251986560667 ) ) ;
#14707=ADVANCED_FACE ( 'NONE', ( #3976 ), #18458, .T. ) ;
#14708=EDGE_CURVE ( 'NONE', #18879, #16685, #15487, .T. ) ;
#14711=CARTESIAN_POINT ( 'NONE',  ( -3.532917577324399261, 36.21708460058427193, 78.46683879953087626 ) ) ;
#14712=EDGE_CURVE ( 'NONE', #2251, #12039, #2604, .T. ) ;
#14713=ORIENTED_EDGE ( 'NONE', *, *, #15507, .F. ) ;
#14714=CARTESIAN_POINT ( 'NONE',  ( 8.221644392715633742, 41.34114708762416512, 77.83751483520470060 ) ) ;
#14715=CARTESIAN_POINT ( 'NONE',  ( 8.887668352622405621, 41.43063037816333605, 75.36022115247205022 ) ) ;
#14718=CARTESIAN_POINT ( 'NONE',  ( -4.383592986664169189, 51.47248658876933547, 78.47566305278908771 ) ) ;
#14719=CARTESIAN_POINT ( 'NONE',  ( 5.428747419638988880, 36.85248135533887393, 77.49967648550449439 ) ) ;
#14721=CARTESIAN_POINT ( 'NONE',  ( -4.051350930180527499, 50.96297916595425193, 76.10127045261064893 ) ) ;
#14724=CARTESIAN_POINT ( 'NONE',  ( 4.224453164177068842, 51.45384152454902704, 77.98100106196224601 ) ) ;
#14726=CARTESIAN_POINT ( 'NONE',  ( 6.573693162767833442, 44.00881163587200717, 72.45433879953087342 ) ) ;
#14729=CARTESIAN_POINT ( 'NONE',  ( -5.389245695702297390, 49.84508174962770255, 72.45433879953087342 ) ) ;
#14730=CARTESIAN_POINT ( 'NONE',  ( 8.107024659646262066, 47.29146611110563470, 76.48622618158429987 ) ) ;
#14731=AXIS2_PLACEMENT_3D ( 'NONE', #7766, #15858, #1178 ) ;
#14732=CARTESIAN_POINT ( 'NONE',  ( -3.509782604184575661, 36.19999572785944508, 77.03801799112748938 ) ) ;
#14733=VERTEX_POINT ( 'NONE', #9101 ) ;
#14735=CARTESIAN_POINT ( 'NONE',  ( 1.199929786271850540, 52.20873427653266674, 79.49721971971477785 ) ) ;
#14738=CARTESIAN_POINT ( 'NONE',  ( 4.668432554735347573, 52.03990683855252541, 77.97037332800861975 ) ) ;
#14740=CARTESIAN_POINT ( 'NONE',  ( 9.327624742576356098, 42.74920758916827168, 78.90414333341678343 ) ) ;
#14741=ORIENTED_EDGE ( 'NONE', *, *, #913, .F. ) ;
#14742=DIRECTION ( 'NONE',  ( 0.9534635866061451637, 0.3015081906286224411, 2.009271279954815058E-16 ) ) ;
#14743=CARTESIAN_POINT ( 'NONE',  ( -5.623541984526494453, 37.76134463469641389, 75.60525969576029581 ) ) ;
#14744=EDGE_LOOP ( 'NONE', ( #16114, #9323, #2141, #6522 ) ) ;
#14746=CARTESIAN_POINT ( 'NONE',  ( -4.517176205512261511, 36.94411680087065264, 76.50360254650976799 ) ) ;
#14748=ORIENTED_EDGE ( 'NONE', *, *, #4151, .F. ) ;
#14749=CARTESIAN_POINT ( 'NONE',  ( -4.806942593991916368, 37.15815555953845717, 77.31392376534303423 ) ) ;
#14750=CARTESIAN_POINT ( 'NONE',  ( -4.517387068041375464, 36.94427255652680486, 78.31852111096432623 ) ) ;
#14751=ORIENTED_EDGE ( 'NONE', *, *, #19223, .T. ) ;
#14752=CARTESIAN_POINT ( 'NONE',  ( -4.762271096064603526, 51.20189707608225405, 76.05031124229590489 ) ) ;
#14754=DIRECTION ( 'NONE',  ( 0.3165065846431827645, 0.9485903129789529098, 0.000000000000000000 ) ) ;
#14757=CARTESIAN_POINT ( 'NONE',  ( 6.780993214391527246, 50.47944337839869888, 75.76076839092205262 ) ) ;
#14758=CARTESIAN_POINT ( 'NONE',  ( 8.797519961583052606, 41.16044993131110630, 77.39661844205990349 ) ) ;
#14759=CARTESIAN_POINT ( 'NONE',  ( 5.288291328326708118, 36.75211657491283290, 75.39318197153889400 ) ) ;
#14760=CARTESIAN_POINT ( 'NONE',  ( 7.726247110976633969, 40.31419528827419185, 79.00897045670630803 ) ) ;
#14764=CARTESIAN_POINT ( 'NONE',  ( 5.740585635973908474, 51.24795054640212300, 75.97198585835440099 ) ) ;
#14765=CARTESIAN_POINT ( 'NONE',  ( 6.197624760850954928, 49.99633915028627484, 77.73730439759678745 ) ) ;
#14768=ORIENTED_EDGE ( 'NONE', *, *, #18206, .T. ) ;
#14772=CARTESIAN_POINT ( 'NONE',  ( -0.8591174924091972143, 52.85316264988993851, 76.01910742181597413 ) ) ;
#14773=CARTESIAN_POINT ( 'NONE',  ( 5.404201196092212278, 50.75047497752489534, 79.54845644658969661 ) ) ;
#14776=CARTESIAN_POINT ( 'NONE',  ( 4.539372959821318609, 52.13523796247791608, 76.58963291717793709 ) ) ;
#14777=CARTESIAN_POINT ( 'NONE',  ( 4.356938870179031476, 51.41061492582127102, 77.85154143510365543 ) ) ;
#14778=DIRECTION ( 'NONE',  ( -0.3165065846431824870, -0.9485903129789529098, 0.000000000000000000 ) ) ;
#14779=B_SPLINE_CURVE_WITH_KNOTS ( 'NONE', 3,
 ( #2591, #7485, #9307, #7793, #14277, #20756, #2494, #6191, #12694, #8988, #19172, #13976, #8107, #13007, #17576, #3111, #8323, #20860, #14490 ),
 .UNSPECIFIED., .F., .F.,
 ( 4, 1, 1, 1, 1, 1, 1, 1, 1, 1, 1, 1, 1, 1, 1, 1, 4 ),
 ( 0.000000000000000000, 0.06114104454794499349, 0.1175581266966176375, 0.1702703359127188676, 0.2207833336891595610, 0.2680835234284920654, 0.3093802502289375589, 0.3470663877653532570, 0.3827844710311357757, 0.4080409699193555118, 0.4487658506906452294, 0.5030388115584650821, 0.5728007717267906695, 0.6580545229227713344, 0.7568648491070055773, 0.8711692811930628055, 1.000000000000000000 ),
 .UNSPECIFIED. ) ;
#14780=EDGE_CURVE ( 'NONE', #14563, #8403, #17384, .T. ) ;
#14782=ORIENTED_EDGE ( 'NONE', *, *, #5329, .T. ) ;
#14784=CARTESIAN_POINT ( 'NONE',  ( -5.569761608070843195, 50.62489392031717728, 79.19259575086972802 ) ) ;
#14785=CARTESIAN_POINT ( 'NONE',  ( 8.349122434088485534, 41.71505415299095176, 75.36168763251107805 ) ) ;
#14786=LINE ( 'NONE', #1607, #4430 ) ;
#14787=CARTESIAN_POINT ( 'NONE',  ( 1.652727357819363974, 35.35299279957455099, 79.45433879953087342 ) ) ;
#14788=ORIENTED_EDGE ( 'NONE', *, *, #8209, .F. ) ;
#14789=CARTESIAN_POINT ( 'NONE',  ( 6.431452980651660489, 38.48875362012321943, 76.25518385353585415 ) ) ;
#14792=CARTESIAN_POINT ( 'NONE',  ( -3.638656433990025807, 36.29518963458221492, 75.82994300095940332 ) ) ;
#14793=CARTESIAN_POINT ( 'NONE',  ( -1.440187084481232338, 38.28092143101017797, 82.45433879953087342 ) ) ;
#14794=VERTEX_POINT ( 'NONE', #18665 ) ;
#14795=CARTESIAN_POINT ( 'NONE',  ( 5.202885763635528349, 50.89499265101085967, 72.45433879953087342 ) ) ;
#14798=CARTESIAN_POINT ( 'NONE',  ( 2.115006836158880521, 52.20160162348516764, 77.84551527011910821 ) ) ;
#14800=EDGE_CURVE ( 'NONE', #13025, #4092, #17097, .T. ) ;
#14801=B_SPLINE_SURFACE_WITH_KNOTS ( 'NONE', 3, 1, ( 
 ( #7450, #12146 ),
 ( #17453, #18837 ),
 ( #2879, #17032 ),
 ( #2461, #963 ),
 ( #8955, #12256 ),
 ( #15441, #15547 ),
 ( #858, #7342 ),
 ( #13834, #20312 ),
 ( #13947, #5744 ),
 ( #20428, #18734 ),
 ( #9166, #15659 ),
 ( #17864, #16072 ),
 ( #9697, #3086 ),
 ( #4659, #1276 ),
 ( #6578, #20729 ),
 ( #14467, #3287 ),
 ( #6475, #13084 ),
 ( #17546, #1384 ),
 ( #9906, #17970 ),
 ( #7768, #7874 ),
 ( #1495, #14247 ),
 ( #6164, #8185 ),
 ( #9793, #17651 ) ),
 .UNSPECIFIED., .F., .F., .F.,
 ( 4, 1, 1, 1, 1, 1, 1, 1, 1, 1, 1, 1, 1, 1, 1, 1, 1, 1, 1, 1, 4 ),
 ( 2, 2 ),
 ( 0.000000000000000000, 0.05038957832574614271, 0.09924218466120336701, 0.1466944942679149211, 0.1933274803506509210, 0.2393051970681265017, 0.2845336341364397836, 0.3290963736026611408, 0.3737734709422849688, 0.4170414937111141529, 0.4581341819676884586, 0.4966705307863439889, 0.5335170563061359950, 0.5686625127317078698, 0.6026561223054673899, 0.6353294289861355360, 0.6676748031221235724, 0.7363421380907280156, 0.8138933404431207830, 0.9017813486866357309, 1.000000000000000000 ),
 ( 0.000000000000000000, 1.000000000000000000 ),
 .UNSPECIFIED. ) ;
#14802=EDGE_CURVE ( 'NONE', #1396, #19108, #6000, .T. ) ;
#14803=PLANE ( 'NONE',  #733 ) ;
#14804=VERTEX_POINT ( 'NONE', #11224 ) ;
#14805=DIRECTION ( 'NONE',  ( -0.9485903129789527988, 0.3165065846431829311, -8.934458285744989980E-17 ) ) ;
#14813=DIRECTION ( 'NONE',  ( -0.9485903129789527988, 0.3165065846431829311, -8.934458285744989980E-17 ) ) ;
#14815=CARTESIAN_POINT ( 'NONE',  ( 8.172753155408216230, 41.66916893826013535, 75.36022115247205022 ) ) ;
#14817=CARTESIAN_POINT ( 'NONE',  ( -4.045487599862485517, 50.96716888712930427, 78.75145056212190298 ) ) ;
#14818=EDGE_CURVE ( 'NONE', #20802, #374, #15700, .T. ) ;
#14823=ORIENTED_EDGE ( 'NONE', *, *, #15609, .T. ) ;
#14825=CARTESIAN_POINT ( 'NONE',  ( -6.770023921829650071, 40.50299573356667793, 77.79645048995966761 ) ) ;
#14827=CARTESIAN_POINT ( 'NONE',  ( -5.835824771109036746, 39.98772221508849611, 72.45432679953087529 ) ) ;
#14828=CARTESIAN_POINT ( 'NONE',  ( 9.026838159693451047, 41.84773111872319618, 78.13669174070733447 ) ) ;
#14830=CARTESIAN_POINT ( 'NONE',  ( -7.079975527142585712, 43.92211762787398044, 72.45433879953085921 ) ) ;
#14831=CARTESIAN_POINT ( 'NONE',  ( -7.725086623296537169, 47.24405475114629382, 77.94747975791852923 ) ) ;
#14832=CARTESIAN_POINT ( 'NONE',  ( -4.472548095981605520, 51.40892252450552036, 75.36471306604558151 ) ) ;
#14835=CARTESIAN_POINT ( 'NONE',  ( 0.3821786226492928651, 35.36301154328572949, 75.45433879953087342 ) ) ;
#14837=B_SPLINE_CURVE_WITH_KNOTS ( 'NONE', 3,
 ( #1270, #9271, #12451, #9474, #20832, #15761, #9372, #1176, #11077, #4654, #2873, #20526, #19047, #4456, #5853, #14139, #15960, #2659, #18931 ),
 .UNSPECIFIED., .F., .F.,
 ( 4, 1, 1, 1, 1, 1, 1, 1, 1, 1, 1, 1, 1, 1, 1, 1, 4 ),
 ( 0.000000000000000000, 0.1010931020334112918, 0.1936883160783454683, 0.2783829231069467891, 0.3553896825508546242, 0.4249031060497730494, 0.4877225005288854942, 0.5445694316561201509, 0.5961453798982884189, 0.6449762784811632343, 0.6930678288708707058, 0.7409100032456262808, 0.7895445362486890328, 0.8390228595812658785, 0.8900783947972482624, 0.9435774522572311085, 1.000000000000000000 ),
 .UNSPECIFIED. ) ;
#14839=DIRECTION ( 'NONE',  ( -0.9485903129789495791, 0.3165065846431928120, -8.934458285744765648E-17 ) ) ;
#14843=CARTESIAN_POINT ( 'NONE',  ( -4.803777751955213837, 38.09182431430669880, 75.42164981362142839 ) ) ;
#14845=LINE ( 'NONE', #4841, #10833 ) ;
#14846=CARTESIAN_POINT ( 'NONE',  ( 0.3458533632374572453, 52.96041607507793714, 76.11020930090303693 ) ) ;
#14847=EDGE_CURVE ( 'NONE', #16377, #2198, #12604, .T. ) ;
#14849=ORIENTED_EDGE ( 'NONE', *, *, #6343, .F. ) ;
#14852=PRODUCT_DEFINITION_CONTEXT ( 'detailed design', #1243, 'design' ) ;
#14855=CARTESIAN_POINT ( 'NONE',  ( 1.978191321044207474, 52.84097467239952550, 75.87687246405737085 ) ) ;
#14857=LINE ( 'NONE', #6451, #11902 ) ;
#14858=CARTESIAN_POINT ( 'NONE',  ( 0.6184261976043861075, 52.96580428404300989, 76.85126224504509196 ) ) ;
#14859=ORIENTED_EDGE ( 'NONE', *, *, #5452, .F. ) ;
#14860=CARTESIAN_POINT ( 'NONE',  ( 4.442698562174268062, 36.14788694334743013, 76.14998054923410109 ) ) ;
#14863=CARTESIAN_POINT ( 'NONE',  ( -5.185247867692305945, 38.27425900083883903, 75.57863954941232976 ) ) ;
#14864=CARTESIAN_POINT ( 'NONE',  ( 9.204112107805267229, 42.37903238726386945, 75.57016332177543916 ) ) ;
#14867=VERTEX_POINT ( 'NONE', #14401 ) ;
#14868=DIRECTION ( 'NONE',  ( 0.3165065846431826535, 0.9485903129789529098, 2.188653791613874008E-16 ) ) ;
#14872=CARTESIAN_POINT ( 'NONE',  ( 9.353328126263708242, 42.82624226067153472, 76.54645538997905874 ) ) ;
#14877=CARTESIAN_POINT ( 'NONE',  ( 4.192089982862425401, 51.46692896115924043, 75.88092117868445996 ) ) ;
#14878=CARTESIAN_POINT ( 'NONE',  ( 4.143017335158133641, 51.51944627275094746, 78.46169174070733732 ) ) ;
#14881=VERTEX_POINT ( 'NONE', #4499 ) ;
#14882=CARTESIAN_POINT ( 'NONE',  ( 5.151473114414916843, 37.39086402708484513, 75.36221941035768168 ) ) ;
#14884=DIRECTION ( 'NONE',  ( 0.8136266022444372803, 0.5813877811927012917, 2.295812393977109100E-16 ) ) ;
#14885=CARTESIAN_POINT ( 'NONE',  ( -4.492578824834620121, 37.68058364860989684, 78.86751516113972116 ) ) ;
#14886=DIRECTION ( 'NONE',  ( 0.007885122365275663500, 0.9999689119394085113, 1.805443505845543142E-16 ) ) ;
#14887=CARTESIAN_POINT ( 'NONE',  ( -7.885657102084565828, 41.56435211639550431, 79.54845644658969661 ) ) ;
#14888=DIRECTION ( 'NONE',  ( -0.8136266022444372803, -0.5813877811927012917, -2.295812393977109100E-16 ) ) ;
#14889=ORIENTED_EDGE ( 'NONE', *, *, #17525, .T. ) ;
#14891=LINE ( 'NONE', #19366, #13548 ) ;
#14892=CARTESIAN_POINT ( 'NONE',  ( 6.418481717452356961, 38.47948483034925715, 77.68698088877128782 ) ) ;
#14893=CARTESIAN_POINT ( 'NONE',  ( 4.100026115879673583, 51.54044873340893673, 76.58963291717793709 ) ) ;
#14894=CARTESIAN_POINT ( 'NONE',  ( 0.8317120302326751480, 52.95673948731686664, 76.08306827724030086 ) ) ;
#14895=VERTEX_POINT ( 'NONE', #12705 ) ;
#14896=CARTESIAN_POINT ( 'NONE',  ( 8.940907051378230719, 41.59019013573462331, 76.11674899411023887 ) ) ;
#14897=AXIS2_PLACEMENT_3D ( 'NONE', #7156, #10057, #14930 ) ;
#14901=CARTESIAN_POINT ( 'NONE',  ( -7.831942942175630584, 41.38181678794802565, 78.91953837536544825 ) ) ;
#14902=CARTESIAN_POINT ( 'NONE',  ( -3.603146387903926051, 36.26895979397031056, 78.01078865174693533 ) ) ;
#14906=ORIENTED_EDGE ( 'NONE', *, *, #10316, .T. ) ;
#14909=VERTEX_POINT ( 'NONE', #4596 ) ;
#14910=B_SPLINE_CURVE_WITH_KNOTS ( 'NONE', 3,
 ( #8696, #5488, #10513, #16980, #16568, #15176, #6764, #20056, #1989, #13275, #12003, #18474, #5165, #10410 ),
 .UNSPECIFIED., .F., .F.,
 ( 4, 2, 2, 2, 2, 2, 4 ),
 ( 0.000000000000000000, 0.0002739962706728955389, 0.0005479925413457910777, 0.0008219888120186866166, 0.001095985082691582155, 0.001643977624037381473, 0.002191970165383179923 ),
 .UNSPECIFIED. ) ;
#14913=ORIENTED_EDGE ( 'NONE', *, *, #2750, .F. ) ;
#14914=DIRECTION ( 'NONE',  ( -0.5813877811926938532, 0.8136266022444424983, 5.636455622144827492E-17 ) ) ;
#14915=CARTESIAN_POINT ( 'NONE',  ( 8.740212021938845055, 40.98869440064952130, 75.38759329643264095 ) ) ;
#14916=CARTESIAN_POINT ( 'NONE',  ( 5.937214047150960461, 51.10270905974117994, 76.26580079864017137 ) ) ;
#14919=CARTESIAN_POINT ( 'NONE',  ( 0.4211168079077332038, 52.35552251280865477, 78.89168391585492657 ) ) ;
#14921=CARTESIAN_POINT ( 'NONE',  ( -4.423683986466107498, 51.44383902813605403, 76.03815620566271605 ) ) ;
#14922=VECTOR ( 'NONE', #7334, 1000.000000000000114 ) ;
#14925=CARTESIAN_POINT ( 'NONE',  ( -7.457252456121344686, 40.19216126113897758, 77.97023824993468111 ) ) ;
#14928=CARTESIAN_POINT ( 'NONE',  ( -6.210882734309923769, 46.73118581782181025, 75.45433879953087342 ) ) ;
#14930=DIRECTION ( 'NONE',  ( 0.3165065846431826535, 0.9485903129789529098, 2.188653791613874008E-16 ) ) ;
#14933=CARTESIAN_POINT ( 'NONE',  ( -7.087950778502929872, 47.02707019024424540, 77.87251963618699335 ) ) ;
#14935=AXIS2_PLACEMENT_3D ( 'NONE', #4321, #7313, #16892 ) ;
#14936=CLOSED_SHELL ( 'NONE', ( #5684, #6462, #20337, #5145, #14558, #16775, #16301, #5962, #14703, #18753, #5595, #9132, #7968, #3140, #14173, #1195, #2856, #8860, #382, #1009, #20101, #14560, #11715, #15481, #10839, #6248, #5977, #2129, #8997, #13530, #20512, #11059, #14566, #11630, #7266, #10584, #11548, #10711, #13425, #7304, #17184, #14286, #7821, #14588, #16393, #5825, #16802, #1254, #5600, #9321, #8628, #5707, #13520, #8196, #12200, #6994, #8349, #4740, #18985, #10807, #6891, #13221, #20317, #2276, #7697, #12102, #10574, #15584, #10516, #19225, #13614, #2756, #7186, #20126, #6299, #13951, #15001, #13941, #18740, #12769, #17034, #13271, #16830, #17895, #15754, #5091, #8559, #17558, #9715, #17404, #9351, #2711, #7149, #6089, #4949, #20486, #4366, #4893, #9798, #2061, #2753, #15022, #18404, #18235, #20797, #1792, #8736, #5408, #4899, #1077, #4251, #5703, #11184, #6971, #6495, #10543, #4545, #20170, #14167, #15842, #18842, #8105, #7277, #4517, #12638, #15895, #10542, #9280, #15638, #18592, #20834, #16664, #20938, #11476, #6612, #683, #15470, #18596, #1054, #6817, #14707, #10913, #12086, #4505, #14298, #1523, #3481, #5314, #9947, #5176, #10958, #4865, #7309, #13903, #8985, #12721, #5207, #1947, #19076, #8556, #10303, #15765, #18894, #4306, #12618, #6969, #3911, #3007, #2597, #15077, #1727, #6394, #3653, #257, #2361, #10038, #3892, #1573, #9255, #6088, #10437, #10970, #17299, #10538, #153, #5440, #14527, #18331, #15863, #3271, #1136, #11444, #10986, #20885, #1500, #18822, #6123, #8666, #4137, #8636, #17715, #16076, #11926, #1701, #21029, #12406, #2490, #923, #14071, #7668, #5481, #8678, #11400, #383, #10180, #4943, #9898, #11373, #15092, #3940, #14031, #20374, #19744, #11179 ) ) ;
#14937=VERTEX_POINT ( 'NONE', #9944 ) ;
#14938=CARTESIAN_POINT ( 'NONE',  ( -1.769308508470985863, 51.40850462968639079, 75.45433879953087342 ) ) ;
#14939=CARTESIAN_POINT ( 'NONE',  ( 5.092481412199395763, 37.36999664754328876, 78.16244716952144245 ) ) ;
#14940=ORIENTED_EDGE ( 'NONE', *, *, #13177, .T. ) ;
#14942=EDGE_CURVE ( 'NONE', #12487, #6196, #1748, .T. ) ;
#14946=ORIENTED_EDGE ( 'NONE', *, *, #10339, .F. ) ;
#14952=CARTESIAN_POINT ( 'NONE',  ( 0.5234039149397815560, 52.96221744815497345, 75.97427060055225922 ) ) ;
#14955=CARTESIAN_POINT ( 'NONE',  ( -3.944959226007136888, 38.51060946023304865, 77.05433879953086773 ) ) ;
#14958=ORIENTED_EDGE ( 'NONE', *, *, #13422, .T. ) ;
#14959=CARTESIAN_POINT ( 'NONE',  ( 0.8337132176892476654, 52.35626200026493393, 77.58758220374809866 ) ) ;
#14960=CARTESIAN_POINT ( 'NONE',  ( 1.725557703326630499, 52.87986937373156593, 75.61804811561941619 ) ) ;
#14963=CARTESIAN_POINT ( 'NONE',  ( 6.695638642021790155, 50.54249136271632636, 75.66183449524544358 ) ) ;
#14965=CARTESIAN_POINT ( 'NONE',  ( 5.467682621026056289, 50.70306757362737926, 77.28284099877059532 ) ) ;
#14966=EDGE_CURVE ( 'NONE', #20991, #7197, #19495, .T. ) ;
#14967=CARTESIAN_POINT ( 'NONE',  ( -7.203865160062882467, 41.41469608315769335, 78.54945882271483981 ) ) ;
#14969=EDGE_CURVE ( 'NONE', #597, #20036, #1408, .T. ) ;
#14972=CARTESIAN_POINT ( 'NONE',  ( 7.676901518817963677, 40.16630341814867933, 78.16120960217517677 ) ) ;
#14974=VERTEX_POINT ( 'NONE', #8119 ) ;
#14979=ORIENTED_EDGE ( 'NONE', *, *, #17423, .T. ) ;
#14983=CARTESIAN_POINT ( 'NONE',  ( 6.103551234968451311, 50.05500953258444952, 77.68963291717794561 ) ) ;
#14985=CARTESIAN_POINT ( 'NONE',  ( -3.495065479208315562, 36.18912478048144266, 76.62933879953087057 ) ) ;
#14987=CARTESIAN_POINT ( 'NONE',  ( -3.167417508397908588, 51.48567728911131525, 79.16276250595325337 ) ) ;
#14988=CARTESIAN_POINT ( 'NONE',  ( 0.002918113473574554962, 52.94761665455641975, 75.41770058766584839 ) ) ;
#14990=B_SPLINE_SURFACE_WITH_KNOTS ( 'NONE', 3, 1, ( 
 ( #3276, #9573 ),
 ( #16261, #8170 ),
 ( #4962, #9994 ),
 ( #11483, #6565 ),
 ( #11276, #7967 ),
 ( #21022, #14452 ),
 ( #12854, #1585 ),
 ( #17958, #5172 ),
 ( #1800, #4751 ),
 ( #84, #6667 ),
 ( #1893, #6771 ),
 ( #14657, #14557 ),
 ( #19645, #13071 ),
 ( #16370, #19443 ),
 ( #16472, #8381 ),
 ( #14864, #281 ),
 ( #13281, #18167 ),
 ( #1995, #8490 ),
 ( #16574, #3584 ),
 ( #10091, #3458 ),
 ( #17722, #19306 ),
 ( #9655, #6428 ),
 ( #13047, #9858 ) ),
 .UNSPECIFIED., .F., .F., .F.,
 ( 4, 1, 1, 1, 1, 1, 1, 1, 1, 1, 1, 1, 1, 1, 1, 1, 1, 1, 1, 1, 4 ),
 ( 2, 2 ),
 ( 0.000000000000000000, 0.04300144207505136179, 0.08353165498080591944, 0.1209955408344369626, 0.1553840623654753617, 0.1873435814759382700, 0.2162479910858959298, 0.2424976236983500399, 0.2660452007499324312, 0.3104933729322157387, 0.3556083049253406791, 0.4034864083407884716, 0.4540969056831142825, 0.5078508224766279389, 0.5647468969590679899, 0.6259022191770886590, 0.6917657563094725681, 0.7621492621511971599, 0.8365553829333508551, 0.9158190838930461153, 1.000000000000000000 ),
 ( 0.000000000000000000, 1.000000000000000000 ),
 .UNSPECIFIED. ) ;
#14991=FACE_OUTER_BOUND ( 'NONE', #11931, .T. ) ;
#14992=DIRECTION ( 'NONE',  ( -0.8033560671169786005, -0.5954989751681698529, -2.305299702067830011E-16 ) ) ;
#14993=DIRECTION ( 'NONE',  ( 0.3165065846431826535, 0.9485903129789529098, 2.188653791613874008E-16 ) ) ;
#14997=CARTESIAN_POINT ( 'NONE',  ( 3.962887037559272407, 36.71897260862575507, 76.53559901244523189 ) ) ;
#14999=DIRECTION ( 'NONE',  ( -0.9534635866061451637, -0.3015081906286224411, -2.009271279954815058E-16 ) ) ;
#15000=CARTESIAN_POINT ( 'NONE',  ( -8.190409139795066906, 42.92474528817020740, 76.06610350541322418 ) ) ;
#15001=ADVANCED_FACE ( 'NONE', ( #19807 ), #3325, .T. ) ;
#15002=CARTESIAN_POINT ( 'NONE',  ( -4.895222749246778804, 37.22336455408366618, 78.59503622499423159 ) ) ;
#15004=CARTESIAN_POINT ( 'NONE',  ( 8.356946452252621782, 41.76007885337365622, 77.44430071719698105 ) ) ;
#15005=DIRECTION ( 'NONE',  ( 1.540237394707284220E-16, 1.793354297423764243E-16, -1.000000000000000000 ) ) ;
#15008=ORIENTED_EDGE ( 'NONE', *, *, #12906, .T. ) ;
#15009=VECTOR ( 'NONE', #3652, 1000.000000000000114 ) ;
#15010=DIRECTION ( 'NONE',  ( 0.3165065846431827645, 0.9485903129789529098, 0.000000000000000000 ) ) ;
#15013=ORIENTED_EDGE ( 'NONE', *, *, #19975, .F. ) ;
#15017=CARTESIAN_POINT ( 'NONE',  ( -5.968382836370076383, 47.45797339585421071, 78.32492703482499508 ) ) ;
#15020=CARTESIAN_POINT ( 'NONE',  ( 1.700675709985738804, 52.20486877668423631, 76.92027168626151479 ) ) ;
#15021=CARTESIAN_POINT ( 'NONE',  ( -3.108234509380449762, 36.81740333079968508, 78.23707788297487298 ) ) ;
#15022=ADVANCED_FACE ( 'NONE', ( #10150 ), #2432, .T. ) ;
#15025=CARTESIAN_POINT ( 'NONE',  ( 8.433872151619121738, 42.00521257461706170, 79.52184654923091500 ) ) ;
#15028=DIRECTION ( 'NONE',  ( -0.3015081906286169455, 0.9534635866061470511, 1.245503830460480420E-16 ) ) ;
#15030=CARTESIAN_POINT ( 'NONE',  ( -4.340948238162491535, 40.55733868359232730, 72.45433879953085921 ) ) ;
#15032=ORIENTED_EDGE ( 'NONE', *, *, #11596, .F. ) ;
#15035=DIRECTION ( 'NONE',  ( 1.540237394707284220E-16, 1.793354297423764243E-16, -1.000000000000000000 ) ) ;
#15036=CARTESIAN_POINT ( 'NONE',  ( 0.3327559098722669417, 52.96757255913198748, 78.50066232894263862 ) ) ;
#15038=PLANE ( 'NONE',  #1709 ) ;
#15041=ORIENTED_EDGE ( 'NONE', *, *, #8442, .F. ) ;
#15042=DIRECTION ( 'NONE',  ( -0.3165065846431971419, -0.9485903129789481358, 0.000000000000000000 ) ) ;
#15043=CARTESIAN_POINT ( 'NONE',  ( -7.537584518443389392, 40.44619647026995324, 77.53559663939034863 ) ) ;
#15045=DIRECTION ( 'NONE',  ( 1.540237394707284220E-16, 1.793354297423764243E-16, -1.000000000000000000 ) ) ;
#15046=CARTESIAN_POINT ( 'NONE',  ( -3.098709854545130593, 36.80491647020841128, 78.46683879953087626 ) ) ;
#15049=B_SPLINE_CURVE_WITH_KNOTS ( 'NONE', 3,
 ( #15686, #5892, #20653, #15795, #887, #5783, #7693, #17270, #15577, #2692, #992, #6083, #18768, #19079, #4182, #4585 ),
 .UNSPECIFIED., .F., .F.,
 ( 4, 2, 2, 2, 2, 2, 2, 4 ),
 ( 0.000000000000000000, 0.0001355735443734605323, 0.0002711470887469210646, 0.0004067206331203815427, 0.0005422941774938421292, 0.0006778677218673026614, 0.0008134412662407630853, 0.001084588354987687294 ),
 .UNSPECIFIED. ) ;
#15051=EDGE_CURVE ( 'NONE', #8901, #3406, #897, .T. ) ;
#15053=CYLINDRICAL_SURFACE ( 'NONE', #3377, 8.199999999999995737 ) ;
#15054=CARTESIAN_POINT ( 'NONE',  ( 1.083001295814570053, 52.34297901104275041, 76.77198585835439815 ) ) ;
#15056=VECTOR ( 'NONE', #20067, 1000.000000000000114 ) ;
#15062=CARTESIAN_POINT ( 'NONE',  ( -5.503510928868301733, 38.60868902512070377, 76.46818962967083166 ) ) ;
#15063=EDGE_LOOP ( 'NONE', ( #15177, #5128, #227, #311 ) ) ;
#15064=CARTESIAN_POINT ( 'NONE',  ( 5.614631715549363022, 51.34098763368633911, 78.82175487302160377 ) ) ;
#15067=DIRECTION ( 'NONE',  ( 1.540237394707284220E-16, 1.793354297423764243E-16, -1.000000000000000000 ) ) ;
#15069=ORIENTED_EDGE ( 'NONE', *, *, #1298, .T. ) ;
#15070=CARTESIAN_POINT ( 'NONE',  ( -4.788785806866687089, 51.18295063450860738, 76.15325518536063498 ) ) ;
#15074=CARTESIAN_POINT ( 'NONE',  ( 6.298904310734356748, 49.91071008481807070, 75.70960632971019777 ) ) ;
#15075=CARTESIAN_POINT ( 'NONE',  ( 0.4896586383660414543, 52.96222063074647224, 78.92934190660548666 ) ) ;
#15077=ADVANCED_FACE ( 'NONE', ( #7500 ), #11767, .T. ) ;
#15078=ORIENTED_EDGE ( 'NONE', *, *, #18480, .F. ) ;
#15079=VERTEX_POINT ( 'NONE', #16317 ) ;
#15080=CARTESIAN_POINT ( 'NONE',  ( 3.965773623613683796, 36.72686942586689440, 76.47837415541054895 ) ) ;
#15081=CARTESIAN_POINT ( 'NONE',  ( 7.825649284229865721, 40.61210990747041905, 79.30521328845429707 ) ) ;
#15082=ORIENTED_EDGE ( 'NONE', *, *, #14317, .F. ) ;
#15084=DIRECTION ( 'NONE',  ( 1.540237394707284220E-16, 1.793354297423764243E-16, -1.000000000000000000 ) ) ;
#15089=CARTESIAN_POINT ( 'NONE',  ( 6.486361464680296507, 49.78306097819143616, 78.52964612251847143 ) ) ;
#15091=CARTESIAN_POINT ( 'NONE',  ( 5.384092268968043271, 50.76532863195453160, 75.97198585835440099 ) ) ;
#15092=ADVANCED_FACE ( 'NONE', ( #14292 ), #7910, .T. ) ;
#15093=CARTESIAN_POINT ( 'NONE',  ( 7.933465412281296203, 40.95200839197739384, 75.44378286633819641 ) ) ;
#15095=CARTESIAN_POINT ( 'NONE',  ( -3.012418977206551052, 51.56146524693782141, 78.90943149866365047 ) ) ;
#15096=EDGE_CURVE ( 'NONE', #54, #10557, #16005, .T. ) ;
#15099=CARTESIAN_POINT ( 'NONE',  ( 0.7990284332011086121, 52.35254253780928480, 77.48826545068648386 ) ) ;
#15101=CARTESIAN_POINT ( 'NONE',  ( 4.634072907867718527, 52.06528692560263494, 75.88092117868445996 ) ) ;
#15102=EDGE_CURVE ( 'NONE', #14794, #17396, #14342, .T. ) ;
#15103=CARTESIAN_POINT ( 'NONE',  ( 5.564133502460520297, 36.94922329332227662, 77.75193993234761081 ) ) ;
#15106=DIRECTION ( 'NONE',  ( -0.5954989751681698529, 0.8033560671169786005, 5.234922652618076394E-17 ) ) ;
#15107=ORIENTED_EDGE ( 'NONE', *, *, #4564, .F. ) ;
#15108=CARTESIAN_POINT ( 'NONE',  ( 0.5596655318826941894, 52.96576883007725911, 75.97250646058495249 ) ) ;
#15110=CARTESIAN_POINT ( 'NONE',  ( 0.3821786226492928651, 35.36301154328572949, 78.57639762306027365 ) ) ;
#15112=CARTESIAN_POINT ( 'NONE',  ( -4.505166693174837533, 37.68988179988254217, 78.83844719616611485 ) ) ;
#15114=CARTESIAN_POINT ( 'NONE',  ( -5.087398782055174706, 37.36531724819641909, 77.33565342272370913 ) ) ;
#15115=DIRECTION ( 'NONE',  ( -1.540237394707284220E-16, -1.793354297423764243E-16, 1.000000000000000000 ) ) ;
#15117=ORIENTED_EDGE ( 'NONE', *, *, #4294, .F. ) ;
#15118=VERTEX_POINT ( 'NONE', #3225 ) ;
#15119=CARTESIAN_POINT ( 'NONE',  ( 8.243324203357053293, 41.86390813689740753, 79.54154676390322720 ) ) ;
#15121=CARTESIAN_POINT ( 'NONE',  ( 8.787829143201870252, 41.13140593384865440, 77.14698585835439815 ) ) ;
#15123=CARTESIAN_POINT ( 'NONE',  ( 0.4151831860546061348, 52.36151757739148849, 76.98461824414090415 ) ) ;
#15124=CARTESIAN_POINT ( 'NONE',  ( 5.599231707071657738, 51.35236299959863970, 78.30875056423674607 ) ) ;
#15127=EDGE_CURVE ( 'NONE', #20811, #10206, #10050, .T. ) ;
#15128=CARTESIAN_POINT ( 'NONE',  ( -7.219979407079431866, 41.47817498120593882, 78.85792113001433279 ) ) ;
#15130=B_SPLINE_CURVE_WITH_KNOTS ( 'NONE', 3,
 ( #6690, #3199, #16180, #16494, #107, #16395, #1821, #18087, #306, #8090, #12987, #16284, #11717, #19464, #8304, #17871, #16597, #1713, #4985 ),
 .UNSPECIFIED., .F., .F.,
 ( 4, 1, 1, 1, 1, 1, 1, 1, 1, 1, 1, 1, 1, 1, 1, 1, 4 ),
 ( 0.000000000000000000, 0.09472651553281030701, 0.1809448578637775085, 0.2575849355004761199, 0.3257111939256314703, 0.3842597268839244573, 0.4332657528852557616, 0.4727039292014991179, 0.5037345896081361074, 0.5551104982754543338, 0.6060435029138766527, 0.6590687186606726256, 0.7172582036121251114, 0.7797016678215834551, 0.8463570695623257034, 0.9189979831805518140, 1.000000000000000000 ),
 .UNSPECIFIED. ) ;
#15140=FACE_OUTER_BOUND ( 'NONE', #7659, .T. ) ;
#15141=CARTESIAN_POINT ( 'NONE',  ( -2.952897068019848525, 51.57503392883338478, 78.68920376838389075 ) ) ;
#15142=LINE ( 'NONE', #2261, #16242 ) ;
#15143=CARTESIAN_POINT ( 'NONE',  ( 5.349358414356570002, 50.78229839341420160, 77.28795170149270177 ) ) ;
#15144=CARTESIAN_POINT ( 'NONE',  ( 0.5886303079273511596, 52.96555489546793183, 78.93669174070734584 ) ) ;
#15150=CARTESIAN_POINT ( 'NONE',  ( 5.359863228392665491, 37.54119487609694517, 75.97600981932362174 ) ) ;
#15153=CARTESIAN_POINT ( 'NONE',  ( 5.544276951911416340, 50.64433212932689088, 78.27786821129558348 ) ) ;
#15155=CARTESIAN_POINT ( 'NONE',  ( 8.797946357469053069, 41.16172786683149099, 78.83414475571305502 ) ) ;
#15162=CARTESIAN_POINT ( 'NONE',  ( -7.880650121838598032, 41.52863557963361529, 77.91116350996777840 ) ) ;
#15163=ORIENTED_EDGE ( 'NONE', *, *, #9247, .T. ) ;
#15165=FACE_OUTER_BOUND ( 'NONE', #15871, .T. ) ;
#15166=PLANE ( 'NONE',  #3166 ) ;
#15167=ORIENTED_EDGE ( 'NONE', *, *, #2841, .T. ) ;
#15168=CARTESIAN_POINT ( 'NONE',  ( 2.070819430837580022, 52.21461655967870996, 78.80944668400142916 ) ) ;
#15170=CARTESIAN_POINT ( 'NONE',  ( -4.802822372555619168, 51.17292061857877172, 76.30694920102484957 ) ) ;
#15171=LINE ( 'NONE', #10729, #9527 ) ;
#15174=CARTESIAN_POINT ( 'NONE',  ( -3.554968601118877469, 36.23337280359183410, 78.17158301229430606 ) ) ;
#15176=CARTESIAN_POINT ( 'NONE',  ( -3.245728885430589017, 36.87898507402727688, 79.07903280936416479 ) ) ;
#15177=ORIENTED_EDGE ( 'NONE', *, *, #15609, .F. ) ;
#15179=EDGE_CURVE ( 'NONE', #19082, #8044, #7032, .T. ) ;
#15180=CARTESIAN_POINT ( 'NONE',  ( 4.394267649348433835, 36.11327998621098345, 76.69403369658814995 ) ) ;
#15182=CARTESIAN_POINT ( 'NONE',  ( -0.9234155522616860345, 52.23375968936932168, 78.59964918550147672 ) ) ;
#15185=CARTESIAN_POINT ( 'NONE',  ( -3.364492789658395377, 52.20069827791003547, 76.33204918460485544 ) ) ;
#15186=ORIENTED_EDGE ( 'NONE', *, *, #10821, .F. ) ;
#15188=CIRCLE ( 'NONE', #11131, 8.199999999999995737 ) ;
#15189=CARTESIAN_POINT ( 'NONE',  ( 6.761793986577667503, 50.49362507459272820, 79.13556070921569585 ) ) ;
#15192=CARTESIAN_POINT ( 'NONE',  ( 5.991756872021341884, 37.25478729691962343, 75.38041148603002739 ) ) ;
#15193=CARTESIAN_POINT ( 'NONE',  ( 8.572560397843592028, 40.48623184761532912, 75.53366564255911442 ) ) ;
#15196=CARTESIAN_POINT ( 'NONE',  ( 4.539372959821318609, 52.13523796247791608, 76.58963291717793709 ) ) ;
#15197=LINE ( 'NONE', #8290, #2471 ) ;
#15199=LINE ( 'NONE', #14512, #9787 ) ;
#15204=CARTESIAN_POINT ( 'NONE',  ( 8.362028646804796850, 41.75872088733057552, 76.06672873082523267 ) ) ;
#15207=CARTESIAN_POINT ( 'NONE',  ( 0.4810581700086011270, 52.35504993940188001, 75.98243536310876323 ) ) ;
#15208=EDGE_CURVE ( 'NONE', #5035, #6017, #1850, .T. ) ;
#15209=EDGE_CURVE ( 'NONE', #20066, #2125, #10260, .T. ) ;
#15212=CARTESIAN_POINT ( 'NONE',  ( 9.271561067608034890, 45.68041113525027441, 79.47125056423675460 ) ) ;
#15213=CARTESIAN_POINT ( 'NONE',  ( -2.055347584452832166, 51.31805217249780782, 75.45433879953087342 ) ) ;
#15217=FACE_OUTER_BOUND ( 'NONE', #5411, .T. ) ;
#15219=EDGE_CURVE ( 'NONE', #9753, #3490, #7141, .T. ) ;
#15220=DIRECTION ( 'NONE',  ( -0.9485903129789529098, 0.3165065846431826535, -8.934458285744997376E-17 ) ) ;
#15222=CIRCLE ( 'NONE', #14193, 8.199999999999995737 ) ;
#15223=CARTESIAN_POINT ( 'NONE',  ( 9.177137044501376906, 42.29818641127601353, 79.38025142445083304 ) ) ;
#15225=CARTESIAN_POINT ( 'NONE',  ( 0.6324608792002816005, 52.96167523169288671, 75.97329777450663357 ) ) ;
#15226=VERTEX_POINT ( 'NONE', #10369 ) ;
#15227=CARTESIAN_POINT ( 'NONE',  ( 0.4849271306368859724, 52.36220339060425033, 78.92934173667400444 ) ) ;
#15232=CARTESIAN_POINT ( 'NONE',  ( -7.787617544678308690, 41.24164596078931311, 78.75487387812985673 ) ) ;
#15233=CARTESIAN_POINT ( 'NONE',  ( -3.188853836583637413, 36.87695358026009274, 77.96849812480175501 ) ) ;
#15235=CARTESIAN_POINT ( 'NONE',  ( 6.882613847952937292, 37.89136107556471700, 76.65924029158320252 ) ) ;
#15238=CARTESIAN_POINT ( 'NONE',  ( -1.493738069816088920, 38.45421922485636657, 72.45433879953085921 ) ) ;
#15240=DIRECTION ( 'NONE',  ( -1.540237394707283727E-16, -1.793354297423763257E-16, 1.000000000000000000 ) ) ;
#15241=EDGE_CURVE ( 'NONE', #13048, #8338, #18430, .T. ) ;
#15244=CARTESIAN_POINT ( 'NONE',  ( 8.443422548343662015, 42.04239353520513589, 78.13669174070733447 ) ) ;
#15246=EDGE_CURVE ( 'NONE', #4372, #9222, #5439, .T. ) ;
#15248=CARTESIAN_POINT ( 'NONE',  ( -3.850375455727051310, 51.85350431403718119, 79.38294305353919356 ) ) ;
#15250=CARTESIAN_POINT ( 'NONE',  ( 0.8456369902943451367, 52.35216224083615089, 76.46781884397893236 ) ) ;
#15251=CARTESIAN_POINT ( 'NONE',  ( 0.3352349842281855952, 52.35619972255046406, 78.67509294885779525 ) ) ;
#15253=CARTESIAN_POINT ( 'NONE',  ( 8.300594306733913186, 41.56682737740558764, 77.52492703482499792 ) ) ;
#15254=ORIENTED_EDGE ( 'NONE', *, *, #2874, .T. ) ;
#15256=CARTESIAN_POINT ( 'NONE',  ( 6.960009239587057195, 50.34721145179211987, 76.80946857459053945 ) ) ;
#15258=CARTESIAN_POINT ( 'NONE',  ( -7.407177866501955421, 40.34522932431062969, 77.72181725404989550 ) ) ;
#15260=CARTESIAN_POINT ( 'NONE',  ( -4.716387082485073989, 37.09126585098686490, 75.36022115247205022 ) ) ;
#15261=AXIS2_PLACEMENT_3D ( 'NONE', #14689, #6487, #17778 ) ;
#15265=EDGE_LOOP ( 'NONE', ( #2277, #10686, #11611, #14958 ) ) ;
#15266=CARTESIAN_POINT ( 'NONE',  ( -3.872072204604002810, 50.91822502938001094, 75.38014013087713749 ) ) ;
#15267=EDGE_CURVE ( 'NONE', #11453, #1174, #3431, .T. ) ;
#15270=VERTEX_POINT ( 'NONE', #13334 ) ;
#15271=CARTESIAN_POINT ( 'NONE',  ( -7.611372734017124664, 43.12018948500615778, 75.45433879953087342 ) ) ;
#15273=DIRECTION ( 'NONE',  ( 1.540237394707284220E-16, 1.793354297423764243E-16, -1.000000000000000000 ) ) ;
#15274=CARTESIAN_POINT ( 'NONE',  ( -7.077609990433002096, 44.22210830145579763, 72.45432679953087529 ) ) ;
#15275=B_SPLINE_CURVE_WITH_KNOTS ( 'NONE', 3,
 ( #16727, #2469, #542, #20435, #7244, #16832, #17145, #5429, #12051, #650, #18422, #7022, #11836, #18309, #13839, #5546 ),
 .UNSPECIFIED., .F., .F.,
 ( 4, 2, 2, 2, 2, 2, 2, 4 ),
 ( 0.000000000000000000, 0.0002723625545810964919, 0.0005447251091621929837, 0.001089450218324406784, 0.001361812772905513684, 0.001634175327486620368, 0.001906537882067727485, 0.002178900436648834385 ),
 .UNSPECIFIED. ) ;
#15276=ORIENTED_EDGE ( 'NONE', *, *, #12314, .F. ) ;
#15278=AXIS2_PLACEMENT_3D ( 'NONE', #14082, #15894, #6087 ) ;
#15280=VERTEX_POINT ( 'NONE', #13644 ) ;
#15281=CARTESIAN_POINT ( 'NONE',  ( -4.445462123736771076, 50.68136173637071096, 76.24916814194597237 ) ) ;
#15282=DIRECTION ( 'NONE',  ( -1.540237394707284220E-16, -1.793354297423764243E-16, 1.000000000000000000 ) ) ;
#15283=VECTOR ( 'NONE', #15845, 1000.000000000000114 ) ;
#15284=CARTESIAN_POINT ( 'NONE',  ( -4.894326847483571719, 37.22270278754029960, 76.26481528174605273 ) ) ;
#15287=AXIS2_PLACEMENT_3D ( 'NONE', #12242, #19118, #19312 ) ;
#15288=DIRECTION ( 'NONE',  ( -0.3165065846431827090, -0.9485903129789527988, 0.000000000000000000 ) ) ;
#15289=EDGE_CURVE ( 'NONE', #16499, #10028, #8333, .T. ) ;
#15292=CARTESIAN_POINT ( 'NONE',  ( 2.032153066220215631, 52.20217092279865767, 76.00457246026148539 ) ) ;
#15294=AXIS2_PLACEMENT_3D ( 'NONE', #8039, #19519, #14526 ) ;
#15298=CARTESIAN_POINT ( 'NONE',  ( -7.210081352984018643, 41.43222958516458476, 78.77893318671775091 ) ) ;
#15299=ORIENTED_EDGE ( 'NONE', *, *, #4557, .T. ) ;
#15300=EDGE_LOOP ( 'NONE', ( #14302, #2081, #18061, #5359 ) ) ;
#15302=CARTESIAN_POINT ( 'NONE',  ( -5.955451856753747997, 38.00651308716548726, 78.18375056423674607 ) ) ;
#15305=CARTESIAN_POINT ( 'NONE',  ( 2.119851040271390374, 52.81592988514039178, 76.48963291717792856 ) ) ;
#15307=DIRECTION ( 'NONE',  ( 0.3165065846431826535, 0.9485903129789529098, 2.188653791613874008E-16 ) ) ;
#15308=CARTESIAN_POINT ( 'NONE',  ( 0.5221537403065009686, 44.16218137147968292, 79.40903933791013003 ) ) ;
#15311=CARTESIAN_POINT ( 'NONE',  ( 0.7823402848519026564, 52.35267412999201042, 77.46299673659909502 ) ) ;
#15313=VECTOR ( 'NONE', #15777, 1000.000000000000000 ) ;
#15315=CARTESIAN_POINT ( 'NONE',  ( 4.290864208700578608, 51.39396841940111926, 75.72008365543779007 ) ) ;
#15318=CARTESIAN_POINT ( 'NONE',  ( -7.948766803159697858, 41.75119145221206196, 78.75998376317852490 ) ) ;
#15319=ORIENTED_EDGE ( 'NONE', *, *, #8479, .F. ) ;
#15320=PLANE ( 'NONE',  #11201 ) ;
#15321=B_SPLINE_CURVE_WITH_KNOTS ( 'NONE', 3,
 ( #6329, #19009, #20692, #16142, #17518, #11257, #17727, #3159 ),
 .UNSPECIFIED., .F., .F.,
 ( 4, 2, 2, 4 ),
 ( 0.000000000000000000, 0.0002990901329414861185, 0.0004486351994122288796, 0.0005981802658829716950 ),
 .UNSPECIFIED. ) ;
#15324=EDGE_CURVE ( 'NONE', #14379, #6954, #11744, .T. ) ;
#15328=CARTESIAN_POINT ( 'NONE',  ( -4.603341302083753028, 37.00776348676620842, 77.20593245741272881 ) ) ;
#15330=CARTESIAN_POINT ( 'NONE',  ( 1.087740465381641375, 52.94398708878058102, 76.77198585835439815 ) ) ;
#15331=CARTESIAN_POINT ( 'NONE',  ( 5.847431522242757751, 51.16902779423016767, 77.98758453411963387 ) ) ;
#15333=CARTESIAN_POINT ( 'NONE',  ( 8.913594855155908547, 41.50833375100289402, 79.54698768757486960 ) ) ;
#15335=CARTESIAN_POINT ( 'NONE',  ( 8.951594291416542504, 41.62222047211530906, 76.36070165242202279 ) ) ;
#15338=CARTESIAN_POINT ( 'NONE',  ( 5.631785411401764918, 36.99756487055721976, 77.76022115247205591 ) ) ;
#15341=CARTESIAN_POINT ( 'NONE',  ( 2.421193248165596668, 49.85372324935340060, 82.45433879953087342 ) ) ;
#15342=CARTESIAN_POINT ( 'NONE',  ( -7.088838830337594210, 47.02440864255881081, 77.61879955032603107 ) ) ;
#15344=B_SPLINE_SURFACE_WITH_KNOTS ( 'NONE', 3, 1, ( 
 ( #12514, #18996 ),
 ( #7722, #4413 ),
 ( #11034, #6115 ),
 ( #17403, #2830 ),
 ( #2928, #1231 ),
 ( #14204, #12620 ),
 ( #17504, #16025 ),
 ( #8245, #19300 ),
 ( #16129, #4827 ),
 ( #1547, #6221 ),
 ( #16334, #19198 ),
 ( #6316, #4613 ),
 ( #53, #7828 ),
 ( #8033, #13040 ),
 ( #12720, #14732 ),
 ( #4714, #154 ),
 ( #11135, #20986 ),
 ( #1443, #3245 ),
 ( #14520, #6420 ) ),
 .UNSPECIFIED., .F., .F., .F.,
 ( 4, 1, 1, 1, 1, 1, 1, 1, 1, 1, 1, 1, 1, 1, 1, 1, 4 ),
 ( 2, 2 ),
 ( 0.000000000000000000, 0.05434379794353864229, 0.1062390698768248820, 0.1553778989748225425, 0.2029887854916514467, 0.2486500052201169320, 0.2921085583616858661, 0.3352193261980264682, 0.3771870632897987852, 0.4223876994541358454, 0.4752030700363142346, 0.5373302487560115415, 0.6091097927081512431, 0.6911313100281405442, 0.7836801803933998167, 0.8864064767870927231, 1.000000000000000000 ),
 ( 0.000000000000000000, 1.000000000000000000 ),
 .UNSPECIFIED. ) ;
#15345=CARTESIAN_POINT ( 'NONE',  ( 6.658811665516601863, 37.73144022991658630, 75.70392102816973079 ) ) ;
#15346=ORIENTED_EDGE ( 'NONE', *, *, #11714, .F. ) ;
#15347=CARTESIAN_POINT ( 'NONE',  ( 5.574007247060956516, 50.61635935010243514, 77.05868164888072158 ) ) ;
#15350=PLANE ( 'NONE',  #7132 ) ;
#15351=VECTOR ( 'NONE', #8427, 1000.000000000000114 ) ;
#15356=CARTESIAN_POINT ( 'NONE',  ( -3.355600405723123902, 52.20705244989922988, 78.36353918055804968 ) ) ;
#15362=LINE ( 'NONE', #3958, #12903 ) ;
#15363=ORIENTED_EDGE ( 'NONE', *, *, #10714, .T. ) ;
#15367=PLANE ( 'NONE',  #20970 ) ;
#15368=CARTESIAN_POINT ( 'NONE',  ( 6.030184373421643151, 51.03403562479821431, 79.53335372712579954 ) ) ;
#15369=CARTESIAN_POINT ( 'NONE',  ( 6.522436035574397550, 49.75115376156129798, 75.45433879953087342 ) ) ;
#15370=VECTOR ( 'NONE', #7939, 1000.000000000000114 ) ;
#15372=CARTESIAN_POINT ( 'NONE',  ( 6.267060310175591731, 50.01365258206436692, 79.25094314227297332 ) ) ;
#15376=CARTESIAN_POINT ( 'NONE',  ( 8.284287939682402069, 41.54251913719888734, 78.93613448519710118 ) ) ;
#15377=EDGE_CURVE ( 'NONE', #496, #1879, #4167, .T. ) ;
#15378=ORIENTED_EDGE ( 'NONE', *, *, #253, .F. ) ;
#15379=CARTESIAN_POINT ( 'NONE',  ( -7.202537930885374529, 41.41097462079392955, 78.61536821129558916 ) ) ;
#15382=CARTESIAN_POINT ( 'NONE',  ( -7.208606195151301854, 41.85401949100505448, 77.76017221056694950 ) ) ;
#15385=CARTESIAN_POINT ( 'NONE',  ( 0.5021497504818818181, 52.96224978603238043, 77.38972049658568153 ) ) ;
#15386=B_SPLINE_CURVE_WITH_KNOTS ( 'NONE', 3,
 ( #3905, #13394, #18383, #10213, #15095, #10428, #14987, #505, #8711, #7316, #6982, #18595, #2429, #13488 ),
 .UNSPECIFIED., .F., .F.,
 ( 4, 2, 2, 2, 2, 2, 4 ),
 ( 0.000000000000000000, 0.0006081318354814772235, 0.0009121977532222158352, 0.001216263670962954230, 0.001824395506444449885, 0.002128461424185192508, 0.002432527341925936649 ),
 .UNSPECIFIED. ) ;
#15387=CARTESIAN_POINT ( 'NONE',  ( 5.632375035844972899, 36.99798619459680538, 75.36061873398452349 ) ) ;
#15388=CARTESIAN_POINT ( 'NONE',  ( -4.804534436424639843, 51.17169724042062739, 78.47639829077699858 ) ) ;
#15391=FACE_BOUND ( 'NONE', #6461, .T. ) ;
#15393=ORIENTED_EDGE ( 'NONE', *, *, #17392, .T. ) ;
#15394=CARTESIAN_POINT ( 'NONE',  ( -4.429725150862205751, 50.69260680101952232, 76.11505395997643575 ) ) ;
#15398=CARTESIAN_POINT ( 'NONE',  ( 6.153536035488349043, 50.12267912296926653, 77.68963291717793140 ) ) ;
#15400=CARTESIAN_POINT ( 'NONE',  ( 0.4081407667913234394, 52.96145465813116004, 78.87521754079256198 ) ) ;
#15401=CARTESIAN_POINT ( 'NONE',  ( -7.230623167723755351, 41.49097751518757349, 78.30226502014330947 ) ) ;
#15404=CARTESIAN_POINT ( 'NONE',  ( 2.078566409199763765, 52.20180493653207776, 76.15080458372598571 ) ) ;
#15408=VERTEX_POINT ( 'NONE', #2574 ) ;
#15411=CARTESIAN_POINT ( 'NONE',  ( 4.396638484636539168, 51.32665516437340614, 79.26957207196610966 ) ) ;
#15415=CARTESIAN_POINT ( 'NONE',  ( 0.5221537403065015237, 44.16218137147968292, 75.45433879953088763 ) ) ;
#15418=CARTESIAN_POINT ( 'NONE',  ( 0.8140313835477279714, 52.35242423403212086, 77.51877209028926075 ) ) ;
#15420=DIRECTION ( 'NONE',  ( 0.8033560671169786005, 0.5954989751681698529, 2.305299702067830011E-16 ) ) ;
#15422=CARTESIAN_POINT ( 'NONE',  ( -4.348661956197086731, 37.56557963644259956, 78.93669174070734584 ) ) ;
#15426=DIRECTION ( 'NONE',  ( -0.5941461771851693774, -0.8043570849667760481, -2.357623395011396791E-16 ) ) ;
#15430=CARTESIAN_POINT ( 'NONE',  ( -4.877877647307895970, 37.21055242598473001, 76.09452555557021469 ) ) ;
#15431=CARTESIAN_POINT ( 'NONE',  ( -8.275363242949740794, 42.78218605590705437, 78.99227765976493743 ) ) ;
#15432=CARTESIAN_POINT ( 'NONE',  ( 5.427780505986065762, 36.85179043424346190, 77.43080938776617472 ) ) ;
#15434=VERTEX_POINT ( 'NONE', #17563 ) ;
#15436=CARTESIAN_POINT ( 'NONE',  ( 8.534545774096850224, 42.73671765915654674, 79.25343573416346032 ) ) ;
#15437=CARTESIAN_POINT ( 'NONE',  ( 8.214799251806553571, 41.32260305165857517, 77.14698585835439815 ) ) ;
#15438=LINE ( 'NONE', #10456, #12323 ) ;
#15440=CARTESIAN_POINT ( 'NONE',  ( 5.571366797620176392, 51.37294568574342435, 77.09285305542944400 ) ) ;
#15441=CARTESIAN_POINT ( 'NONE',  ( 9.131267103411046193, 42.16071128789349132, 78.09998440036279987 ) ) ;
#15444=CARTESIAN_POINT ( 'NONE',  ( -3.652148518534829247, 36.30515569394113129, 77.93013364623398331 ) ) ;
#15446=DIRECTION ( 'NONE',  ( 1.540237394707284220E-16, 1.793354297423764243E-16, -1.000000000000000000 ) ) ;
#15448=ORIENTED_EDGE ( 'NONE', *, *, #1941, .F. ) ;
#15449=CARTESIAN_POINT ( 'NONE',  ( 5.939849532777430774, 51.10076233267274404, 76.96076274685535168 ) ) ;
#15451=EDGE_CURVE ( 'NONE', #14291, #16499, #440, .T. ) ;
#15452=CARTESIAN_POINT ( 'NONE',  ( -4.424094442032265206, 50.69663029939598431, 78.82882669246485818 ) ) ;
#15454=VERTEX_POINT ( 'NONE', #12573 ) ;
#15456=LINE ( 'NONE', #13534, #17961 ) ;
#15457=CARTESIAN_POINT ( 'NONE',  ( -3.373742936343101739, 52.19408846175863204, 78.58955347608575437 ) ) ;
#15458=CARTESIAN_POINT ( 'NONE',  ( 0.8019072594418875655, 52.95773867775533716, 77.48431196819693412 ) ) ;
#15459=CARTESIAN_POINT ( 'NONE',  ( 0.3395551853511908913, 52.36014964445268305, 77.58553591360387713 ) ) ;
#15460=DIRECTION ( 'NONE',  ( -0.5941461771851693774, -0.8043570849667760481, -2.357623395011396791E-16 ) ) ;
#15461=VERTEX_POINT ( 'NONE', #9493 ) ;
#15462=CARTESIAN_POINT ( 'NONE',  ( 5.262940487106410714, 50.85284745661634531, 78.03948491463276582 ) ) ;
#15464=EDGE_LOOP ( 'NONE', ( #7523, #17806, #11716, #5324 ) ) ;
#15466=CARTESIAN_POINT ( 'NONE',  ( 4.539621438837683876, 52.13505442103787857, 76.64209438045911327 ) ) ;
#15467=CARTESIAN_POINT ( 'NONE',  ( 2.119851040271389930, 52.81592988514039178, 78.16610350541323271 ) ) ;
#15469=CARTESIAN_POINT ( 'NONE',  ( 7.862039597456297102, 47.81814697137103565, 79.15362846919002493 ) ) ;
#15470=ADVANCED_FACE ( 'NONE', ( #19065 ), #367, .T. ) ;
#15471=LINE ( 'NONE', #17269, #11185 ) ;
#15473=DIRECTION ( 'NONE',  ( -0.9534635866061452747, -0.3015081906286225522, -2.009271279954815797E-16 ) ) ;
#15474=B_SPLINE_SURFACE_WITH_KNOTS ( 'NONE', 3, 1, ( 
 ( #5003, #4584 ),
 ( #9507, #15991 ),
 ( #8106, #14596 ),
 ( #16303, #1735 ),
 ( #14699, #13108 ),
 ( #19894, #12048 ),
 ( #3420, #3837 ),
 ( #7018, #18418 ),
 ( #9931, #3527 ),
 ( #15020, #8648 ),
 ( #19993, #18205 ),
 ( #10031, #5315 ),
 ( #2038, #3625 ),
 ( #13214, #8535 ),
 ( #6708, #10358 ),
 ( #11831, #16828 ),
 ( #16414, #10135 ),
 ( #13519, #439 ),
 ( #6922, #16724 ),
 ( #222, #16617 ),
 ( #1837, #645 ),
 ( #13323, #5216 ),
 ( #14798, #13426 ) ),
 .UNSPECIFIED., .F., .F., .F.,
 ( 4, 1, 1, 1, 1, 1, 1, 1, 1, 1, 1, 1, 1, 1, 1, 1, 1, 1, 1, 1, 4 ),
 ( 2, 2 ),
 ( 0.000000000000000000, 0.04996570031508023452, 0.09882111805538688898, 0.1466986691414003396, 0.1933343388926866968, 0.2389025989959846497, 0.2841336389028531473, 0.3290918654023432532, 0.3737715338516285901, 0.4170420466396844161, 0.4581370997277735002, 0.4966756662638874276, 0.5332138716254802846, 0.5686376898124313461, 0.6026332556748308367, 0.6353084426624004966, 0.6676556782331927176, 0.7363269649188709520, 0.8138826302435128168, 0.9017756963292008487, 1.000000000000000000 ),
 ( 0.000000000000000000, 1.000000000000000000 ),
 .UNSPECIFIED. ) ;
#15478=EDGE_CURVE ( 'NONE', #7860, #10020, #19161, .T. ) ;
#15479=ORIENTED_EDGE ( 'NONE', *, *, #6250, .F. ) ;
#15481=ADVANCED_FACE ( 'NONE', ( #19653 ), #11594, .F. ) ;
#15483=CARTESIAN_POINT ( 'NONE',  ( -8.139710801171299082, 42.34786680499500733, 76.77997794206987692 ) ) ;
#15487=LINE ( 'NONE', #16866, #2486 ) ;
#15488=ORIENTED_EDGE ( 'NONE', *, *, #3595, .T. ) ;
#15489=CARTESIAN_POINT ( 'NONE',  ( 5.201216021426783520, 36.68989574863261538, 75.41205140984322952 ) ) ;
#15490=CARTESIAN_POINT ( 'NONE',  ( -0.9504375969237850441, 51.37401713635502887, 77.21536821129558348 ) ) ;
#15493=CARTESIAN_POINT ( 'NONE',  ( 1.132007891697332846, 52.34004019480227754, 79.51057667246605831 ) ) ;
#15500=CARTESIAN_POINT ( 'NONE',  ( -3.533008836142935927, 36.21715200979740246, 78.43912781517941823 ) ) ;
#15501=CARTESIAN_POINT ( 'NONE',  ( 5.317959575120520199, 50.80701191653712101, 78.92241520643889885 ) ) ;
#15503=ORIENTED_EDGE ( 'NONE', *, *, #4183, .F. ) ;
#15504=CARTESIAN_POINT ( 'NONE',  ( 2.100548972721439256, 52.95446970717261337, 76.22990676838142576 ) ) ;
#15505=VERTEX_POINT ( 'NONE', #1898 ) ;
#15506=CARTESIAN_POINT ( 'NONE',  ( -0.8350644498690075190, 52.24919065719213762, 78.94532217087298420 ) ) ;
#15507=EDGE_CURVE ( 'NONE', #15510, #1549, #3489, .T. ) ;
#15510=VERTEX_POINT ( 'NONE', #16477 ) ;
#15512=CARTESIAN_POINT ( 'NONE',  ( 6.117874454611452961, 50.05524748896710463, 79.34836068132329956 ) ) ;
#15514=CARTESIAN_POINT ( 'NONE',  ( 4.335841838902815937, 51.37156319753863443, 79.19424447893550223 ) ) ;
#15515=CARTESIAN_POINT ( 'NONE',  ( 0.5221537403065014127, 44.16218137147968292, 76.16022115247204738 ) ) ;
#15517=CARTESIAN_POINT ( 'NONE',  ( -4.517974409599069041, 36.94470640207596546, 78.25995115514949418 ) ) ;
#15518=CARTESIAN_POINT ( 'NONE',  ( -4.383473025373058718, 51.47257230871590394, 76.47051527011910821 ) ) ;
#15519=CARTESIAN_POINT ( 'NONE',  ( -0.1944850259765472933, 35.99355670886600933, 76.86610350541323555 ) ) ;
#15521=DIRECTION ( 'NONE',  ( 0.9429220365244121993, -0.3330135628418984250, 8.551124769255302663E-17 ) ) ;
#15522=CARTESIAN_POINT ( 'NONE',  ( -5.403172002243911365, 49.82415717112796472, 76.65235776097600251 ) ) ;
#15523=CARTESIAN_POINT ( 'NONE',  ( 4.942331607238935831, 51.83758864179496584, 75.54250430092201896 ) ) ;
#15524=EDGE_CURVE ( 'NONE', #14895, #18369, #5502, .T. ) ;
#15526=CARTESIAN_POINT ( 'NONE',  ( -7.302004416484622951, 40.13443851219999914, 78.72624606083481069 ) ) ;
#15527=CARTESIAN_POINT ( 'NONE',  ( 8.951433321995803993, 41.62173803654965099, 78.54183882225588320 ) ) ;
#15532=CARTESIAN_POINT ( 'NONE',  ( -4.539611090124166637, 51.36100176422416297, 79.54777180229389444 ) ) ;
#15534=CARTESIAN_POINT ( 'NONE',  ( -4.570740025688047048, 36.98368223715222314, 77.15538146413656762 ) ) ;
#15535=CARTESIAN_POINT ( 'NONE',  ( -7.604387687253306716, 43.11263983757604024, 78.56936110682462981 ) ) ;
#15536=CARTESIAN_POINT ( 'NONE',  ( 8.647930352917317265, 43.06138273419885820, 77.20731746004976515 ) ) ;
#15537=CARTESIAN_POINT ( 'NONE',  ( -4.219041845479045705, 37.47853290070158039, 76.02016401025396419 ) ) ;
#15539=VERTEX_POINT ( 'NONE', #18487 ) ;
#15540=CARTESIAN_POINT ( 'NONE',  ( 8.279961632505596469, 41.50566914870238122, 78.93448121625959857 ) ) ;
#15541=CARTESIAN_POINT ( 'NONE',  ( 8.787829143201870252, 41.13140593384865440, 77.14698585835439815 ) ) ;
#15542=CARTESIAN_POINT ( 'NONE',  ( 8.921551879414991504, 41.53218145749156776, 76.03029119948048731 ) ) ;
#15544=CARTESIAN_POINT ( 'NONE',  ( 5.349754812510225221, 50.78352605546763954, 77.95044976498417100 ) ) ;
#15545=B_SPLINE_CURVE_WITH_KNOTS ( 'NONE', 3,
 ( #20012, #2485, #777, #7259, #15462, #15568, #8764, #11850 ),
 .UNSPECIFIED., .F., .F.,
 ( 4, 2, 2, 4 ),
 ( 0.000000000000000000, 0.0001162705178784993038, 0.0002325410357569986076, 0.0004650820715139567202 ),
 .UNSPECIFIED. ) ;
#15547=CARTESIAN_POINT ( 'NONE',  ( 8.421385860420697256, 42.39757021913804635, 78.09998440036279987 ) ) ;
#15554=EDGE_LOOP ( 'NONE', ( #1936, #19674, #448, #15117 ) ) ;
#15555=CARTESIAN_POINT ( 'NONE',  ( 5.547944990773469698, 50.63561048897027916, 77.19464465032660883 ) ) ;
#15556=EDGE_LOOP ( 'NONE', ( #19805, #16517, #16932, #9838 ) ) ;
#15558=CARTESIAN_POINT ( 'NONE',  ( -4.802657821332910082, 51.17303820085790278, 78.59458524649963351 ) ) ;
#15560=ORIENTED_EDGE ( 'NONE', *, *, #13589, .T. ) ;
#15563=CARTESIAN_POINT ( 'NONE',  ( 0.3821786226492924210, 35.36301154328572949, 78.57639762306027365 ) ) ;
#15564=CARTESIAN_POINT ( 'NONE',  ( -1.493738069816089364, 38.45421922485636657, 75.45433879953087342 ) ) ;
#15568=CARTESIAN_POINT ( 'NONE',  ( 5.242206828355853609, 50.86750652479793189, 78.15346193224233673 ) ) ;
#15571=DIRECTION ( 'NONE',  ( -0.9534635866061452747, -0.3015081906286226077, -2.009271279954815304E-16 ) ) ;
#15575=CARTESIAN_POINT ( 'NONE',  ( -7.292692585215720946, 46.64628091931714948, 79.36031032450011935 ) ) ;
#15576=CARTESIAN_POINT ( 'NONE',  ( 8.787829143201870252, 41.13140593384865440, 78.45948585835439815 ) ) ;
#15577=CARTESIAN_POINT ( 'NONE',  ( -4.322630238256937041, 37.54627981234005318, 77.92970022298523247 ) ) ;
#15578=CARTESIAN_POINT ( 'NONE',  ( 5.277046726144507538, 37.48121749977929795, 78.28595324781899478 ) ) ;
#15580=FACE_OUTER_BOUND ( 'NONE', #10296, .T. ) ;
#15581=CIRCLE ( 'NONE', #3675, 8.199999999999995737 ) ;
#15582=ORIENTED_EDGE ( 'NONE', *, *, #8155, .F. ) ;
#15584=ADVANCED_FACE ( 'NONE', ( #9025 ), #501, .T. ) ;
#15586=CARTESIAN_POINT ( 'NONE',  ( -7.398469273655679856, 42.45442617122637330, 76.93555611204594413 ) ) ;
#15587=EDGE_LOOP ( 'NONE', ( #7568, #20436, #7459, #16964 ) ) ;
#15589=CARTESIAN_POINT ( 'NONE',  ( 2.447781712115293828, 38.42313889284341144, 75.45433879953087342 ) ) ;
#15590=FACE_BOUND ( 'NONE', #11563, .T. ) ;
#15592=DIRECTION ( 'NONE',  ( 0.2896293787568423594, -0.9158990529585747664, 0.2779275944387522568 ) ) ;
#15594=EDGE_CURVE ( 'NONE', #4812, #10826, #604, .T. ) ;
#15596=DIRECTION ( 'NONE',  ( -1.540237394707284467E-16, -1.793354297423764243E-16, 1.000000000000000000 ) ) ;
#15597=CARTESIAN_POINT ( 'NONE',  ( 0.7971270633857517884, 52.35255750736508418, 78.82560697059345500 ) ) ;
#15598=ORIENTED_EDGE ( 'NONE', *, *, #13251, .F. ) ;
#15599=CARTESIAN_POINT ( 'NONE',  ( -5.329330622855473543, 49.90705297800482754, 78.91939974476616726 ) ) ;
#15600=CARTESIAN_POINT ( 'NONE',  ( 5.122276503711423956, 37.37399599821077345, 76.07344584094424533 ) ) ;
#15601=EDGE_CURVE ( 'NONE', #8055, #476, #18378, .T. ) ;
#15605=CARTESIAN_POINT ( 'NONE',  ( 5.438900134727234992, 36.85973611382630821, 76.29939265556315320 ) ) ;
#15606=CARTESIAN_POINT ( 'NONE',  ( 5.521494261397323022, 36.91875485278077207, 76.01263398532663018 ) ) ;
#15607=DIRECTION ( 'NONE',  ( -0.3165065846431826535, -0.9485903129789527988, 0.000000000000000000 ) ) ;
#15609=EDGE_CURVE ( 'NONE', #14794, #6491, #2310, .T. ) ;
#15610=CARTESIAN_POINT ( 'NONE',  ( 1.472692277483312218, 52.20658247672307795, 75.49332451037695080 ) ) ;
#15615=ORIENTED_EDGE ( 'NONE', *, *, #18306, .F. ) ;
#15616=AXIS2_PLACEMENT_3D ( 'NONE', #6933, #13437, #17804 ) ;
#15617=VERTEX_POINT ( 'NONE', #2530 ) ;
#15619=ORIENTED_EDGE ( 'NONE', *, *, #14847, .F. ) ;
#15621=DIRECTION ( 'NONE',  ( -0.5941461771851692664, -0.8043570849667761591, -2.357623395011396791E-16 ) ) ;
#15622=CARTESIAN_POINT ( 'NONE',  ( 8.385851074499695912, 39.92665216093506331, 76.98031643592585738 ) ) ;
#15625=DIRECTION ( 'NONE',  ( 0.9999689119394085113, -0.007885122365285377952, 1.526048693634335642E-16 ) ) ;
#15626=CARTESIAN_POINT ( 'NONE',  ( -7.511311626346421022, 40.36128364442370042, 79.17963929739188700 ) ) ;
#15627=LINE ( 'NONE', #2537, #5085 ) ;
#15629=CARTESIAN_POINT ( 'NONE',  ( 0.5221537403065015237, 44.16218137147968292, 75.45433879953087342 ) ) ;
#15632=CARTESIAN_POINT ( 'NONE',  ( -5.569494948991628114, 50.62508446513216143, 75.69846806870741318 ) ) ;
#15634=EDGE_CURVE ( 'NONE', #1549, #597, #8808, .T. ) ;
#15637=CARTESIAN_POINT ( 'NONE',  ( -7.777085147165724521, 41.23087250612003629, 79.53766176265342835 ) ) ;
#15638=ADVANCED_FACE ( 'NONE', ( #12212 ), #11603, .T. ) ;
#15639=CARTESIAN_POINT ( 'NONE',  ( 8.950289981099260217, 41.61831137135051506, 78.71610475470291135 ) ) ;
#15640=EDGE_CURVE ( 'NONE', #6443, #10025, #9558, .T. ) ;
#15641=CIRCLE ( 'NONE', #14263, 8.199999999999995737 ) ;
#15642=DIRECTION ( 'NONE',  ( 1.540237394707283727E-16, 1.793354297423763257E-16, -1.000000000000000000 ) ) ;
#15644=DIRECTION ( 'NONE',  ( 1.540237394707284220E-16, 1.793354297423764243E-16, -1.000000000000000000 ) ) ;
#15645=CARTESIAN_POINT ( 'NONE',  ( -3.926839636664805511, 51.79886580987140832, 79.42193487995672285 ) ) ;
#15646=( LENGTH_UNIT ( ) NAMED_UNIT ( * ) SI_UNIT ( .MILLI., .METRE. ) );
#15647=CARTESIAN_POINT ( 'NONE',  ( -8.309364629785569889, 42.88970911912626605, 78.56936110682462981 ) ) ;
#15648=CARTESIAN_POINT ( 'NONE',  ( 0.5221537403065015237, 44.16218137147968292, 75.45433879953088763 ) ) ;
#15649=AXIS2_PLACEMENT_3D ( 'NONE', #20255, #8690, #702 ) ;
#15650=ORIENTED_EDGE ( 'NONE', *, *, #14055, .F. ) ;
#15651=VECTOR ( 'NONE', #13143, 1000.000000000000227 ) ;
#15652=CARTESIAN_POINT ( 'NONE',  ( 9.347650859976274873, 42.80922713344904196, 78.67881838835081965 ) ) ;
#15653=CARTESIAN_POINT ( 'NONE',  ( -4.152600114974411838, 50.89932002992104998, 75.97646144330421691 ) ) ;
#15655=CARTESIAN_POINT ( 'NONE',  ( 5.908589799165438805, 51.12385263867304275, 77.19464465032660883 ) ) ;
#15656=B_SPLINE_SURFACE_WITH_KNOTS ( 'NONE', 3, 1, ( 
 ( #9067, #10685 ),
 ( #7674, #866 ),
 ( #2568, #12053 ),
 ( #3945, #18845 ),
 ( #9287, #4358 ),
 ( #13841, #15666 ),
 ( #17045, #15555 ),
 ( #7350, #7574 ),
 ( #8964, #20111 ),
 ( #971, #10469 ),
 ( #16933, #15347 ),
 ( #10884, #7246 ),
 ( #15449, #20437 ),
 ( #12370, #4256 ),
 ( #5645, #2784 ) ),
 .UNSPECIFIED., .F., .F., .F.,
 ( 4, 1, 1, 1, 1, 1, 1, 1, 1, 1, 1, 1, 4 ),
 ( 2, 2 ),
 ( 0.000000000000000000, 0.1112587825215290704, 0.2075697215801151074, 0.2973595701983123840, 0.3838682041569268510, 0.4304545292676484891, 0.4853887544929457731, 0.5479167518276804039, 0.6204346596782769341, 0.7008860551074163059, 0.7907659637769564043, 0.8904818903857688595, 1.000000000000000000 ),
 ( 0.000000000000000000, 1.000000000000000000 ),
 .UNSPECIFIED. ) ;
#15658=VECTOR ( 'NONE', #1289, 1000.000000000000000 ) ;
#15659=CARTESIAN_POINT ( 'NONE',  ( 8.532965227243460404, 42.73198065996890449, 77.95057265855270145 ) ) ;
#15664=CARTESIAN_POINT ( 'NONE',  ( -4.359893715479207899, 37.57388776543446340, 75.36022115247205022 ) ) ;
#15666=CARTESIAN_POINT ( 'NONE',  ( 5.534096227355138176, 50.64584001264518065, 77.22227766523002401 ) ) ;
#15671=ORIENTED_EDGE ( 'NONE', *, *, #10579, .T. ) ;
#15673=CARTESIAN_POINT ( 'NONE',  ( -0.8988261294859191119, 52.21915217126601050, 76.13122899883298089 ) ) ;
#15674=CARTESIAN_POINT ( 'NONE',  ( 8.850612593395874583, 41.31957191698789700, 78.01079203130994699 ) ) ;
#15676=PLANE ( 'NONE',  #7718 ) ;
#15677=CARTESIAN_POINT ( 'NONE',  ( -4.895593109503408868, 37.22363812428621088, 78.53742703482498655 ) ) ;
#15678=ORIENTED_EDGE ( 'NONE', *, *, #7288, .F. ) ;
#15679=PLANE ( 'NONE',  #10207 ) ;
#15680=ORIENTED_EDGE ( 'NONE', *, *, #647, .T. ) ;
#15684=LINE ( 'NONE', #1307, #9646 ) ;
#15686=CARTESIAN_POINT ( 'NONE',  ( -4.158578283022523969, 37.42937009194850617, 78.34992703482498655 ) ) ;
#15687=CARTESIAN_POINT ( 'NONE',  ( -4.756616962678585026, 37.12098204292738757, 75.36046818803191627 ) ) ;
#15689=B_SPLINE_CURVE_WITH_KNOTS ( 'NONE', 3,
 ( #14032, #20405, #9039, #15844, #15526, #5836, #12342, #12540, #17330, #2648, #1368, #941, #18820, #15637, #20513, #7857 ),
 .UNSPECIFIED., .F., .F.,
 ( 4, 2, 2, 2, 2, 2, 2, 4 ),
 ( 0.000000000000000000, 0.0001315995296408621585, 0.0002631990592817243170, 0.0005263981185634489593, 0.0007895971778451736558, 0.001052796237126898135, 0.001579194355690331482, 0.002105592474253764612 ),
 .UNSPECIFIED. ) ;
#15690=VERTEX_POINT ( 'NONE', #17312 ) ;
#15691=CARTESIAN_POINT ( 'NONE',  ( 0.5221537403065008576, 44.16218137147968292, 80.45433879953087342 ) ) ;
#15693=EDGE_LOOP ( 'NONE', ( #19008, #19116, #3760, #18759 ) ) ;
#15696=CARTESIAN_POINT ( 'NONE',  ( 5.531249400824703955, 51.40257879072892422, 75.36789977960694387 ) ) ;
#15697=ORIENTED_EDGE ( 'NONE', *, *, #18545, .F. ) ;
#15698=EDGE_CURVE ( 'NONE', #9664, #4990, #10279, .T. ) ;
#15700=LINE ( 'NONE', #16109, #3150 ) ;
#15701=CARTESIAN_POINT ( 'NONE',  ( -4.517072128342573656, 36.94403992325788977, 78.58080938776616620 ) ) ;
#15703=ORIENTED_EDGE ( 'NONE', *, *, #11293, .T. ) ;
#15705=CARTESIAN_POINT ( 'NONE',  ( -5.917125461193805336, 40.64525615903904310, 75.45433879953087342 ) ) ;
#15710=( GEOMETRIC_REPRESENTATION_CONTEXT ( 3 ) GLOBAL_UNCERTAINTY_ASSIGNED_CONTEXT ( ( #9772 ) ) GLOBAL_UNIT_ASSIGNED_CONTEXT ( ( #15646, #12547, #7438 ) ) REPRESENTATION_CONTEXT ( 'NONE', 'WORKASPACE' ) );
#15714=CARTESIAN_POINT ( 'NONE',  ( 5.434476177758928550, 36.85657491614816195, 76.36627918048426977 ) ) ;
#15715=CARTESIAN_POINT ( 'NONE',  ( 8.790110392356673685, 41.13824298228534104, 76.23356602378127889 ) ) ;
#15716=CARTESIAN_POINT ( 'NONE',  ( -7.347204055457580374, 41.85239250246546305, 77.69936312477425133 ) ) ;
#15718=CARTESIAN_POINT ( 'NONE',  ( 2.112264789766074458, 52.95437732364958094, 76.31288873172051979 ) ) ;
#15719=ORIENTED_EDGE ( 'NONE', *, *, #4670, .F. ) ;
#15721=CARTESIAN_POINT ( 'NONE',  ( 6.154942347677927472, 50.94188193477284443, 75.39427037473855364 ) ) ;
#15724=VECTOR ( 'NONE', #9273, 1000.000000000000227 ) ;
#15726=ORIENTED_EDGE ( 'NONE', *, *, #16614, .T. ) ;
#15727=ORIENTED_EDGE ( 'NONE', *, *, #17314, .F. ) ;
#15728=CARTESIAN_POINT ( 'NONE',  ( -3.763323997310421554, 36.38727654169121450, 75.66260743385902288 ) ) ;
#15729=CARTESIAN_POINT ( 'NONE',  ( -5.208859716003345852, 50.02743738586465838, 75.74732467541012682 ) ) ;
#15731=CARTESIAN_POINT ( 'NONE',  ( -6.427915807670530945, 42.26053564693651055, 78.13669174070733447 ) ) ;
#15732=DIRECTION ( 'NONE',  ( -0.9485903129789495791, 0.3165065846431928120, -8.934458285744765648E-17 ) ) ;
#15735=CARTESIAN_POINT ( 'NONE',  ( 5.424439005889565735, 37.58880062289685497, 77.71652930830589412 ) ) ;
#15736=CARTESIAN_POINT ( 'NONE',  ( -6.711977078592299861, 40.31944429845940903, 78.72343487459158951 ) ) ;
#15737=LINE ( 'NONE', #17626, #11911 ) ;
#15739=DIRECTION ( 'NONE',  ( -0.8043570849667761591, 0.5941461771851692664, -1.733862608106489734E-17 ) ) ;
#15747=CARTESIAN_POINT ( 'NONE',  ( 8.375217360078613282, 41.81485783204666262, 78.44085888008430629 ) ) ;
#15749=DIRECTION ( 'NONE',  ( 1.540237394707284220E-16, 1.793354297423764243E-16, -1.000000000000000000 ) ) ;
#15750=LINE ( 'NONE', #17334, #7196 ) ;
#15751=CARTESIAN_POINT ( 'NONE',  ( 8.394097411062748648, 39.95136695475236621, 78.67376765716130649 ) ) ;
#15752=LINE ( 'NONE', #1171, #2441 ) ;
#15753=EDGE_CURVE ( 'NONE', #5246, #11086, #5929, .T. ) ;
#15754=ADVANCED_FACE ( 'NONE', ( #5050 ), #168, .T. ) ;
#15755=VECTOR ( 'NONE', #4968, 1000.000000000000000 ) ;
#15759=ORIENTED_EDGE ( 'NONE', *, *, #529, .T. ) ;
#15760=CARTESIAN_POINT ( 'NONE',  ( 8.255316794306208905, 41.43478779768023657, 78.91184774808348834 ) ) ;
#15761=CARTESIAN_POINT ( 'NONE',  ( -4.189188114579791566, 36.70184521026505564, 79.48068319027247242 ) ) ;
#15762=EDGE_CURVE ( 'NONE', #17246, #15617, #4401, .T. ) ;
#15763=LINE ( 'NONE', #2771, #15724 ) ;
#15764=DIRECTION ( 'NONE',  ( -0.9534635866061452747, -0.3015081906286225522, -2.009271279954815797E-16 ) ) ;
#15765=ADVANCED_FACE ( 'NONE', ( #17497 ), #4936, .F. ) ;
#15767=CARTESIAN_POINT ( 'NONE',  ( -4.159599872275752119, 50.89444720483701445, 78.93089747760657815 ) ) ;
#15773=PLANE ( 'NONE',  #8543 ) ;
#15774=CARTESIAN_POINT ( 'NONE',  ( 5.887048643069795695, 51.13976422295020541, 78.81551702238962775 ) ) ;
#15775=DIRECTION ( 'NONE',  ( 1.540237394707284220E-16, 1.793354297423764243E-16, -1.000000000000000000 ) ) ;
#15776=ORIENTED_EDGE ( 'NONE', *, *, #2434, .F. ) ;
#15777=DIRECTION ( 'NONE',  ( -0.5941461771851693774, -0.8043570849667760481, -2.357623395011396791E-16 ) ) ;
#15779=EDGE_LOOP ( 'NONE', ( #3742, #15809, #7723, #621 ) ) ;
#15780=DIRECTION ( 'NONE',  ( -1.540237394707284220E-16, -1.793354297423764243E-16, 1.000000000000000000 ) ) ;
#15781=VECTOR ( 'NONE', #20793, 1000.000000000000227 ) ;
#15782=CARTESIAN_POINT ( 'NONE',  ( 2.421193248165596668, 49.85372324935340060, 82.45433879953087342 ) ) ;
#15783=CARTESIAN_POINT ( 'NONE',  ( -4.286600153180515349, 50.80436647093155500, 75.97348986337627252 ) ) ;
#15785=CARTESIAN_POINT ( 'NONE',  ( 0.8418751258662160453, 52.35219190451967108, 76.22640136859038762 ) ) ;
#15787=CARTESIAN_POINT ( 'NONE',  ( -3.244219893606751892, 36.91785025630225192, 79.10742496273583413 ) ) ;
#15790=ORIENTED_EDGE ( 'NONE', *, *, #5756, .T. ) ;
#15791=CARTESIAN_POINT ( 'NONE',  ( 6.260406454228516715, 50.01997504955222240, 77.76256480524379811 ) ) ;
#15794=DIRECTION ( 'NONE',  ( 0.3165065846431826535, 0.9485903129789529098, 2.188653791613874008E-16 ) ) ;
#15795=CARTESIAN_POINT ( 'NONE',  ( -4.168645781477386514, 37.43637816616016067, 78.16907664373232478 ) ) ;
#15796=PLANE ( 'NONE',  #17067 ) ;
#15798=DIRECTION ( 'NONE',  ( 1.540237394707284220E-16, 1.793354297423764243E-16, -1.000000000000000000 ) ) ;
#15799=ORIENTED_EDGE ( 'NONE', *, *, #19135, .T. ) ;
#15800=CARTESIAN_POINT ( 'NONE',  ( -2.949171347157247602, 51.57769619255444837, 76.19075138459079710 ) ) ;
#15802=DIRECTION ( 'NONE',  ( 1.540237394707284220E-16, 1.793354297423764243E-16, -1.000000000000000000 ) ) ;
#15804=CARTESIAN_POINT ( 'NONE',  ( -4.574316323987746458, 51.33620267474496757, 79.54845644658969661 ) ) ;
#15807=CARTESIAN_POINT ( 'NONE',  ( -4.165371047737147947, 37.43888844440124331, 78.75608284215286403 ) ) ;
#15808=CARTESIAN_POINT ( 'NONE',  ( -4.451527680475927617, 51.42394294381934117, 78.89116106075270807 ) ) ;
#15809=ORIENTED_EDGE ( 'NONE', *, *, #5185, .T. ) ;
#15810=DIRECTION ( 'NONE',  ( -0.3165065846431827645, -0.9485903129789529098, 0.000000000000000000 ) ) ;
#15811=CARTESIAN_POINT ( 'NONE',  ( 0.7139826536211262287, 52.35321313159215606, 78.90093525964157095 ) ) ;
#15813=CARTESIAN_POINT ( 'NONE',  ( -4.554812065480294159, 50.60227710243181320, 79.52115730712957031 ) ) ;
#15814=CARTESIAN_POINT ( 'NONE',  ( 5.248154646208118557, 37.46097559620424278, 75.97540876731110870 ) ) ;
#15815=B_SPLINE_CURVE_WITH_KNOTS ( 'NONE', 3,
 ( #2269, #18445, #15150, #3750, #2171, #10383, #16852, #20130, #5567, #18550, #3963, #17373 ),
 .UNSPECIFIED., .F., .F.,
 ( 4, 2, 2, 2, 2, 4 ),
 ( 0.000000000000000000, 9.318763199797678004E-05, 0.0001863752639959535601, 0.0002795628959939303266, 0.0003727505279919071201, 0.0007455010559837727153 ),
 .UNSPECIFIED. ) ;
#15817=CARTESIAN_POINT ( 'NONE',  ( 5.074967109082280103, 37.34659833035915710, 76.61095391776262886 ) ) ;
#15818=CARTESIAN_POINT ( 'NONE',  ( 5.649834628789608182, 51.31498465973561451, 78.90029747732744170 ) ) ;
#15819=FACE_OUTER_BOUND ( 'NONE', #15587, .T. ) ;
#15820=ORIENTED_EDGE ( 'NONE', *, *, #12458, .F. ) ;
#15821=CARTESIAN_POINT ( 'NONE',  ( 2.118024385280204314, 52.95416971904506909, 78.36218633565054859 ) ) ;
#15823=ORIENTED_EDGE ( 'NONE', *, *, #8850, .F. ) ;
#15824=CARTESIAN_POINT ( 'NONE',  ( 5.939900590116411472, 51.10072461867315496, 76.38301527011910252 ) ) ;
#15825=DIRECTION ( 'NONE',  ( -1.540237394707284467E-16, -1.793354297423764243E-16, 1.000000000000000000 ) ) ;
#15827=CARTESIAN_POINT ( 'NONE',  ( -2.918060694704116553, 51.60562986935836705, 76.59715360994732691 ) ) ;
#15829=VERTEX_POINT ( 'NONE', #19601 ) ;
#15830=CARTESIAN_POINT ( 'NONE',  ( -4.412760631825748625, 36.86698922270429790, 75.37821288891845484 ) ) ;
#15831=CARTESIAN_POINT ( 'NONE',  ( -6.776146237002087069, 40.42343150244711580, 77.93113452919423878 ) ) ;
#15835=CARTESIAN_POINT ( 'NONE',  ( -6.888911687209406942, 40.65211947644671397, 79.25535243502660876 ) ) ;
#15836=CARTESIAN_POINT ( 'NONE',  ( 8.390845173051939554, 39.94161979111582639, 76.38443001783366526 ) ) ;
#15838=CARTESIAN_POINT ( 'NONE',  ( 6.462272072047026583, 49.81511955649013146, 75.97564824412397400 ) ) ;
#15839=CARTESIAN_POINT ( 'NONE',  ( 5.785641543149844246, 51.21466956273390991, 77.95070864408322109 ) ) ;
#15840=CARTESIAN_POINT ( 'NONE',  ( 6.440194062841372968, 38.48619335307391509, 76.30003524316248331 ) ) ;
#15842=ADVANCED_FACE ( 'NONE', ( #9530 ), #8643, .T. ) ;
#15843=CARTESIAN_POINT ( 'NONE',  ( 8.616653853821931719, 45.47331367307960193, 79.47125056423675460 ) ) ;
#15844=CARTESIAN_POINT ( 'NONE',  ( -7.297414422513008425, 40.12555000982377607, 78.68345068850670998 ) ) ;
#15845=DIRECTION ( 'NONE',  ( 0.007885122365275663500, 0.9999689119394085113, 1.805443505845543142E-16 ) ) ;
#15849=CARTESIAN_POINT ( 'NONE',  ( 8.638826686988997139, 40.68483612003910110, 79.45050910333212357 ) ) ;
#15850=VERTEX_POINT ( 'NONE', #5023 ) ;
#15851=CARTESIAN_POINT ( 'NONE',  ( -7.584911022892848464, 43.05104850827407148, 78.89751519991851580 ) ) ;
#15852=CARTESIAN_POINT ( 'NONE',  ( 5.658108625003792191, 37.01637447524286273, 75.97198585835440099 ) ) ;
#15853=EDGE_CURVE ( 'NONE', #17396, #18944, #10774, .T. ) ;
#15858=DIRECTION ( 'NONE',  ( -0.7938652969193448206, 0.6080936526121289987, -1.322136515275012895E-17 ) ) ;
#15859=CARTESIAN_POINT ( 'NONE',  ( 5.627315617218822119, 51.33161854646183997, 78.02054163389647101 ) ) ;
#15860=CARTESIAN_POINT ( 'NONE',  ( -4.032527917761953518, 50.98089643325306497, 78.50425692432636993 ) ) ;
#15863=ADVANCED_FACE ( 'NONE', ( #11232 ), #3132, .T. ) ;
#15865=VECTOR ( 'NONE', #6808, 999.9999999999998863 ) ;
#15866=ORIENTED_EDGE ( 'NONE', *, *, #5047, .T. ) ;
#15870=CARTESIAN_POINT ( 'NONE',  ( 5.254337203439246373, 50.85892981167459936, 78.80131646080216967 ) ) ;
#15871=EDGE_LOOP ( 'NONE', ( #2274, #6744, #12057, #8495 ) ) ;
#15874=ORIENTED_EDGE ( 'NONE', *, *, #1162, .T. ) ;
#15875=CARTESIAN_POINT ( 'NONE',  ( 5.493694769708608483, 50.67720340734032902, 78.89719962956496602 ) ) ;
#15876=CARTESIAN_POINT ( 'NONE',  ( -0.9244181309328289853, 52.21935397360262954, 76.32609705745309725 ) ) ;
#15877=VECTOR ( 'NONE', #20015, 1000.000000000000000 ) ;
#15878=CARTESIAN_POINT ( 'NONE',  ( 4.772654808018759631, 51.96292205838052070, 79.19424447893550223 ) ) ;
#15879=CARTESIAN_POINT ( 'NONE',  ( 5.385255718775495026, 47.76702405936703855, 72.45433879953087342 ) ) ;
#15887=CARTESIAN_POINT ( 'NONE',  ( 0.5221537403065010796, 44.16218137147968292, 78.79551527011911105 ) ) ;
#15888=DIRECTION ( 'NONE',  ( -0.5813877811927012917, 0.8136266022444372803, 5.636455622144620416E-17 ) ) ;
#15892=ORIENTED_EDGE ( 'NONE', *, *, #647, .F. ) ;
#15894=DIRECTION ( 'NONE',  ( 0.3165065846431827090, 0.9485903129789529098, 2.188653791613874994E-16 ) ) ;
#15895=ADVANCED_FACE ( 'NONE', ( #7919 ), #12919, .T. ) ;
#15897=ORIENTED_EDGE ( 'NONE', *, *, #17932, .F. ) ;
#15898=CARTESIAN_POINT ( 'NONE',  ( -3.555031842569258416, 52.06454604677990972, 75.79042024895623797 ) ) ;
#15900=CARTESIAN_POINT ( 'NONE',  ( 8.617838889373357958, 45.46597658821364263, 78.74919174070734584 ) ) ;
#15901=EDGE_LOOP ( 'NONE', ( #5490, #13404, #17152, #7639, #3056, #3297, #4831, #16374 ) ) ;
#15902=CARTESIAN_POINT ( 'NONE',  ( -5.134596719205594795, 50.01589981793483020, 79.19259575086972802 ) ) ;
#15903=DIRECTION ( 'NONE',  ( -0.9485903129789527988, 0.3165065846431829311, -8.934458285744989980E-17 ) ) ;
#15905=CARTESIAN_POINT ( 'NONE',  ( 6.388813065772197319, 37.53850911581889704, 78.31663032931759005 ) ) ;
#15906=CARTESIAN_POINT ( 'NONE',  ( 5.202764418357927134, 50.89058147309204827, 76.27120023672567584 ) ) ;
#15910=AXIS2_PLACEMENT_3D ( 'NONE', #20696, #18908, #7312 ) ;
#15913=PLANE ( 'NONE',  #13595 ) ;
#15915=CARTESIAN_POINT ( 'NONE',  ( 0.3869120917952212912, 35.96329670974014192, 76.16022115247204738 ) ) ;
#15916=CARTESIAN_POINT ( 'NONE',  ( 0.5221537403065005245, 44.16218137147968292, 82.45433879953087342 ) ) ;
#15918=CARTESIAN_POINT ( 'NONE',  ( 5.939862031672385356, 51.10075310024252815, 76.36217657474753651 ) ) ;
#15919=VERTEX_POINT ( 'NONE', #639 ) ;
#15921=CARTESIAN_POINT ( 'NONE',  ( -6.946982443395988582, 47.54813533618698074, 78.32326721260994873 ) ) ;
#15922=LINE ( 'NONE', #17607, #6581 ) ;
#15923=ORIENTED_EDGE ( 'NONE', *, *, #9548, .T. ) ;
#15925=CARTESIAN_POINT ( 'NONE',  ( 0.4729534506053946763, 52.36291882769025818, 75.36214536511981521 ) ) ;
#15928=ORIENTED_EDGE ( 'NONE', *, *, #19210, .F. ) ;
#15930=ORIENTED_EDGE ( 'NONE', *, *, #14059, .T. ) ;
#15931=CARTESIAN_POINT ( 'NONE',  ( -3.716790732209381165, 36.35290429323532635, 75.71473766112499959 ) ) ;
#15932=CARTESIAN_POINT ( 'NONE',  ( -5.405939962049822078, 49.82766502745145942, 72.45433879953087342 ) ) ;
#15933=CARTESIAN_POINT ( 'NONE',  ( 5.461659944059998217, 50.53996671397857909, 79.54598470662274678 ) ) ;
#15935=CARTESIAN_POINT ( 'NONE',  ( -4.529824687616612167, 37.72822084386444885, 77.32461911834714385 ) ) ;
#15936=CARTESIAN_POINT ( 'NONE',  ( 8.211795273144437246, 41.32505156136733149, 77.24417474779077963 ) ) ;
#15937=AXIS2_PLACEMENT_3D ( 'NONE', #13862, #9200, #15794 ) ;
#15939=CARTESIAN_POINT ( 'NONE',  ( 5.497232476171135751, 37.64385397974522363, 77.42016051845197921 ) ) ;
#15940=CARTESIAN_POINT ( 'NONE',  ( 5.901631269491789844, 51.12899262423628954, 78.24916896818955081 ) ) ;
#15944=EDGE_CURVE ( 'NONE', #1872, #9681, #5422, .T. ) ;
#15945=CARTESIAN_POINT ( 'NONE',  ( 5.787513446439723985, 51.21328686317854562, 75.36061482756318242 ) ) ;
#15947=DIRECTION ( 'NONE',  ( -0.3165065846431826535, -0.9485903129789529098, -2.188653791613874008E-16 ) ) ;
#15948=VECTOR ( 'NONE', #5013, 1000.000000000000000 ) ;
#15949=CARTESIAN_POINT ( 'NONE',  ( -0.4845124703328578253, 52.97630383655213393, 79.30111418114536548 ) ) ;
#15950=ORIENTED_EDGE ( 'NONE', *, *, #18874, .F. ) ;
#15953=CARTESIAN_POINT ( 'NONE',  ( 8.557023814081752278, 40.43966772045860125, 79.34450935619591405 ) ) ;
#15954=FILL_AREA_STYLE ('',( #18720 ) ) ;
#15956=ORIENTED_EDGE ( 'NONE', *, *, #16758, .F. ) ;
#15957=ORIENTED_EDGE ( 'NONE', *, *, #15051, .T. ) ;
#15959=CARTESIAN_POINT ( 'NONE',  ( 8.161249387665455046, 41.17249610787522585, 75.37807442913842237 ) ) ;
#15960=CARTESIAN_POINT ( 'NONE',  ( -3.535132420242971474, 36.21872061582891433, 78.58910375170351870 ) ) ;
#15961=CARTESIAN_POINT ( 'NONE',  ( -4.873991315592629547, 37.20768174929764882, 78.81125587425833601 ) ) ;
#15965=CARTESIAN_POINT ( 'NONE',  ( 6.737194059699555204, 50.51179604963209613, 77.55733179791843668 ) ) ;
#15968=VECTOR ( 'NONE', #5811, 1000.000000000000114 ) ;
#15970=VERTEX_POINT ( 'NONE', #2559 ) ;
#15973=FACE_OUTER_BOUND ( 'NONE', #20419, .T. ) ;
#15977=DIRECTION ( 'NONE',  ( 0.5941461771851728191, 0.8043570849667734945, 2.357623395011397284E-16 ) ) ;
#15979=EDGE_LOOP ( 'NONE', ( #5604, #10387, #15163, #10545 ) ) ;
#15981=CARTESIAN_POINT ( 'NONE',  ( -0.7091505932202195606, 52.97684993034207679, 75.80943630940421940 ) ) ;
#15983=CARTESIAN_POINT ( 'NONE',  ( 5.319542448682613944, 51.55895818820005871, 79.51138782552760631 ) ) ;
#15984=CARTESIAN_POINT ( 'NONE',  ( 5.309255083855641821, 37.50457964663987553, 75.97198585835440099 ) ) ;
#15986=ORIENTED_EDGE ( 'NONE', *, *, #2645, .F. ) ;
#15987=CARTESIAN_POINT ( 'NONE',  ( 8.296801588964658691, 41.57982088258064124, 75.97261045075327957 ) ) ;
#15988=ORIENTED_EDGE ( 'NONE', *, *, #12169, .F. ) ;
#15990=LINE ( 'NONE', #6188, #5898 ) ;
#15991=CARTESIAN_POINT ( 'NONE',  ( 1.116468592199672649, 52.94813999089376466, 76.77233108029956554 ) ) ;
#15994=DIRECTION ( 'NONE',  ( -1.540237394707283727E-16, -1.793354297423763257E-16, 1.000000000000000000 ) ) ;
#15995=B_SPLINE_SURFACE_WITH_KNOTS ( 'NONE', 3, 1, ( 
 ( #6561, #9679 ),
 ( #1580, #7752 ),
 ( #8061, #14230 ),
 ( #1889, #13168 ),
 ( #5166, #9884 ),
 ( #14759, #18163 ),
 ( #5375, #11477 ),
 ( #13379, #16364 ),
 ( #277, #11585 ),
 ( #18260, #5067 ),
 ( #1795, #11785 ),
 ( #3580, #3368 ),
 ( #8377, #18058 ),
 ( #8277, #2100 ),
 ( #19849, #8601 ),
 ( #3478, #17954 ),
 ( #11686, #181 ),
 ( #6664, #6766 ),
 ( #19642, #9990 ),
 ( #16469, #3680 ),
 ( #14860, #16782 ),
 ( #13277, #19746 ),
 ( #18370, #10087 ),
 ( #16569, #15080 ),
 ( #10197, #19946 ),
 ( #15180, #13577 ),
 ( #1991, #16677 ) ),
 .UNSPECIFIED., .F., .F., .F.,
 ( 4, 1, 1, 1, 1, 1, 1, 1, 1, 1, 1, 1, 1, 1, 1, 1, 1, 1, 1, 1, 1, 1, 1, 1, 4 ),
 ( 2, 2 ),
 ( 0.000000000000000000, 0.04992685941337848821, 0.09871136507264777205, 0.1457954968408328167, 0.1915776562037285746, 0.2364429891513756543, 0.2798905081306632403, 0.3226114784840122263, 0.3640369619956516645, 0.4040931382756795531, 0.4423864865660626644, 0.4791244981183566676, 0.5145420102664520767, 0.5484747442263178119, 0.5814193454185596632, 0.6141157465626525536, 0.6462545211269067336, 0.6795390940691592441, 0.7156628256359011120, 0.7545220547839790459, 0.7966562418723396322, 0.8423152836035615598, 0.8912945236129800053, 0.9437207944264596193, 1.000000000000000000 ),
 ( 0.000000000000000000, 1.000000000000000000 ),
 .UNSPECIFIED. ) ;
#15996=AXIS2_PLACEMENT_3D ( 'NONE', #4360, #14153, #15977 ) ;
#15998=DIRECTION ( 'NONE',  ( -0.3165065846431825980, -0.9485903129789527988, 0.000000000000000000 ) ) ;
#15999=VERTEX_POINT ( 'NONE', #18521 ) ;
#16005=LINE ( 'NONE', #1530, #8940 ) ;
#16007=CARTESIAN_POINT ( 'NONE',  ( 4.464802119779007761, 36.16368133634887982, 76.05895398371444571 ) ) ;
#16008=CARTESIAN_POINT ( 'NONE',  ( 5.201045719205120932, 50.89185100692279207, 76.32883089164610624 ) ) ;
#16019=CARTESIAN_POINT ( 'NONE',  ( -5.403286049735823049, 49.82407567696579065, 76.72345405564152543 ) ) ;
#16024=CARTESIAN_POINT ( 'NONE',  ( 0.5221537403065015237, 44.16218137147968292, 75.45433879953087342 ) ) ;
#16025=CARTESIAN_POINT ( 'NONE',  ( -3.711266317373846046, 36.34882363053331744, 77.55767546204062057 ) ) ;
#16027=CARTESIAN_POINT ( 'NONE',  ( 2.075775165176096060, 52.95450286967243159, 78.81257284323012868 ) ) ;
#16028=CARTESIAN_POINT ( 'NONE',  ( 4.100026115879673583, 51.54044873340893673, 76.58963291717793709 ) ) ;
#16031=CARTESIAN_POINT ( 'NONE',  ( 5.470702040720124337, 37.62937602372697654, 77.62670008255557264 ) ) ;
#16032=CARTESIAN_POINT ( 'NONE',  ( 8.886583547266173611, 41.42737914769194418, 79.54795956895829079 ) ) ;
#16033=CARTESIAN_POINT ( 'NONE',  ( 8.685073573159321825, 40.82344097173932340, 79.49103220525971381 ) ) ;
#16035=CARTESIAN_POINT ( 'NONE',  ( -8.192078482032012943, 42.93655631659661509, 78.28007409364852265 ) ) ;
#16037=VECTOR ( 'NONE', #3152, 1000.000000000000000 ) ;
#16039=CARTESIAN_POINT ( 'NONE',  ( -4.537713647263720951, 36.95928698179384497, 76.12832907849806929 ) ) ;
#16040=CARTESIAN_POINT ( 'NONE',  ( -6.710037999761452987, 40.29754613885109649, 78.44771795036322715 ) ) ;
#16043=CARTESIAN_POINT ( 'NONE',  ( -4.770044440429790811, 37.13090037985040226, 77.30667006270941499 ) ) ;
#16044=CARTESIAN_POINT ( 'NONE',  ( -4.702170908118536552, 37.85552605441999674, 77.90218689189877921 ) ) ;
#16048=CARTESIAN_POINT ( 'NONE',  ( -4.971268510706558175, 38.07201989387243657, 79.49652848452727483 ) ) ;
#16049=EDGE_CURVE ( 'NONE', #13175, #20173, #19637, .T. ) ;
#16052=AXIS2_PLACEMENT_3D ( 'NONE', #8375, #16053, #11377 ) ;
#16053=DIRECTION ( 'NONE',  ( -1.540237394707283727E-16, -1.793354297423763257E-16, 1.000000000000000000 ) ) ;
#16055=VECTOR ( 'NONE', #7011, 1000.000000000000000 ) ;
#16056=CARTESIAN_POINT ( 'NONE',  ( -0.9334096104468154742, 52.21740282451978743, 78.43306491891449639 ) ) ;
#16058=CARTESIAN_POINT ( 'NONE',  ( -4.537099264183359182, 37.70896829297682729, 78.18375056423674607 ) ) ;
#16060=CARTESIAN_POINT ( 'NONE',  ( 5.653389158101303380, 51.31235907211823388, 75.98863418974025308 ) ) ;
#16061=CARTESIAN_POINT ( 'NONE',  ( 6.903329084842819263, 50.38907879888579089, 78.20944795639196911 ) ) ;
#16063=ORIENTED_EDGE ( 'NONE', *, *, #763, .F. ) ;
#16065=CARTESIAN_POINT ( 'NONE',  ( 9.296966826988569466, 42.65732387124978686, 75.81656704941096336 ) ) ;
#16070=CARTESIAN_POINT ( 'NONE',  ( -3.944959226007137776, 38.51060946023304865, 78.18375056423674607 ) ) ;
#16071=CARTESIAN_POINT ( 'NONE',  ( -3.184806123434658964, 36.84768901790411633, 75.88014116946466459 ) ) ;
#16072=CARTESIAN_POINT ( 'NONE',  ( 8.551362112893849954, 42.78711729333979719, 77.91040118276930571 ) ) ;
#16073=CARTESIAN_POINT ( 'NONE',  ( -1.769308508470985419, 51.40850462968639079, 72.45433879953087342 ) ) ;
#16074=CARTESIAN_POINT ( 'NONE',  ( 6.519609470440952848, 49.74768407388893365, 76.59575135851817151 ) ) ;
#16076=ADVANCED_FACE ( 'NONE', ( #8076 ), #17762, .T. ) ;
#16079=CARTESIAN_POINT ( 'NONE',  ( -3.087839404999279225, 36.79949025498288506, 77.19021729766356543 ) ) ;
#16082=FACE_OUTER_BOUND ( 'NONE', #12396, .T. ) ;
#16083=VERTEX_POINT ( 'NONE', #18933 ) ;
#16084=CARTESIAN_POINT ( 'NONE',  ( 6.866536783559561208, 37.87987299396810670, 76.25518385353585415 ) ) ;
#16085=CARTESIAN_POINT ( 'NONE',  ( 4.833451453752482863, 51.91801402521529241, 79.26957207196610966 ) ) ;
#16087=CARTESIAN_POINT ( 'NONE',  ( 0.8466962780023906676, 52.96359677974843549, 76.22640136859038762 ) ) ;
#16089=VERTEX_POINT ( 'NONE', #14141 ) ;
#16090=CARTESIAN_POINT ( 'NONE',  ( 5.848554534127551108, 37.15246014923294382, 77.40928489470421425 ) ) ;
#16091=AXIS2_PLACEMENT_3D ( 'NONE', #19398, #8124, #1433 ) ;
#16092=EDGE_LOOP ( 'NONE', ( #18317, #11795, #10266, #7134 ) ) ;
#16095=DIRECTION ( 'NONE',  ( -0.3165065846431827645, -0.9485903129789529098, 0.000000000000000000 ) ) ;
#16097=CARTESIAN_POINT ( 'NONE',  ( -5.954976305145398108, 38.00616181634879354, 76.59693911441793546 ) ) ;
#16101=CARTESIAN_POINT ( 'NONE',  ( 4.577225057937401864, 52.10727814237509392, 78.46169174070733732 ) ) ;
#16104=DIRECTION ( 'NONE',  ( 1.540237394707284220E-16, 1.793354297423764243E-16, -1.000000000000000000 ) ) ;
#16106=CARTESIAN_POINT ( 'NONE',  ( 4.826069222465897646, 51.92346698209227895, 75.62563104034643402 ) ) ;
#16107=ORIENTED_EDGE ( 'NONE', *, *, #12739, .F. ) ;
#16108=CARTESIAN_POINT ( 'NONE',  ( 1.932239457924184167, 52.24021385314885180, 77.09260542632576119 ) ) ;
#16109=CARTESIAN_POINT ( 'NONE',  ( -7.075244453723417593, 44.52209897503762193, 72.45432679953087529 ) ) ;
#16114=ORIENTED_EDGE ( 'NONE', *, *, #19794, .F. ) ;
#16115=LINE ( 'NONE', #11230, #11901 ) ;
#16119=DIRECTION ( 'NONE',  ( 0.9485903129789529098, -0.3165065846431827090, 8.934458285744996143E-17 ) ) ;
#16122=CARTESIAN_POINT ( 'NONE',  ( 5.902048492000326441, 51.12868443877599134, 78.59183879953087626 ) ) ;
#16125=EDGE_CURVE ( 'NONE', #5246, #14083, #4761, .T. ) ;
#16126=DIRECTION ( 'NONE',  ( 0.3165065846431826535, 0.9485903129789529098, 2.188653791613874008E-16 ) ) ;
#16129=CARTESIAN_POINT ( 'NONE',  ( -3.197219379186972521, 36.89395081135501897, 77.48323649892105891 ) ) ;
#16130=ORIENTED_EDGE ( 'NONE', *, *, #17036, .T. ) ;
#16131=CARTESIAN_POINT ( 'NONE',  ( 2.051935062045836311, 52.95469085764700878, 78.89969410769322167 ) ) ;
#16132=CARTESIAN_POINT ( 'NONE',  ( -3.799282117832336603, 36.41383735683930212, 77.78682928037112276 ) ) ;
#16134=ORIENTED_EDGE ( 'NONE', *, *, #18715, .F. ) ;
#16136=EDGE_CURVE ( 'NONE', #18561, #9638, #9694, .T. ) ;
#16138=CARTESIAN_POINT ( 'NONE',  ( -2.938479363457391358, 51.59616431484483456, 76.29466226208309365 ) ) ;
#16140=FACE_OUTER_BOUND ( 'NONE', #19474, .T. ) ;
#16141=EDGE_LOOP ( 'NONE', ( #6068, #9965, #15866, #12231 ) ) ;
#16142=CARTESIAN_POINT ( 'NONE',  ( -7.932261308893451712, 41.72020721241317176, 78.84683602641649713 ) ) ;
#16143=CARTESIAN_POINT ( 'NONE',  ( -4.165071384785050235, 37.43866709544969495, 76.22840587216694530 ) ) ;
#16145=ORIENTED_EDGE ( 'NONE', *, *, #12606, .T. ) ;
#16146=CARTESIAN_POINT ( 'NONE',  ( 4.578029447411149810, 52.10668397227361481, 78.50413411530853125 ) ) ;
#16147=DIRECTION ( 'NONE',  ( 1.540237394707284220E-16, 1.793354297423764243E-16, -1.000000000000000000 ) ) ;
#16150=CARTESIAN_POINT ( 'NONE',  ( -4.774380534136511756, 51.19324411499089678, 76.08363728426196815 ) ) ;
#16152=CARTESIAN_POINT ( 'NONE',  ( 6.062689023816073330, 38.11643952539938596, 75.52723796482321461 ) ) ;
#16153=CARTESIAN_POINT ( 'NONE',  ( 0.000000000000000000, 0.000000000000000000, 0.000000000000000000 ) ) ;
#16154=CARTESIAN_POINT ( 'NONE',  ( -5.809877882140231264, 50.45331562208507847, 76.21531548689122815 ) ) ;
#16155=CARTESIAN_POINT ( 'NONE',  ( 0.5221537403065019678, 44.16218137147968292, 72.45433879953087342 ) ) ;
#16156=EDGE_CURVE ( 'NONE', #17907, #17272, #14361, .T. ) ;
#16159=EDGE_LOOP ( 'NONE', ( #3033, #1036, #4635, #19055 ) ) ;
#16163=CARTESIAN_POINT ( 'NONE',  ( 8.872773925109784798, 41.38599083402314704, 79.54845644658969661 ) ) ;
#16164=CARTESIAN_POINT ( 'NONE',  ( 0.8435675618935688513, 52.95685645435612088, 79.54466172167512639 ) ) ;
#16165=EDGE_CURVE ( 'NONE', #6925, #8823, #6161, .T. ) ;
#16166=ORIENTED_EDGE ( 'NONE', *, *, #16650, .T. ) ;
#16167=CARTESIAN_POINT ( 'NONE',  ( 9.346906861638174746, 42.80699732323137852, 76.23134092453109645 ) ) ;
#16169=CARTESIAN_POINT ( 'NONE',  ( 5.081851840395362530, 37.34681921564990859, 77.59303304176042104 ) ) ;
#16171=CARTESIAN_POINT ( 'NONE',  ( 4.202107083175826929, 51.49017039810478735, 78.89819502495319625 ) ) ;
#16172=CARTESIAN_POINT ( 'NONE',  ( 0.3279640439667344531, 52.35988168082469940, 78.50066232894263862 ) ) ;
#16173=PLANE ( 'NONE',  #254 ) ;
#16174=CARTESIAN_POINT ( 'NONE',  ( 0.3279640439667345642, 52.35988168082470651, 77.76169174070734869 ) ) ;
#16175=CARTESIAN_POINT ( 'NONE',  ( 6.545534159973747990, 50.65336749702785113, 77.68963291717794561 ) ) ;
#16176=CARTESIAN_POINT ( 'NONE',  ( 4.147036873812957047, 51.51748372786249064, 78.29064342123426457 ) ) ;
#16178=ORIENTED_EDGE ( 'NONE', *, *, #191, .F. ) ;
#16179=CARTESIAN_POINT ( 'NONE',  ( -5.086258153195711174, 37.36447471160525424, 79.53654225555244750 ) ) ;
#16180=CARTESIAN_POINT ( 'NONE',  ( 8.951736416449948663, 41.62264642985666541, 78.48252796260671005 ) ) ;
#16181=CARTESIAN_POINT ( 'NONE',  ( 5.298894634962917571, 50.82722828506639701, 78.90485198387828802 ) ) ;
#16182=CARTESIAN_POINT ( 'NONE',  ( 8.375199775097003752, 41.81478521990748476, 77.14698585835439815 ) ) ;
#16183=CARTESIAN_POINT ( 'NONE',  ( 8.621533274486752774, 40.63300666569625008, 75.47105533938442079 ) ) ;
#16184=EDGE_LOOP ( 'NONE', ( #2725, #5923, #9051, #19289 ) ) ;
#16185=CARTESIAN_POINT ( 'NONE',  ( 5.722750437672663892, 37.06256514788822898, 75.36130176902827316 ) ) ;
#16186=CARTESIAN_POINT ( 'NONE',  ( 0.5975752275646775136, 52.20533044642586162, 79.54835876252475657 ) ) ;
#16187=CARTESIAN_POINT ( 'NONE',  ( 6.395088259259853913, 38.46276872161406146, 77.80469260682309596 ) ) ;
#16193=EDGE_LOOP ( 'NONE', ( #10039, #7404, #4816, #2256 ) ) ;
#16196=CARTESIAN_POINT ( 'NONE',  ( -7.759339030830453510, 47.14028884343398573, 79.12207947904607863 ) ) ;
#16197=CARTESIAN_POINT ( 'NONE',  ( -3.101538578788242351, 36.81245731659976883, 78.30834307773316993 ) ) ;
#16198=CARTESIAN_POINT ( 'NONE',  ( -3.566438244846302119, 38.23101125920473464, 78.34992703482498655 ) ) ;
#16199=LINE ( 'NONE', #5114, #15351 ) ;
#16200=ORIENTED_EDGE ( 'NONE', *, *, #5248, .T. ) ;
#16204=B_SPLINE_CURVE_WITH_KNOTS ( 'NONE', 3,
 ( #4423, #15925, #12422, #17410, #10840, #17305, #1344, #8040, #1555, #2835, #20890, #6019, #3040, #14422, #12519, #20493, #4620, #5925 ),
 .UNSPECIFIED., .F., .F.,
 ( 4, 2, 2, 2, 2, 2, 2, 2, 4 ),
 ( 0.000000000000000000, 0.0003585842996636947450, 0.0007171685993273894900, 0.001075752898991083964, 0.001434337198654778546, 0.001792921498318473129, 0.001972213648150300362, 0.002151505797982128029, 0.002868674397309438698 ),
 .UNSPECIFIED. ) ;
#16205=CARTESIAN_POINT ( 'NONE',  ( -2.914604833731050615, 51.60239615748798059, 76.69845644658968808 ) ) ;
#16209=CARTESIAN_POINT ( 'NONE',  ( -5.835675398032521777, 50.43488166173578691, 78.31711373209397209 ) ) ;
#16210=CARTESIAN_POINT ( 'NONE',  ( -5.954796862783079625, 38.00602926950412552, 78.58503192925951453 ) ) ;
#16211=CARTESIAN_POINT ( 'NONE',  ( -5.838428831739583380, 50.43291415881836315, 78.10580938776615767 ) ) ;
#16214=CARTESIAN_POINT ( 'NONE',  ( 5.088724926954141026, 37.35642916330452579, 77.64535406911728899 ) ) ;
#16219=CARTESIAN_POINT ( 'NONE',  ( 4.987972048783305468, 51.80387588613526617, 77.70137231118654597 ) ) ;
#16220=DIRECTION ( 'NONE',  ( 1.540237394707283727E-16, 1.793354297423763257E-16, -1.000000000000000000 ) ) ;
#16221=CARTESIAN_POINT ( 'NONE',  ( -5.387797286270752828, 50.75491896253648605, 75.54244301425877950 ) ) ;
#16223=VECTOR ( 'NONE', #1788, 1000.000000000000114 ) ;
#16227=CARTESIAN_POINT ( 'NONE',  ( 5.579143690744149175, 50.61256526606223360, 76.32243632687685420 ) ) ;
#16230=CARTESIAN_POINT ( 'NONE',  ( 1.762171107682031002, 52.95697575291716674, 79.26556901187228732 ) ) ;
#16235=CARTESIAN_POINT ( 'NONE',  ( 9.307108147255313213, 42.68771805144258735, 79.03485483908291087 ) ) ;
#16237=CARTESIAN_POINT ( 'NONE',  ( -8.294722968033532595, 42.83806395776854714, 76.13058770837619704 ) ) ;
#16238=EDGE_LOOP ( 'NONE', ( #15719, #6588, #11325, #14913, #12427, #13716, #8688, #4176, #17230, #16134, #8300, #9370, #8663 ) ) ;
#16240=CARTESIAN_POINT ( 'NONE',  ( -5.046391490720765205, 38.27103331005528730, 75.52011153330033721 ) ) ;
#16242=VECTOR ( 'NONE', #18046, 1000.000000000000114 ) ;
#16244=B_SPLINE_CURVE_WITH_KNOTS ( 'NONE', 3,
 ( #4953, #10187, #11881, #8478, #16670, #14855, #11472, #274, #14960, #9876, #175, #17944, #18156, #5262, #11778, #18254 ),
 .UNSPECIFIED., .F., .F.,
 ( 4, 2, 2, 2, 2, 2, 2, 4 ),
 ( 0.000000000000000000, 0.0002718550652617190348, 0.0005437101305234380696, 0.0008155651957851571586, 0.001087420261046876139, 0.001631130391570334483, 0.001902985456832064414, 0.002174840522093794346 ),
 .UNSPECIFIED. ) ;
#16245=CARTESIAN_POINT ( 'NONE',  ( 8.378595026212774854, 41.81348187568733721, 78.70760583312296887 ) ) ;
#16247=ORIENTED_EDGE ( 'NONE', *, *, #19610, .F. ) ;
#16248=DIRECTION ( 'NONE',  ( 0.8136266022444372803, 0.5813877811927012917, 2.295812393977109100E-16 ) ) ;
#16249=CARTESIAN_POINT ( 'NONE',  ( -6.739013063861042596, 40.35217951880748188, 78.85334789288012303 ) ) ;
#16250=VERTEX_POINT ( 'NONE', #16273 ) ;
#16251=CARTESIAN_POINT ( 'NONE',  ( -4.612897897929109980, 51.30863369456805145, 75.97269380145769446 ) ) ;
#16253=FACE_OUTER_BOUND ( 'NONE', #9688, .T. ) ;
#16254=EDGE_CURVE ( 'NONE', #4917, #19886, #13293, .T. ) ;
#16255=VECTOR ( 'NONE', #11105, 1000.000000000000114 ) ;
#16256=CARTESIAN_POINT ( 'NONE',  ( 5.939984016379080245, 38.00650938446680271, 78.33981856787941922 ) ) ;
#16257=CARTESIAN_POINT ( 'NONE',  ( 8.869748494521283888, 41.37692342661967615, 77.52492703482499792 ) ) ;
#16261=CARTESIAN_POINT ( 'NONE',  ( 9.353743827924017040, 42.82748814491910139, 76.70850639745313515 ) ) ;
#16263=CARTESIAN_POINT ( 'NONE',  ( 6.436934174446692580, 49.81957092643428808, 78.08828162113617566 ) ) ;
#16266=ORIENTED_EDGE ( 'NONE', *, *, #8821, .T. ) ;
#16267=EDGE_CURVE ( 'NONE', #13330, #20802, #19765, .T. ) ;
#16268=CARTESIAN_POINT ( 'NONE',  ( 7.739670491838285038, 40.27007090160952174, 75.95778646784575017 ) ) ;
#16272=CARTESIAN_POINT ( 'NONE',  ( 5.939900590116411472, 51.10072461867315496, 76.90580938776616904 ) ) ;
#16273=CARTESIAN_POINT ( 'NONE',  ( -7.079975527142585712, 43.92211762787398044, 75.45433879953087342 ) ) ;
#16276=CARTESIAN_POINT ( 'NONE',  ( 4.293446294024885646, 51.44367749308788973, 77.90149807450526964 ) ) ;
#16283=CARTESIAN_POINT ( 'NONE',  ( 8.837344731589769964, 41.27980729345753730, 78.92656146296575059 ) ) ;
#16284=CARTESIAN_POINT ( 'NONE',  ( 8.941920682866751235, 41.59322805360929465, 78.83412695248559032 ) ) ;
#16285=LINE ( 'NONE', #14473, #17430 ) ;
#16286=DIRECTION ( 'NONE',  ( 0.007885122365275663500, 0.9999689119394085113, 1.805443505845543142E-16 ) ) ;
#16287=CARTESIAN_POINT ( 'NONE',  ( 8.387016861607721196, 39.93014609885396027, 76.70090004521539129 ) ) ;
#16291=FACE_OUTER_BOUND ( 'NONE', #18394, .T. ) ;
#16293=CARTESIAN_POINT ( 'NONE',  ( 6.447652509444688818, 38.50032921029611543, 77.26022115247205591 ) ) ;
#16294=CARTESIAN_POINT ( 'NONE',  ( -3.501354354950023229, 36.19377011966047775, 76.40804902690982203 ) ) ;
#16295=FACE_OUTER_BOUND ( 'NONE', #17286, .T. ) ;
#16297=CARTESIAN_POINT ( 'NONE',  ( 8.947997572694543322, 41.61144087793389446, 76.20405737193274831 ) ) ;
#16301=ADVANCED_FACE ( 'NONE', ( #18598 ), #17216, .F. ) ;
#16303=CARTESIAN_POINT ( 'NONE',  ( 1.251324093324716946, 52.20841207932105021, 76.78082255713043480 ) ) ;
#16305=CARTESIAN_POINT ( 'NONE',  ( 8.314165830633189813, 41.60776736370225848, 75.97520393624411383 ) ) ;
#16307=AXIS2_PLACEMENT_3D ( 'NONE', #3583, #18264, #13383 ) ;
#16308=CARTESIAN_POINT ( 'NONE',  ( 8.639127872212812420, 42.99760432031693824, 78.86684150954961581 ) ) ;
#16317=CARTESIAN_POINT ( 'NONE',  ( 0.5706356501935867520, 52.36203804732553380, 75.97198585835440099 ) ) ;
#16319=CARTESIAN_POINT ( 'NONE',  ( 5.740585635973905809, 51.24795054640212300, 75.97198585835440099 ) ) ;
#16320=DIRECTION ( 'NONE',  ( 1.540237394707284220E-16, 1.793354297423764243E-16, -1.000000000000000000 ) ) ;
#16322=ORIENTED_EDGE ( 'NONE', *, *, #20561, .F. ) ;
#16323=AXIS2_PLACEMENT_3D ( 'NONE', #17092, #15282, #18790 ) ;
#16324=CARTESIAN_POINT ( 'NONE',  ( -4.095068233311042860, 50.93174038172981000, 76.01002907825849775 ) ) ;
#16326=DIRECTION ( 'NONE',  ( -0.009567942452870459302, 0.9999542261909885044, 1.778535306010345054E-16 ) ) ;
#16327=VERTEX_POINT ( 'NONE', #2640 ) ;
#16329=CARTESIAN_POINT ( 'NONE',  ( -6.794221408397769224, 40.57951578525081260, 77.67144260532384692 ) ) ;
#16332=VECTOR ( 'NONE', #9553, 1000.000000000000227 ) ;
#16334=CARTESIAN_POINT ( 'NONE',  ( -3.137939750588703003, 36.85016333763859109, 77.38751485876633751 ) ) ;
#16335=ORIENTED_EDGE ( 'NONE', *, *, #9049, .F. ) ;
#16338=CARTESIAN_POINT ( 'NONE',  ( -5.531051774427891310, 44.10426199826898142, 75.45433879953087342 ) ) ;
#16340=ORIENTED_EDGE ( 'NONE', *, *, #8421, .F. ) ;
#16341=CARTESIAN_POINT ( 'NONE',  ( 1.250118884985844225, 46.34393909133126499, 82.45433879953087342 ) ) ;
#16346=CARTESIAN_POINT ( 'NONE',  ( -5.950833756536988872, 38.00310188256379007, 76.46818962967083166 ) ) ;
#16347=EDGE_LOOP ( 'NONE', ( #18515, #8787, #18886, #1591 ) ) ;
#16348=DIRECTION ( 'NONE',  ( -0.5941461771851693774, -0.8043570849667760481, -2.357623395011396791E-16 ) ) ;
#16350=DIRECTION ( 'NONE',  ( -0.8136266022444372803, -0.5813877811927012917, -2.295812393977109100E-16 ) ) ;
#16357=CARTESIAN_POINT ( 'NONE',  ( -7.866550369700228806, 41.50330127738815378, 78.93669174070734584 ) ) ;
#16358=CARTESIAN_POINT ( 'NONE',  ( 8.889576793745449734, 46.88836537034026719, 78.73595644658969661 ) ) ;
#16361=CARTESIAN_POINT ( 'NONE',  ( 6.025664479182668565, 50.11254134161350038, 75.49932683761802821 ) ) ;
#16362=CARTESIAN_POINT ( 'NONE',  ( 8.214799251806553571, 41.32260305165857517, 72.45433879953087342 ) ) ;
#16364=CARTESIAN_POINT ( 'NONE',  ( 4.681897302132870919, 37.23858518757540281, 75.43572969368668168 ) ) ;
#16366=EDGE_CURVE ( 'NONE', #14291, #18616, #10533, .T. ) ;
#16369=CARTESIAN_POINT ( 'NONE',  ( -4.361665858399769391, 37.57520132541210245, 75.97198585835440099 ) ) ;
#16370=CARTESIAN_POINT ( 'NONE',  ( 9.271487163511554996, 42.58095970340946934, 75.72637824826109920 ) ) ;
#16371=CARTESIAN_POINT ( 'NONE',  ( -7.376743071288318632, 41.96049357349896525, 78.13669174070733447 ) ) ;
#16372=CARTESIAN_POINT ( 'NONE',  ( 6.575642869179847416, 50.63112740639009246, 77.70577767651062118 ) ) ;
#16373=VECTOR ( 'NONE', #11923, 1000.000000000000227 ) ;
#16374=ORIENTED_EDGE ( 'NONE', *, *, #10808, .F. ) ;
#16375=CARTESIAN_POINT ( 'NONE',  ( 5.853612939038055352, 51.16446183064613251, 78.89719962956496602 ) ) ;
#16377=VERTEX_POINT ( 'NONE', #16798 ) ;
#16378=EDGE_CURVE ( 'NONE', #15919, #1549, #2216, .T. ) ;
#16379=CARTESIAN_POINT ( 'NONE',  ( 4.973101328672442811, 51.81486028805201727, 77.67439681936272677 ) ) ;
#16380=DIRECTION ( 'NONE',  ( -0.9534635866061492715, -0.3015081906286096181, -2.009271279954799034E-16 ) ) ;
#16384=EDGE_CURVE ( 'NONE', #13636, #16959, #12333, .T. ) ;
#16385=VECTOR ( 'NONE', #4795, 1000.000000000000227 ) ;
#16387=FACE_OUTER_BOUND ( 'NONE', #17941, .T. ) ;
#16388=CARTESIAN_POINT ( 'NONE',  ( -4.526965251788245936, 37.70598351703077356, 76.16751655709613544 ) ) ;
#16389=VECTOR ( 'NONE', #12011, 1000.000000000000000 ) ;
#16391=ORIENTED_EDGE ( 'NONE', *, *, #19583, .T. ) ;
#16392=CARTESIAN_POINT ( 'NONE',  ( 8.865792162213244509, 41.36506604770743678, 78.93669174070734584 ) ) ;
#16393=ADVANCED_FACE ( 'NONE', ( #8713 ), #17115, .F. ) ;
#16395=CARTESIAN_POINT ( 'NONE',  ( 8.950958007118590132, 41.62031348770922534, 78.64183653779139149 ) ) ;
#16397=CARTESIAN_POINT ( 'NONE',  ( 8.648170029844118645, 43.06315486489794608, 76.74257409364851412 ) ) ;
#16398=CARTESIAN_POINT ( 'NONE',  ( 8.876519138579782364, 41.39721547638464472, 77.52397343602532942 ) ) ;
#16399=EDGE_CURVE ( 'NONE', #18638, #14895, #5688, .T. ) ;
#16401=CARTESIAN_POINT ( 'NONE',  ( 8.475713225669114337, 40.19597472873837063, 75.74322883085581282 ) ) ;
#16403=ORIENTED_EDGE ( 'NONE', *, *, #20820, .F. ) ;
#16404=CARTESIAN_POINT ( 'NONE',  ( 6.416235914874578228, 38.47788006205125555, 76.12774863075016185 ) ) ;
#16405=CARTESIAN_POINT ( 'NONE',  ( -0.02252005271732430980, 52.21022012559965475, 79.48573486738433758 ) ) ;
#16406=CARTESIAN_POINT ( 'NONE',  ( -5.412716252285423302, 48.91899944357702879, 75.45433879953087342 ) ) ;
#16407=CARTESIAN_POINT ( 'NONE',  ( 4.324106654390397431, 51.42778090780855393, 75.70619357739094824 ) ) ;
#16408=CARTESIAN_POINT ( 'NONE',  ( 5.391786323697940198, 50.75965653268888644, 77.94845644658968808 ) ) ;
#16411=LINE ( 'NONE', #6597, #10118 ) ;
#16412=VERTEX_POINT ( 'NONE', #14828 ) ;
#16414=CARTESIAN_POINT ( 'NONE',  ( 2.021804202196959555, 52.20233656050648818, 77.22796645847455466 ) ) ;
#16415=B_SPLINE_CURVE_WITH_KNOTS ( 'NONE', 3,
 ( #14459, #5082, #16480, #14872, #292, #20924, #12860, #16167, #6785, #13289, #9579, #11175, #16065, #8072, #14565, #609, #5183, #12019, #5283, #13704, #19862, #16584, #10212 ),
 .UNSPECIFIED., .F., .F.,
 ( 4, 1, 1, 1, 1, 1, 1, 1, 1, 1, 1, 1, 1, 1, 1, 1, 1, 1, 1, 1, 4 ),
 ( 0.000000000000000000, 0.04300144207505136179, 0.08353165498080591944, 0.1209955408344369626, 0.1553840623654753617, 0.1873435814759382700, 0.2162479910858959298, 0.2424976236983500399, 0.2660452007499324312, 0.3104933729322157387, 0.3556083049253406791, 0.4034864083407884716, 0.4540969056831142825, 0.5078508224766279389, 0.5647468969590679899, 0.6259022191770886590, 0.6917657563094725681, 0.7621492621511971599, 0.8365553829333508551, 0.9158190838930461153, 1.000000000000000000 ),
 .UNSPECIFIED. ) ;
#16418=DIRECTION ( 'NONE',  ( -0.9480563259966798828, -0.3181025035074024343, -2.030702297275143506E-16 ) ) ;
#16423=CARTESIAN_POINT ( 'NONE',  ( 1.652727357819364418, 35.35299279957455099, 76.86610350541323555 ) ) ;
#16424=EDGE_CURVE ( 'NONE', #19082, #10941, #9482, .T. ) ;
#16427=EDGE_LOOP ( 'NONE', ( #17132, #13466, #11090, #13566 ) ) ;
#16432=LINE ( 'NONE', #6725, #2012 ) ;
#16436=CARTESIAN_POINT ( 'NONE',  ( 0.8402443429964431276, 52.35221751176949567, 78.65078808693101564 ) ) ;
#16438=CARTESIAN_POINT ( 'NONE',  ( 4.572162582958037014, 51.19700258348528621, 77.68963291717793140 ) ) ;
#16439=FACE_OUTER_BOUND ( 'NONE', #18648, .T. ) ;
#16443=CARTESIAN_POINT ( 'NONE',  ( 9.353817388681445522, 42.82770861117572281, 76.74257409364852833 ) ) ;
#16446=EDGE_LOOP ( 'NONE', ( #1506, #1189, #7363, #20295, #6847, #4474, #5576, #3655, #2452, #3587, #5352, #14427, #14751, #14979, #5193, #13256, #9917, #20123, #18465, #19830, #9066, #2487, #9190, #4726, #20244, #10669, #11005, #14287, #14494, #11566, #9098, #3795, #8528, #11731, #3877, #526, #6806, #15393, #19682, #3689 ) ) ;
#16447=CARTESIAN_POINT ( 'NONE',  ( 8.951667845840693971, 41.62244091939069790, 76.38301527011910252 ) ) ;
#16448=CARTESIAN_POINT ( 'NONE',  ( 5.389492195292208798, 36.82443100924615464, 78.09625056423674039 ) ) ;
#16449=ORIENTED_EDGE ( 'NONE', *, *, #11071, .F. ) ;
#16450=FACE_BOUND ( 'NONE', #4383, .T. ) ;
#16451=CARTESIAN_POINT ( 'NONE',  ( -5.529385682154831727, 44.31555110708731604, 75.45433879953087342 ) ) ;
#16453=ORIENTED_EDGE ( 'NONE', *, *, #16914, .F. ) ;
#16454=CARTESIAN_POINT ( 'NONE',  ( -5.474200200999507437, 38.58703837115216828, 76.14635491738357587 ) ) ;
#16456=DIRECTION ( 'NONE',  ( -0.5813877811927011807, 0.8136266022444372803, 5.636455622144619183E-17 ) ) ;
#16457=CARTESIAN_POINT ( 'NONE',  ( 0.3351286093508437092, 52.96019378912382791, 76.24030412541705459 ) ) ;
#16459=ORIENTED_EDGE ( 'NONE', *, *, #9120, .T. ) ;
#16460=CARTESIAN_POINT ( 'NONE',  ( -4.517072128342596748, 36.94403992325786135, 78.34992703482498655 ) ) ;
#16462=CARTESIAN_POINT ( 'NONE',  ( 6.575359255040893913, 44.22010074469034180, 72.45433879953087342 ) ) ;
#16463=CARTESIAN_POINT ( 'NONE',  ( 0.3279640439667344531, 52.35988168082469940, 78.50066232894263862 ) ) ;
#16466=CARTESIAN_POINT ( 'NONE',  ( 5.417149068951104596, 50.56202716265563168, 75.36137945677606353 ) ) ;
#16467=DIRECTION ( 'NONE',  ( -1.540237394707284220E-16, -1.793354297423764243E-16, 1.000000000000000000 ) ) ;
#16468=B_SPLINE_CURVE_WITH_KNOTS ( 'NONE', 3,
 ( #6919, #320, #19791, #3935, #5213, #11730, #18303, #20102, #19892, #11828, #16613 ),
 .UNSPECIFIED., .F., .F.,
 ( 4, 1, 1, 1, 1, 1, 1, 1, 4 ),
 ( 0.000000000000000000, 0.2014779019512820402, 0.3683355476270177564, 0.4986267722911685296, 0.6014797591950403755, 0.6911751734036410966, 0.7846115128848750730, 0.8848135988872103397, 1.000000000000000000 ),
 .UNSPECIFIED. ) ;
#16469=CARTESIAN_POINT ( 'NONE',  ( 4.464802119779007761, 36.16368133634887982, 76.05895398371444571 ) ) ;
#16470=VERTEX_POINT ( 'NONE', #562 ) ;
#16472=CARTESIAN_POINT ( 'NONE',  ( 9.240682951717872129, 42.48863752648103542, 75.64289537645213102 ) ) ;
#16474=CARTESIAN_POINT ( 'NONE',  ( -7.723582874747324745, 47.23591325229828186, 75.45433879953087342 ) ) ;
#16476=ORIENTED_EDGE ( 'NONE', *, *, #1692, .F. ) ;
#16477=CARTESIAN_POINT ( 'NONE',  ( -4.895593109503407980, 37.22363812428621088, 78.18375056423674607 ) ) ;
#16478=EDGE_LOOP ( 'NONE', ( #11247, #12466, #3659, #6022 ) ) ;
#16479=CARTESIAN_POINT ( 'NONE',  ( -3.557428649121368469, 36.23518994195450205, 77.32142682847380399 ) ) ;
#16480=CARTESIAN_POINT ( 'NONE',  ( 9.353600933836910158, 42.82705988227500882, 76.64232882509132594 ) ) ;
#16481=DIRECTION ( 'NONE',  ( -0.8236492988270761595, -0.5670994908670485835, -2.285625759191147486E-16 ) ) ;
#16485=CARTESIAN_POINT ( 'NONE',  ( 5.599418364623888422, 51.35222512318382826, 78.27515171461519117 ) ) ;
#16486=LINE ( 'NONE', #615, #10570 ) ;
#16487=CARTESIAN_POINT ( 'NONE',  ( 4.198599642040965030, 51.49202303595968999, 78.03894196152546670 ) ) ;
#16491=CARTESIAN_POINT ( 'NONE',  ( 0.3327557958309655950, 52.96755809673673099, 76.44919174070734869 ) ) ;
#16492=VERTEX_POINT ( 'NONE', #15046 ) ;
#16493=EDGE_CURVE ( 'NONE', #10557, #7365, #5748, .T. ) ;
#16494=CARTESIAN_POINT ( 'NONE',  ( 8.951433321995803993, 41.62173803654965099, 78.54183882225588320 ) ) ;
#16495=CARTESIAN_POINT ( 'NONE',  ( -4.534948301111438873, 37.71188027398896736, 78.53742703482498655 ) ) ;
#16496=LINE ( 'NONE', #1914, #1383 ) ;
#16497=EDGE_CURVE ( 'NONE', #17442, #3406, #16952, .T. ) ;
#16498=CARTESIAN_POINT ( 'NONE',  ( 8.648380609495486482, 40.71346983188059454, 75.44378286633819641 ) ) ;
#16499=VERTEX_POINT ( 'NONE', #19918 ) ;
#16500=ORIENTED_EDGE ( 'NONE', *, *, #7272, .T. ) ;
#16502=CARTESIAN_POINT ( 'NONE',  ( 7.866866907225194439, 40.51444835331399474, 79.25767082237931049 ) ) ;
#16503=CARTESIAN_POINT ( 'NONE',  ( -3.538420156175611009, 36.22114913392427127, 76.12177974158937843 ) ) ;
#16504=CARTESIAN_POINT ( 'NONE',  ( 0.8450176760924454911, 52.95625770591603754, 76.16933217328414685 ) ) ;
#16506=( BOUNDED_CURVE ( )  B_SPLINE_CURVE ( 3, ( #17681, #14276, #1518, #3110 ),
 .UNSPECIFIED., .F., .F. ) 
 B_SPLINE_CURVE_WITH_KNOTS ( ( 4, 4 ),
 ( 1.579404754493129337, 1.650417730407532479 ),
 .UNSPECIFIED. ) 
 CURVE ( )  GEOMETRIC_REPRESENTATION_ITEM ( )  RATIONAL_B_SPLINE_CURVE ( ( 1.000000000000000000, 0.9995798072522218414, 0.9995798072522218414, 1.000000000000000000 ) ) 
 REPRESENTATION_ITEM ( '' )  );
#16508=CARTESIAN_POINT ( 'NONE',  ( 8.949991632966883159, 41.61741720307092152, 76.25788209700408515 ) ) ;
#16509=EDGE_CURVE ( 'NONE', #14083, #6021, #17559, .T. ) ;
#16510=DIRECTION ( 'NONE',  ( -0.003070188988870460947, 0.009708901767422541129, 0.9999481542390301625 ) ) ;
#16513=CARTESIAN_POINT ( 'NONE',  ( -7.863115711494208071, 41.48039487425794647, 78.93576421268289778 ) ) ;
#16514=EDGE_CURVE ( 'NONE', #9686, #17850, #15815, .T. ) ;
#16516=LINE ( 'NONE', #5220, #1078 ) ;
#16517=ORIENTED_EDGE ( 'NONE', *, *, #18715, .T. ) ;
#16518=LINE ( 'NONE', #18212, #1123 ) ;
#16519=ORIENTED_EDGE ( 'NONE', *, *, #913, .T. ) ;
#16520=LINE ( 'NONE', #229, #11564 ) ;
#16521=DIRECTION ( 'NONE',  ( -0.9999689119394086223, 0.007885122365275665235, -1.526048693634353392E-16 ) ) ;
#16522=ORIENTED_EDGE ( 'NONE', *, *, #12127, .F. ) ;
#16523=CARTESIAN_POINT ( 'NONE',  ( -1.202011496911927324, 49.96493122755408223, 72.45433879953087342 ) ) ;
#16524=CARTESIAN_POINT ( 'NONE',  ( 8.774405178022840701, 41.09117345860662596, 75.37437276336991943 ) ) ;
#16525=CARTESIAN_POINT ( 'NONE',  ( -4.344504932464894331, 37.57120742909659583, 78.93669174070734584 ) ) ;
#16527=CARTESIAN_POINT ( 'NONE',  ( 0.5838098623046882318, 52.35423961828406192, 78.93669174070734584 ) ) ;
#16528=ORIENTED_EDGE ( 'NONE', *, *, #15594, .T. ) ;
#16529=EDGE_CURVE ( 'NONE', #12999, #19914, #15684, .T. ) ;
#16530=CARTESIAN_POINT ( 'NONE',  ( -4.030259451132765847, 50.97805036467345019, 76.44257241107362688 ) ) ;
#16531=ORIENTED_EDGE ( 'NONE', *, *, #8070, .F. ) ;
#16533=EDGE_CURVE ( 'NONE', #9230, #2058, #5984, .T. ) ;
#16535=CARTESIAN_POINT ( 'NONE',  ( -4.225701142979731095, 37.47645191542193999, 77.17835598703557309 ) ) ;
#16537=CARTESIAN_POINT ( 'NONE',  ( 1.658154530501163570, 36.04125148601230677, 76.16022115247204738 ) ) ;
#16539=CARTESIAN_POINT ( 'NONE',  ( 5.487461103983354072, 37.64135143674641171, 76.14207271482608519 ) ) ;
#16540=EDGE_CURVE ( 'NONE', #12382, #17793, #14513, .T. ) ;
#16541=CARTESIAN_POINT ( 'NONE',  ( -7.600722970659354871, 47.61678050758295200, 78.31366413292410300 ) ) ;
#16544=EDGE_LOOP ( 'NONE', ( #6429, #15254, #4718, #10495 ) ) ;
#16546=CARTESIAN_POINT ( 'NONE',  ( 5.590052860727733552, 36.96774431777176062, 78.26671861549210973 ) ) ;
#16549=CARTESIAN_POINT ( 'NONE',  ( 2.119851040271390819, 52.81592988514039178, 72.45433879953087342 ) ) ;
#16551=ORIENTED_EDGE ( 'NONE', *, *, #20250, .T. ) ;
#16552=CARTESIAN_POINT ( 'NONE',  ( 8.850612593395874583, 41.31957191698789700, 78.01079203130994699 ) ) ;
#16554=ORIENTED_EDGE ( 'NONE', *, *, #6245, .F. ) ;
#16556=CARTESIAN_POINT ( 'NONE',  ( 0.5968135028669416808, 52.96212007873675276, 76.86006965461024265 ) ) ;
#16561=CARTESIAN_POINT ( 'NONE',  ( -4.385738940255031970, 50.72403773668145277, 76.01646854312687651 ) ) ;
#16562=DIRECTION ( 'NONE',  ( -1.540237394707284220E-16, -1.793354297423764243E-16, 1.000000000000000000 ) ) ;
#16565=CARTESIAN_POINT ( 'NONE',  ( 6.848903495604322877, 50.42928078925980628, 75.87133531663224062 ) ) ;
#16566=LINE ( 'NONE', #5163, #6793 ) ;
#16568=CARTESIAN_POINT ( 'NONE',  ( -3.168337701141985541, 36.83946597969015357, 78.91793020585129170 ) ) ;
#16569=CARTESIAN_POINT ( 'NONE',  ( 4.400857426521584514, 36.11798879971178167, 76.47837415541054895 ) ) ;
#16570=CARTESIAN_POINT ( 'NONE',  ( 8.390051116449676272, 39.93923995310483832, 78.49952087821802138 ) ) ;
#16574=CARTESIAN_POINT ( 'NONE',  ( 9.064651367107570579, 41.96105970016846243, 75.41143022427675646 ) ) ;
#16576=CARTESIAN_POINT ( 'NONE',  ( -7.215762730499807098, 41.44826869547889459, 78.81763548507551320 ) ) ;
#16578=ORIENTED_EDGE ( 'NONE', *, *, #5979, .F. ) ;
#16579=DIRECTION ( 'NONE',  ( 0.3165065846431827645, 0.9485903129789529098, 0.000000000000000000 ) ) ;
#16581=CARTESIAN_POINT ( 'NONE',  ( -3.509782604184570776, 36.19999572785945219, 77.03801799112748938 ) ) ;
#16583=EDGE_CURVE ( 'NONE', #10025, #6298, #15990, .T. ) ;
#16584=CARTESIAN_POINT ( 'NONE',  ( 8.908783915644443496, 41.49391506008672792, 75.36120592425527320 ) ) ;
#16585=CARTESIAN_POINT ( 'NONE',  ( 4.226735822238441465, 51.44133747523171252, 77.44183710417100031 ) ) ;
#16586=CARTESIAN_POINT ( 'NONE',  ( -5.389245695702296501, 49.84508174962770255, 75.45433879953088763 ) ) ;
#16588=CARTESIAN_POINT ( 'NONE',  ( 0.5867509473165513079, 52.35421642379873930, 77.38375056423674891 ) ) ;
#16594=CARTESIAN_POINT ( 'NONE',  ( 0.4466774018966609971, 52.96665978300602262, 75.99769453967874711 ) ) ;
#16595=VERTEX_POINT ( 'NONE', #17167 ) ;
#16596=FACE_OUTER_BOUND ( 'NONE', #12101, .T. ) ;
#16597=CARTESIAN_POINT ( 'NONE',  ( 8.882918921757626762, 41.41639603256331981, 78.93548851266230315 ) ) ;
#16598=CARTESIAN_POINT ( 'NONE',  ( 8.504176331704195846, 42.28161211148372445, 75.44322627322523545 ) ) ;
#16601=CARTESIAN_POINT ( 'NONE',  ( 8.951667845840693971, 41.62244091939069790, 77.14698585835439815 ) ) ;
#16604=VERTEX_POINT ( 'NONE', #2588 ) ;
#16606=CARTESIAN_POINT ( 'NONE',  ( 7.956821099345868120, 40.70147494987158154, 79.37917410394513240 ) ) ;
#16608=LINE ( 'NONE', #14793, #10292 ) ;
#16613=CARTESIAN_POINT ( 'NONE',  ( -4.705149740856862550, 37.08296527939383935, 78.93669174070734584 ) ) ;
#16614=EDGE_CURVE ( 'NONE', #5130, #15999, #8951, .T. ) ;
#16615=ORIENTED_EDGE ( 'NONE', *, *, #1866, .F. ) ;
#16617=CARTESIAN_POINT ( 'NONE',  ( 2.105044654678958960, 52.94034470533341619, 77.53128952716078004 ) ) ;
#16618=B_SPLINE_CURVE_WITH_KNOTS ( 'NONE', 3,
 ( #2229, #9044, #8829, #10760, #9154, #4023, #10549, #625, #7106, #17016, #13820, #12235, #20086, #18719, #5523, #948, #4132, #12444, #15645, #736, #17125, #7219, #4340, #2548, #13719, #15532, #1062 ),
 .UNSPECIFIED., .F., .F.,
 ( 4, 1, 1, 1, 1, 1, 1, 1, 1, 1, 1, 1, 1, 1, 1, 1, 1, 1, 1, 1, 1, 1, 1, 1, 4 ),
 ( 0.000000000000000000, 0.05524556061070538121, 0.1069179814647366472, 0.1553727729060086771, 0.2000758033479648479, 0.2417614041178833273, 0.2799066487053696317, 0.3152370222690974444, 0.3476361288249658066, 0.3788200842211088548, 0.4103815830948299714, 0.4425365161269811387, 0.4758329365342930384, 0.5105782220665333604, 0.5468313811506283484, 0.5849849847693828764, 0.6253480228319793222, 0.6671656491570584491, 0.7102157423341657339, 0.7546653220675233475, 0.8003710923354008244, 0.8474641787091774514, 0.8966644363699035614, 0.9474646149202431422, 1.000000000000000000 ),
 .UNSPECIFIED. ) ;
#16622=FACE_OUTER_BOUND ( 'NONE', #6665, .T. ) ;
#16623=VECTOR ( 'NONE', #19810, 1000.000000000000114 ) ;
#16624=VERTEX_POINT ( 'NONE', #11270 ) ;
#16629=CARTESIAN_POINT ( 'NONE',  ( 8.405094150187295554, 41.90291579521269227, 78.13275527786953489 ) ) ;
#16630=CARTESIAN_POINT ( 'NONE',  ( 7.992842972995377160, 41.12996670827969581, 75.40210940951681096 ) ) ;
#16631=DIRECTION ( 'NONE',  ( -0.5941461771851692664, -0.8043570849667761591, -2.357623395011396791E-16 ) ) ;
#16632=AXIS2_PLACEMENT_3D ( 'NONE', #2858, #4643, #21017 ) ;
#16634=CARTESIAN_POINT ( 'NONE',  ( 0.3955195401054462656, 52.96707764484158787, 78.86056079792015794 ) ) ;
#16636=CARTESIAN_POINT ( 'NONE',  ( -4.592862224480082745, 51.32295045326189609, 75.97198585835440099 ) ) ;
#16637=VECTOR ( 'NONE', #18353, 1000.000000000000000 ) ;
#16639=ORIENTED_EDGE ( 'NONE', *, *, #3001, .F. ) ;
#16640=CARTESIAN_POINT ( 'NONE',  ( -3.431593788640828535, 36.97795561491845007, 77.76122236671984922 ) ) ;
#16641=CARTESIAN_POINT ( 'NONE',  ( -7.496610734713931912, 40.31662449841055462, 77.72888818034803649 ) ) ;
#16642=AXIS2_PLACEMENT_3D ( 'NONE', #6973, #1892, #11588 ) ;
#16643=FACE_OUTER_BOUND ( 'NONE', #20068, .T. ) ;
#16646=VECTOR ( 'NONE', #13969, 1000.000000000000114 ) ;
#16648=LINE ( 'NONE', #5036, #4386 ) ;
#16649=CARTESIAN_POINT ( 'NONE',  ( 5.388220764666090012, 37.58132116110721199, 78.33482135361461474 ) ) ;
#16650=EDGE_CURVE ( 'NONE', #2739, #10557, #13767, .T. ) ;
#16657=EDGE_LOOP ( 'NONE', ( #9765, #6979, #4931, #11280 ) ) ;
#16658=VECTOR ( 'NONE', #5326, 1000.000000000000114 ) ;
#16659=CARTESIAN_POINT ( 'NONE',  ( -4.709702680700027955, 38.02233484874552261, 75.39928922905468767 ) ) ;
#16662=CARTESIAN_POINT ( 'NONE',  ( -4.156729428781747337, 37.43250522858453877, 76.44623874561141008 ) ) ;
#16663=EDGE_CURVE ( 'NONE', #16858, #5644, #17832, .T. ) ;
#16664=ADVANCED_FACE ( 'NONE', ( #12648 ), #12117, .T. ) ;
#16665=ORIENTED_EDGE ( 'NONE', *, *, #20787, .T. ) ;
#16666=PLANE ( 'NONE',  #18695 ) ;
#16667=CIRCLE ( 'NONE', #7489, 6.000000000000002665 ) ;
#16669=CARTESIAN_POINT ( 'NONE',  ( -4.804273704418943858, 51.17188354996588373, 76.37148643835737971 ) ) ;
#16670=CARTESIAN_POINT ( 'NONE',  ( 2.054490523354237208, 52.82782863985672606, 76.04066109323893841 ) ) ;
#16673=CARTESIAN_POINT ( 'NONE',  ( 6.398363615859712361, 50.76207644957375464, 75.46588380158773646 ) ) ;
#16675=CARTESIAN_POINT ( 'NONE',  ( 5.574863508716481064, 50.62051970816712299, 77.07851092216984057 ) ) ;
#16676=LINE ( 'NONE', #16779, #7553 ) ;
#16677=CARTESIAN_POINT ( 'NONE',  ( 3.958912314344054550, 36.72196658547137815, 76.73963291717792856 ) ) ;
#16678=CARTESIAN_POINT ( 'NONE',  ( 8.515342467852711650, 40.31474608159486195, 79.26294543469528264 ) ) ;
#16681=CARTESIAN_POINT ( 'NONE',  ( -0.9435709597102902579, 52.23013218523595214, 78.24716094272973521 ) ) ;
#16685=VERTEX_POINT ( 'NONE', #1708 ) ;
#16686=EDGE_CURVE ( 'NONE', #4858, #1116, #8451, .T. ) ;
#16687=DIRECTION ( 'NONE',  ( -1.540237394707284220E-16, -1.793354297423764243E-16, 1.000000000000000000 ) ) ;
#16689=FACE_OUTER_BOUND ( 'NONE', #20135, .T. ) ;
#16691=CARTESIAN_POINT ( 'NONE',  ( -3.004571163435685310, 37.81598267955332915, 77.68963291717793140 ) ) ;
#16692=LINE ( 'NONE', #2006, #14360 ) ;
#16694=B_SPLINE_SURFACE_WITH_KNOTS ( 'NONE', 3, 1, ( 
 ( #13889, #12511 ),
 ( #20372, #10930 ),
 ( #17401, #15817 ),
 ( #5918, #11133 ),
 ( #17295, #20784 ),
 ( #15714, #12718 ),
 ( #15605, #2827 ),
 ( #7620, #2617 ),
 ( #5806, #14102 ),
 ( #18792, #1229 ),
 ( #1132, #20584 ),
 ( #7720, #1021 ),
 ( #6218, #12616 ),
 ( #12415, #14200 ),
 ( #4513, #14001 ),
 ( #10731, #10831 ),
 ( #17502, #4207 ),
 ( #19103, #20678 ),
 ( #20484, #2926 ) ),
 .UNSPECIFIED., .F., .F., .F.,
 ( 4, 1, 1, 1, 1, 1, 1, 1, 1, 1, 1, 1, 1, 1, 1, 1, 4 ),
 ( 2, 2 ),
 ( 0.000000000000000000, 0.1068357064626556524, 0.2062857352809531475, 0.2975635024103033266, 0.3806658168942347320, 0.4556695234475648948, 0.5225582867794639208, 0.5822950421180911329, 0.6340416422721021350, 0.6795378779249960921, 0.7218021178892558565, 0.7627433693661896941, 0.8042009657065650741, 0.8472253578321278233, 0.8932235139329930407, 0.9440217631200717996, 0.9999999999999998890 ),
 ( 0.000000000000000000, 1.000000000000000000 ),
 .UNSPECIFIED. ) ;
#16695=CARTESIAN_POINT ( 'NONE',  ( 8.240650035186204647, 41.41153111371846762, 76.01674029036281866 ) ) ;
#16697=FACE_OUTER_BOUND ( 'NONE', #11044, .T. ) ;
#16698=CARTESIAN_POINT ( 'NONE',  ( 5.243738908420800371, 37.46719647903651662, 77.75916469768418438 ) ) ;
#16701=EDGE_LOOP ( 'NONE', ( #3261, #10280, #6150, #14382 ) ) ;
#16702=CARTESIAN_POINT ( 'NONE',  ( 0.5245867512892138373, 52.35470670054147035, 75.97350791242078571 ) ) ;
#16703=CIRCLE ( 'NONE', #13639, 8.199999999999995737 ) ;
#16704=VERTEX_POINT ( 'NONE', #2881 ) ;
#16705=CARTESIAN_POINT ( 'NONE',  ( -4.699348147190204550, 37.07867987585472491, 75.97299512023676016 ) ) ;
#16707=CARTESIAN_POINT ( 'NONE',  ( -4.470581213684321042, 37.66433489937099210, 78.89646723195187406 ) ) ;
#16709=CARTESIAN_POINT ( 'NONE',  ( -4.900087432442488122, 37.22695789959892920, 77.32461911834714385 ) ) ;
#16711=CARTESIAN_POINT ( 'NONE',  ( 5.884818748728627646, 51.14141135607439992, 78.06587361566768379 ) ) ;
#16712=ORIENTED_EDGE ( 'NONE', *, *, #18315, .F. ) ;
#16714=CIRCLE ( 'NONE', #1414, 8.199999999999995737 ) ;
#16715=CARTESIAN_POINT ( 'NONE',  ( 6.482969723869566714, 49.79324824044548592, 77.22012844410386379 ) ) ;
#16717=DIRECTION ( 'NONE',  ( 0.3165065846431826535, 0.9485903129789529098, 2.188653791613874008E-16 ) ) ;
#16718=ORIENTED_EDGE ( 'NONE', *, *, #11073, .T. ) ;
#16721=DIRECTION ( 'NONE',  ( 0.007885122365275663500, 0.9999689119394085113, 1.805443505845543142E-16 ) ) ;
#16724=CARTESIAN_POINT ( 'NONE',  ( 2.082493151224042549, 52.94052253222597670, 77.39871602076138402 ) ) ;
#16727=CARTESIAN_POINT ( 'NONE',  ( -7.885657102084565828, 41.56435211639550431, 79.54845644658969661 ) ) ;
#16728=ORIENTED_EDGE ( 'NONE', *, *, #920, .F. ) ;
#16731=ORIENTED_EDGE ( 'NONE', *, *, #8184, .F. ) ;
#16732=CARTESIAN_POINT ( 'NONE',  ( -7.694987716518704168, 47.31164717387682828, 78.21926933574907537 ) ) ;
#16734=ORIENTED_EDGE ( 'NONE', *, *, #8972, .T. ) ;
#16735=CARTESIAN_POINT ( 'NONE',  ( 1.964251312053305165, 36.08998497932209659, 72.45433879953085921 ) ) ;
#16737=CARTESIAN_POINT ( 'NONE',  ( -4.104527287216266807, 50.75212113806905023, 79.54777180229389444 ) ) ;
#16741=CARTESIAN_POINT ( 'NONE',  ( 4.004906909697989015, 36.73854140438177041, 77.43080938776617472 ) ) ;
#16745=VECTOR ( 'NONE', #5274, 1000.000000000000227 ) ;
#16746=CARTESIAN_POINT ( 'NONE',  ( -7.056725745502300029, 41.40963693795823275, 76.59276269229415846 ) ) ;
#16749=CARTESIAN_POINT ( 'NONE',  ( 6.853523395152754105, 50.42586825556427499, 78.95155228521747404 ) ) ;
#16750=EDGE_CURVE ( 'NONE', #2871, #14563, #1386, .T. ) ;
#16752=CARTESIAN_POINT ( 'NONE',  ( 5.471586674567812558, 37.63000815068602378, 76.06531707679772580 ) ) ;
#16754=CARTESIAN_POINT ( 'NONE',  ( 3.117507734380600581, 51.94062193790708903, 75.45433879953088763 ) ) ;
#16755=ORIENTED_EDGE ( 'NONE', *, *, #17674, .F. ) ;
#16756=B_SPLINE_CURVE_WITH_KNOTS ( 'NONE', 3,
 ( #10071, #11870, #8574, #18349, #16552, #13361, #19831, #18243, #16763, #20038, #3664 ),
 .UNSPECIFIED., .F., .F.,
 ( 4, 1, 1, 1, 1, 1, 1, 1, 4 ),
 ( 0.000000000000000000, 0.1094333067106434410, 0.2184679721593839052, 0.3300813608894926365, 0.4462978032959263319, 0.5702501687912749917, 0.7022991718047063570, 0.8456887798043180027, 0.9999999999999998890 ),
 .UNSPECIFIED. ) ;
#16757=DIRECTION ( 'NONE',  ( -1.540237394707284467E-16, -1.793354297423764243E-16, 1.000000000000000000 ) ) ;
#16758=EDGE_CURVE ( 'NONE', #11489, #6337, #17767, .T. ) ;
#16761=CARTESIAN_POINT ( 'NONE',  ( -7.191377436723248806, 41.79953674621017257, 77.84082762752957763 ) ) ;
#16762=ORIENTED_EDGE ( 'NONE', *, *, #1300, .T. ) ;
#16763=CARTESIAN_POINT ( 'NONE',  ( 8.985665979147935190, 41.72433548171385098, 78.13399373581940210 ) ) ;
#16765=ORIENTED_EDGE ( 'NONE', *, *, #9650, .F. ) ;
#16768=ORIENTED_EDGE ( 'NONE', *, *, #13310, .T. ) ;
#16769=CARTESIAN_POINT ( 'NONE',  ( 1.690580188175442533, 52.27889548997219293, 79.31285334339766280 ) ) ;
#16770=ORIENTED_EDGE ( 'NONE', *, *, #19848, .F. ) ;
#16771=CARTESIAN_POINT ( 'NONE',  ( 0.6935063668540784043, 52.36041438938426040, 77.40588291575248547 ) ) ;
#16773=EDGE_CURVE ( 'NONE', #8766, #2112, #4097, .T. ) ;
#16775=ADVANCED_FACE ( 'NONE', ( #13190 ), #16877, .F. ) ;
#16777=CARTESIAN_POINT ( 'NONE',  ( -4.887610060180215932, 37.21774136732800997, 76.16751655709613544 ) ) ;
#16779=CARTESIAN_POINT ( 'NONE',  ( 5.427780505986065762, 36.85179043424346190, 77.43080938776617472 ) ) ;
#16781=EDGE_CURVE ( 'NONE', #12015, #9638, #4980, .T. ) ;
#16782=CARTESIAN_POINT ( 'NONE',  ( 4.007614759266367344, 36.75676756950254287, 76.14998054923410109 ) ) ;
#16783=B_SPLINE_CURVE_WITH_KNOTS ( 'NONE', 3,
 ( #857, #20205, #12144, #15440, #3721, #18624, #3934, #18415, #16924, #5538, #11827 ),
 .UNSPECIFIED., .F., .F.,
 ( 4, 1, 1, 1, 1, 1, 1, 1, 4 ),
 ( 0.000000000000000000, 0.2026380577750736822, 0.3699241180509920679, 0.5036394156482512097, 0.6074627879459471025, 0.6969630674522783176, 0.7888943515530689732, 0.8885774882565341537, 1.000000000000000000 ),
 .UNSPECIFIED. ) ;
#16784=VERTEX_POINT ( 'NONE', #15398 ) ;
#16786=DIRECTION ( 'NONE',  ( -0.3014928876834147564, 0.9534151938875496946, -0.01007505536868189694 ) ) ;
#16788=ORIENTED_EDGE ( 'NONE', *, *, #13526, .T. ) ;
#16789=ORIENTED_EDGE ( 'NONE', *, *, #18627, .F. ) ;
#16791=CARTESIAN_POINT ( 'NONE',  ( 6.374498485212880539, 49.86568965500833883, 79.04700635913849283 ) ) ;
#16792=ORIENTED_EDGE ( 'NONE', *, *, #1588, .T. ) ;
#16793=CARTESIAN_POINT ( 'NONE',  ( -3.495943983152252965, 36.18977369595653926, 76.77671532909576513 ) ) ;
#16794=CARTESIAN_POINT ( 'NONE',  ( 6.774925554820337759, 37.81441096401221102, 75.87985893138584004 ) ) ;
#16795=DIRECTION ( 'NONE',  ( 0.8136266022444372803, 0.5813877811927012917, 2.295812393977109100E-16 ) ) ;
#16796=CARTESIAN_POINT ( 'NONE',  ( 4.098112526425296664, 51.53634632258648907, 76.74217282813371810 ) ) ;
#16797=DIRECTION ( 'NONE',  ( 0.3165065846431827645, 0.9485903129789529098, 0.000000000000000000 ) ) ;
#16798=CARTESIAN_POINT ( 'NONE',  ( 8.787829143201872029, 41.13140593384864729, 78.45948585835439815 ) ) ;
#16799=CARTESIAN_POINT ( 'NONE',  ( 0.8446148313103564176, 52.35218307230691437, 77.70257284945761000 ) ) ;
#16801=CARTESIAN_POINT ( 'NONE',  ( 4.169442455018850247, 51.48365777767921969, 75.94315254166910734 ) ) ;
#16802=ADVANCED_FACE ( 'NONE', ( #18575 ), #2077, .F. ) ;
#16804=CARTESIAN_POINT ( 'NONE',  ( 8.378499831177387946, 41.81317597918418016, 76.33673353730570454 ) ) ;
#16806=EDGE_CURVE ( 'NONE', #4528, #4917, #200, .T. ) ;
#16807=CARTESIAN_POINT ( 'NONE',  ( 0.5548452009814999197, 52.35446810154547848, 75.97250646058495249 ) ) ;
#16808=EDGE_CURVE ( 'NONE', #2288, #559, #8186, .T. ) ;
#16810=CARTESIAN_POINT ( 'NONE',  ( -4.718161399584266391, 37.09257646755418847, 75.97198585835440099 ) ) ;
#16812=CARTESIAN_POINT ( 'NONE',  ( 8.618999050077414736, 42.86439581318003178, 75.78893996921105725 ) ) ;
#16814=DIRECTION ( 'NONE',  ( 1.540237394707283727E-16, 1.793354297423763257E-16, -1.000000000000000000 ) ) ;
#16817=CARTESIAN_POINT ( 'NONE',  ( 5.425723373820400930, 50.72741113942812063, 77.95070864408322109 ) ) ;
#16820=CARTESIAN_POINT ( 'NONE',  ( 8.990918003704509331, 41.74007613249212767, 79.53018343098241871 ) ) ;
#16821=DIRECTION ( 'NONE',  ( -0.5800177190770277047, -0.8146038580541355989, -2.354238310054624259E-16 ) ) ;
#16822=CARTESIAN_POINT ( 'NONE',  ( -4.221808390846331527, 37.47367089672861340, 78.89427195578772967 ) ) ;
#16828=CARTESIAN_POINT ( 'NONE',  ( 2.000053588515297243, 52.94117259847497792, 77.17808573571203112 ) ) ;
#16829=CARTESIAN_POINT ( 'NONE',  ( -3.166333418787979248, 36.86031865481220393, 78.01078865174693533 ) ) ;
#16830=ADVANCED_FACE ( 'NONE', ( #1441 ), #16694, .T. ) ;
#16832=CARTESIAN_POINT ( 'NONE',  ( -8.071517288156909942, 42.25946119754487995, 79.44950456819475448 ) ) ;
#16836=CARTESIAN_POINT ( 'NONE',  ( 0.5221537403065015237, 44.16218137147968292, 75.45433879953088763 ) ) ;
#16841=CARTESIAN_POINT ( 'NONE',  ( -3.118414543444179010, 51.45676120087671279, 79.13154374754441278 ) ) ;
#16843=CARTESIAN_POINT ( 'NONE',  ( 0.8440572370183208051, 52.35217469777130361, 76.31365475201417325 ) ) ;
#16845=VERTEX_POINT ( 'NONE', #19196 ) ;
#16847=ORIENTED_EDGE ( 'NONE', *, *, #9856, .T. ) ;
#16849=CARTESIAN_POINT ( 'NONE',  ( 5.037341483232629535, 37.31725042616477594, 72.45433879953087342 ) ) ;
#16850=CARTESIAN_POINT ( 'NONE',  ( 6.616107328214575034, 50.60123794050897317, 77.65065976741861675 ) ) ;
#16851=DIRECTION ( 'NONE',  ( -0.3165065846431827645, -0.9485903129789529098, 0.000000000000000000 ) ) ;
#16852=CARTESIAN_POINT ( 'NONE',  ( 5.483018176437226998, 37.63302714415535632, 76.07972420133452829 ) ) ;
#16854=CARTESIAN_POINT ( 'NONE',  ( 8.474591150375477611, 46.20736444405172705, 75.44552964019689512 ) ) ;
#16855=CARTESIAN_POINT ( 'NONE',  ( -4.652687709939232086, 51.28020135170361016, 75.36022115247205022 ) ) ;
#16857=CARTESIAN_POINT ( 'NONE',  ( 8.211364901683856132, 41.32396416616596468, 78.49453464888588883 ) ) ;
#16858=VERTEX_POINT ( 'NONE', #1336 ) ;
#16863=VERTEX_POINT ( 'NONE', #2720 ) ;
#16866=CARTESIAN_POINT ( 'NONE',  ( -1.598719209087998694, 36.85794301744668644, 72.45432679953087529 ) ) ;
#16867=ORIENTED_EDGE ( 'NONE', *, *, #755, .T. ) ;
#16868=DIRECTION ( 'NONE',  ( -0.9534635866061453857, -0.3015081906286223856, -2.009271279954815304E-16 ) ) ;
#16869=DIRECTION ( 'NONE',  ( -0.9534635866061452747, -0.3015081906286225522, -2.009271279954815797E-16 ) ) ;
#16871=CARTESIAN_POINT ( 'NONE',  ( 1.916709343768108864, 52.24291296276840768, 79.11969604467107331 ) ) ;
#16873=VERTEX_POINT ( 'NONE', #15915 ) ;
#16877=CYLINDRICAL_SURFACE ( 'NONE', #9313, 4.200000000000003730 ) ;
#16882=CARTESIAN_POINT ( 'NONE',  ( 1.187762653619208075, 52.20882925152060494, 75.41083127720757773 ) ) ;
#16883=ORIENTED_EDGE ( 'NONE', *, *, #14966, .F. ) ;
#16885=CARTESIAN_POINT ( 'NONE',  ( 0.5221537403065015237, 44.16218137147968292, 75.45433879953088763 ) ) ;
#16886=CARTESIAN_POINT ( 'NONE',  ( -7.269305757963094194, 41.60587264541594976, 78.93240053410227119 ) ) ;
#16889=CARTESIAN_POINT ( 'NONE',  ( 8.889576793745449734, 46.88836537034026719, 78.73595644658969661 ) ) ;
#16892=DIRECTION ( 'NONE',  ( 0.5813877811926937422, -0.8136266022444427204, -5.636455622144829957E-17 ) ) ;
#16893=CARTESIAN_POINT ( 'NONE',  ( 7.835155343763541502, 40.65736687995521237, 75.56834740413086138 ) ) ;
#16895=PLANE ( 'NONE',  #1274 ) ;
#16896=CARTESIAN_POINT ( 'NONE',  ( -7.340541098479197224, 41.83271662774721733, 79.54689003211581166 ) ) ;
#16898=CARTESIAN_POINT ( 'NONE',  ( 8.213642321612983466, 41.33058728280212080, 76.23356602378127889 ) ) ;
#16900=CARTESIAN_POINT ( 'NONE',  ( 4.500348682233642705, 51.23923067735156422, 75.54250430092201896 ) ) ;
#16902=VECTOR ( 'NONE', #18518, 1000.000000000000114 ) ;
#16904=CARTESIAN_POINT ( 'NONE',  ( 8.374753614891972120, 41.81346795830285146, 78.59502675972919405 ) ) ;
#16905=ORIENTED_EDGE ( 'NONE', *, *, #10781, .T. ) ;
#16906=LINE ( 'NONE', #6904, #655 ) ;
#16911=DIRECTION ( 'NONE',  ( -0.3165065846431827090, -0.9485903129789527988, 0.000000000000000000 ) ) ;
#16912=DIRECTION ( 'NONE',  ( 1.540237394707284220E-16, 1.793354297423764243E-16, -1.000000000000000000 ) ) ;
#16914=EDGE_CURVE ( 'NONE', #17483, #18148, #11345, .T. ) ;
#16915=FACE_OUTER_BOUND ( 'NONE', #13076, .T. ) ;
#16916=ORIENTED_EDGE ( 'NONE', *, *, #4402, .T. ) ;
#16918=B_SPLINE_CURVE_WITH_KNOTS ( 'NONE', 3,
 ( #4766, #781, #13757, #20228, #14075, #18649, #10595, #20556, #17062, #12481, #18963, #2489, #8983, #15466, #882 ),
 .UNSPECIFIED., .F., .F.,
 ( 4, 1, 1, 1, 1, 1, 1, 1, 1, 1, 1, 1, 4 ),
 ( 0.000000000000000000, 0.1027118292588455328, 0.1981555131143932502, 0.2874887429483043433, 0.3729525961046017413, 0.4183424594053214429, 0.4719402630404010424, 0.5343443080544488799, 0.6066182697135418245, 0.6887512500569755725, 0.7816623524051020677, 0.8855466611608181493, 1.000000000000000000 ),
 .UNSPECIFIED. ) ;
#16919=CARTESIAN_POINT ( 'NONE',  ( 8.491509432166619575, 42.60773501221702730, 79.34093170394821470 ) ) ;
#16922=DIRECTION ( 'NONE',  ( -1.540237394707284220E-16, -1.793354297423764243E-16, 1.000000000000000000 ) ) ;
#16924=CARTESIAN_POINT ( 'NONE',  ( 5.710003222748535556, 51.27054054311695808, 77.28795170149270177 ) ) ;
#16925=DIRECTION ( 'NONE',  ( -0.5813877811927011807, 0.8136266022444372803, 5.636455622144619183E-17 ) ) ;
#16928=CARTESIAN_POINT ( 'NONE',  ( -0.5048357562844464352, 52.90269622882259881, 79.29516791311903035 ) ) ;
#16929=CARTESIAN_POINT ( 'NONE',  ( -7.073844619497298147, 47.06934724366217182, 78.18191347276355430 ) ) ;
#16931=CARTESIAN_POINT ( 'NONE',  ( 6.837774032321189743, 37.85932018500469809, 76.05683950549904182 ) ) ;
#16932=ORIENTED_EDGE ( 'NONE', *, *, #13386, .T. ) ;
#16933=CARTESIAN_POINT ( 'NONE',  ( 5.934652055452926511, 51.10460149980519873, 77.05868164888072158 ) ) ;
#16934=ORIENTED_EDGE ( 'NONE', *, *, #14063, .T. ) ;
#16935=FACE_OUTER_BOUND ( 'NONE', #16347, .T. ) ;
#16937=ORIENTED_EDGE ( 'NONE', *, *, #12361, .F. ) ;
#16939=AXIS2_PLACEMENT_3D ( 'NONE', #12471, #14262, #4574 ) ;
#16940=DIRECTION ( 'NONE',  ( -0.9999689119394085113, 0.007885122365275831768, -1.526048693634352652E-16 ) ) ;
#16941=CARTESIAN_POINT ( 'NONE',  ( -4.139232521079847515, 50.72732204858985483, 79.54845644658969661 ) ) ;
#16942=CARTESIAN_POINT ( 'NONE',  ( 6.531299583006453524, 48.82481648921748274, 72.45433879953087342 ) ) ;
#16943=CARTESIAN_POINT ( 'NONE',  ( 0.8457719648580424021, 52.35216117651211221, 76.42615000023204175 ) ) ;
#16945=CARTESIAN_POINT ( 'NONE',  ( 0.5271520053606592038, 52.96603967447732231, 78.93427191990714675 ) ) ;
#16946=ORIENTED_EDGE ( 'NONE', *, *, #7772, .F. ) ;
#16948=VERTEX_POINT ( 'NONE', #18025 ) ;
#16951=CARTESIAN_POINT ( 'NONE',  ( -7.845278861804691140, 41.41922261456151233, 76.30903472146037814 ) ) ;
#16952=LINE ( 'NONE', #8670, #1498 ) ;
#16953=PLANE ( 'NONE',  #14897 ) ;
#16956=CIRCLE ( 'NONE', #8806, 8.199999999999995737 ) ;
#16957=EDGE_LOOP ( 'NONE', ( #6006, #8064, #20362, #4286 ) ) ;
#16958=CARTESIAN_POINT ( 'NONE',  ( 8.824963465026481657, 41.24269985211446254, 78.91056401563228917 ) ) ;
#16959=VERTEX_POINT ( 'NONE', #50 ) ;
#16963=CARTESIAN_POINT ( 'NONE',  ( -7.980074661670381708, 41.84304719859172650, 77.46376836651262465 ) ) ;
#16964=ORIENTED_EDGE ( 'NONE', *, *, #15096, .T. ) ;
#16966=CARTESIAN_POINT ( 'NONE',  ( 0.4220451763538803913, 52.96170309347347427, 77.42739368347497475 ) ) ;
#16970=CARTESIAN_POINT ( 'NONE',  ( -5.927888611570137911, 47.57933715648534445, 78.78375056423675460 ) ) ;
#16972=ORIENTED_EDGE ( 'NONE', *, *, #2952, .T. ) ;
#16973=CARTESIAN_POINT ( 'NONE',  ( -4.451329120265561379, 50.67716939545569232, 76.44036821129557779 ) ) ;
#16974=DIRECTION ( 'NONE',  ( -0.9485903129789495791, 0.3165065846431928120, -8.934458285744765648E-17 ) ) ;
#16975=AXIS2_PLACEMENT_3D ( 'NONE', #11893, #3788, #10309 ) ;
#16977=CARTESIAN_POINT ( 'NONE',  ( 0.5221537403065005245, 44.16218137147968292, 82.45433879953087342 ) ) ;
#16978=CARTESIAN_POINT ( 'NONE',  ( 5.398882651910504649, 50.75441279359508684, 77.28963291717792572 ) ) ;
#16980=CARTESIAN_POINT ( 'NONE',  ( -3.140505196763866191, 36.82560845944811945, 78.82932626445051483 ) ) ;
#16981=ORIENTED_EDGE ( 'NONE', *, *, #1866, .T. ) ;
#16982=EDGE_LOOP ( 'NONE', ( #4790, #903, #18100, #13301 ) ) ;
#16983=CARTESIAN_POINT ( 'NONE',  ( 1.389792438032094735, 52.96007428365597036, 75.46169036918907125 ) ) ;
#16987=CARTESIAN_POINT ( 'NONE',  ( 6.946924939155297629, 50.35687629745329019, 76.28194508213313441 ) ) ;
#16990=B_SPLINE_SURFACE_WITH_KNOTS ( 'NONE', 3, 1, ( 
 ( #2247, #8746 ),
 ( #3727, #8322 ),
 ( #19688, #5112 ),
 ( #10246, #15232 ),
 ( #6816, #19795 ),
 ( #15128, #537 ),
 ( #5423, #11942 ),
 ( #11733, #14901 ),
 ( #7127, #13628 ),
 ( #20104, #16513 ),
 ( #5541, #11631 ) ),
 .UNSPECIFIED., .F., .F., .F.,
 ( 4, 1, 1, 1, 1, 1, 1, 1, 4 ),
 ( 2, 2 ),
 ( 0.000000000000000000, 0.1532941345222613438, 0.2882053437387906425, 0.4087820921566970855, 0.5188196696909340710, 0.6272811593758456095, 0.7389121241215087510, 0.8614321729660930904, 1.000000000000000000 ),
 ( 0.000000000000000000, 1.000000000000000000 ),
 .UNSPECIFIED. ) ;
#16991=CARTESIAN_POINT ( 'NONE',  ( -3.416741549526295163, 52.16336322705762996, 76.06019729239972094 ) ) ;
#16993=EDGE_CURVE ( 'NONE', #13992, #18313, #15049, .T. ) ;
#16994=AXIS2_PLACEMENT_3D ( 'NONE', #5799, #4200, #4703 ) ;
#16995=CARTESIAN_POINT ( 'NONE',  ( -0.9436870690626137925, 52.23009998296729606, 72.45433879953087342 ) ) ;
#16997=CARTESIAN_POINT ( 'NONE',  ( 4.552551799799910981, 51.21148827903365941, 79.39429067157672648 ) ) ;
#17000=CARTESIAN_POINT ( 'NONE',  ( 4.104125825492272561, 51.53190454079617666, 76.88467537290178200 ) ) ;
#17004=CARTESIAN_POINT ( 'NONE',  ( 8.790110392356673685, 41.13824298228534104, 76.23356602378127889 ) ) ;
#17012=CARTESIAN_POINT ( 'NONE',  ( 8.348147950866749767, 41.73372909538741027, 78.88894238123772595 ) ) ;
#17016=CARTESIAN_POINT ( 'NONE',  ( -3.448881463449838591, 52.14039722128521959, 78.93778436892569061 ) ) ;
#17018=CARTESIAN_POINT ( 'NONE',  ( -4.518657848439217695, 36.94521123081658942, 76.91875223014945107 ) ) ;
#17020=DIRECTION ( 'NONE',  ( -0.5941461771852041274, -0.8043570849667502909, 3.170109439321510848E-15 ) ) ;
#17021=EDGE_CURVE ( 'NONE', #20176, #14506, #1207, .T. ) ;
#17024=ORIENTED_EDGE ( 'NONE', *, *, #2413, .F. ) ;
#17027=CARTESIAN_POINT ( 'NONE',  ( 6.461593583102923866, 49.81579045121515747, 77.32164228125272132 ) ) ;
#17028=FACE_OUTER_BOUND ( 'NONE', #17776, .T. ) ;
#17032=CARTESIAN_POINT ( 'NONE',  ( 8.344156084401983975, 42.16610768104432339, 78.13567616980381558 ) ) ;
#17034=ADVANCED_FACE ( 'NONE', ( #9201 ), #9403, .T. ) ;
#17036=EDGE_CURVE ( 'NONE', #19846, #15434, #14779, .T. ) ;
#17037=CARTESIAN_POINT ( 'NONE',  ( -4.388425821632080392, 51.46903322184264340, 76.24813767079230331 ) ) ;
#17039=CARTESIAN_POINT ( 'NONE',  ( -7.726407013549337677, 47.24009745779464708, 77.87251963618699335 ) ) ;
#17041=B_SPLINE_SURFACE_WITH_KNOTS ( 'NONE', 3, 1, ( 
 ( #14776, #12025 ),
 ( #3600, #8296 ),
 ( #3810, #10329 ),
 ( #8620, #197 ),
 ( #19869, #3698 ),
 ( #19661, #1906 ),
 ( #5088, #18081 ),
 ( #10009, #8398 ),
 ( #5290, #16801 ),
 ( #15101, #14877 ),
 ( #6988, #6791 ),
 ( #13297, #19768 ),
 ( #5190, #15315 ),
 ( #12437, #20401 ),
 ( #9037, #20287 ),
 ( #5832, #727 ),
 ( #15523, #16900 ),
 ( #1160, #8818 ),
 ( #938, #17327 ),
 ( #7425, #13810 ),
 ( #18916, #5719 ),
 ( #4228, #12337 ),
 ( #4331, #4121 ),
 ( #13919, #2322 ),
 ( #19024, #10436 ),
 ( #1053, #7210 ),
 ( #13711, #20186 ) ),
 .UNSPECIFIED., .F., .F., .F.,
 ( 4, 1, 1, 1, 1, 1, 1, 1, 1, 1, 1, 1, 1, 1, 1, 1, 1, 1, 1, 1, 1, 1, 1, 1, 4 ),
 ( 2, 2 ),
 ( 0.000000000000000000, 0.05111620615384394190, 0.09904209687041264087, 0.1432334450931441461, 0.1843589373079111415, 0.2222937343119009146, 0.2574440974212286459, 0.2893637488079585096, 0.3188910630028964910, 0.3474602836591745292, 0.3767670824238625316, 0.4074295047838343287, 0.4392621747742110894, 0.4730325979957886173, 0.5084852716492808122, 0.5462542205972961140, 0.5860610780164621225, 0.6283505634423164343, 0.6729648726644925638, 0.7201947540188263774, 0.7701882088044430530, 0.8230700400259792771, 0.8789456997408242600, 0.9378877171948971636, 1.000000000000000000 ),
 ( 0.000000000000000000, 1.000000000000000000 ),
 .UNSPECIFIED. ) ;
#17045=CARTESIAN_POINT ( 'NONE',  ( 5.908589799165438805, 51.12385263867304275, 77.19464465032660883 ) ) ;
#17046=VERTEX_POINT ( 'NONE', #19481 ) ;
#17047=AXIS2_PLACEMENT_3D ( 'NONE', #14056, #15775, #1187 ) ;
#17051=ORIENTED_EDGE ( 'NONE', *, *, #7806, .T. ) ;
#17054=CARTESIAN_POINT ( 'NONE',  ( -3.657653629913878657, 51.07144069248850116, 79.48422614141084352 ) ) ;
#17056=CARTESIAN_POINT ( 'NONE',  ( 0.4173134239696620895, 52.36160896100310680, 77.42739361215659244 ) ) ;
#17057=CARTESIAN_POINT ( 'NONE',  ( -3.361985906478571984, 37.00483926610629482, 79.26586447293077242 ) ) ;
#17058=ORIENTED_EDGE ( 'NONE', *, *, #4824, .T. ) ;
#17059=DIRECTION ( 'NONE',  ( 1.540237394707284220E-16, 1.793354297423764243E-16, -1.000000000000000000 ) ) ;
#17060=ORIENTED_EDGE ( 'NONE', *, *, #9049, .T. ) ;
#17061=CARTESIAN_POINT ( 'NONE',  ( 6.389146928619912735, 49.89105453160614445, 77.93146757323737006 ) ) ;
#17062=CARTESIAN_POINT ( 'NONE',  ( 4.584522445964598347, 52.10188785579612158, 77.22170381446332499 ) ) ;
#17063=DIRECTION ( 'NONE',  ( -1.540237394707284220E-16, -1.793354297423764243E-16, 1.000000000000000000 ) ) ;
#17067=AXIS2_PLACEMENT_3D ( 'NONE', #12791, #15994, #1208 ) ;
#17070=CARTESIAN_POINT ( 'NONE',  ( -5.561099455747291032, 37.71522085402570212, 75.56266266290518274 ) ) ;
#17072=ORIENTED_EDGE ( 'NONE', *, *, #863, .F. ) ;
#17074=CARTESIAN_POINT ( 'NONE',  ( 4.183728870144529211, 51.49929324773223271, 77.32903872825052360 ) ) ;
#17075=ORIENTED_EDGE ( 'NONE', *, *, #2865, .F. ) ;
#17076=CARTESIAN_POINT ( 'NONE',  ( 8.865792162213244509, 41.36506604770743678, 78.93669174070734584 ) ) ;
#17081=ORIENTED_EDGE ( 'NONE', *, *, #1943, .F. ) ;
#17091=CARTESIAN_POINT ( 'NONE',  ( -4.863118049607145110, 50.34667215411423058, 79.41941354504645290 ) ) ;
#17092=CARTESIAN_POINT ( 'NONE',  ( 0.5221537403065015237, 44.16218137147968292, 75.45433879953087342 ) ) ;
#17094=PRODUCT_CONTEXT ( 'NONE', #2614, 'mechanical' ) ;
#17095=CARTESIAN_POINT ( 'NONE',  ( -4.718161399584267279, 37.09257646755418847, 75.97198585835440099 ) ) ;
#17096=CARTESIAN_POINT ( 'NONE',  ( 5.239313537742215310, 50.86510457629285042, 78.59183879953087626 ) ) ;
#17097=CIRCLE ( 'NONE', #18781, 8.199999999999995737 ) ;
#17099=ORIENTED_EDGE ( 'NONE', *, *, #10957, .T. ) ;
#17100=CARTESIAN_POINT ( 'NONE',  ( -1.123656915330052408, 35.37488560990637865, 76.86610350541323555 ) ) ;
#17102=CARTESIAN_POINT ( 'NONE',  ( 6.961907239250668233, 50.34580947589670075, 76.63889762306028786 ) ) ;
#17105=ORIENTED_EDGE ( 'NONE', *, *, #3619, .T. ) ;
#17106=CARTESIAN_POINT ( 'NONE',  ( 6.266852414816192152, 50.85921847619028568, 79.48482414599367019 ) ) ;
#17108=CARTESIAN_POINT ( 'NONE',  ( 5.760694563098077481, 51.23309689197250094, 79.54845644658969661 ) ) ;
#17110=CARTESIAN_POINT ( 'NONE',  ( 7.671391872361274622, 40.16655736720171888, 76.83374382764255017 ) ) ;
#17111=VECTOR ( 'NONE', #10001, 1000.000000000000114 ) ;
#17112=CARTESIAN_POINT ( 'NONE',  ( -4.917446439638588629, 37.23978029895123143, 77.90454030471208569 ) ) ;
#17113=CARTESIAN_POINT ( 'NONE',  ( 4.539621438837683876, 52.13505442103787857, 76.64209438045911327 ) ) ;
#17114=CARTESIAN_POINT ( 'NONE',  ( -7.600977292165548072, 43.04172748006588023, 78.91532537708295081 ) ) ;
#17115=PLANE ( 'NONE',  #14394 ) ;
#17120=CARTESIAN_POINT ( 'NONE',  ( 8.871704507997348443, 41.38278572309461367, 78.93627637315103129 ) ) ;
#17121=VECTOR ( 'NONE', #17544, 1000.000000000000227 ) ;
#17122=VERTEX_POINT ( 'NONE', #7900 ) ;
#17124=CARTESIAN_POINT ( 'NONE',  ( -6.254105203661088908, 41.71089193230473313, 78.61536821129558916 ) ) ;
#17125=CARTESIAN_POINT ( 'NONE',  ( -4.092737432821778931, 51.68032131864361389, 79.48422614141084352 ) ) ;
#17127=CARTESIAN_POINT ( 'NONE',  ( -4.641234702847270910, 37.03575381547093315, 77.24798498253255730 ) ) ;
#17128=CARTESIAN_POINT ( 'NONE',  ( -7.883865680119443553, 46.78753189708820770, 79.41298732254628590 ) ) ;
#17129=CARTESIAN_POINT ( 'NONE',  ( 5.435172323252741577, 36.85707235623052469, 77.60331851759366373 ) ) ;
#17131=CARTESIAN_POINT ( 'NONE',  ( -4.357516591192299060, 37.58081861725695205, 75.97198585835440099 ) ) ;
#17132=ORIENTED_EDGE ( 'NONE', *, *, #14052, .F. ) ;
#17134=DIRECTION ( 'NONE',  ( -0.9480563259966822143, -0.3181025035073955509, -2.030702297275135124E-16 ) ) ;
#17135=CARTESIAN_POINT ( 'NONE',  ( -4.412760631825748625, 36.86698922270430501, 75.37821288891845484 ) ) ;
#17138=CARTESIAN_POINT ( 'NONE',  ( 8.921473627994183531, 41.53194693301924190, 77.48121952543638713 ) ) ;
#17139=LINE ( 'NONE', #4040, #7831 ) ;
#17141=DIRECTION ( 'NONE',  ( -0.6080936526121289987, -0.7938652969193448206, -2.360290325043240801E-16 ) ) ;
#17143=CARTESIAN_POINT ( 'NONE',  ( -7.686167599515409066, 47.36069753439516461, 78.25347377718505015 ) ) ;
#17144=CARTESIAN_POINT ( 'NONE',  ( -5.507474035114395150, 38.61161641206103212, 78.58503192925951453 ) ) ;
#17145=CARTESIAN_POINT ( 'NONE',  ( -8.106954325919813797, 42.43031530731593648, 79.37810177255154542 ) ) ;
#17146=VERTEX_POINT ( 'NONE', #19272 ) ;
#17147=LINE ( 'NONE', #10782, #19081 ) ;
#17149=ORIENTED_EDGE ( 'NONE', *, *, #2497, .T. ) ;
#17150=CARTESIAN_POINT ( 'NONE',  ( -4.618682869335207108, 51.30449996580257022, 78.93596273702843291 ) ) ;
#17152=ORIENTED_EDGE ( 'NONE', *, *, #16424, .F. ) ;
#17155=CARTESIAN_POINT ( 'NONE',  ( -0.7151367401353951880, 52.21770371292401336, 75.80943630940421940 ) ) ;
#17156=CARTESIAN_POINT ( 'NONE',  ( -3.653812822066824673, 51.99396077543343608, 79.24282704039583791 ) ) ;
#17157=CARTESIAN_POINT ( 'NONE',  ( 6.691294758883309157, 37.75465145915448062, 79.45433879953087342 ) ) ;
#17158=CARTESIAN_POINT ( 'NONE',  ( 5.394726803408538274, 50.74878659197170805, 77.28963291717792572 ) ) ;
#17159=CARTESIAN_POINT ( 'NONE',  ( -3.533668833548941013, 36.21763952329489200, 78.50831005042292077 ) ) ;
#17160=EDGE_LOOP ( 'NONE', ( #5884, #2958, #7789, #15448 ) ) ;
#17164=DIRECTION ( 'NONE',  ( 0.3165065846431828200, 0.9485903129789527988, 0.000000000000000000 ) ) ;
#17166=LINE ( 'NONE', #3065, #18338 ) ;
#17167=CARTESIAN_POINT ( 'NONE',  ( 0.6452163281857689059, 52.96132085210302165, 79.54845644658969661 ) ) ;
#17170=CARTESIAN_POINT ( 'NONE',  ( 5.081221074959174189, 37.34619514398751505, 78.14228948390012874 ) ) ;
#17171=ORIENTED_EDGE ( 'NONE', *, *, #4599, .F. ) ;
#17172=CARTESIAN_POINT ( 'NONE',  ( -0.02399531697664270338, 35.98038931794833672, 79.45433879953087342 ) ) ;
#17173=VERTEX_POINT ( 'NONE', #6392 ) ;
#17176=CARTESIAN_POINT ( 'NONE',  ( -7.228585422969530327, 41.91720008378919005, 77.67112630499640602 ) ) ;
#17177=EDGE_LOOP ( 'NONE', ( #7598, #15727, #14458, #18347 ) ) ;
#17178=EDGE_CURVE ( 'NONE', #3682, #13937, #17790, .T. ) ;
#17181=CARTESIAN_POINT ( 'NONE',  ( 0.5221537403065019678, 44.16218137147968292, 72.45433879953087342 ) ) ;
#17183=CARTESIAN_POINT ( 'NONE',  ( -4.655845291449849377, 51.27794505956256188, 78.93463708245236887 ) ) ;
#17184=ADVANCED_FACE ( 'NONE', ( #19581 ), #6643, .F. ) ;
#17185=ORIENTED_EDGE ( 'NONE', *, *, #10036, .T. ) ;
#17187=CARTESIAN_POINT ( 'NONE',  ( 0.7836272451433452524, 52.96402169819676686, 78.85266037376247539 ) ) ;
#17189=CARTESIAN_POINT ( 'NONE',  ( -5.395957697070454806, 49.83809498072223931, 78.51765637652050600 ) ) ;
#17191=EDGE_CURVE ( 'NONE', #18638, #14937, #6535, .T. ) ;
#17195=CARTESIAN_POINT ( 'NONE',  ( -3.955205046931956403, 36.52901134360649138, 77.68963291717793140 ) ) ;
#17196=CARTESIAN_POINT ( 'NONE',  ( 5.239545088994572275, 50.86493353871018286, 78.62371398036725623 ) ) ;
#17199=CARTESIAN_POINT ( 'NONE',  ( 1.773874092659751600, 52.95704565865690228, 75.65494847458032268 ) ) ;
#17200=ORIENTED_EDGE ( 'NONE', *, *, #4257, .T. ) ;
#17201=CARTESIAN_POINT ( 'NONE',  ( 6.323093812904748923, 50.81767522096397727, 75.43719735689487038 ) ) ;
#17206=ORIENTED_EDGE ( 'NONE', *, *, #3758, .T. ) ;
#17208=CARTESIAN_POINT ( 'NONE',  ( -1.376885767552595174, 38.47063949360596524, 80.45433879953087342 ) ) ;
#17209=CARTESIAN_POINT ( 'NONE',  ( 7.675929975837751051, 40.18015835121261858, 76.38443001783366526 ) ) ;
#17212=CARTESIAN_POINT ( 'NONE',  ( 5.282950423531485917, 37.48574407745871895, 77.76022115247205591 ) ) ;
#17213=CARTESIAN_POINT ( 'NONE',  ( -7.419930862061532295, 40.07230896987099555, 78.54487611535471103 ) ) ;
#17214=CARTESIAN_POINT ( 'NONE',  ( 1.652727357819363974, 35.35299279957455099, 79.45433879953087342 ) ) ;
#17215=EDGE_CURVE ( 'NONE', #16470, #11222, #12376, .T. ) ;
#17216=CYLINDRICAL_SURFACE ( 'NONE', #812, 4.200000000000003730 ) ;
#17218=CARTESIAN_POINT ( 'NONE',  ( 0.8498507653315134913, 52.95607782800728813, 78.57205668465995529 ) ) ;
#17222=VECTOR ( 'NONE', #14571, 1000.000000000000000 ) ;
#17223=PLANE ( 'NONE',  #13922 ) ;
#17225=CARTESIAN_POINT ( 'NONE',  ( -4.249412910294118717, 50.83092575845958550, 78.93669174070734584 ) ) ;
#17227=CARTESIAN_POINT ( 'NONE',  ( 5.734785278855812685, 51.25223503655262647, 77.94915300234312383 ) ) ;
#17228=CARTESIAN_POINT ( 'NONE',  ( -7.897028013293802218, 46.74808354956180523, 79.45433879953087342 ) ) ;
#17229=DIRECTION ( 'NONE',  ( 1.540237394707284220E-16, 1.793354297423764243E-16, -1.000000000000000000 ) ) ;
#17230=ORIENTED_EDGE ( 'NONE', *, *, #11092, .F. ) ;
#17231=CARTESIAN_POINT ( 'NONE',  ( -4.348661956197086731, 37.56557963644259956, 78.93669174070734584 ) ) ;
#17233=DIRECTION ( 'NONE',  ( -0.5813877811927011807, 0.8136266022444372803, 5.636455622144619183E-17 ) ) ;
#17240=CARTESIAN_POINT ( 'NONE',  ( -4.397525688316068937, 51.46253079027765409, 76.14127734336351239 ) ) ;
#17242=CARTESIAN_POINT ( 'NONE',  ( -5.441938187485694911, 38.56320772136268715, 79.03330530165142420 ) ) ;
#17243=EDGE_CURVE ( 'NONE', #6944, #5156, #14314, .T. ) ;
#17245=CARTESIAN_POINT ( 'NONE',  ( 0.8451174997408289480, 52.35581882004084520, 78.57205694827298714 ) ) ;
#17246=VERTEX_POINT ( 'NONE', #9435 ) ;
#17247=CARTESIAN_POINT ( 'NONE',  ( 1.920999019869927826, 52.24223821644631727, 75.80014879453128174 ) ) ;
#17248=VERTEX_POINT ( 'NONE', #16028 ) ;
#17250=CARTESIAN_POINT ( 'NONE',  ( -4.598246518171406727, 51.31910303412164609, 78.93669174070734584 ) ) ;
#17253=EDGE_LOOP ( 'NONE', ( #3050, #16712, #28, #1046 ) ) ;
#17255=EDGE_CURVE ( 'NONE', #10941, #8009, #15922, .T. ) ;
#17256=CARTESIAN_POINT ( 'NONE',  ( -0.5282253955477689278, 52.97542326866732054, 75.64626500862765113 ) ) ;
#17266=CARTESIAN_POINT ( 'NONE',  ( 5.241460166982748525, 50.86801069014953924, 78.59183879953087626 ) ) ;
#17269=CARTESIAN_POINT ( 'NONE',  ( 9.273778039597953438, 45.67340037358405169, 78.74919174070734584 ) ) ;
#17270=CARTESIAN_POINT ( 'NONE',  ( -4.285954277864442830, 37.51963121091066711, 77.94459252611197542 ) ) ;
#17271=CARTESIAN_POINT ( 'NONE',  ( 5.126612573611699197, 37.37671407926408307, 78.18547655874309044 ) ) ;
#17272=VERTEX_POINT ( 'NONE', #1446 ) ;
#17278=CARTESIAN_POINT ( 'NONE',  ( 5.159368991072407873, 51.67727186915629289, 75.44114465464750197 ) ) ;
#17281=CARTESIAN_POINT ( 'NONE',  ( -5.261478123908109872, 50.84518201112111058, 79.40394833312912226 ) ) ;
#17284=EDGE_CURVE ( 'NONE', #2386, #6017, #19615, .T. ) ;
#17286=EDGE_LOOP ( 'NONE', ( #480, #7882, #1818, #12881 ) ) ;
#17288=CARTESIAN_POINT ( 'NONE',  ( 0.6268041787565157286, 52.35390056590507868, 78.93480014378108933 ) ) ;
#17289=EDGE_LOOP ( 'NONE', ( #18856, #2860, #9670, #19929 ) ) ;
#17290=FACE_OUTER_BOUND ( 'NONE', #12298, .T. ) ;
#17295=CARTESIAN_POINT ( 'NONE',  ( 5.431844598077052666, 36.85469448565577011, 76.44059830477070250 ) ) ;
#17296=CARTESIAN_POINT ( 'NONE',  ( 5.658108625003792191, 37.01637447524286273, 75.97198585835440099 ) ) ;
#17298=FACE_OUTER_BOUND ( 'NONE', #5572, .T. ) ;
#17299=ADVANCED_FACE ( 'NONE', ( #19725 ), #3453, .T. ) ;
#17301=CARTESIAN_POINT ( 'NONE',  ( 2.008116822278622760, 52.95519856864822827, 75.93722239247614425 ) ) ;
#17305=CARTESIAN_POINT ( 'NONE',  ( -0.2332032163833130112, 52.32814213131982939, 75.48592037115906805 ) ) ;
#17309=ORIENTED_EDGE ( 'NONE', *, *, #11991, .F. ) ;
#17311=CARTESIAN_POINT ( 'NONE',  ( -3.557579061748612048, 36.23530104570325250, 76.03954924220039402 ) ) ;
#17312=CARTESIAN_POINT ( 'NONE',  ( 0.3869120917952214023, 35.96329670974014192, 75.45433879953087342 ) ) ;
#17313=ORIENTED_EDGE ( 'NONE', *, *, #10762, .F. ) ;
#17314=EDGE_CURVE ( 'NONE', #496, #4878, #5142, .T. ) ;
#17315=CARTESIAN_POINT ( 'NONE',  ( 5.319542448682613944, 51.55895818820005871, 79.51138782552760631 ) ) ;
#17319=AXIS2_PLACEMENT_3D ( 'NONE', #13067, #12652, #9463 ) ;
#17321=CARTESIAN_POINT ( 'NONE',  ( 6.521955874970234213, 49.75166928465916527, 76.54279163422609145 ) ) ;
#17322=CARTESIAN_POINT ( 'NONE',  ( -6.796670188453681760, 40.58727050948505166, 79.17963929739188700 ) ) ;
#17327=CARTESIAN_POINT ( 'NONE',  ( 4.638945281793899866, 51.13685495226798139, 75.47011219584838670 ) ) ;
#17329=VECTOR ( 'NONE', #13607, 1000.000000000000227 ) ;
#17330=CARTESIAN_POINT ( 'NONE',  ( -7.409257659412860519, 40.34942259774520323, 79.14159390612334732 ) ) ;
#17332=CARTESIAN_POINT ( 'NONE',  ( -0.9375046559398532153, 52.97987584641302305, 77.82884852524264829 ) ) ;
#17334=CARTESIAN_POINT ( 'NONE',  ( 0.3279640439667353413, 52.35988168082470651, 72.45433879953087342 ) ) ;
#17336=CARTESIAN_POINT ( 'NONE',  ( -4.383473025373059606, 51.47257230871590394, 78.45066232894264147 ) ) ;
#17338=CARTESIAN_POINT ( 'NONE',  ( -7.222486564444017709, 46.56685618261736437, 79.41298732254628590 ) ) ;
#17339=CARTESIAN_POINT ( 'NONE',  ( 5.428747419638988880, 36.85248135533887393, 77.49967648550449439 ) ) ;
#17342=CARTESIAN_POINT ( 'NONE',  ( 7.978846747739011036, 40.74910683537441258, 75.50210680925209772 ) ) ;
#17343=CARTESIAN_POINT ( 'NONE',  ( -4.036988424348830762, 50.97791528042453990, 76.24981967119607873 ) ) ;
#17346=B_SPLINE_SURFACE_WITH_KNOTS ( 'NONE', 3, 1, ( 
 ( #12460, #1082 ),
 ( #17144, #13838 ),
 ( #20318, #12562 ),
 ( #2565, #4466 ),
 ( #10778, #17460 ),
 ( #17242, #10569 ),
 ( #4156, #6479 ),
 ( #12771, #19563 ),
 ( #14679, #19155 ),
 ( #104, #8189 ),
 ( #17769, #20937 ),
 ( #4566, #360 ),
 ( #1604, #6584 ),
 ( #11186, #19250 ),
 ( #3292, #9700 ),
 ( #17869, #16179 ),
 ( #14365, #4662 ),
 ( #20842, #17655 ),
 ( #3196, #6269 ) ),
 .UNSPECIFIED., .F., .F., .F.,
 ( 4, 1, 1, 1, 1, 1, 1, 1, 1, 1, 1, 1, 1, 1, 1, 1, 4 ),
 ( 2, 2 ),
 ( 0.000000000000000000, 0.07046818618994758754, 0.1352139183126853383, 0.1951004221781245107, 0.2505542266086520642, 0.3026661728221104464, 0.3524186183690131702, 0.4011907228821319227, 0.4500572973727005044, 0.5012199576353847386, 0.5567639849620312775, 0.6168130928284528691, 0.6819767269214894734, 0.7529340711039560485, 0.8292206168931396393, 0.9117786016023526896, 1.000000000000000000 ),
 ( 0.000000000000000000, 1.000000000000000000 ),
 .UNSPECIFIED. ) ;
#17348=CIRCLE ( 'NONE', #699, 8.199999999999995737 ) ;
#17349=CARTESIAN_POINT ( 'NONE',  ( -4.042113542615705768, 50.97449326430325556, 78.71838125468477187 ) ) ;
#17351=EDGE_LOOP ( 'NONE', ( #1875, #1216, #20571, #15488 ) ) ;
#17354=CARTESIAN_POINT ( 'NONE',  ( -5.510796958474739604, 38.60848837797752964, 77.05433879953086773 ) ) ;
#17356=CARTESIAN_POINT ( 'NONE',  ( 2.107928617576430241, 52.20740276032782390, 76.30768396657595076 ) ) ;
#17357=ORIENTED_EDGE ( 'NONE', *, *, #8741, .F. ) ;
#17358=CARTESIAN_POINT ( 'NONE',  ( -7.600593896485820622, 45.28511094584521146, 72.45433879953085921 ) ) ;
#17362=CARTESIAN_POINT ( 'NONE',  ( -0.9377844550628051667, 52.97865279236703628, 77.21536821129558348 ) ) ;
#17363=CARTESIAN_POINT ( 'NONE',  ( 8.644901377098817008, 43.03925179711409754, 72.45433879953087342 ) ) ;
#17365=DIRECTION ( 'NONE',  ( 0.007885122365275663500, 0.9999689119394085113, 1.805443505845543142E-16 ) ) ;
#17366=ORIENTED_EDGE ( 'NONE', *, *, #3395, .F. ) ;
#17368=DIRECTION ( 'NONE',  ( 1.540237394707284220E-16, 1.793354297423764243E-16, -1.000000000000000000 ) ) ;
#17369=EDGE_CURVE ( 'NONE', #585, #15690, #3346, .T. ) ;
#17370=ORIENTED_EDGE ( 'NONE', *, *, #268, .F. ) ;
#17372=DIRECTION ( 'NONE',  ( 1.540237394707284220E-16, 1.793354297423764243E-16, -1.000000000000000000 ) ) ;
#17373=CARTESIAN_POINT ( 'NONE',  ( 5.497743849324332466, 37.64424434608246628, 76.58742703482498371 ) ) ;
#17376=LINE ( 'NONE', #13865, #20778 ) ;
#17378=ORIENTED_EDGE ( 'NONE', *, *, #13517, .F. ) ;
#17379=CARTESIAN_POINT ( 'NONE',  ( 8.284178787249310005, 41.51768607177196913, 75.97387361979315301 ) ) ;
#17382=CARTESIAN_POINT ( 'NONE',  ( -4.089052737068717747, 51.68295426732343856, 75.42336258079946276 ) ) ;
#17384=B_SPLINE_CURVE_WITH_KNOTS ( 'NONE', 3,
 ( #898, #7172, #13671, #7386, #20146, #10501, #16966, #15385, #2396, #8898 ),
 .UNSPECIFIED., .F., .F.,
 ( 4, 2, 2, 2, 4 ),
 ( 0.000000000000000000, 0.0001324019452384074113, 0.0002648038904768148225, 0.0003972058357152222609, 0.0005296077809536294282 ),
 .UNSPECIFIED. ) ;
#17385=CARTESIAN_POINT ( 'NONE',  ( -7.785946528631249919, 41.22915307650257688, 78.55785233681892521 ) ) ;
#17387=CARTESIAN_POINT ( 'NONE',  ( -5.528784567355424784, 50.65417461334718752, 79.23104009678212378 ) ) ;
#17390=CARTESIAN_POINT ( 'NONE',  ( 6.880715602165139444, 37.89000465862396538, 77.41265765549051991 ) ) ;
#17391=CARTESIAN_POINT ( 'NONE',  ( -4.137897255279099795, 50.90113633070201615, 78.91875292420674270 ) ) ;
#17392=EDGE_CURVE ( 'NONE', #17442, #6443, #5037, .T. ) ;
#17393=ORIENTED_EDGE ( 'NONE', *, *, #6628, .T. ) ;
#17396=VERTEX_POINT ( 'NONE', #15054 ) ;
#17401=CARTESIAN_POINT ( 'NONE',  ( 5.428282431822193388, 36.85214909206928269, 76.61095391776262886 ) ) ;
#17402=CARTESIAN_POINT ( 'NONE',  ( 5.268505869694503296, 50.84354137661855333, 78.86786983087660019 ) ) ;
#17403=CARTESIAN_POINT ( 'NONE',  ( -3.405066831027640184, 37.04747935142366089, 77.64672866243046201 ) ) ;
#17404=ADVANCED_FACE ( 'NONE', ( #8248 ), #13294, .T. ) ;
#17405=ORIENTED_EDGE ( 'NONE', *, *, #16136, .T. ) ;
#17406=CARTESIAN_POINT ( 'NONE',  ( 2.119851040271390374, 52.81592988514039178, 77.84551527011910821 ) ) ;
#17409=CARTESIAN_POINT ( 'NONE',  ( 6.848903495604322877, 50.42928078925980628, 75.87133531663224062 ) ) ;
#17410=CARTESIAN_POINT ( 'NONE',  ( 0.1157200918968281783, 52.35296189364724739, 75.39535632244431440 ) ) ;
#17412=VECTOR ( 'NONE', #9606, 1000.000000000000227 ) ;
#17413=DIRECTION ( 'NONE',  ( -0.5941461771851691553, -0.8043570849667760481, -2.357623395011396791E-16 ) ) ;
#17416=CARTESIAN_POINT ( 'NONE',  ( -3.709553250900186061, 37.27239120432235353, 75.43521673441158271 ) ) ;
#17417=CARTESIAN_POINT ( 'NONE',  ( -6.920926855474425210, 40.72042203567113461, 77.43482967097732228 ) ) ;
#17419=CARTESIAN_POINT ( 'NONE',  ( 4.676321589340446394, 52.03407952647943091, 79.02133806855546538 ) ) ;
#17420=EDGE_CURVE ( 'NONE', #10020, #3468, #3628, .T. ) ;
#17421=DIRECTION ( 'NONE',  ( -0.3165065846431827645, -0.9485903129789529098, 0.000000000000000000 ) ) ;
#17423=EDGE_CURVE ( 'NONE', #11304, #13330, #17892, .T. ) ;
#17425=CARTESIAN_POINT ( 'NONE',  ( -4.608953993764351331, 37.01190935601766085, 77.97288938838475758 ) ) ;
#17426=CARTESIAN_POINT ( 'NONE',  ( 5.900862589321786977, 51.12956041731354873, 78.19629421043239859 ) ) ;
#17427=CARTESIAN_POINT ( 'NONE',  ( -5.312295682859165424, 38.39999490510201952, 79.30838064730033921 ) ) ;
#17429=VECTOR ( 'NONE', #6203, 1000.000000000000000 ) ;
#17430=VECTOR ( 'NONE', #14578, 1000.000000000000114 ) ;
#17431=EDGE_CURVE ( 'NONE', #9854, #7365, #16199, .T. ) ;
#17432=CARTESIAN_POINT ( 'NONE',  ( -5.170918566808907713, 50.90989255502720567, 75.43678921887351407 ) ) ;
#17435=CARTESIAN_POINT ( 'NONE',  ( -0.3533744273842052697, 52.21282903393489505, 79.37504392981026058 ) ) ;
#17439=CARTESIAN_POINT ( 'NONE',  ( 0.8457835444558534643, 52.35579252807401929, 76.43141481149322658 ) ) ;
#17442=VERTEX_POINT ( 'NONE', #18001 ) ;
#17443=AXIS2_PLACEMENT_3D ( 'NONE', #18589, #8921, #13390 ) ;
#17444=CARTESIAN_POINT ( 'NONE',  ( -7.999076009197850112, 41.90847905551897412, 79.52797380487967871 ) ) ;
#17445=CARTESIAN_POINT ( 'NONE',  ( 5.694963103159264683, 37.04270933600420079, 75.97340568087561508 ) ) ;
#17447=CARTESIAN_POINT ( 'NONE',  ( 8.637769616985924159, 43.04608606469359700, 78.67881838835081965 ) ) ;
#17448=DIRECTION ( 'NONE',  ( 0.007885122365275663500, 0.9999689119394085113, 1.805443505845543142E-16 ) ) ;
#17450=CARTESIAN_POINT ( 'NONE',  ( 4.621588727139584130, 51.26391586304784198, 77.68963291717793140 ) ) ;
#17453=CARTESIAN_POINT ( 'NONE',  ( 9.035997676120972599, 41.87518277052537030, 78.13634973986094678 ) ) ;
#17455=CARTESIAN_POINT ( 'NONE',  ( 5.203359478703453611, 50.89466331855276593, 76.29855684506968316 ) ) ;
#17459=EDGE_LOOP ( 'NONE', ( #7280, #5143, #789, #8862 ) ) ;
#17460=CARTESIAN_POINT ( 'NONE',  ( -5.919594526472896412, 37.98002672170838423, 78.92638042842689572 ) ) ;
#17461=CARTESIAN_POINT ( 'NONE',  ( -4.574316323987747346, 51.33620267474496757, 79.54845644658969661 ) ) ;
#17467=CARTESIAN_POINT ( 'NONE',  ( 5.527130473740349714, 50.65250579964440902, 78.81551702238962775 ) ) ;
#17468=LINE ( 'NONE', #15782, #18640 ) ;
#17469=CARTESIAN_POINT ( 'NONE',  ( 5.389492195292208798, 36.82443100924615464, 78.79551527011911105 ) ) ;
#17471=CARTESIAN_POINT ( 'NONE',  ( 0.7579357306838750974, 52.35285379749892343, 76.01945459498423929 ) ) ;
#17472=CARTESIAN_POINT ( 'NONE',  ( -3.437559636576261290, 37.06066253623392726, 79.33401574558745040 ) ) ;
#17474=CARTESIAN_POINT ( 'NONE',  ( 5.631785411401764918, 36.99756487055721976, 77.76022115247205591 ) ) ;
#17476=EDGE_LOOP ( 'NONE', ( #13155, #15650, #9472, #6598 ) ) ;
#17478=EDGE_CURVE ( 'NONE', #158, #17483, #16516, .T. ) ;
#17482=LINE ( 'NONE', #6289, #16385 ) ;
#17483=VERTEX_POINT ( 'NONE', #19484 ) ;
#17484=CARTESIAN_POINT ( 'NONE',  ( 4.577678780824717464, 52.10694299555530051, 78.38317481739672132 ) ) ;
#17485=ORIENTED_EDGE ( 'NONE', *, *, #20291, .F. ) ;
#17486=CARTESIAN_POINT ( 'NONE',  ( -3.471062581449894768, 51.20477182418656525, 75.48713596493043099 ) ) ;
#17488=CARTESIAN_POINT ( 'NONE',  ( 4.694131320935415630, 52.02092419516998234, 75.77039595153209461 ) ) ;
#17490=CARTESIAN_POINT ( 'NONE',  ( -5.569761608070843195, 50.62489392031717728, 79.19259575086972802 ) ) ;
#17492=CARTESIAN_POINT ( 'NONE',  ( 5.116981105040771638, 36.62970456142029008, 75.43572969368668168 ) ) ;
#17494=CARTESIAN_POINT ( 'NONE',  ( -4.098212357736016109, 50.92949370552946675, 78.89116106075270807 ) ) ;
#17497=FACE_OUTER_BOUND ( 'NONE', #9312, .T. ) ;
#17498=ORIENTED_EDGE ( 'NONE', *, *, #10319, .T. ) ;
#17499=FACE_OUTER_BOUND ( 'NONE', #13840, .T. ) ;
#17502=CARTESIAN_POINT ( 'NONE',  ( 5.618638386382252214, 36.98817048782158423, 75.97391373086902888 ) ) ;
#17503=CARTESIAN_POINT ( 'NONE',  ( 8.807466118993687587, 41.19025919604325026, 76.04813117819971069 ) ) ;
#17504=CARTESIAN_POINT ( 'NONE',  ( -3.269283392368544927, 36.94718159497673327, 77.55767546204062057 ) ) ;
#17506=CARTESIAN_POINT ( 'NONE',  ( 2.097007766388983008, 52.95433544280876248, 78.67719617274387645 ) ) ;
#17507=CARTESIAN_POINT ( 'NONE',  ( 5.562039828671766273, 37.70552590032356477, 78.36928251986560667 ) ) ;
#17508=CARTESIAN_POINT ( 'NONE',  ( -3.847046057864465851, 36.44911865529216755, 77.75315568452884918 ) ) ;
#17511=CARTESIAN_POINT ( 'NONE',  ( -7.794114027700602243, 41.28466036262712890, 78.36261600855591780 ) ) ;
#17512=CARTESIAN_POINT ( 'NONE',  ( 5.495636600878563982, 37.64719334750368063, 77.37492703482499223 ) ) ;
#17514=B_SPLINE_SURFACE_WITH_KNOTS ( 'NONE', 3, 1, ( 
 ( #18854, #3852 ),
 ( #15250, #4266 ),
 ( #16943, #2370 ),
 ( #10793, #10373 ),
 ( #16843, #7145 ),
 ( #13649, #18541 ),
 ( #15785, #16087 ),
 ( #4370, #20644 ),
 ( #1510, #11099 ),
 ( #7785, #12781 ),
 ( #14266, #6074 ),
 ( #11000, #20747 ),
 ( #12685, #9296 ),
 ( #17471, #4782 ),
 ( #1296, #10896 ),
 ( #17670, #7996 ),
 ( #3102, #12579 ),
 ( #2895, #19069 ),
 ( #6181, #9605 ) ),
 .UNSPECIFIED., .F., .F., .F.,
 ( 4, 1, 1, 1, 1, 1, 1, 1, 1, 1, 1, 1, 1, 1, 1, 1, 4 ),
 ( 2, 2 ),
 ( 0.000000000000000000, 0.09451313814127135227, 0.1805372682721389788, 0.2570047093480871125, 0.3249775091219202494, 0.3834231080405892667, 0.4323187449081173361, 0.4717396676274380751, 0.5027004295337662576, 0.5542129903573291827, 0.6050312652222360477, 0.6586042779580459916, 0.7158509153455059337, 0.7781537217524819861, 0.8456603787764748192, 0.9191804452816982884, 1.000000000000000000 ),
 ( 0.000000000000000000, 1.000000000000000000 ),
 .UNSPECIFIED. ) ;
#17517=ORIENTED_EDGE ( 'NONE', *, *, #18055, .F. ) ;
#17518=CARTESIAN_POINT ( 'NONE',  ( -7.922094096367543692, 41.68495194371154611, 78.88458188491442513 ) ) ;
#17519=CARTESIAN_POINT ( 'NONE',  ( -4.699348147190207214, 37.07867987585471781, 75.97299512023676016 ) ) ;
#17520=CARTESIAN_POINT ( 'NONE',  ( -7.308127660158699967, 41.72770130593617210, 76.16022115247204738 ) ) ;
#17521=ORIENTED_EDGE ( 'NONE', *, *, #6981, .F. ) ;
#17523=CARTESIAN_POINT ( 'NONE',  ( -6.709785530345820703, 40.29707390701430825, 78.55233631870791555 ) ) ;
#17525=EDGE_CURVE ( 'NONE', #16948, #6337, #1739, .T. ) ;
#17526=ORIENTED_EDGE ( 'NONE', *, *, #17946, .T. ) ;
#17531=CARTESIAN_POINT ( 'NONE',  ( 5.750640099535992533, 51.24052371918730842, 75.36022115247205022 ) ) ;
#17532=B_SPLINE_CURVE_WITH_KNOTS ( 'NONE', 3,
 ( #5956, #7448, #13945, #12555, #4657, #6262, #17138, #17545, #5857, #6162, #11082 ),
 .UNSPECIFIED., .F., .F.,
 ( 4, 1, 1, 1, 1, 1, 1, 1, 4 ),
 ( 0.000000000000000000, 0.1891742793480645779, 0.3478164846204494509, 0.4767017694705349973, 0.5812052966572537338, 0.6755649002106222101, 0.7721207368275812000, 0.8786749842102796748, 1.000000000000000000 ),
 .UNSPECIFIED. ) ;
#17535=CARTESIAN_POINT ( 'NONE',  ( -0.6601304159688821116, 52.21524791763957296, 79.16576412035692556 ) ) ;
#17536=CARTESIAN_POINT ( 'NONE',  ( -4.195947902387222150, 37.45549797810746639, 76.06494828368110461 ) ) ;
#17537=DIRECTION ( 'NONE',  ( 0.007885122365275663500, 0.9999689119394085113, 1.805443505845543142E-16 ) ) ;
#17540=ORIENTED_EDGE ( 'NONE', *, *, #6633, .F. ) ;
#17541=CARTESIAN_POINT ( 'NONE',  ( 8.643837405878704416, 43.06427161293860451, 78.44945682776121032 ) ) ;
#17543=CARTESIAN_POINT ( 'NONE',  ( 6.920970967149330910, 50.37604745108433946, 78.34373887323252461 ) ) ;
#17544=DIRECTION ( 'NONE',  ( -0.5941461771851691553, -0.8043570849667760481, -2.357623395011396791E-16 ) ) ;
#17545=CARTESIAN_POINT ( 'NONE',  ( 8.907015937602837496, 41.48861631773759484, 77.50814924735175282 ) ) ;
#17546=CARTESIAN_POINT ( 'NONE',  ( 9.333517871656532350, 42.76686967087471913, 77.60952670463396430 ) ) ;
#17550=ORIENTED_EDGE ( 'NONE', *, *, #8959, .T. ) ;
#17551=CARTESIAN_POINT ( 'NONE',  ( 8.851169967151879092, 41.32124240149376249, 78.93505401271374922 ) ) ;
#17552=EDGE_CURVE ( 'NONE', #11899, #502, #2837, .T. ) ;
#17553=CARTESIAN_POINT ( 'NONE',  ( 0.8455950101471346736, 52.35579997042385259, 78.52566232894263010 ) ) ;
#17554=EDGE_CURVE ( 'NONE', #13579, #14654, #19584, .T. ) ;
#17555=CARTESIAN_POINT ( 'NONE',  ( -7.611372734017126440, 43.12018948500615778, 78.28007409364852265 ) ) ;
#17556=ORIENTED_EDGE ( 'NONE', *, *, #11962, .F. ) ;
#17557=CARTESIAN_POINT ( 'NONE',  ( 1.250118884985844447, 46.34393909133126499, 80.45433879953087342 ) ) ;
#17558=ADVANCED_FACE ( 'NONE', ( #8325 ), #14803, .T. ) ;
#17559=B_SPLINE_CURVE_WITH_KNOTS ( 'NONE', 3,
 ( #20019, #885, #13446, #11856, #20342, #18652, #12070, #2492, #15258, #13657, #5781, #7371, #12286, #5454, #18765, #18334 ),
 .UNSPECIFIED., .F., .F.,
 ( 4, 2, 2, 2, 2, 2, 2, 4 ),
 ( 0.000000000000000000, 0.0007158805460618166512, 0.001431761092123633302, 0.001789701365154541682, 0.002147641638185449845, 0.002505581911216358225, 0.002684552047731790080, 0.002863522184247221502 ),
 .UNSPECIFIED. ) ;
#17563=CARTESIAN_POINT ( 'NONE',  ( 5.848951923618479931, 37.15274410921379911, 76.58742703482498371 ) ) ;
#17564=CARTESIAN_POINT ( 'NONE',  ( -0.9115598319063860089, 52.97844600157573325, 76.23506554152810111 ) ) ;
#17566=CARTESIAN_POINT ( 'NONE',  ( -4.385945807438902833, 50.73113084894660574, 76.01479905091014189 ) ) ;
#17567=CARTESIAN_POINT ( 'NONE',  ( 5.939900590116411472, 51.10072461867315496, 76.90580938776616904 ) ) ;
#17570=EDGE_LOOP ( 'NONE', ( #12827, #5236, #17149, #12637 ) ) ;
#17571=CARTESIAN_POINT ( 'NONE',  ( 8.896031707678503153, 41.45569588382780779, 75.98771331677210128 ) ) ;
#17572=ORIENTED_EDGE ( 'NONE', *, *, #5168, .F. ) ;
#17575=PLANE ( 'NONE',  #18974 ) ;
#17576=CARTESIAN_POINT ( 'NONE',  ( 5.845446004764687231, 37.15023890796076245, 76.33129752952908120 ) ) ;
#17577=CARTESIAN_POINT ( 'NONE',  ( -7.306329150795409788, 41.74985974580818748, 78.93438826577718714 ) ) ;
#17578=CIRCLE ( 'NONE', #18604, 8.199999999999995737 ) ;
#17580=CARTESIAN_POINT ( 'NONE',  ( 4.577379499810326990, 52.10716406238486087, 78.43496551412393103 ) ) ;
#17582=CARTESIAN_POINT ( 'NONE',  ( -3.269139879056130571, 51.34905839445515596, 75.61719165653033770 ) ) ;
#17585=CARTESIAN_POINT ( 'NONE',  ( 4.776132423410367700, 51.96035328397762498, 75.67068799376596644 ) ) ;
#17586=ORIENTED_EDGE ( 'NONE', *, *, #16583, .T. ) ;
#17587=CARTESIAN_POINT ( 'NONE',  ( -5.384655767683054428, 49.83721677713893428, 78.57924047249254329 ) ) ;
#17589=AXIS2_PLACEMENT_3D ( 'NONE', #15124, #3833, #8740 ) ;
#17590=CARTESIAN_POINT ( 'NONE',  ( 4.410764955181007529, 36.12506835695402430, 76.35980278528342069 ) ) ;
#17591=CARTESIAN_POINT ( 'NONE',  ( 5.724311780639353309, 51.25997138778688367, 75.97249762499970416 ) ) ;
#17597=CARTESIAN_POINT ( 'NONE',  ( 4.140865811708774658, 51.51558413471341424, 78.38317481739672132 ) ) ;
#17599=CARTESIAN_POINT ( 'NONE',  ( 0.8308482478495438084, 52.95678316823124732, 78.75697940203460234 ) ) ;
#17602=LINE ( 'NONE', #17714, #20013 ) ;
#17604=FACE_OUTER_BOUND ( 'NONE', #2400, .T. ) ;
#17606=CARTESIAN_POINT ( 'NONE',  ( -7.099600269029870958, 47.18725423407072128, 78.26805218182843760 ) ) ;
#17607=CARTESIAN_POINT ( 'NONE',  ( 5.760694563098077481, 51.23309689197249384, 79.54845644658969661 ) ) ;
#17609=CARTESIAN_POINT ( 'NONE',  ( -7.802862648839750115, 41.30999248941007806, 78.30232473790640313 ) ) ;
#17611=CARTESIAN_POINT ( 'NONE',  ( 9.244427017087200937, 42.49985872791199881, 79.25343573416346032 ) ) ;
#17613=DIRECTION ( 'NONE',  ( 1.540237394707283727E-16, 1.793354297423763257E-16, -1.000000000000000000 ) ) ;
#17614=ORIENTED_EDGE ( 'NONE', *, *, #1581, .F. ) ;
#17615=CARTESIAN_POINT ( 'NONE',  ( -4.274404157479777311, 37.68962381543027362, 75.36022115247205022 ) ) ;
#17617=CARTESIAN_POINT ( 'NONE',  ( -7.042421365581803983, 40.99363011463105977, 77.06266651728316219 ) ) ;
#17619=CARTESIAN_POINT ( 'NONE',  ( 4.577225057937401864, 52.10727814237509392, 78.46169174070733732 ) ) ;
#17620=CARTESIAN_POINT ( 'NONE',  ( -4.790295051490115696, 37.92061980927154963, 77.90139762306027649 ) ) ;
#17622=VECTOR ( 'NONE', #5580, 1000.000000000000114 ) ;
#17624=CARTESIAN_POINT ( 'NONE',  ( 8.617838889373357958, 45.46597658821364263, 78.74919174070734584 ) ) ;
#17626=CARTESIAN_POINT ( 'NONE',  ( 5.939900590116411472, 51.10072461867315496, 76.38301527011910252 ) ) ;
#17628=EDGE_CURVE ( 'NONE', #14506, #4469, #15275, .T. ) ;
#17629=CARTESIAN_POINT ( 'NONE',  ( 6.319761386105714251, 38.36299381901618233, 78.05707163992254038 ) ) ;
#17630=CARTESIAN_POINT ( 'NONE',  ( 0.5283203121033563932, 52.96651480206464413, 76.89772265631788173 ) ) ;
#17633=CARTESIAN_POINT ( 'NONE',  ( -0.4245371128412744888, 52.21339017786244341, 79.34012451928875009 ) ) ;
#17634=ORIENTED_EDGE ( 'NONE', *, *, #18874, .T. ) ;
#17637=CARTESIAN_POINT ( 'NONE',  ( 8.579956030688345336, 40.50839702842124268, 79.37958223971880045 ) ) ;
#17638=CARTESIAN_POINT ( 'NONE',  ( 6.923000991621626632, 50.37454795378102546, 78.43783143115764744 ) ) ;
#17643=CARTESIAN_POINT ( 'NONE',  ( 7.887664428531886429, 40.55654679518931260, 75.60913502469634295 ) ) ;
#17644=DIRECTION ( 'NONE',  ( 0.9539696396349547358, -0.2999031954727301441, 9.315070279690498823E-17 ) ) ;
#17650=PLANE ( 'NONE',  #5668 ) ;
#17651=CARTESIAN_POINT ( 'NONE',  ( 8.643936145691096584, 43.06456754242027074, 77.06316232894263862 ) ) ;
#17653=AXIS2_PLACEMENT_3D ( 'NONE', #595, #7077, #10517 ) ;
#17655=CARTESIAN_POINT ( 'NONE',  ( -4.859530362865112529, 37.19700002604054134, 79.54807357191100436 ) ) ;
#17656=EDGE_CURVE ( 'NONE', #15461, #14881, #20210, .T. ) ;
#17658=CARTESIAN_POINT ( 'NONE',  ( 5.410058914415630582, 36.83912723373610731, 78.11840496518735222 ) ) ;
#17660=VECTOR ( 'NONE', #11560, 1000.000000000000114 ) ;
#17664=CARTESIAN_POINT ( 'NONE',  ( 8.386307069575464013, 39.92801880710491957, 76.83374382764255017 ) ) ;
#17665=ORIENTED_EDGE ( 'NONE', *, *, #10455, .T. ) ;
#17666=CARTESIAN_POINT ( 'NONE',  ( 6.386300776676741897, 37.53671392601205525, 75.49608936836499140 ) ) ;
#17667=VECTOR ( 'NONE', #2798, 1000.000000000000000 ) ;
#17668=CARTESIAN_POINT ( 'NONE',  ( 8.879174460483845621, 41.40517364458161609, 78.05744560429982926 ) ) ;
#17670=CARTESIAN_POINT ( 'NONE',  ( 0.6753953261465888147, 52.35350465892279459, 75.98308111960244560 ) ) ;
#17671=DIRECTION ( 'NONE',  ( 0.9999689119394086223, -0.007885122365275665235, 1.526048693634353392E-16 ) ) ;
#17672=EDGE_CURVE ( 'NONE', #17850, #12203, #18529, .T. ) ;
#17673=EDGE_LOOP ( 'NONE', ( #3567, #1401, #8905, #2915 ) ) ;
#17674=EDGE_CURVE ( 'NONE', #18944, #15539, #3840, .T. ) ;
#17675=FACE_OUTER_BOUND ( 'NONE', #13541, .T. ) ;
#17677=EDGE_LOOP ( 'NONE', ( #7679, #9910, #12770, #1786 ) ) ;
#17678=LINE ( 'NONE', #1306, #10134 ) ;
#17681=CARTESIAN_POINT ( 'NONE',  ( 0.3869120917952209582, 35.96329670974013482, 78.57639762306027365 ) ) ;
#17683=B_SPLINE_CURVE_WITH_KNOTS ( 'NONE', 3,
 ( #13484, #19955, #12111, #5607, #5504, #1900, #10099, #11700, #6782, #10320, #8810, #16479, #20069, #290, #16581, #3591, #16793, #503, #14985 ),
 .UNSPECIFIED., .F., .F.,
 ( 4, 1, 1, 1, 1, 1, 1, 1, 1, 1, 1, 1, 1, 1, 1, 1, 4 ),
 ( 0.000000000000000000, 0.05434379794353864229, 0.1062390698768248820, 0.1553778989748225425, 0.2029887854916514467, 0.2486500052201169320, 0.2921085583616858661, 0.3352193261980264682, 0.3771870632897987852, 0.4223876994541358454, 0.4752030700363142346, 0.5373302487560115415, 0.6091097927081512431, 0.6911313100281405442, 0.7836801803933998167, 0.8864064767870927231, 1.000000000000000000 ),
 .UNSPECIFIED. ) ;
#17686=EDGE_CURVE ( 'NONE', #4618, #11143, #6627, .T. ) ;
#17687=B_SPLINE_SURFACE_WITH_KNOTS ( 'NONE', 3, 1, ( 
 ( #5103, #18095 ),
 ( #16186, #11621 ),
 ( #19571, #19470 ),
 ( #1612, #11408 ),
 ( #17985, #4887 ),
 ( #8414, #12994 ),
 ( #11306, #9920 ),
 ( #16405, #1827 ),
 ( #3301, #8312 ),
 ( #20612, #11064 ),
 ( #12751, #6149 ),
 ( #17435, #4549 ),
 ( #17633, #3178 ),
 ( #9680, #15949 ),
 ( #7859, #6251 ),
 ( #3069, #1370 ),
 ( #17535, #14348 ),
 ( #4644, #12851 ),
 ( #8062, #1478 ),
 ( #21019, #9571 ),
 ( #20822, #19228 ),
 ( #11165, #2956 ),
 ( #14232, #14554 ),
 ( #18920, #4336 ),
 ( #16056, #2859 ),
 ( #20915, #12543 ),
 ( #19031, #7964 ),
 ( #14449, #17748 ),
 ( #9464, #10862 ),
 ( #1260, #17332 ),
 ( #6348, #7753 ) ),
 .UNSPECIFIED., .F., .F., .F.,
 ( 4, 1, 1, 1, 1, 1, 1, 1, 1, 1, 1, 1, 1, 1, 1, 1, 1, 1, 1, 1, 1, 1, 1, 1, 1, 1, 1, 1, 4 ),
 ( 2, 2 ),
 ( 0.000000000000000000, 0.04384681544484739235, 0.08567827314907716652, 0.1254967717429318341, 0.1636614238475955219, 0.1996619864010514556, 0.2341576300211750672, 0.2670604349552898049, 0.2981387414117787626, 0.3278414694467580159, 0.3565940729939165998, 0.3842752990321527395, 0.4112124433481792463, 0.4371802474119553250, 0.4623137086418128150, 0.4873144965356236424, 0.5115863199873472711, 0.5585256650453194194, 0.6022882070645410035, 0.6442466772295868394, 0.6853175287114940950, 0.7081315191531365461, 0.7355471538020152966, 0.7678357380769914586, 0.8047386325758049130, 0.8465390724922580157, 0.8929683470010029156, 0.9440341083467609362, 1.000000000000000000 ),
 ( 0.000000000000000000, 1.000000000000000000 ),
 .UNSPECIFIED. ) ;
#17688=AXIS2_PLACEMENT_3D ( 'NONE', #951, #18402, #16911 ) ;
#17691=ORIENTED_EDGE ( 'NONE', *, *, #20735, .F. ) ;
#17692=CARTESIAN_POINT ( 'NONE',  ( -3.358136819263964234, 52.20524002164697208, 76.41354228756682687 ) ) ;
#17693=CARTESIAN_POINT ( 'NONE',  ( -7.890048607039471307, 46.74575480130646099, 79.45433879953087342 ) ) ;
#17694=CARTESIAN_POINT ( 'NONE',  ( 4.544296722651392173, 52.13160097721661401, 76.36737811492949390 ) ) ;
#17696=CARTESIAN_POINT ( 'NONE',  ( 6.635267586053947397, 39.64667042487232607, 72.45432679953087529 ) ) ;
#17698=CARTESIAN_POINT ( 'NONE',  ( -4.588243132438925009, 36.99661107704093865, 78.89954634079194307 ) ) ;
#17699=CARTESIAN_POINT ( 'NONE',  ( -4.073823749297678098, 50.94692091219555152, 78.85744209785094938 ) ) ;
#17700=CARTESIAN_POINT ( 'NONE',  ( 5.442040249694054310, 36.86197992501465137, 77.64535406911728899 ) ) ;
#17705=CARTESIAN_POINT ( 'NONE',  ( 4.661266133293011649, 52.04520038539091331, 77.98100106196224601 ) ) ;
#17708=DIRECTION ( 'NONE',  ( -1.540237394707284220E-16, -1.793354297423764243E-16, 1.000000000000000000 ) ) ;
#17709=CARTESIAN_POINT ( 'NONE',  ( 0.5886017282102210535, 52.96193049659134999, 78.93669174070734584 ) ) ;
#17713=VECTOR ( 'NONE', #10168, 1000.000000000000227 ) ;
#17714=CARTESIAN_POINT ( 'NONE',  ( 2.029186242314200861, 35.35002428291939225, 76.86610350541323555 ) ) ;
#17715=ADVANCED_FACE ( 'NONE', ( #12772 ), #15773, .T. ) ;
#17716=CARTESIAN_POINT ( 'NONE',  ( 5.939900590116411472, 51.10072461867315496, 76.38301527011910252 ) ) ;
#17718=CARTESIAN_POINT ( 'NONE',  ( 1.984707218798539730, 52.83985775011834107, 77.14939308509356408 ) ) ;
#17719=ORIENTED_EDGE ( 'NONE', *, *, #947, .F. ) ;
#17720=DIRECTION ( 'NONE',  ( -0.3330135628418914862, -0.9429220365244147528, -2.203913228770411492E-16 ) ) ;
#17721=CARTESIAN_POINT ( 'NONE',  ( 8.214799251806553571, 41.32260305165857517, 72.45433879953087342 ) ) ;
#17722=CARTESIAN_POINT ( 'NONE',  ( 8.949781629519392823, 41.61678780941641520, 75.36311794487049553 ) ) ;
#17724=CARTESIAN_POINT ( 'NONE',  ( 8.385679600361122255, 39.92613824206362949, 77.13595644658970230 ) ) ;
#17727=CARTESIAN_POINT ( 'NONE',  ( -7.881634263515648442, 41.55089060731901185, 78.93495394624521566 ) ) ;
#17728=CARTESIAN_POINT ( 'NONE',  ( -4.525716193177020230, 36.95042494574692427, 76.22840587216694530 ) ) ;
#17732=CARTESIAN_POINT ( 'NONE',  ( -5.087398782055177371, 37.36531724819641198, 77.33565342272370913 ) ) ;
#17733=CARTESIAN_POINT ( 'NONE',  ( -7.313565574299385474, 41.74526126053015673, 79.54845644658969661 ) ) ;
#17735=ORIENTED_EDGE ( 'NONE', *, *, #4760, .F. ) ;
#17736=CARTESIAN_POINT ( 'NONE',  ( -7.788095026490401196, 41.26728263494260318, 78.81763427810251699 ) ) ;
#17737=CARTESIAN_POINT ( 'NONE',  ( 5.544276951911416340, 50.64433212932689088, 78.59183879953087626 ) ) ;
#17741=CARTESIAN_POINT ( 'NONE',  ( -4.924280525269182363, 51.08613106951644767, 75.37785507730471579 ) ) ;
#17742=CARTESIAN_POINT ( 'NONE',  ( -4.361665858399769391, 37.57520132541210245, 75.97198585835440099 ) ) ;
#17744=FACE_OUTER_BOUND ( 'NONE', #3525, .T. ) ;
#17748=CARTESIAN_POINT ( 'NONE',  ( -0.9366413518729753696, 52.97986903894317834, 78.07640427701528552 ) ) ;
#17752=CARTESIAN_POINT ( 'NONE',  ( 8.414968994577074923, 40.01392041461337357, 78.89537297773202340 ) ) ;
#17753=CARTESIAN_POINT ( 'NONE',  ( 6.873747143562635387, 50.41092978727617435, 78.08828162113617566 ) ) ;
#17757=CARTESIAN_POINT ( 'NONE',  ( 0.5221537403065019678, 44.16218137147968292, 72.45433879953087342 ) ) ;
#17759=CARTESIAN_POINT ( 'NONE',  ( -4.889784912074394363, 37.21934784281386044, 78.69750623079058016 ) ) ;
#17761=CIRCLE ( 'NONE', #20476, 4.200000000000003730 ) ;
#17762=PLANE ( 'NONE',  #14731 ) ;
#17764=LINE ( 'NONE', #10702, #1261 ) ;
#17765=CARTESIAN_POINT ( 'NONE',  ( 6.519277697500823976, 49.74792914119518628, 76.69700829373513784 ) ) ;
#17767=LINE ( 'NONE', #8910, #18469 ) ;
#17769=CARTESIAN_POINT ( 'NONE',  ( -5.159531558744112623, 38.35460532074419859, 79.39214668191834789 ) ) ;
#17772=EDGE_CURVE ( 'NONE', #19487, #6017, #8208, .T. ) ;
#17773=CARTESIAN_POINT ( 'NONE',  ( 5.270142054182215041, 50.84773347817210265, 78.86068376280545067 ) ) ;
#17775=CARTESIAN_POINT ( 'NONE',  ( 8.491906929791015912, 40.24450828730113727, 75.69429397690826988 ) ) ;
#17776=EDGE_LOOP ( 'NONE', ( #1340, #6121, #18412, #4802 ) ) ;
#17777=CARTESIAN_POINT ( 'NONE',  ( 6.877103025211564358, 37.88742324339783352, 76.41040896618429201 ) ) ;
#17778=DIRECTION ( 'NONE',  ( 0.3165065846431828200, 0.9485903129789527988, 0.000000000000000000 ) ) ;
#17779=CARTESIAN_POINT ( 'NONE',  ( 6.467096401101858127, 37.59444752110963606, 78.28436300994860630 ) ) ;
#17780=DIRECTION ( 'NONE',  ( -0.9534635866061451637, -0.3015081906286225522, -2.009271279954815797E-16 ) ) ;
#17781=DIRECTION ( 'NONE',  ( -0.9485903129789527988, 0.3165065846431829311, -8.934458285744989980E-17 ) ) ;
#17783=CARTESIAN_POINT ( 'NONE',  ( 8.951454296033540814, 41.62180089707131003, 76.31823237213514233 ) ) ;
#17784=VECTOR ( 'NONE', #20725, 1000.000000000000000 ) ;
#17785=EDGE_CURVE ( 'NONE', #10020, #13175, #9440, .T. ) ;
#17789=CARTESIAN_POINT ( 'NONE',  ( -7.861899879695211091, 46.83617027511139241, 79.36034011475112493 ) ) ;
#17790=LINE ( 'NONE', #19378, #18486 ) ;
#17793=VERTEX_POINT ( 'NONE', #9173 ) ;
#17795=ORIENTED_EDGE ( 'NONE', *, *, #287, .T. ) ;
#17796=VECTOR ( 'NONE', #9090, 1000.000000000000227 ) ;
#17797=CARTESIAN_POINT ( 'NONE',  ( -2.938357031425011812, 51.58542370663933241, 76.25796290525131838 ) ) ;
#17804=DIRECTION ( 'NONE',  ( 0.3165065846431826535, 0.9485903129789529098, 2.188653791613874008E-16 ) ) ;
#17805=DIRECTION ( 'NONE',  ( -0.3165065846431826535, -0.9485903129789529098, -2.188653791613874008E-16 ) ) ;
#17806=ORIENTED_EDGE ( 'NONE', *, *, #17369, .F. ) ;
#17807=CARTESIAN_POINT ( 'NONE',  ( 2.029186242314200861, 35.35002428291939225, 76.86610350541323555 ) ) ;
#17808=CARTESIAN_POINT ( 'NONE',  ( 0.8501571860830551275, 52.96349708516230237, 78.54797669815580718 ) ) ;
#17809=ORIENTED_EDGE ( 'NONE', *, *, #4818, .T. ) ;
#17810=CARTESIAN_POINT ( 'NONE',  ( 4.577678780824717464, 52.10694299555530051, 78.38317481739672132 ) ) ;
#17812=CARTESIAN_POINT ( 'NONE',  ( -5.483735557913453462, 50.68636498614493036, 75.61447646545406087 ) ) ;
#17817=CARTESIAN_POINT ( 'NONE',  ( 1.853273245406973135, 52.20358242324970632, 79.18222496875146987 ) ) ;
#17823=CARTESIAN_POINT ( 'NONE',  ( 9.092498755203211047, 42.04452008889646208, 79.47377622490290605 ) ) ;
#17824=VERTEX_POINT ( 'NONE', #15664 ) ;
#17825=CARTESIAN_POINT ( 'NONE',  ( 5.599418364623888422, 51.35222512318382826, 78.27515171461519117 ) ) ;
#17826=CARTESIAN_POINT ( 'NONE',  ( -5.810228987958478086, 37.89924280392040856, 75.80435357840198662 ) ) ;
#17827=VERTEX_POINT ( 'NONE', #17354 ) ;
#17828=CARTESIAN_POINT ( 'NONE',  ( 6.882736312352589536, 37.89144858414100270, 77.26022115247205591 ) ) ;
#17829=CARTESIAN_POINT ( 'NONE',  ( 8.372294911086104463, 41.79245952794141772, 78.82125883816432577 ) ) ;
#17832=B_SPLINE_CURVE_WITH_KNOTS ( 'NONE', 3,
 ( #10959, #14228, #9676, #1577, #16256, #6037, #14550, #2855, #9774, #17629, #1256, #3063, #7749, #20707, #19133, #6146 ),
 .UNSPECIFIED., .F., .F.,
 ( 4, 2, 2, 2, 2, 2, 2, 4 ),
 ( 0.000000000000000000, 0.0002224803680995706247, 0.0004449607361991412494, 0.0006674411042987119826, 0.0008899214723982824989, 0.001112401840497853015, 0.001334882208597423965, 0.001779842944796567817 ),
 .UNSPECIFIED. ) ;
#17834=PLANE ( 'NONE',  #10825 ) ;
#17835=CARTESIAN_POINT ( 'NONE',  ( -6.757590673342858345, 40.38754831509554322, 78.93286798364411538 ) ) ;
#17837=EDGE_CURVE ( 'NONE', #6003, #8200, #4976, .T. ) ;
#17838=ORIENTED_EDGE ( 'NONE', *, *, #5161, .T. ) ;
#17839=CARTESIAN_POINT ( 'NONE',  ( -4.802822372555619168, 51.17292061857877172, 76.30694920102484957 ) ) ;
#17841=DIRECTION ( 'NONE',  ( 0.5670994908670431434, -0.8236492988270800453, -6.036271672687318437E-17 ) ) ;
#17843=EDGE_CURVE ( 'NONE', #7860, #492, #12874, .T. ) ;
#17845=CARTESIAN_POINT ( 'NONE',  ( -5.831867965436852153, 50.43760231366965030, 76.45423404125398292 ) ) ;
#17846=CARTESIAN_POINT ( 'NONE',  ( -4.536948752023380216, 37.70884965637360153, 76.29326043209479735 ) ) ;
#17847=FACE_OUTER_BOUND ( 'NONE', #12184, .T. ) ;
#17848=DIRECTION ( 'NONE',  ( 1.540237394707284220E-16, 1.793354297423764243E-16, -1.000000000000000000 ) ) ;
#17849=CARTESIAN_POINT ( 'NONE',  ( 8.535530527220215546, 40.37525097622586401, 79.30521328845429707 ) ) ;
#17850=VERTEX_POINT ( 'NONE', #19356 ) ;
#17853=DIRECTION ( 'NONE',  ( 0.9585804129707224952, 0.2848220354341971516, 1.987228219138359058E-16 ) ) ;
#17854=CARTESIAN_POINT ( 'NONE',  ( 6.275326403410204534, 49.93894407694084236, 77.80505143490314879 ) ) ;
#17857=CARTESIAN_POINT ( 'NONE',  ( 7.843838371297746193, 40.46900263578136503, 75.68048307330049340 ) ) ;
#17860=CARTESIAN_POINT ( 'NONE',  ( 4.270697848799480667, 51.45532176823032700, 79.05703599080955257 ) ) ;
#17864=CARTESIAN_POINT ( 'NONE',  ( 9.261243355884198891, 42.55025836209524215, 77.91040118276930571 ) ) ;
#17865=CARTESIAN_POINT ( 'NONE',  ( 8.616653853821931719, 45.47331367307960193, 79.47125056423675460 ) ) ;
#17866=CARTESIAN_POINT ( 'NONE',  ( 6.513673912301411129, 49.75206843158775172, 76.39262467917644983 ) ) ;
#17869=CARTESIAN_POINT ( 'NONE',  ( -4.638935325527024034, 37.97006185416216795, 79.53654225555244750 ) ) ;
#17871=CARTESIAN_POINT ( 'NONE',  ( 8.898741081898894123, 41.46381605024582484, 78.92561463894257656 ) ) ;
#17872=CARTESIAN_POINT ( 'NONE',  ( 5.308722110161348873, 50.82017868225404555, 78.91297906391670836 ) ) ;
#17873=DIRECTION ( 'NONE',  ( -1.540237394707284467E-16, -1.793354297423764243E-16, 1.000000000000000000 ) ) ;
#17874=CARTESIAN_POINT ( 'NONE',  ( 8.740212021938845055, 40.98869440064952130, 75.38759329643264095 ) ) ;
#17876=ORIENTED_EDGE ( 'NONE', *, *, #7667, .T. ) ;
#17877=CARTESIAN_POINT ( 'NONE',  ( -0.3307199010476375989, 52.21467244487229209, 75.52908203832478762 ) ) ;
#17879=CARTESIAN_POINT ( 'NONE',  ( -4.592862224480081856, 51.32295045326188898, 75.97198585835440099 ) ) ;
#17880=CARTESIAN_POINT ( 'NONE',  ( 4.765539811858917396, 51.17942285908035416, 75.44429008213492693 ) ) ;
#17882=ORIENTED_EDGE ( 'NONE', *, *, #12341, .F. ) ;
#17883=CARTESIAN_POINT ( 'NONE',  ( 4.577225057937401864, 52.10727814237509392, 78.46169174070733732 ) ) ;
#17884=AXIS2_PLACEMENT_3D ( 'NONE', #13803, #15625, #10952 ) ;
#17885=ORIENTED_EDGE ( 'NONE', *, *, #9893, .T. ) ;
#17888=CARTESIAN_POINT ( 'NONE',  ( 0.3279640439667347862, 52.35988168082469940, 76.44919174070734869 ) ) ;
#17889=B_SPLINE_CURVE_WITH_KNOTS ( 'NONE', 3,
 ( #4541, #15940, #17426, #2638, #9139, #14122, #2851, #9354, #15839, #1251, #6241 ),
 .UNSPECIFIED., .F., .F.,
 ( 4, 1, 1, 1, 1, 1, 1, 1, 4 ),
 ( 0.000000000000000000, 0.1975140844462248968, 0.3638949407180063211, 0.4989527813026914393, 0.6061909113956662765, 0.6984313814761610173, 0.7906255499708312318, 0.8898677993983585832, 1.000000000000000000 ),
 .UNSPECIFIED. ) ;
#17890=CARTESIAN_POINT ( 'NONE',  ( -3.533185125431083762, 36.21728222759317362, 78.38559710128819802 ) ) ;
#17891=CARTESIAN_POINT ( 'NONE',  ( 8.334265403641039072, 41.66992841543623172, 75.99902581847530314 ) ) ;
#17892=LINE ( 'NONE', #10140, #10604 ) ;
#17895=ADVANCED_FACE ( 'NONE', ( #204 ), #9701, .T. ) ;
#17897=AXIS2_PLACEMENT_3D ( 'NONE', #6809, #5105, #17780 ) ;
#17902=CARTESIAN_POINT ( 'NONE',  ( 1.640639625673125712, 52.28578529826535259, 76.88709351585207230 ) ) ;
#17903=CARTESIAN_POINT ( 'NONE',  ( 0.3821786226492924210, 35.36301154328572949, 78.57639762306027365 ) ) ;
#17904=CARTESIAN_POINT ( 'NONE',  ( 5.889143815203415677, 51.13821660369377753, 76.04053158567903381 ) ) ;
#17905=CARTESIAN_POINT ( 'NONE',  ( -2.914604833731050171, 51.60239615748798059, 78.10580938776615767 ) ) ;
#17907=VERTEX_POINT ( 'NONE', #13090 ) ;
#17910=VERTEX_POINT ( 'NONE', #9912 ) ;
#17911=CARTESIAN_POINT ( 'NONE',  ( 4.314250362499145730, 51.38751195140030603, 77.86982703766624070 ) ) ;
#17912=CARTESIAN_POINT ( 'NONE',  ( -6.906571818728131085, 40.93480306606039676, 77.18350490445806145 ) ) ;
#17913=CARTESIAN_POINT ( 'NONE',  ( -4.489196722361281644, 50.47725044336133493, 75.37785507730471579 ) ) ;
#17915=VECTOR ( 'NONE', #12664, 1000.000000000000114 ) ;
#17919=CARTESIAN_POINT ( 'NONE',  ( 5.787239255393352266, 51.21348939705941206, 75.97375991483075097 ) ) ;
#17921=CARTESIAN_POINT ( 'NONE',  ( 0.7060283986096523856, 52.21262887048612811, 79.54746358246200089 ) ) ;
#17923=ORIENTED_EDGE ( 'NONE', *, *, #18961, .T. ) ;
#17925=EDGE_CURVE ( 'NONE', #1396, #6827, #15130, .T. ) ;
#17927=CARTESIAN_POINT ( 'NONE',  ( 9.353525637756030520, 42.82683421514393274, 78.50890480505780999 ) ) ;
#17930=CARTESIAN_POINT ( 'NONE',  ( -5.679243918435854965, 37.80248940946448499, 75.65168154244369703 ) ) ;
#17932=EDGE_CURVE ( 'NONE', #19237, #2125, #13196, .T. ) ;
#17941=EDGE_LOOP ( 'NONE', ( #3246, #15363, #12834, #20691 ) ) ;
#17943=DIRECTION ( 'NONE',  ( -1.540237394707284467E-16, -1.793354297423764243E-16, 1.000000000000000000 ) ) ;
#17944=CARTESIAN_POINT ( 'NONE',  ( 1.048114967784774310, 52.94689884418070136, 75.38689734427310896 ) ) ;
#17946=EDGE_CURVE ( 'NONE', #15829, #10630, #5096, .T. ) ;
#17951=LINE ( 'NONE', #16362, #3378 ) ;
#17952=DIRECTION ( 'NONE',  ( 0.3165065846431827645, 0.9485903129789529098, 0.000000000000000000 ) ) ;
#17954=CARTESIAN_POINT ( 'NONE',  ( 4.162128861264472235, 36.86717768966805409, 75.77524573853747825 ) ) ;
#17955=EDGE_CURVE ( 'NONE', #8338, #10035, #16703, .T. ) ;
#17958=CARTESIAN_POINT ( 'NONE',  ( 9.346906861638174746, 42.80699732323137852, 76.23134092453109645 ) ) ;
#17960=CARTESIAN_POINT ( 'NONE',  ( 6.484157998033387216, 49.78468859024245319, 78.34373887323252461 ) ) ;
#17961=VECTOR ( 'NONE', #872, 1000.000000000000227 ) ;
#17963=CARTESIAN_POINT ( 'NONE',  ( 5.466176856163651010, 50.69752978158682311, 78.92065061514911406 ) ) ;
#17964=ORIENTED_EDGE ( 'NONE', *, *, #15219, .T. ) ;
#17967=CARTESIAN_POINT ( 'NONE',  ( 4.686687817024941083, 51.22644301457940941, 79.43421539708423040 ) ) ;
#17969=CARTESIAN_POINT ( 'NONE',  ( 4.393996117251955269, 36.11308595931626542, 76.73963291717792856 ) ) ;
#17970=CARTESIAN_POINT ( 'NONE',  ( 8.631800694748326563, 43.02819682608614471, 77.50995918449682165 ) ) ;
#17971=CARTESIAN_POINT ( 'NONE',  ( 4.143578761807024335, 51.51916996771892343, 78.37598241635205909 ) ) ;
#17972=CARTESIAN_POINT ( 'NONE',  ( -4.883901707777988932, 37.21500215679002821, 76.12782976279942204 ) ) ;
#17975=EDGE_CURVE ( 'NONE', #13018, #13741, #20192, .T. ) ;
#17977=CARTESIAN_POINT ( 'NONE',  ( -5.838300394258943093, 50.43300593553962585, 78.21416447440572028 ) ) ;
#17978=CARTESIAN_POINT ( 'NONE',  ( -4.344504932464893443, 37.57120742909659583, 78.93669174070734584 ) ) ;
#17979=CARTESIAN_POINT ( 'NONE',  ( 8.921473627994183531, 41.53194693301924190, 77.48121952543638713 ) ) ;
#17980=CARTESIAN_POINT ( 'NONE',  ( 8.387827792284632267, 39.93257650953714943, 76.58175473889373563 ) ) ;
#17982=VERTEX_POINT ( 'NONE', #15000 ) ;
#17984=CARTESIAN_POINT ( 'NONE',  ( 6.402690229413289025, 38.46820081115981083, 76.05683950549904182 ) ) ;
#17985=CARTESIAN_POINT ( 'NONE',  ( 0.2833753639608733721, 52.20780802782073238, 79.53425070713537082 ) ) ;
#17986=CARTESIAN_POINT ( 'NONE',  ( 7.823713835575672348, 40.42945125626696523, 79.18036419938457016 ) ) ;
#17987=CARTESIAN_POINT ( 'NONE',  ( -3.557579061748611160, 36.23530104570325250, 76.03954924220039402 ) ) ;
#17989=ORIENTED_EDGE ( 'NONE', *, *, #9076, .T. ) ;
#17991=DIRECTION ( 'NONE',  ( 0.007885122365275663500, 0.9999689119394085113, 1.805443505845543142E-16 ) ) ;
#17992=CIRCLE ( 'NONE', #20350, 8.199999999999995737 ) ;
#17993=CIRCLE ( 'NONE', #4057, 8.199999999999995737 ) ;
#18001=CARTESIAN_POINT ( 'NONE',  ( 7.691771551572208487, 40.18266124458227750, 72.45433879953087342 ) ) ;
#18003=DIRECTION ( 'NONE',  ( -0.9429220365244147528, 0.3330135628418914862, -8.551124769255465366E-17 ) ) ;
#18006=LINE ( 'NONE', #15030, #12918 ) ;
#18008=DIRECTION ( 'NONE',  ( -0.5941461771851691553, -0.8043570849667760481, -2.357623395011396791E-16 ) ) ;
#18009=ORIENTED_EDGE ( 'NONE', *, *, #9383, .F. ) ;
#18010=CARTESIAN_POINT ( 'NONE',  ( -5.616859571223690395, 50.59123944021462904, 79.13778479689705136 ) ) ;
#18012=CARTESIAN_POINT ( 'NONE',  ( 5.939788499136119171, 51.10080741576499719, 76.32243632687685420 ) ) ;
#18013=CARTESIAN_POINT ( 'NONE',  ( -4.383473025373059606, 51.47257230871590394, 78.45066232894264147 ) ) ;
#18018=CARTESIAN_POINT ( 'NONE',  ( 0.7261808065621055963, 52.35991697419684243, 76.81167236361466166 ) ) ;
#18020=CARTESIAN_POINT ( 'NONE',  ( 4.685757199431944464, 52.02710982139440432, 77.94290914044947272 ) ) ;
#18022=CARTESIAN_POINT ( 'NONE',  ( -4.204074076407136040, 37.46120757759153719, 77.13799123457000917 ) ) ;
#18024=VECTOR ( 'NONE', #6802, 1000.000000000000000 ) ;
#18025=CARTESIAN_POINT ( 'NONE',  ( 8.951667845840693971, 41.62244091939069790, 77.14698585835439815 ) ) ;
#18026=CARTESIAN_POINT ( 'NONE',  ( 5.482029497793807771, 37.63747020982715696, 76.09175310361966638 ) ) ;
#18028=CARTESIAN_POINT ( 'NONE',  ( 5.579217223280415361, 50.61251095053976456, 76.36217657474753651 ) ) ;
#18029=ORIENTED_EDGE ( 'NONE', *, *, #11688, .T. ) ;
#18032=VERTEX_POINT ( 'NONE', #18506 ) ;
#18036=CARTESIAN_POINT ( 'NONE',  ( 9.335797811945472091, 42.77370279655738017, 78.83313045764568017 ) ) ;
#18038=ORIENTED_EDGE ( 'NONE', *, *, #13153, .T. ) ;
#18040=CARTESIAN_POINT ( 'NONE',  ( -4.891113921371359474, 38.15633602453890916, 75.45005776384208218 ) ) ;
#18046=DIRECTION ( 'NONE',  ( 0.8136266022444373913, 0.5813877811927010697, 2.295812393977109593E-16 ) ) ;
#18047=CARTESIAN_POINT ( 'NONE',  ( -4.537329489133296256, 36.95900321965768143, 78.11020518223413944 ) ) ;
#18050=CARTESIAN_POINT ( 'NONE',  ( -7.854101642381717596, 41.46402583572638889, 78.93502120504803088 ) ) ;
#18052=CARTESIAN_POINT ( 'NONE',  ( 4.100190290135135029, 51.54036911970691648, 72.45433879953087342 ) ) ;
#18053=VECTOR ( 'NONE', #6945, 1000.000000000000000 ) ;
#18055=EDGE_CURVE ( 'NONE', #6977, #10346, #18718, .T. ) ;
#18056=CARTESIAN_POINT ( 'NONE',  ( 0.3278485956581845273, 52.34524085292903095, 77.10139762306027933 ) ) ;
#18057=ORIENTED_EDGE ( 'NONE', *, *, #14966, .T. ) ;
#18058=CARTESIAN_POINT ( 'NONE',  ( 4.318075228076872385, 36.97861125383128922, 75.61597629374708163 ) ) ;
#18061=ORIENTED_EDGE ( 'NONE', *, *, #16366, .T. ) ;
#18062=VECTOR ( 'NONE', #4552, 1000.000000000000114 ) ;
#18063=DIRECTION ( 'NONE',  ( -0.3165065846431827645, -0.9485903129789529098, 0.000000000000000000 ) ) ;
#18066=CARTESIAN_POINT ( 'NONE',  ( 6.486188022505683826, 49.78318909293913919, 78.43783143115764744 ) ) ;
#18069=ORIENTED_EDGE ( 'NONE', *, *, #10762, .T. ) ;
#18070=EDGE_CURVE ( 'NONE', #19191, #17483, #8828, .T. ) ;
#18072=VERTEX_POINT ( 'NONE', #2445 ) ;
#18073=CARTESIAN_POINT ( 'NONE',  ( -2.167873396875370950, 37.04784696823259793, 72.45432679953087529 ) ) ;
#18074=CARTESIAN_POINT ( 'NONE',  ( 4.728442938187240152, 51.99557958566231264, 77.51131257087278925 ) ) ;
#18076=CARTESIAN_POINT ( 'NONE',  ( -0.9259701616170338268, 52.84221263810348290, 76.43547538781149342 ) ) ;
#18077=DIRECTION ( 'NONE',  ( 1.540237394707284220E-16, 1.793354297423764243E-16, -1.000000000000000000 ) ) ;
#18080=VECTOR ( 'NONE', #2592, 1000.000000000000114 ) ;
#18081=CARTESIAN_POINT ( 'NONE',  ( 4.133675539746122674, 51.51007735721194791, 76.08931382966170531 ) ) ;
#18082=CARTESIAN_POINT ( 'NONE',  ( -3.068202438178982749, 36.79865119415181596, 76.30596599901106458 ) ) ;
#18083=VECTOR ( 'NONE', #5727, 1000.000000000000114 ) ;
#18085=ORIENTED_EDGE ( 'NONE', *, *, #4880, .T. ) ;
#18086=DIRECTION ( 'NONE',  ( 1.540237394707284220E-16, 1.793354297423764243E-16, -1.000000000000000000 ) ) ;
#18087=CARTESIAN_POINT ( 'NONE',  ( 8.950289981099260217, 41.61831137135051506, 78.71610475470291135 ) ) ;
#18088=CARTESIAN_POINT ( 'NONE',  ( -4.796313072339920325, 37.15030396007738744, 78.92026643871187730 ) ) ;
#18091=EDGE_CURVE ( 'NONE', #10540, #54, #13818, .T. ) ;
#18093=CARTESIAN_POINT ( 'NONE',  ( 8.550070540977731781, 40.41882831985841307, 75.56834740413086138 ) ) ;
#18094=ORIENTED_EDGE ( 'NONE', *, *, #16384, .T. ) ;
#18095=CARTESIAN_POINT ( 'NONE',  ( 0.6452642261158869630, 52.96739513210086159, 79.54845644658969661 ) ) ;
#18096=CARTESIAN_POINT ( 'NONE',  ( 6.435710703716235770, 38.49179603313996978, 77.55645576794258034 ) ) ;
#18097=CARTESIAN_POINT ( 'NONE',  ( 5.394152393224890041, 50.75790946820724514, 75.36022115247205022 ) ) ;
#18099=CARTESIAN_POINT ( 'NONE',  ( 0.8505168181936991756, 52.95605297189983673, 76.43141495382415940 ) ) ;
#18100=ORIENTED_EDGE ( 'NONE', *, *, #2, .T. ) ;
#18101=DIRECTION ( 'NONE',  ( -1.540237394707284220E-16, -1.793354297423764243E-16, 1.000000000000000000 ) ) ;
#18102=EDGE_CURVE ( 'NONE', #3603, #13955, #10661, .T. ) ;
#18104=LINE ( 'NONE', #15017, #12916 ) ;
#18108=AXIS2_PLACEMENT_3D ( 'NONE', #17696, #14400, #36 ) ;
#18110=CARTESIAN_POINT ( 'NONE',  ( 8.627730818565934712, 42.92075920536279199, 79.03125282521155270 ) ) ;
#18111=ORIENTED_EDGE ( 'NONE', *, *, #20955, .T. ) ;
#18113=ORIENTED_EDGE ( 'NONE', *, *, #17191, .T. ) ;
#18116=CARTESIAN_POINT ( 'NONE',  ( 0.3821786226492928651, 35.36301154328572949, 75.45433879953087342 ) ) ;
#18119=DIRECTION ( 'NONE',  ( -0.5941461771851693774, -0.8043570849667760481, -2.357623395011396791E-16 ) ) ;
#18120=CARTESIAN_POINT ( 'NONE',  ( -5.919594526472893747, 37.98002672170838423, 78.92638042842689572 ) ) ;
#18123=CARTESIAN_POINT ( 'NONE',  ( -4.393892947181490705, 51.46512661408927869, 78.70491066849456274 ) ) ;
#18125=CARTESIAN_POINT ( 'NONE',  ( 0.3279818009034626280, 52.35625691656657210, 78.52223653336807274 ) ) ;
#18126=ORIENTED_EDGE ( 'NONE', *, *, #5047, .F. ) ;
#18127=CARTESIAN_POINT ( 'NONE',  ( -4.219550833609926777, 50.84278967315511721, 75.97260225988416948 ) ) ;
#18128=EDGE_LOOP ( 'NONE', ( #14782, #4258, #1979, #9659, #17526, #5356, #4840, #567, #14555, #16145, #13463 ) ) ;
#18129=DIRECTION ( 'NONE',  ( 0.9999689119394086223, -0.007885122365275665235, 1.526048693634353392E-16 ) ) ;
#18130=CARTESIAN_POINT ( 'NONE',  ( -7.704497869805115862, 40.97402890596596592, 76.84875211988632770 ) ) ;
#18131=CARTESIAN_POINT ( 'NONE',  ( -4.385150316929264491, 37.59252787896735981, 77.30162809418146708 ) ) ;
#18134=CARTESIAN_POINT ( 'NONE',  ( 5.433479250907716995, 37.60277798094034551, 76.01697444493925104 ) ) ;
#18135=CARTESIAN_POINT ( 'NONE',  ( -7.079689812751086997, 47.05182882866842675, 78.14247693707426379 ) ) ;
#18138=LINE ( 'NONE', #14938, #1358 ) ;
#18139=CARTESIAN_POINT ( 'NONE',  ( 5.410058914415630582, 36.83912723373610731, 78.11840496518735222 ) ) ;
#18140=VERTEX_POINT ( 'NONE', #8723 ) ;
#18143=LINE ( 'NONE', #2075, #11633 ) ;
#18145=ORIENTED_EDGE ( 'NONE', *, *, #6533, .T. ) ;
#18146=CARTESIAN_POINT ( 'NONE',  ( 6.882736312352589536, 37.89144858414100270, 76.69330938776616335 ) ) ;
#18147=CARTESIAN_POINT ( 'NONE',  ( -5.420941400696308143, 38.54769824076353046, 75.91870325888974946 ) ) ;
#18148=VERTEX_POINT ( 'NONE', #4339 ) ;
#18149=CARTESIAN_POINT ( 'NONE',  ( -0.9436870690626151248, 52.23009998296728895, 77.21536821129558348 ) ) ;
#18150=CARTESIAN_POINT ( 'NONE',  ( 0.3329543312200850536, 52.96014725284622671, 76.39696649187393973 ) ) ;
#18153=FACE_OUTER_BOUND ( 'NONE', #12737, .T. ) ;
#18156=CARTESIAN_POINT ( 'NONE',  ( 0.9589043286300715785, 52.95179583173001703, 75.37608287192134071 ) ) ;
#18158=CARTESIAN_POINT ( 'NONE',  ( 6.090066878584988075, 50.06496988346189880, 75.53514883118299394 ) ) ;
#18161=PLANE ( 'NONE',  #1434 ) ;
#18162=ORIENTED_EDGE ( 'NONE', *, *, #12739, .T. ) ;
#18163=CARTESIAN_POINT ( 'NONE',  ( 4.853207525418807400, 37.36099720106794564, 75.39318197153889400 ) ) ;
#18166=CARTESIAN_POINT ( 'NONE',  ( 6.882736312352589536, 37.89144858414100270, 77.26022115247205591 ) ) ;
#18167=CARTESIAN_POINT ( 'NONE',  ( 8.452544761179964894, 42.49095542139739479, 75.50722976489458915 ) ) ;
#18169=CARTESIAN_POINT ( 'NONE',  ( -7.202951829524388394, 41.41213674333113914, 78.65672070501008761 ) ) ;
#18170=ORIENTED_EDGE ( 'NONE', *, *, #11282, .T. ) ;
#18171=ORIENTED_EDGE ( 'NONE', *, *, #14367, .F. ) ;
#18173=CARTESIAN_POINT ( 'NONE',  ( -4.895593109503407980, 37.22363812428621088, 78.18375056423674607 ) ) ;
#18175=CARTESIAN_POINT ( 'NONE',  ( -4.006646489220814011, 48.09791109810387155, 80.45433879953087342 ) ) ;
#18176=CARTESIAN_POINT ( 'NONE',  ( -2.167873396875370950, 37.04784696823259793, 75.45433879953087342 ) ) ;
#18177=CARTESIAN_POINT ( 'NONE',  ( 4.367780705229349358, 51.33715330180078951, 77.58315289018165117 ) ) ;
#18178=CARTESIAN_POINT ( 'NONE',  ( 8.352692957205995583, 41.72820301203469739, 77.48007297599048115 ) ) ;
#18181=CARTESIAN_POINT ( 'NONE',  ( 8.211401091253357265, 41.32387017323333112, 76.34522901481825841 ) ) ;
#18187=CARTESIAN_POINT ( 'NONE',  ( 3.961507247562192635, 36.71833509068318335, 76.73963291717792856 ) ) ;
#18188=CARTESIAN_POINT ( 'NONE',  ( 0.8377421044266869510, 51.35991668224300355, 77.76169174070734869 ) ) ;
#18189=CARTESIAN_POINT ( 'NONE',  ( 8.563160678057862185, 42.55264511967046559, 75.54928777999336376 ) ) ;
#18190=CARTESIAN_POINT ( 'NONE',  ( 8.951218635964366399, 41.62109460889399770, 77.24172240072661566 ) ) ;
#18195=ORIENTED_EDGE ( 'NONE', *, *, #6343, .T. ) ;
#18196=CARTESIAN_POINT ( 'NONE',  ( 6.761578195034432248, 37.80487342938723572, 78.00072712051441215 ) ) ;
#18197=DIRECTION ( 'NONE',  ( 0.9480563259966798828, 0.3181025035074024343, 2.030702297275143506E-16 ) ) ;
#18198=CARTESIAN_POINT ( 'NONE',  ( 5.451031912548643277, 50.71558463665398619, 77.95462253026452970 ) ) ;
#18200=CARTESIAN_POINT ( 'NONE',  ( -4.398802922602397913, 51.46161812541917868, 78.75145056212190298 ) ) ;
#18201=CARTESIAN_POINT ( 'NONE',  ( -4.158578283022523081, 37.42937009194850617, 76.53375056423675460 ) ) ;
#18205=CARTESIAN_POINT ( 'NONE',  ( 1.770248540159448103, 52.94298469573600130, 76.95808337915808295 ) ) ;
#18206=EDGE_CURVE ( 'NONE', #5478, #14218, #5138, .T. ) ;
#18208=B_SPLINE_SURFACE_WITH_KNOTS ( 'NONE', 3, 1, ( 
 ( #15852, #10974 ),
 ( #7760, #1267 ),
 ( #17445, #12550 ),
 ( #6050, #19041 ),
 ( #4453, #5031 ),
 ( #247, #18134 ),
 ( #3555, #11657 ),
 ( #5137, #16752 ),
 ( #11550, #18026 ),
 ( #2066, #3447 ),
 ( #10059, #16539 ),
 ( #6843, #13349 ),
 ( #11858, #5457 ),
 ( #19820, #9960 ),
 ( #13547, #565 ),
 ( #5242, #20023 ),
 ( #11758, #7048 ),
 ( #3862, #6943 ),
 ( #8563, #18232 ) ),
 .UNSPECIFIED., .F., .F., .F.,
 ( 4, 1, 1, 1, 1, 1, 1, 1, 1, 1, 1, 1, 1, 1, 1, 1, 4 ),
 ( 2, 2 ),
 ( 0.000000000000000000, 0.06114104454794499349, 0.1175581266966176375, 0.1702703359127188676, 0.2207833336891595610, 0.2680835234284920654, 0.3093802502289375589, 0.3470663877653532570, 0.3827844710311357757, 0.4080409699193555118, 0.4487658506906452294, 0.5030388115584650821, 0.5728007717267906695, 0.6580545229227713344, 0.7568648491070055773, 0.8711692811930628055, 1.000000000000000000 ),
 ( 0.000000000000000000, 1.000000000000000000 ),
 .UNSPECIFIED. ) ;
#18211=EDGE_CURVE ( 'NONE', #3672, #19886, #7862, .T. ) ;
#18212=CARTESIAN_POINT ( 'NONE',  ( 4.393996117251955269, 36.11308595931626542, 76.96022115247204454 ) ) ;
#18214=ORIENTED_EDGE ( 'NONE', *, *, #1162, .F. ) ;
#18217=ORIENTED_EDGE ( 'NONE', *, *, #4422, .F. ) ;
#18219=CARTESIAN_POINT ( 'NONE',  ( 8.159484030927535159, 41.62940053041398158, 75.36031793586835192 ) ) ;
#18221=AXIS2_PLACEMENT_3D ( 'NONE', #4888, #3615, #14690 ) ;
#18222=CARTESIAN_POINT ( 'NONE',  ( -4.388990501910972952, 51.46862972198961472, 78.65149807507090429 ) ) ;
#18223=CARTESIAN_POINT ( 'NONE',  ( 0.3328907573102549700, 52.96757149581038249, 78.56344688395670062 ) ) ;
#18225=CARTESIAN_POINT ( 'NONE',  ( -4.385532207686900996, 51.47110089242590902, 76.31459635612003467 ) ) ;
#18227=DIRECTION ( 'NONE',  ( 0.3165065846431827645, 0.9485903129789529098, 0.000000000000000000 ) ) ;
#18229=LINE ( 'NONE', #14827, #6442 ) ;
#18232=CARTESIAN_POINT ( 'NONE',  ( 5.495636600878563982, 37.64719334750368063, 76.58742703482498371 ) ) ;
#18233=VECTOR ( 'NONE', #13965, 1000.000000000000000 ) ;
#18235=ADVANCED_FACE ( 'NONE', ( #9265 ), #12753, .T. ) ;
#18236=CARTESIAN_POINT ( 'NONE',  ( 8.296628936784257391, 41.55497301399228149, 78.93669174070734584 ) ) ;
#18237=CARTESIAN_POINT ( 'NONE',  ( 5.746684213116473039, 37.07966734754892713, 78.33482135361461474 ) ) ;
#18239=LINE ( 'NONE', #469, #2041 ) ;
#18242=ORIENTED_EDGE ( 'NONE', *, *, #1486, .T. ) ;
#18243=CARTESIAN_POINT ( 'NONE',  ( 8.946756316568102108, 41.60772075457913388, 78.11862058389174024 ) ) ;
#18244=CARTESIAN_POINT ( 'NONE',  ( -4.948764291328629383, 37.26291353443464516, 75.36972643424059015 ) ) ;
#18245=ORIENTED_EDGE ( 'NONE', *, *, #4287, .F. ) ;
#18250=CARTESIAN_POINT ( 'NONE',  ( -4.517974409599093910, 36.94470640207592993, 78.25995115514949418 ) ) ;
#18252=ORIENTED_EDGE ( 'NONE', *, *, #4434, .T. ) ;
#18253=CARTESIAN_POINT ( 'NONE',  ( 0.6087969908866583957, 52.36175308762906155, 77.38466870788910512 ) ) ;
#18254=CARTESIAN_POINT ( 'NONE',  ( 0.5981602388297567741, 52.96185312741366857, 75.36022115247205022 ) ) ;
#18256=CARTESIAN_POINT ( 'NONE',  ( 5.513055384645696222, 50.66842935564089601, 77.25219493245084834 ) ) ;
#18259=ORIENTED_EDGE ( 'NONE', *, *, #287, .F. ) ;
#18260=CARTESIAN_POINT ( 'NONE',  ( 4.958128353061608706, 36.51619420082643330, 75.49492869865662215 ) ) ;
#18261=CARTESIAN_POINT ( 'NONE',  ( 7.705087751586725098, 40.25077934585792860, 78.89537297773202340 ) ) ;
#18262=VECTOR ( 'NONE', #16821, 999.9999999999998863 ) ;
#18264=DIRECTION ( 'NONE',  ( 1.540237394707284220E-16, 1.793354297423764243E-16, -1.000000000000000000 ) ) ;
#18268=EDGE_LOOP ( 'NONE', ( #14859, #14593 ) ) ;
#18269=CARTESIAN_POINT ( 'NONE',  ( 6.811311454328823345, 50.45704851585021800, 79.04700635913849283 ) ) ;
#18271=CARTESIAN_POINT ( 'NONE',  ( 5.507916691552521726, 50.67237191677704544, 76.01238189972890780 ) ) ;
#18273=VECTOR ( 'NONE', #11986, 1000.000000000000000 ) ;
#18275=CARTESIAN_POINT ( 'NONE',  ( 4.113283266163863416, 51.52514030825627600, 77.01204236660041147 ) ) ;
#18276=CARTESIAN_POINT ( 'NONE',  ( 8.377962481724168242, 41.81109640710783282, 77.32528637492231383 ) ) ;
#18278=CARTESIAN_POINT ( 'NONE',  ( 8.230998048249997368, 41.38260349656003001, 76.04813117819971069 ) ) ;
#18284=CARTESIAN_POINT ( 'NONE',  ( 4.984017504316113900, 37.27956383785731731, 75.37664775417469798 ) ) ;
#18285=CIRCLE ( 'NONE', #16939, 8.199999999999995737 ) ;
#18287=CARTESIAN_POINT ( 'NONE',  ( 5.398882651910504649, 50.75441279359508684, 77.28963291717792572 ) ) ;
#18289=CARTESIAN_POINT ( 'NONE',  ( 5.374105918413365046, 50.77268445065888613, 78.93541288588724569 ) ) ;
#18291=CARTESIAN_POINT ( 'NONE',  ( -4.808920012916950704, 37.15961619924308934, 75.98775578934684916 ) ) ;
#18293=EDGE_CURVE ( 'NONE', #20173, #2871, #15750, .T. ) ;
#18294=CARTESIAN_POINT ( 'NONE',  ( 5.902048492000326441, 51.12868443877599134, 78.27786821129558348 ) ) ;
#18295=VERTEX_POINT ( 'NONE', #2862 ) ;
#18297=CARTESIAN_POINT ( 'NONE',  ( 8.303614452336031349, 41.57589654819728509, 79.54845644658969661 ) ) ;
#18298=PLANE ( 'NONE',  #14495 ) ;
#18302=CIRCLE ( 'NONE', #2677, 8.199999999999995737 ) ;
#18303=CARTESIAN_POINT ( 'NONE',  ( -4.588243132438923233, 36.99661107704094576, 78.89954634079194307 ) ) ;
#18305=FACE_OUTER_BOUND ( 'NONE', #9288, .T. ) ;
#18306=EDGE_CURVE ( 'NONE', #15079, #4532, #2652, .T. ) ;
#18309=CARTESIAN_POINT ( 'NONE',  ( -8.191743529290757664, 42.93415629907709530, 78.46397878055076092 ) ) ;
#18312=CIRCLE ( 'NONE', #15261, 8.799999999999995381 ) ;
#18313=VERTEX_POINT ( 'NONE', #20518 ) ;
#18315=EDGE_CURVE ( 'NONE', #2056, #2184, #5945, .T. ) ;
#18317=ORIENTED_EDGE ( 'NONE', *, *, #13213, .F. ) ;
#18319=CARTESIAN_POINT ( 'NONE',  ( 8.302046940891129267, 41.57028864366792931, 78.04666919979170814 ) ) ;
#18321=CARTESIAN_POINT ( 'NONE',  ( 0.3821786226492927541, 35.36301154328572949, 76.16022115247204738 ) ) ;
#18323=CARTESIAN_POINT ( 'NONE',  ( -3.713457647669470063, 51.95134076679423174, 79.29276450469329518 ) ) ;
#18325=ORIENTED_EDGE ( 'NONE', *, *, #2, .F. ) ;
#18326=DIRECTION ( 'NONE',  ( 0.3165065846431826535, 0.9485903129789529098, 2.188653791613874008E-16 ) ) ;
#18328=EDGE_LOOP ( 'NONE', ( #6308, #16522, #7711, #14330, #162, #3118, #10936, #14004, #20791, #19568, #7578, #17313, #7971, #19712, #3588, #7624, #4216, #6930, #18423, #15013, #18697 ) ) ;
#18329=PLANE ( 'NONE',  #18921 ) ;
#18330=CARTESIAN_POINT ( 'NONE',  ( -7.022721810984192459, 41.30210581816755422, 76.72474157890661672 ) ) ;
#18331=ADVANCED_FACE ( 'NONE', ( #8066 ), #11382, .F. ) ;
#18333=DIRECTION ( 'NONE',  ( -0.02533578529877749883, -0.9996789974703351733, -1.831801750099157288E-16 ) ) ;
#18334=CARTESIAN_POINT ( 'NONE',  ( -7.290527651941959952, 40.11224193202943411, 78.50801527011910252 ) ) ;
#18337=AXIS2_PLACEMENT_3D ( 'NONE', #10746, #10642, #15621 ) ;
#18338=VECTOR ( 'NONE', #1475, 1000.000000000000114 ) ;
#18342=EDGE_LOOP ( 'NONE', ( #12138, #15671, #11960, #11792 ) ) ;
#18347=ORIENTED_EDGE ( 'NONE', *, *, #12013, .T. ) ;
#18349=CARTESIAN_POINT ( 'NONE',  ( 8.825683451842801119, 41.24485769827808213, 77.95380709400741637 ) ) ;
#18350=DIRECTION ( 'NONE',  ( -0.5941461771851693774, -0.8043570849667760481, -2.357623395011396791E-16 ) ) ;
#18351=EDGE_LOOP ( 'NONE', ( #5503, #8100, #17989, #17964 ) ) ;
#18352=CARTESIAN_POINT ( 'NONE',  ( 5.567302800327750489, 36.95148795754280258, 75.36140480012781495 ) ) ;
#18353=DIRECTION ( 'NONE',  ( 1.540237394707284220E-16, 1.793354297423764243E-16, -1.000000000000000000 ) ) ;
#18356=CARTESIAN_POINT ( 'NONE',  ( -4.275220640117388449, 37.54015509005341045, 77.94562699264550076 ) ) ;
#18359=CARTESIAN_POINT ( 'NONE',  ( -4.739054262994943478, 51.21848697497132719, 76.01646854312687651 ) ) ;
#18365=CARTESIAN_POINT ( 'NONE',  ( -3.532917577324399261, 36.21708460058427193, 78.46683879953087626 ) ) ;
#18366=AXIS2_PLACEMENT_3D ( 'NONE', #16153, #12647, #3061 ) ;
#18368=CARTESIAN_POINT ( 'NONE',  ( 6.575359255040893913, 44.22010074469034180, 72.45432679953087529 ) ) ;
#18369=VERTEX_POINT ( 'NONE', #12962 ) ;
#18370=CARTESIAN_POINT ( 'NONE',  ( 4.410764955181007529, 36.12506835695402430, 76.35980278528342069 ) ) ;
#18374=CARTESIAN_POINT ( 'NONE',  ( 0.3327559137711116333, 52.96757305357242984, 77.76169174070734869 ) ) ;
#18377=ORIENTED_EDGE ( 'NONE', *, *, #20561, .T. ) ;
#18378=LINE ( 'NONE', #16995, #3172 ) ;
#18381=CARTESIAN_POINT ( 'NONE',  ( 0.5278000597222750612, 52.96709611985676247, 75.36134551364482093 ) ) ;
#18382=DIRECTION ( 'NONE',  ( 0.5813877811927012917, -0.8136266022444372803, -5.636455622144620416E-17 ) ) ;
#18383=CARTESIAN_POINT ( 'NONE',  ( -2.925772203269236371, 51.60219236238361873, 78.51222722775425211 ) ) ;
#18386=PRODUCT ( 'Number Dial Wheels', 'Number Dial Wheels', '', ( #17094 ) ) ;
#18387=CARTESIAN_POINT ( 'NONE',  ( 0.8348233090668778500, 52.35226028205824633, 77.59858114993788547 ) ) ;
#18390=CARTESIAN_POINT ( 'NONE',  ( 5.597054231160713655, 36.97274724074663510, 77.75916469768418438 ) ) ;
#18393=CARTESIAN_POINT ( 'NONE',  ( -7.372922797599690270, 41.96044977055945679, 78.56636689789523587 ) ) ;
#18394=EDGE_LOOP ( 'NONE', ( #19265, #4723, #3534, #3358 ) ) ;
#18395=CARTESIAN_POINT ( 'NONE',  ( -4.537099264183358294, 37.70896829297682729, 76.38448585835440952 ) ) ;
#18397=ORIENTED_EDGE ( 'NONE', *, *, #9125, .T. ) ;
#18400=CARTESIAN_POINT ( 'NONE',  ( 5.497743849324331578, 37.64424434608246628, 77.37492703482499223 ) ) ;
#18402=DIRECTION ( 'NONE',  ( 1.540237394707284220E-16, 1.793354297423764243E-16, -1.000000000000000000 ) ) ;
#18404=ADVANCED_FACE ( 'NONE', ( #11691 ), #14990, .T. ) ;
#18405=CARTESIAN_POINT ( 'NONE',  ( 5.541713100162347416, 50.64173420093050026, 78.24916896818955081 ) ) ;
#18406=VERTEX_POINT ( 'NONE', #6642 ) ;
#18408=AXIS2_PLACEMENT_3D ( 'NONE', #820, #7305, #13794 ) ;
#18409=FACE_OUTER_BOUND ( 'NONE', #465, .T. ) ;
#18410=CARTESIAN_POINT ( 'NONE',  ( -4.537099264183358294, 37.70896829297682729, 77.05433879953086773 ) ) ;
#18411=CARTESIAN_POINT ( 'NONE',  ( -5.590960105440975880, 48.67769231808699715, 75.45433879953087342 ) ) ;
#18412=ORIENTED_EDGE ( 'NONE', *, *, #4669, .T. ) ;
#18415=CARTESIAN_POINT ( 'NONE',  ( 5.668901936282467524, 51.30090040776863702, 77.27261723006257910 ) ) ;
#18418=CARTESIAN_POINT ( 'NONE',  ( 1.567270154302307761, 52.94458525490427547, 76.85511030890285156 ) ) ;
#18421=B_SPLINE_CURVE_WITH_KNOTS ( 'NONE', 3,
 ( #8056, #16251, #9671, #6338, #3363, #14752, #16150, #3266, #14543, #4951, #11576, #17839, #20907, #12951, #19431 ),
 .UNSPECIFIED., .F., .F.,
 ( 4, 1, 1, 1, 1, 1, 1, 1, 1, 1, 1, 1, 4 ),
 ( 0.000000000000000000, 0.1176523470896303353, 0.2161622001139844318, 0.3003057309359747351, 0.3785980537073788676, 0.4226998745584166772, 0.4746596431302817498, 0.5370400780653459272, 0.6084305140821594238, 0.6909958779695384301, 0.7839813792576545426, 0.8861497511813531958, 0.9999999999999998890 ),
 .UNSPECIFIED. ) ;
#18422=CARTESIAN_POINT ( 'NONE',  ( -8.180775199338105708, 42.85845644839661617, 78.91515802863237639 ) ) ;
#18423=ORIENTED_EDGE ( 'NONE', *, *, #4772, .F. ) ;
#18427=CARTESIAN_POINT ( 'NONE',  ( 2.108290839596759447, 51.34989793853182505, 76.48963291717792856 ) ) ;
#18429=VERTEX_POINT ( 'NONE', #1659 ) ;
#18430=LINE ( 'NONE', #16523, #9300 ) ;
#18431=LINE ( 'NONE', #8548, #12529 ) ;
#18433=CARTESIAN_POINT ( 'NONE',  ( -2.914969352113478518, 51.60213568599777290, 78.15066919019970726 ) ) ;
#18435=CARTESIAN_POINT ( 'NONE',  ( 0.5221537403065008576, 44.16218137147968292, 80.45433879953087342 ) ) ;
#18436=DIRECTION ( 'NONE',  ( -1.540237394707284220E-16, -1.793354297423764243E-16, 1.000000000000000000 ) ) ;
#18437=ORIENTED_EDGE ( 'NONE', *, *, #17843, .F. ) ;
#18438=CARTESIAN_POINT ( 'NONE',  ( 8.218856723678189979, 41.33361459021993767, 77.32290381395976908 ) ) ;
#18440=ORIENTED_EDGE ( 'NONE', *, *, #7976, .T. ) ;
#18443=CARTESIAN_POINT ( 'NONE',  ( 8.789147962602239517, 47.20595287382010241, 75.43669174070734584 ) ) ;
#18444=EDGE_CURVE ( 'NONE', #9854, #16845, #11457, .T. ) ;
#18445=CARTESIAN_POINT ( 'NONE',  ( 5.334770775912043739, 37.52292652420527475, 75.97297093591537021 ) ) ;
#18449=CARTESIAN_POINT ( 'NONE',  ( 8.860816794629821302, 41.35015455542848173, 78.93613448519710118 ) ) ;
#18451=ORIENTED_EDGE ( 'NONE', *, *, #13105, .T. ) ;
#18456=ORIENTED_EDGE ( 'NONE', *, *, #12099, .F. ) ;
#18457=DIRECTION ( 'NONE',  ( -0.5941461771851691553, -0.8043570849667760481, -2.357623395011396791E-16 ) ) ;
#18458=PLANE ( 'NONE',  #7570 ) ;
#18460=CARTESIAN_POINT ( 'NONE',  ( 8.951667845840693971, 41.62244091939069790, 78.41904468188381827 ) ) ;
#18463=CARTESIAN_POINT ( 'NONE',  ( -4.598246518171406727, 51.31910303412164609, 78.93669174070734584 ) ) ;
#18465=ORIENTED_EDGE ( 'NONE', *, *, #3511, .T. ) ;
#18466=CARTESIAN_POINT ( 'NONE',  ( -4.449507049815707660, 50.67847138028889020, 76.30694920102484957 ) ) ;
#18467=FACE_OUTER_BOUND ( 'NONE', #2127, .T. ) ;
#18469=VECTOR ( 'NONE', #11501, 1000.000000000000000 ) ;
#18471=CARTESIAN_POINT ( 'NONE',  ( -4.374766499958361976, 37.59356042999372960, 75.97251605650340878 ) ) ;
#18472=CARTESIAN_POINT ( 'NONE',  ( -3.955205046931956403, 36.52901134360649138, 77.68963291717793140 ) ) ;
#18474=CARTESIAN_POINT ( 'NONE',  ( -4.157569799700691959, 37.42619470865965070, 79.54087410433339755 ) ) ;
#18476=ORIENTED_EDGE ( 'NONE', *, *, #19772, .F. ) ;
#18477=CARTESIAN_POINT ( 'NONE',  ( 1.885276772082373542, 52.95616720758849283, 75.75738117569228791 ) ) ;
#18480=EDGE_CURVE ( 'NONE', #10614, #6705, #9820, .T. ) ;
#18481=CARTESIAN_POINT ( 'NONE',  ( 0.3917809267179716559, 52.96710761965328373, 77.46088296688223807 ) ) ;
#18486=VECTOR ( 'NONE', #3214, 1000.000000000000114 ) ;
#18487=CARTESIAN_POINT ( 'NONE',  ( 0.3279640439667347862, 52.35988168082469940, 76.44919174070734869 ) ) ;
#18488=ORIENTED_EDGE ( 'NONE', *, *, #811, .T. ) ;
#18489=EDGE_CURVE ( 'NONE', #2672, #16604, #18925, .T. ) ;
#18490=CARTESIAN_POINT ( 'NONE',  ( 5.545031559531118148, 50.64376324557171216, 76.06405336652188964 ) ) ;
#18491=PLANE ( 'NONE',  #14935 ) ;
#18492=CARTESIAN_POINT ( 'NONE',  ( 7.857645200629401749, 40.72477040771212842, 75.53366564255911442 ) ) ;
#18493=CARTESIAN_POINT ( 'NONE',  ( 5.282950423531485917, 37.48574407745871895, 77.76022115247205591 ) ) ;
#18497=CARTESIAN_POINT ( 'NONE',  ( 8.211374823828526459, 41.32379144809473104, 76.38644048143638088 ) ) ;
#18501=CARTESIAN_POINT ( 'NONE',  ( 8.306997239855295589, 41.58599280843245793, 75.97301370697266520 ) ) ;
#18503=CARTESIAN_POINT ( 'NONE',  ( 0.5294070821904082180, 52.96600742907325099, 75.97350791242078571 ) ) ;
#18504=EDGE_LOOP ( 'NONE', ( #322, #3984, #13378, #3462, #14713, #17572, #6674, #6502, #6398, #2301, #14693, #7407, #924, #8599, #18217, #1219, #5296, #128, #12418, #9736, #20014 ) ) ;
#18505=CARTESIAN_POINT ( 'NONE',  ( -4.517072128342570991, 36.94403992325788977, 76.53375056423675460 ) ) ;
#18506=CARTESIAN_POINT ( 'NONE',  ( -2.073200253767598866, 36.38374080505226971, 80.45433879953087342 ) ) ;
#18508=CARTESIAN_POINT ( 'NONE',  ( -4.394494991871735756, 50.72473661586263916, 78.89396334764496999 ) ) ;
#18510=CARTESIAN_POINT ( 'NONE',  ( -4.735411308350331083, 37.10531828029096602, 75.97251605650340878 ) ) ;
#18513=CARTESIAN_POINT ( 'NONE',  ( 5.901631269491789844, 51.12899262423628954, 78.24916896818955081 ) ) ;
#18515=ORIENTED_EDGE ( 'NONE', *, *, #12353, .F. ) ;
#18516=MANIFOLD_SOLID_BREP ( 'Stock-MAS-160-1', #14936 ) ;
#18517=DIRECTION ( 'NONE',  ( -1.540237394707284220E-16, -1.793354297423764243E-16, 1.000000000000000000 ) ) ;
#18518=DIRECTION ( 'NONE',  ( -0.9485903129789527988, 0.3165065846431829311, -8.934458285744989980E-17 ) ) ;
#18521=CARTESIAN_POINT ( 'NONE',  ( -4.652687709939232086, 51.28020135170361016, 75.36022115247205022 ) ) ;
#18522=CARTESIAN_POINT ( 'NONE',  ( 6.012275498921958672, 37.26944915646792822, 78.37198585835440667 ) ) ;
#18523=CARTESIAN_POINT ( 'NONE',  ( 9.353817388681445522, 42.82770861117572281, 77.06316232894263862 ) ) ;
#18525=CARTESIAN_POINT ( 'NONE',  ( -7.333990156426536622, 40.19720935722482835, 76.16022115247204738 ) ) ;
#18526=CARTESIAN_POINT ( 'NONE',  ( -6.983651697411273673, 47.33966115288628629, 78.30768265673681583 ) ) ;
#18528=CARTESIAN_POINT ( 'NONE',  ( -3.682072889308531494, 36.32725962120449026, 77.89282216559597316 ) ) ;
#18529=LINE ( 'NONE', #19995, #7526 ) ;
#18531=CARTESIAN_POINT ( 'NONE',  ( 2.114036233085143657, 52.20617982865869067, 76.39831061904099840 ) ) ;
#18538=CARTESIAN_POINT ( 'NONE',  ( -3.278373844761569345, 51.34246014063911900, 79.29276450469329518 ) ) ;
#18539=B_SPLINE_CURVE_WITH_KNOTS ( 'NONE', 3,
 ( #996, #7377, #12291, #10713, #3865, #13867, #4078, #18555, #17074, #10493, #12074, #8774, #9094, #20348 ),
 .UNSPECIFIED., .F., .F.,
 ( 4, 2, 2, 2, 2, 2, 4 ),
 ( 0.000000000000000000, 0.0001700352343923301106, 0.0003400704687846602212, 0.0005101057031769903318, 0.0006801409375693204425, 0.001020211406354016659, 0.001360281875138712876 ),
 .UNSPECIFIED. ) ;
#18541=CARTESIAN_POINT ( 'NONE',  ( 0.8485110817020684593, 52.96358246935430714, 76.26682227151283655 ) ) ;
#18542=CARTESIAN_POINT ( 'NONE',  ( 0.3467791549783648120, 52.96746198069069322, 78.72223189599347393 ) ) ;
#18543=VERTEX_POINT ( 'NONE', #12659 ) ;
#18545=EDGE_CURVE ( 'NONE', #9005, #1116, #15752, .T. ) ;
#18547=CARTESIAN_POINT ( 'NONE',  ( 6.489847418355314979, 49.78593742637539776, 78.48669174070734300 ) ) ;
#18548=CARTESIAN_POINT ( 'NONE',  ( 4.143017335158133641, 51.51944627275094746, 78.46169174070733732 ) ) ;
#18549=CARTESIAN_POINT ( 'NONE',  ( 6.949446517235058352, 50.35501370930113296, 76.97234655072247733 ) ) ;
#18550=CARTESIAN_POINT ( 'NONE',  ( 5.495005229380907963, 37.64215342952340393, 76.33323713518528564 ) ) ;
#18554=VERTEX_POINT ( 'NONE', #20827 ) ;
#18555=CARTESIAN_POINT ( 'NONE',  ( 4.206193916732119398, 51.48810741143868341, 77.38277586711910772 ) ) ;
#18560=B_SPLINE_SURFACE_WITH_KNOTS ( 'NONE', 3, 1, ( 
 ( #12591, #20757 ),
 ( #19483, #11110 ),
 ( #17577, #19380 ),
 ( #4898, #3113 ),
 ( #19080, #9615 ),
 ( #4490, #8005 ),
 ( #11010, #1520 ),
 ( #2907, #837 ),
 ( #8215, #15318 ),
 ( #10539, #13603 ),
 ( #11807, #3814 ),
 ( #125, #2439 ),
 ( #18393, #6990 ),
 ( #13110, #5722 ),
 ( #12027, #8935 ) ),
 .UNSPECIFIED., .F., .F., .F.,
 ( 4, 1, 1, 1, 1, 1, 1, 1, 1, 1, 1, 1, 4 ),
 ( 2, 2 ),
 ( 0.000000000000000000, 0.1147061202499928684, 0.2167524336893861536, 0.3108875303107388466, 0.4039803747164272818, 0.4534531356382086598, 0.5079179071285299107, 0.5705472921755296856, 0.6391587557001583431, 0.7163993029626264386, 0.8030541331324966281, 0.8966574343170833350, 1.000000000000000000 ),
 ( 0.000000000000000000, 1.000000000000000000 ),
 .UNSPECIFIED. ) ;
#18561=VERTEX_POINT ( 'NONE', #2549 ) ;
#18563=DIRECTION ( 'NONE',  ( 0.3165065846431827645, 0.9485903129789529098, 0.000000000000000000 ) ) ;
#18565=LINE ( 'NONE', #2186, #18273 ) ;
#18567=EDGE_LOOP ( 'NONE', ( #11584, #12303, #744, #19985 ) ) ;
#18568=CARTESIAN_POINT ( 'NONE',  ( 0.6404851603139647409, 52.36132752672286017, 79.54845644658969661 ) ) ;
#18571=EDGE_LOOP ( 'NONE', ( #19652, #11668, #10684, #18440 ) ) ;
#18572=CARTESIAN_POINT ( 'NONE',  ( -4.408955773324692018, 50.70744783779237963, 76.05031124229590489 ) ) ;
#18574=AXIS2_PLACEMENT_3D ( 'NONE', #4555, #7763, #17134 ) ;
#18575=FACE_OUTER_BOUND ( 'NONE', #1673, .T. ) ;
#18580=CARTESIAN_POINT ( 'NONE',  ( 0.5981954327195757593, 52.96631631695955633, 75.36022115247205022 ) ) ;
#18583=CARTESIAN_POINT ( 'NONE',  ( 0.1632948971478923317, 52.35765006764384566, 79.53017257457305789 ) ) ;
#18584=DIRECTION ( 'NONE',  ( 0.3165065846431827645, 0.9485903129789529098, 0.000000000000000000 ) ) ;
#18586=ORIENTED_EDGE ( 'NONE', *, *, #1451, .F. ) ;
#18589=CARTESIAN_POINT ( 'NONE',  ( 0.3821786226492926430, 35.36301154328572949, 76.86610350541323555 ) ) ;
#18591=DIRECTION ( 'NONE',  ( -1.540237394707284467E-16, -1.793354297423764243E-16, 1.000000000000000000 ) ) ;
#18592=ADVANCED_FACE ( 'NONE', ( #1483 ), #8894, .T. ) ;
#18593=FACE_OUTER_BOUND ( 'NONE', #4337, .T. ) ;
#18595=CARTESIAN_POINT ( 'NONE',  ( -4.058243788015966302, 50.96439249353348089, 79.54394747197609661 ) ) ;
#18596=ADVANCED_FACE ( 'NONE', ( #8172 ), #8283, .T. ) ;
#18598=FACE_OUTER_BOUND ( 'NONE', #12569, .T. ) ;
#18599=CARTESIAN_POINT ( 'NONE',  ( 0.6318382202979666573, 52.35386089408143562, 77.38563349023446847 ) ) ;
#18602=EDGE_CURVE ( 'NONE', #16595, #7376, #1188, .T. ) ;
#18604=AXIS2_PLACEMENT_3D ( 'NONE', #15415, #8926, #11799 ) ;
#18606=CARTESIAN_POINT ( 'NONE',  ( 8.370524243984743151, 41.80079226538762072, 78.80177617112552468 ) ) ;
#18607=ORIENTED_EDGE ( 'NONE', *, *, #8741, .T. ) ;
#18611=VECTOR ( 'NONE', #9584, 1000.000000000000000 ) ;
#18612=CARTESIAN_POINT ( 'NONE',  ( -4.894326847483570830, 37.22270278754029960, 76.26481528174605273 ) ) ;
#18613=CARTESIAN_POINT ( 'NONE',  ( -6.926305133125032043, 47.45453072168001540, 78.88364539996459257 ) ) ;
#18614=DIRECTION ( 'NONE',  ( 0.007885122365275663500, 0.9999689119394085113, 1.805443505845543142E-16 ) ) ;
#18615=CARTESIAN_POINT ( 'NONE',  ( 5.401236444110097956, 50.74549864801142718, 77.94923276678728996 ) ) ;
#18616=VERTEX_POINT ( 'NONE', #16474 ) ;
#18618=VECTOR ( 'NONE', #18698, 1000.000000000000227 ) ;
#18619=CARTESIAN_POINT ( 'NONE',  ( 8.514005641241574551, 42.67515757794754450, 79.29919401074631935 ) ) ;
#18624=CARTESIAN_POINT ( 'NONE',  ( 5.605180980092264953, 51.34796851126965578, 77.21343514867072599 ) ) ;
#18627=EDGE_CURVE ( 'NONE', #19487, #20830, #600, .T. ) ;
#18628=AXIS2_PLACEMENT_3D ( 'NONE', #5663, #7479, #2378 ) ;
#18630=CARTESIAN_POINT ( 'NONE',  ( -7.016843279332989347, 47.24018387623220150, 78.28954034321952804 ) ) ;
#18631=CARTESIAN_POINT ( 'NONE',  ( 0.5221537403065014127, 44.16218137147968292, 76.48963291717792856 ) ) ;
#18632=DIRECTION ( 'NONE',  ( -1.540237394707284220E-16, -1.793354297423764243E-16, 1.000000000000000000 ) ) ;
#18633=CARTESIAN_POINT ( 'NONE',  ( 5.826095025493096990, 51.18478820489261949, 78.92065061514911406 ) ) ;
#18638=VERTEX_POINT ( 'NONE', #6774 ) ;
#18640=VECTOR ( 'NONE', #7580, 1000.000000000000000 ) ;
#18642=CARTESIAN_POINT ( 'NONE',  ( -3.838985764043254090, 50.94186738843281859, 79.52610421797659512 ) ) ;
#18644=CARTESIAN_POINT ( 'NONE',  ( 5.561792858816290597, 51.38001756867608094, 76.94115191089467487 ) ) ;
#18645=CARTESIAN_POINT ( 'NONE',  ( -3.096104608208455122, 36.80844346142616530, 78.46683879953087626 ) ) ;
#18646=ORIENTED_EDGE ( 'NONE', *, *, #5529, .T. ) ;
#18647=DIRECTION ( 'NONE',  ( -1.540237394707284220E-16, -1.793354297423764243E-16, 1.000000000000000000 ) ) ;
#18648=EDGE_LOOP ( 'NONE', ( #9344, #1354, #4569, #7216 ) ) ;
#18649=CARTESIAN_POINT ( 'NONE',  ( 4.668718747243733702, 52.03969543967511413, 77.44183710417100031 ) ) ;
#18652=CARTESIAN_POINT ( 'NONE',  ( -7.527492150214135869, 40.60566315307306695, 77.34111263368903622 ) ) ;
#18655=LINE ( 'NONE', #12391, #18080 ) ;
#18656=AXIS2_PLACEMENT_3D ( 'NONE', #18116, #16521, #1939 ) ;
#18657=EDGE_LOOP ( 'NONE', ( #18586, #11319, #20166, #2026, #11024, #8249 ) ) ;
#18658=DIRECTION ( 'NONE',  ( 0.5813877811927011807, -0.8136266022444372803, -5.636455622144619183E-17 ) ) ;
#18665=CARTESIAN_POINT ( 'NONE',  ( 2.115041367457929589, 52.20598078514408513, 77.84551527011910821 ) ) ;
#18666=DIRECTION ( 'NONE',  ( -1.540237394707284220E-16, -1.793354297423764243E-16, 1.000000000000000000 ) ) ;
#18667=CARTESIAN_POINT ( 'NONE',  ( -4.766891056059167298, 51.19859582181767621, 78.86176377286571437 ) ) ;
#18668=ORIENTED_EDGE ( 'NONE', *, *, #19975, .T. ) ;
#18669=DIRECTION ( 'NONE',  ( 0.007885122365275663500, 0.9999689119394085113, 1.805443505845543142E-16 ) ) ;
#18674=DIRECTION ( 'NONE',  ( -0.6080936526121348829, -0.7938652969193401576, -2.360290325043241294E-16 ) ) ;
#18676=DIRECTION ( 'NONE',  ( -0.08379744612499409606, 0.2649938410103908071, 0.9606020259449218335 ) ) ;
#18679=CARTESIAN_POINT ( 'NONE',  ( -4.871646723878168217, 37.20594989384409956, 76.06675994099744287 ) ) ;
#18680=CARTESIAN_POINT ( 'NONE',  ( 5.379229278502258182, 50.76175445474323311, 78.93590013629759028 ) ) ;
#18681=LINE ( 'NONE', #18795, #5164 ) ;
#18684=CARTESIAN_POINT ( 'NONE',  ( 1.926143999677636387, 52.20300684324731577, 75.81376357423876300 ) ) ;
#18691=B_SPLINE_SURFACE_WITH_KNOTS ( 'NONE', 3, 1, ( 
 ( #11195, #12883 ),
 ( #4991, #1722 ),
 ( #8709, #7087 ),
 ( #14478, #1826 ),
 ( #17777, #19258 ),
 ( #8201, #6590 ),
 ( #16084, #14789 ),
 ( #13098, #4673 ),
 ( #6485, #16404 ),
 ( #11512, #17984 ),
 ( #3801, #3408 ),
 ( #16794, #9918 ),
 ( #20944, #6378 ),
 ( #8311, #211 ),
 ( #19364, #3204 ),
 ( #6696, #13201 ),
 ( #17666, #12993 ),
 ( #11407, #607 ),
 ( #9706, #2210 ),
 ( #15192, #3099 ),
 ( #9602, #1507 ),
 ( #16185, #18860 ),
 ( #5564, #9194 ) ),
 .UNSPECIFIED., .F., .F., .F.,
 ( 4, 1, 1, 1, 1, 1, 1, 1, 1, 1, 1, 1, 1, 1, 1, 1, 1, 1, 1, 1, 4 ),
 ( 2, 2 ),
 ( 0.000000000000000000, 0.04338402653469398268, 0.08365674416537959013, 0.1211563976680593846, 0.1555788671761421382, 0.1872558283108043675, 0.2159034631954582228, 0.2418665822845563473, 0.2649561893498845744, 0.3085842690520175235, 0.3528342053628863995, 0.3996013663067077837, 0.4488757727682718413, 0.5007062493018590299, 0.5562201143629579292, 0.6158399466276373024, 0.6805899729784313790, 0.7509145939079137078, 0.8273700343273244773, 0.9100784481637514967, 0.9999999999999998890 ),
 ( 0.000000000000000000, 1.000000000000000000 ),
 .UNSPECIFIED. ) ;
#18692=CARTESIAN_POINT ( 'NONE',  ( -3.384255150065147877, 52.18657681870956111, 76.19075138459079710 ) ) ;
#18693=ORIENTED_EDGE ( 'NONE', *, *, #4599, .T. ) ;
#18695=AXIS2_PLACEMENT_3D ( 'NONE', #14955, #13367, #7063 ) ;
#18697=ORIENTED_EDGE ( 'NONE', *, *, #14151, .F. ) ;
#18698=DIRECTION ( 'NONE',  ( -0.9999689119394085113, 0.007885122365275831768, -1.526048693634352652E-16 ) ) ;
#18699=CARTESIAN_POINT ( 'NONE',  ( -3.539401246598059991, 43.09270903039240608, 82.45433879953087342 ) ) ;
#18701=EDGE_CURVE ( 'NONE', #264, #3603, #13616, .T. ) ;
#18703=DIRECTION ( 'NONE',  ( 0.007885122365275663500, 0.9999689119394085113, 1.805443505845543142E-16 ) ) ;
#18704=CARTESIAN_POINT ( 'NONE',  ( -0.9377071953849747121, 52.84024610139663025, 76.97528204790549466 ) ) ;
#18705=DIRECTION ( 'NONE',  ( -0.9485903129789527988, 0.3165065846431829311, -8.934458285744989980E-17 ) ) ;
#18707=CARTESIAN_POINT ( 'NONE',  ( -5.799282478806809138, 50.46088670938467402, 76.15119298917683466 ) ) ;
#18708=( LENGTH_UNIT ( ) NAMED_UNIT ( * ) SI_UNIT ( .MILLI., .METRE. ) );
#18712=CARTESIAN_POINT ( 'NONE',  ( -4.537099264183358294, 37.70896829297682729, 72.45433879953085921 ) ) ;
#18714=CARTESIAN_POINT ( 'NONE',  ( 5.678707969346596940, 37.03109401252010002, 78.30808796996917920 ) ) ;
#18715=EDGE_CURVE ( 'NONE', #12108, #4079, #6530, .T. ) ;
#18717=DIRECTION ( 'NONE',  ( -0.5941461771851693774, -0.8043570849667760481, -2.357623395011396791E-16 ) ) ;
#18718=LINE ( 'NONE', #7218, #16373 ) ;
#18719=CARTESIAN_POINT ( 'NONE',  ( -3.600277166070542378, 52.03221539514291294, 79.18928797456808866 ) ) ;
#18720=FILL_AREA_STYLE_COLOUR ( '', #6505 ) ;
#18721=CARTESIAN_POINT ( 'NONE',  ( -1.047061061252481107, 36.11373028406117669, 72.45433879953085921 ) ) ;
#18722=CARTESIAN_POINT ( 'NONE',  ( -7.101199524512181505, 46.93036113559941214, 79.11815246340434271 ) ) ;
#18723=CARTESIAN_POINT ( 'NONE',  ( 5.597054231160713655, 36.97274724074663510, 77.75916469768418438 ) ) ;
#18725=CARTESIAN_POINT ( 'NONE',  ( -3.566438244846301231, 38.23101125920473464, 76.53375056423675460 ) ) ;
#18726=ORIENTED_EDGE ( 'NONE', *, *, #5201, .F. ) ;
#18729=CARTESIAN_POINT ( 'NONE',  ( 9.327624742576356098, 42.74920758916827168, 78.90414333341678343 ) ) ;
#18730=CARTESIAN_POINT ( 'NONE',  ( -4.611439147851055687, 37.01374503923339176, 75.36135576041903050 ) ) ;
#18731=CARTESIAN_POINT ( 'NONE',  ( 8.873269659708348911, 41.38747658206386149, 75.97261045075327957 ) ) ;
#18734=CARTESIAN_POINT ( 'NONE',  ( 8.512798039827604413, 42.67153831990107449, 77.98843304575544266 ) ) ;
#18738=CARTESIAN_POINT ( 'NONE',  ( -7.047711364469002149, 47.14767026684477003, 78.25347377718505015 ) ) ;
#18739=DIRECTION ( 'NONE',  ( 0.3165065846432129626, 0.9485903129789426957, 0.000000000000000000 ) ) ;
#18740=ADVANCED_FACE ( 'NONE', ( #13037 ), #1738, .T. ) ;
#18742=ORIENTED_EDGE ( 'NONE', *, *, #2645, .T. ) ;
#18743=EDGE_CURVE ( 'NONE', #12999, #19292, #3019, .T. ) ;
#18744=DIRECTION ( 'NONE',  ( -0.5813877811927011807, 0.8136266022444372803, 5.636455622144619183E-17 ) ) ;
#18745=ORIENTED_EDGE ( 'NONE', *, *, #14055, .T. ) ;
#18746=VECTOR ( 'NONE', #19589, 1000.000000000000000 ) ;
#18747=CARTESIAN_POINT ( 'NONE',  ( -4.655845291449849377, 51.27794505956256188, 78.93463708245236887 ) ) ;
#18749=AXIS2_PLACEMENT_3D ( 'NONE', #1481, #3181, #184 ) ;
#18751=ORIENTED_EDGE ( 'NONE', *, *, #1259, .F. ) ;
#18753=ADVANCED_FACE ( 'NONE', ( #6209, #9633 ), #40, .T. ) ;
#18755=CARTESIAN_POINT ( 'NONE',  ( -3.218729019158923954, 51.38508014927832335, 79.24282704039583791 ) ) ;
#18756=CARTESIAN_POINT ( 'NONE',  ( 0.8496251597415627188, 52.95608624727413627, 77.71799959699670524 ) ) ;
#18757=CARTESIAN_POINT ( 'NONE',  ( 0.5868117437017631444, 52.36192644938283536, 77.38375056423674891 ) ) ;
#18758=CARTESIAN_POINT ( 'NONE',  ( -4.751859364981153355, 37.11746779715601718, 79.54765774203875139 ) ) ;
#18759=ORIENTED_EDGE ( 'NONE', *, *, #3511, .F. ) ;
#18763=CARTESIAN_POINT ( 'NONE',  ( -3.565990957808644168, 37.05209079725128873, 75.50374684392987490 ) ) ;
#18764=CARTESIAN_POINT ( 'NONE',  ( 6.862151516847506016, 50.41949500963030317, 77.39285358288198324 ) ) ;
#18765=CARTESIAN_POINT ( 'NONE',  ( -7.291302197332327317, 40.11373609668280693, 78.44772760609974682 ) ) ;
#18768=CARTESIAN_POINT ( 'NONE',  ( -4.542470680087303592, 37.71301808247110188, 77.90541956767252429 ) ) ;
#18769=CARTESIAN_POINT ( 'NONE',  ( 5.931673172199543487, 50.32702347935969556, 79.47852512212875808 ) ) ;
#18771=ORIENTED_EDGE ( 'NONE', *, *, #3499, .T. ) ;
#18772=CARTESIAN_POINT ( 'NONE',  ( 8.216412660687694824, 41.33909262012433317, 78.80099766627323277 ) ) ;
#18774=DIRECTION ( 'NONE',  ( 1.540237394707284220E-16, 1.793354297423764243E-16, -1.000000000000000000 ) ) ;
#18779=CARTESIAN_POINT ( 'NONE',  ( -4.630794176838950449, 51.29584566888366481, 79.54703672271651271 ) ) ;
#18781=AXIS2_PLACEMENT_3D ( 'NONE', #10613, #2707, #20665 ) ;
#18784=VECTOR ( 'NONE', #5186, 1000.000000000000000 ) ;
#18787=CARTESIAN_POINT ( 'NONE',  ( 0.8296073574565104858, 52.96365912811320698, 78.75172105370583608 ) ) ;
#18788=ORIENTED_EDGE ( 'NONE', *, *, #20911, .F. ) ;
#18790=DIRECTION ( 'NONE',  ( 0.3165065846431827645, 0.9485903129789529098, 0.000000000000000000 ) ) ;
#18792=CARTESIAN_POINT ( 'NONE',  ( 5.455409717288331350, 36.87153325707006957, 76.14053225265315916 ) ) ;
#18793=CARTESIAN_POINT ( 'NONE',  ( 5.739147447831700610, 51.24901287804902239, 78.93590013629759028 ) ) ;
#18794=VECTOR ( 'NONE', #18119, 1000.000000000000000 ) ;
#18795=CARTESIAN_POINT ( 'NONE',  ( 2.643026689701002407, 51.46641972551267941, 72.45432679953087529 ) ) ;
#18798=CARTESIAN_POINT ( 'NONE',  ( 0.6420704436484546695, 52.96597034637404988, 75.36071969156348871 ) ) ;
#18800=CARTESIAN_POINT ( 'NONE',  ( 6.062166292594780792, 51.01041186941530015, 75.37891144279687694 ) ) ;
#18804=ORIENTED_EDGE ( 'NONE', *, *, #20785, .T. ) ;
#18805=CARTESIAN_POINT ( 'NONE',  ( -5.256821130788762453, 49.97995522249031808, 75.81950988351437104 ) ) ;
#18807=CARTESIAN_POINT ( 'NONE',  ( 4.882729479566670250, 50.96759932735817955, 79.51138782552760631 ) ) ;
#18809=PLANE ( 'NONE',  #18337 ) ;
#18810=CARTESIAN_POINT ( 'NONE',  ( 8.415472958870040543, 40.01543082757027747, 76.00709785348774972 ) ) ;
#18812=CARTESIAN_POINT ( 'NONE',  ( 5.549717964907305401, 50.64299944696890776, 75.36188203480982395 ) ) ;
#18813=CARTESIAN_POINT ( 'NONE',  ( -6.705847964633579572, 40.30006211529013882, 78.61740305894309699 ) ) ;
#18814=CARTESIAN_POINT ( 'NONE',  ( -7.611372734017126440, 43.12018948500615778, 78.28007409364852265 ) ) ;
#18816=DIRECTION ( 'NONE',  ( 1.540237394707284220E-16, 1.793354297423764243E-16, -1.000000000000000000 ) ) ;
#18818=CARTESIAN_POINT ( 'NONE',  ( -5.048651755005553632, 50.07748435998981762, 75.61447646545406087 ) ) ;
#18820=CARTESIAN_POINT ( 'NONE',  ( -7.655444683876213574, 40.90690537883764222, 79.47793662387863378 ) ) ;
#18822=ADVANCED_FACE ( 'NONE', ( #13024 ), #19499, .F. ) ;
#18824=CARTESIAN_POINT ( 'NONE',  ( -7.610357185174691175, 43.11228522227810345, 75.86215519470648871 ) ) ;
#18826=DIRECTION ( 'NONE',  ( -1.540237394707284220E-16, -1.793354297423764243E-16, 1.000000000000000000 ) ) ;
#18827=CARTESIAN_POINT ( 'NONE',  ( -4.292896230825959059, 50.79981292070976906, 78.93513991157864496 ) ) ;
#18829=PLANE ( 'NONE',  #1037 ) ;
#18830=CARTESIAN_POINT ( 'NONE',  ( -8.093136328865547569, 42.20592732569928529, 79.45715840112796968 ) ) ;
#18831=CARTESIAN_POINT ( 'NONE',  ( 5.442040249694054310, 36.86197992501465137, 77.64535406911728899 ) ) ;
#18832=CARTESIAN_POINT ( 'NONE',  ( -4.421933507194019342, 37.62019378118617396, 78.93084429746392061 ) ) ;
#18834=CARTESIAN_POINT ( 'NONE',  ( 5.427780505986065762, 36.85179043424346190, 76.70433879953087342 ) ) ;
#18836=LINE ( 'NONE', #12358, #5692 ) ;
#18837=CARTESIAN_POINT ( 'NONE',  ( 8.326116433130623662, 42.11204170176992534, 78.13634973986094678 ) ) ;
#18839=LINE ( 'NONE', #10678, #6397 ) ;
#18840=CARTESIAN_POINT ( 'NONE',  ( 5.902048492000326441, 51.12868443877599134, 78.59183879953087626 ) ) ;
#18841=CARTESIAN_POINT ( 'NONE',  ( 8.787829143201870252, 41.13140593384865440, 77.14698585835439815 ) ) ;
#18842=ADVANCED_FACE ( 'NONE', ( #19598 ), #5020, .T. ) ;
#18844=ORIENTED_EDGE ( 'NONE', *, *, #12077, .F. ) ;
#18845=CARTESIAN_POINT ( 'NONE',  ( 5.478935120625926025, 50.68658530016113417, 77.27318761637275202 ) ) ;
#18846=ORIENTED_EDGE ( 'NONE', *, *, #16686, .T. ) ;
#18851=CARTESIAN_POINT ( 'NONE',  ( -0.9429546156000722101, 52.21950014059650158, 77.04772206183797323 ) ) ;
#18852=CARTESIAN_POINT ( 'NONE',  ( 9.012782495821852535, 41.80560540242532852, 78.13577067582016866 ) ) ;
#18853=CARTESIAN_POINT ( 'NONE',  ( 6.303853310235981056, 37.47779998508790555, 78.34126521887253602 ) ) ;
#18854=CARTESIAN_POINT ( 'NONE',  ( 0.8455663297060546091, 52.35216279802085637, 76.48963291717792856 ) ) ;
#18856=ORIENTED_EDGE ( 'NONE', *, *, #915, .F. ) ;
#18858=CARTESIAN_POINT ( 'NONE',  ( 8.319563636934814710, 41.64804018434459465, 75.98771331677210128 ) ) ;
#18860=CARTESIAN_POINT ( 'NONE',  ( 5.287666634764763174, 37.67144577404334171, 75.36130176902827316 ) ) ;
#18861=DIRECTION ( 'NONE',  ( 1.540237394707284220E-16, 1.793354297423764243E-16, -1.000000000000000000 ) ) ;
#18866=DIRECTION ( 'NONE',  ( 0.3165065846431829311, 0.9485903129789527988, 2.188653791613874255E-16 ) ) ;
#18868=CARTESIAN_POINT ( 'NONE',  ( 6.484722254825411092, 49.79139610127609927, 78.65755348986731121 ) ) ;
#18871=B_SPLINE_SURFACE_WITH_KNOTS ( 'NONE', 3, 1, ( 
 ( #17131, #11148 ),
 ( #2554, #17519 ),
 ( #2940, #9557 ),
 ( #1352, #9050 ),
 ( #15537, #7844 ),
 ( #954, #14326 ),
 ( #14216, #12634 ),
 ( #14536, #16039 ),
 ( #7946, #14429 ),
 ( #16143, #17728 ),
 ( #12832, #9661 ),
 ( #1563, #2083 ),
 ( #16662, #267 ),
 ( #6547, #14746 ),
 ( #13152, #3772 ) ),
 .UNSPECIFIED., .F., .F., .F.,
 ( 4, 1, 1, 1, 1, 1, 1, 1, 1, 1, 1, 1, 4 ),
 ( 2, 2 ),
 ( 0.000000000000000000, 0.09897586389363323411, 0.1834007553115765132, 0.2562582723958196640, 0.3272804813821422187, 0.3687296102942994591, 0.4216358900696890455, 0.4870080516106923274, 0.5645314195351998077, 0.6541098812875514312, 0.7570203673134348055, 0.8723000540617986687, 1.000000000000000000 ),
 ( 0.000000000000000000, 1.000000000000000000 ),
 .UNSPECIFIED. ) ;
#18873=LINE ( 'NONE', #4280, #5076 ) ;
#18874=EDGE_CURVE ( 'NONE', #4092, #11503, #8550, .T. ) ;
#18876=CARTESIAN_POINT ( 'NONE',  ( -5.590960105440975880, 48.67769231808699715, 72.45433879953087342 ) ) ;
#18878=CARTESIAN_POINT ( 'NONE',  ( -7.080689300340610615, 41.44950609765598415, 78.61536821129558916 ) ) ;
#18879=VERTEX_POINT ( 'NONE', #19707 ) ;
#18881=CARTESIAN_POINT ( 'NONE',  ( -4.901409867458520253, 51.10247360423972651, 79.52300236340988704 ) ) ;
#18884=CARTESIAN_POINT ( 'NONE',  ( 4.816229352426441679, 36.41479837022654920, 75.57109918664292536 ) ) ;
#18886=ORIENTED_EDGE ( 'NONE', *, *, #1451, .T. ) ;
#18887=DIRECTION ( 'NONE',  ( 0.5813877811927011807, -0.8136266022444372803, -5.636455622144619183E-17 ) ) ;
#18889=ORIENTED_EDGE ( 'NONE', *, *, #12093, .F. ) ;
#18891=CARTESIAN_POINT ( 'NONE',  ( 5.278955283585622382, 37.48279278996433561, 75.97346894869129130 ) ) ;
#18894=ADVANCED_FACE ( 'NONE', ( #5334 ), #20243, .F. ) ;
#18895=CARTESIAN_POINT ( 'NONE',  ( 5.618638386382252214, 36.98817048782158423, 75.97391373086902888 ) ) ;
#18898=CARTESIAN_POINT ( 'NONE',  ( 1.294600740468589306, 52.96082490517478902, 75.43490186719157009 ) ) ;
#18900=CARTESIAN_POINT ( 'NONE',  ( 5.750640099535992533, 51.24052371918730842, 75.36022115247205022 ) ) ;
#18901=CARTESIAN_POINT ( 'NONE',  ( 5.824017363460040286, 37.13492678543709502, 77.62670008255557264 ) ) ;
#18903=VERTEX_POINT ( 'NONE', #8873 ) ;
#18905=CARTESIAN_POINT ( 'NONE',  ( -3.321341072305123987, 36.98563450613462322, 75.66260743385902288 ) ) ;
#18907=ORIENTED_EDGE ( 'NONE', *, *, #6763, .F. ) ;
#18908=DIRECTION ( 'NONE',  ( -0.8136266022444372803, -0.5813877811927012917, -2.295812393977109100E-16 ) ) ;
#18912=CARTESIAN_POINT ( 'NONE',  ( 5.916087328049406402, 50.33910869090388474, 75.42577415430537258 ) ) ;
#18914=CARTESIAN_POINT ( 'NONE',  ( -4.454500421143473332, 37.64505674804929924, 79.54845644658969661 ) ) ;
#18916=CARTESIAN_POINT ( 'NONE',  ( 5.243485048422129147, 51.61513872599351771, 75.41617184184443090 ) ) ;
#18918=LINE ( 'NONE', #18712, #3808 ) ;
#18919=CARTESIAN_POINT ( 'NONE',  ( 8.951227662965957066, 41.62112166339042574, 78.59502675972919405 ) ) ;
#18920=CARTESIAN_POINT ( 'NONE',  ( -0.9281697048186325905, 52.21736150593820724, 78.52473566685461037 ) ) ;
#18921=AXIS2_PLACEMENT_3D ( 'NONE', #3747, #8667, #8444 ) ;
#18923=CARTESIAN_POINT ( 'NONE',  ( -1.123656915330052408, 35.37488560990637865, 76.16022115247204738 ) ) ;
#18924=CARTESIAN_POINT ( 'NONE',  ( 8.386004485381512552, 39.92711194308005673, 78.01856368782078732 ) ) ;
#18925=LINE ( 'NONE', #6255, #13999 ) ;
#18927=CARTESIAN_POINT ( 'NONE',  ( -7.235648897618376374, 46.52740783509096190, 79.45433879953087342 ) ) ;
#18928=PLANE ( 'NONE',  #5151 ) ;
#18930=CARTESIAN_POINT ( 'NONE',  ( -4.505098289471030526, 37.68399364879952174, 78.84855896664149100 ) ) ;
#18931=CARTESIAN_POINT ( 'NONE',  ( -3.532917577324399261, 36.21708460058427193, 78.46683879953087626 ) ) ;
#18932=CARTESIAN_POINT ( 'NONE',  ( 8.947997572694543322, 41.61144087793389446, 76.20405737193274831 ) ) ;
#18933=CARTESIAN_POINT ( 'NONE',  ( 0.3326973149608341562, 52.96014171822455552, 76.44919174070734869 ) ) ;
#18936=CARTESIAN_POINT ( 'NONE',  ( -4.032707575244007359, 50.98077729755701881, 78.55785450940271630 ) ) ;
#18938=CARTESIAN_POINT ( 'NONE',  ( -0.8923386585764341294, 52.84778144440528536, 78.77565085023587699 ) ) ;
#18940=FACE_OUTER_BOUND ( 'NONE', #11349, .T. ) ;
#18941=AXIS2_PLACEMENT_3D ( 'NONE', #20284, #16220, #20399 ) ;
#18944=VERTEX_POINT ( 'NONE', #3853 ) ;
#18949=CARTESIAN_POINT ( 'NONE',  ( -7.866550369700228806, 41.50330127738815378, 78.93669174070734584 ) ) ;
#18952=CARTESIAN_POINT ( 'NONE',  ( -5.160557796315992540, 37.41935686500602287, 77.33669174070733732 ) ) ;
#18953=DIRECTION ( 'NONE',  ( -1.540237394707284220E-16, -1.793354297423764243E-16, 1.000000000000000000 ) ) ;
#18957=CARTESIAN_POINT ( 'NONE',  ( -3.568428810981487231, 36.24331531840701359, 78.81697279211699936 ) ) ;
#18959=CARTESIAN_POINT ( 'NONE',  ( -3.349688636638950889, 52.21127678364309332, 76.69845644658968808 ) ) ;
#18961=EDGE_CURVE ( 'NONE', #5281, #7102, #8662, .T. ) ;
#18963=CARTESIAN_POINT ( 'NONE',  ( 4.555266191169155654, 52.12349827269967761, 77.01204236660041147 ) ) ;
#18969=ORIENTED_EDGE ( 'NONE', *, *, #3505, .T. ) ;
#18974=AXIS2_PLACEMENT_3D ( 'NONE', #3310, #9613, #6287 ) ;
#18975=ORIENTED_EDGE ( 'NONE', *, *, #16497, .T. ) ;
#18976=CARTESIAN_POINT ( 'NONE',  ( -3.384255150065147877, 52.18657681870956111, 76.19075138459079710 ) ) ;
#18978=CARTESIAN_POINT ( 'NONE',  ( 5.639000274936166512, 51.32298756049275568, 75.36146177662637058 ) ) ;
#18979=ORIENTED_EDGE ( 'NONE', *, *, #12341, .T. ) ;
#18980=CARTESIAN_POINT ( 'NONE',  ( -4.945958930583990387, 50.15069347521357912, 79.33884456587460932 ) ) ;
#18983=CARTESIAN_POINT ( 'NONE',  ( 4.958128353061608706, 36.51619420082643330, 75.49492869865662215 ) ) ;
#18985=ADVANCED_FACE ( 'NONE', ( #12276 ), #8537, .F. ) ;
#18986=ORIENTED_EDGE ( 'NONE', *, *, #9650, .T. ) ;
#18992=AXIS2_PLACEMENT_3D ( 'NONE', #8308, #14888, #208 ) ;
#18994=CARTESIAN_POINT ( 'NONE',  ( -3.847046057864463187, 36.44911865529216755, 77.75315568452884918 ) ) ;
#18995=CARTESIAN_POINT ( 'NONE',  ( 5.429213800673928780, 36.85281461415114279, 76.52220546472133833 ) ) ;
#18996=CARTESIAN_POINT ( 'NONE',  ( -3.955205046931959956, 36.52901134360648427, 77.68963291717793140 ) ) ;
#18997=VERTEX_POINT ( 'NONE', #15677 ) ;
#18998=CARTESIAN_POINT ( 'NONE',  ( 1.087740465381641375, 52.94398708878058102, 76.77198585835439815 ) ) ;
#18999=B_SPLINE_CURVE_WITH_KNOTS ( 'NONE', 3,
 ( #12577, #9496, #19067, #4477, #15983, #2893, #1508, #9393, #20850, #16085, #15878, #1294, #14585, #3410, #113, #3517, #12, #9707, #13202 ),
 .UNSPECIFIED., .F., .F.,
 ( 4, 1, 1, 1, 1, 1, 1, 1, 1, 1, 1, 1, 1, 1, 1, 1, 4 ),
 ( 0.000000000000000000, 0.09548257688036490554, 0.1831260162920692325, 0.2638843215906733763, 0.3377405854367836469, 0.4051287172156797234, 0.4664893278449969150, 0.5228337310946251648, 0.5750047063118850499, 0.6251976803793458659, 0.6747285784134858799, 0.7246222549260739054, 0.7756163566473811555, 0.8279184090424840381, 0.8823814665238148836, 0.9394578349448057253, 1.000000000000000000 ),
 .UNSPECIFIED. ) ;
#19001=CARTESIAN_POINT ( 'NONE',  ( 6.817737414320570899, 50.45230191805777054, 75.81347835631012799 ) ) ;
#19003=CARTESIAN_POINT ( 'NONE',  ( 5.278470088661848969, 37.49201410884710128, 77.76022115247205591 ) ) ;
#19005=CARTESIAN_POINT ( 'NONE',  ( 8.162892682119435861, 41.62284976526770208, 79.54845644658969661 ) ) ;
#19006=VERTEX_POINT ( 'NONE', #10794 ) ;
#19008=ORIENTED_EDGE ( 'NONE', *, *, #4760, .T. ) ;
#19009=CARTESIAN_POINT ( 'NONE',  ( -7.948598133434920499, 41.77757099202272428, 78.60633299199227508 ) ) ;
#19010=EDGE_CURVE ( 'NONE', #16704, #15408, #2482, .T. ) ;
#19011=CARTESIAN_POINT ( 'NONE',  ( 6.635267586053948285, 39.64667042487232607, 72.45433879953087342 ) ) ;
#19013=CARTESIAN_POINT ( 'NONE',  ( 4.989364768915854675, 51.80284713987553857, 79.39429067157672648 ) ) ;
#19014=CARTESIAN_POINT ( 'NONE',  ( -6.710423945119504019, 40.29826376337096150, 78.59662358701670826 ) ) ;
#19019=CARTESIAN_POINT ( 'NONE',  ( -7.687459971419651872, 40.91832003046048527, 79.47750830342025097 ) ) ;
#19023=VECTOR ( 'NONE', #4712, 1000.000000000000000 ) ;
#19024=CARTESIAN_POINT ( 'NONE',  ( 5.639000274936166512, 51.32298756049275568, 75.36146177662637058 ) ) ;
#19025=CARTESIAN_POINT ( 'NONE',  ( 7.860711257786343609, 47.82081138319720282, 79.44551527011911674 ) ) ;
#19026=AXIS2_PLACEMENT_3D ( 'NONE', #587, #5687, #2515 ) ;
#19027=AXIS2_PLACEMENT_3D ( 'NONE', #14738, #11764, #5463 ) ;
#19029=B_SPLINE_CURVE_WITH_KNOTS ( 'NONE', 3,
 ( #506, #8393, #18276, #10214, #18178, #11495, #3805, #6983 ),
 .UNSPECIFIED., .F., .F.,
 ( 4, 2, 2, 4 ),
 ( 0.000000000000000000, 0.0002641548125319239651, 0.0003962322187978856223, 0.0005283096250638472796 ),
 .UNSPECIFIED. ) ;
#19030=CARTESIAN_POINT ( 'NONE',  ( 8.375262368375963717, 41.81499272476909113, 78.48252796260671005 ) ) ;
#19031=CARTESIAN_POINT ( 'NONE',  ( -0.9406373985668743387, 52.21745981828536998, 78.20877650441246942 ) ) ;
#19033=EDGE_LOOP ( 'NONE', ( #1448, #7809, #3122, #3799 ) ) ;
#19035=VECTOR ( 'NONE', #10753, 1000.000000000000114 ) ;
#19037=CARTESIAN_POINT ( 'NONE',  ( 5.740585635973905809, 51.24795054640212300, 75.97198585835440099 ) ) ;
#19038=SURFACE_STYLE_FILL_AREA ( #15954 ) ;
#19041=CARTESIAN_POINT ( 'NONE',  ( 5.376021338371314684, 37.56172066031027867, 75.98270377909689444 ) ) ;
#19042=EDGE_CURVE ( 'NONE', #1372, #12487, #4371, .T. ) ;
#19043=AXIS2_PLACEMENT_3D ( 'NONE', #5394, #3910, #14993 ) ;
#19045=VECTOR ( 'NONE', #16104, 1000.000000000000000 ) ;
#19047=CARTESIAN_POINT ( 'NONE',  ( -3.635499589166287127, 36.29285780047638355, 79.01720576857120193 ) ) ;
#19050=B_SPLINE_SURFACE_WITH_KNOTS ( 'NONE', 3, 1, ( 
 ( #18294, #5630 ),
 ( #18513, #18405 ),
 ( #20092, #10234 ),
 ( #12137, #13725 ),
 ( #16711, #849 ),
 ( #5305, #2135 ),
 ( #15331, #20198 ),
 ( #3825, #13506 ),
 ( #11722, #16817 ),
 ( #8731, #18615 ),
 ( #4030, #524 ) ),
 .UNSPECIFIED., .F., .F., .F.,
 ( 4, 1, 1, 1, 1, 1, 1, 1, 4 ),
 ( 2, 2 ),
 ( 0.000000000000000000, 0.1975140844462248968, 0.3638949407180063211, 0.4989527813026914393, 0.6061909113956662765, 0.6984313814761610173, 0.7906255499708312318, 0.8898677993983585832, 1.000000000000000000 ),
 ( 0.000000000000000000, 1.000000000000000000 ),
 .UNSPECIFIED. ) ;
#19055=ORIENTED_EDGE ( 'NONE', *, *, #6503, .T. ) ;
#19057=( GEOMETRIC_REPRESENTATION_CONTEXT ( 3 ) GLOBAL_UNCERTAINTY_ASSIGNED_CONTEXT ( ( #1679 ) ) GLOBAL_UNIT_ASSIGNED_CONTEXT ( ( #18708, #2540, #4640 ) ) REPRESENTATION_CONTEXT ( 'NONE', 'WORKASPACE' ) );
#19058=EDGE_CURVE ( 'NONE', #18554, #3669, #1200, .T. ) ;
#19059=CARTESIAN_POINT ( 'NONE',  ( 0.6956764376626823898, 52.36037053019133225, 78.90962006023684694 ) ) ;
#19060=CARTESIAN_POINT ( 'NONE',  ( 5.389492195292208798, 36.82443100924615464, 78.09625056423675460 ) ) ;
#19061=ORIENTED_EDGE ( 'NONE', *, *, #17628, .T. ) ;
#19064=ORIENTED_EDGE ( 'NONE', *, *, #11523, .T. ) ;
#19065=FACE_OUTER_BOUND ( 'NONE', #16982, .T. ) ;
#19067=CARTESIAN_POINT ( 'NONE',  ( 5.603594163910166515, 51.34914062846251426, 79.54621928524807117 ) ) ;
#19069=CARTESIAN_POINT ( 'NONE',  ( 0.5940733232197880076, 52.96558880458736240, 75.97241503363285631 ) ) ;
#19070=CARTESIAN_POINT ( 'NONE',  ( -4.036259049554215217, 37.50289767551729625, 79.53329352641277694 ) ) ;
#19072=CARTESIAN_POINT ( 'NONE',  ( -5.462576778579502523, 43.73439565840071452, 82.45433879953087342 ) ) ;
#19073=CARTESIAN_POINT ( 'NONE',  ( 5.801534520520057470, 37.11886136902160160, 77.67950998295866327 ) ) ;
#19076=ADVANCED_FACE ( 'NONE', ( #16295 ), #4676, .F. ) ;
#19078=DIRECTION ( 'NONE',  ( -1.540237394707284220E-16, -1.793354297423764243E-16, 1.000000000000000000 ) ) ;
#19079=CARTESIAN_POINT ( 'NONE',  ( -4.650819492866522964, 37.79909575829982060, 77.90150431758111438 ) ) ;
#19080=CARTESIAN_POINT ( 'NONE',  ( -7.339959452894645686, 41.85620932255213233, 78.89026057757155286 ) ) ;
#19081=VECTOR ( 'NONE', #18744, 1000.000000000000227 ) ;
#19082=VERTEX_POINT ( 'NONE', #3304 ) ;
#19083=CARTESIAN_POINT ( 'NONE',  ( 8.217904656458664192, 41.33102757626289758, 76.21346532620796665 ) ) ;
#19085=VERTEX_POINT ( 'NONE', #12686 ) ;
#19086=CARTESIAN_POINT ( 'NONE',  ( -3.623336461783060791, 52.01573806668144329, 75.70044805065693083 ) ) ;
#19089=CARTESIAN_POINT ( 'NONE',  ( -7.803183483682971655, 41.28366174159560842, 78.36017682096837689 ) ) ;
#19090=EDGE_LOOP ( 'NONE', ( #6750, #8587, #11851, #19529 ) ) ;
#19092=CARTESIAN_POINT ( 'NONE',  ( 4.394792124162911762, 36.11365475671116343, 76.60595702694484999 ) ) ;
#19093=CARTESIAN_POINT ( 'NONE',  ( 5.653389158101303380, 51.31235907211823388, 75.98863418974025308 ) ) ;
#19096=CARTESIAN_POINT ( 'NONE',  ( 0.8388742597782140598, 52.96358605518274487, 78.70464370717459701 ) ) ;
#19101=VECTOR ( 'NONE', #14529, 1000.000000000000000 ) ;
#19103=CARTESIAN_POINT ( 'NONE',  ( 5.644533139590786064, 37.00667393039697828, 75.97264893529829521 ) ) ;
#19104=CARTESIAN_POINT ( 'NONE',  ( 5.605329808110463219, 51.34785857800776654, 78.76051003739772227 ) ) ;
#19107=CARTESIAN_POINT ( 'NONE',  ( -7.154050613567645378, 47.04591530683940448, 77.81003234944267888 ) ) ;
#19108=VERTEX_POINT ( 'NONE', #7786 ) ;
#19111=FACE_OUTER_BOUND ( 'NONE', #20943, .T. ) ;
#19113=VECTOR ( 'NONE', #9692, 1000.000000000000000 ) ;
#19114=CARTESIAN_POINT ( 'NONE',  ( 8.140610423635045834, 41.55606842302987047, 79.54734031390459847 ) ) ;
#19115=ORIENTED_EDGE ( 'NONE', *, *, #10386, .F. ) ;
#19116=ORIENTED_EDGE ( 'NONE', *, *, #19255, .F. ) ;
#19118=DIRECTION ( 'NONE',  ( -0.8136266022444382795, -0.5813877811926999595, -2.295812393977108607E-16 ) ) ;
#19119=CARTESIAN_POINT ( 'NONE',  ( -5.044784019589553026, 50.18482011045266944, 75.55565227853020360 ) ) ;
#19120=EDGE_LOOP ( 'NONE', ( #2683, #11074, #10898, #10132 ) ) ;
#19121=CARTESIAN_POINT ( 'NONE',  ( 5.603594163910166515, 51.34914062846251426, 79.54621928524807117 ) ) ;
#19122=CARTESIAN_POINT ( 'NONE',  ( 8.850663652843866913, 41.31972494539268581, 77.52203278780699236 ) ) ;
#19123=CARTESIAN_POINT ( 'NONE',  ( 8.475713225669114337, 40.19597472873837063, 75.74322883085581282 ) ) ;
#19125=CARTESIAN_POINT ( 'NONE',  ( -5.130197398460194513, 37.39693086210137807, 77.90166954077812989 ) ) ;
#19126=CARTESIAN_POINT ( 'NONE',  ( -7.449024937915255329, 40.16431357463694241, 78.92129748799239053 ) ) ;
#19127=CARTESIAN_POINT ( 'NONE',  ( 6.127653894365867160, 38.17679652135131363, 75.57100681021411503 ) ) ;
#19129=EDGE_CURVE ( 'NONE', #19214, #4579, #12990, .T. ) ;
#19130=CIRCLE ( 'NONE', #4175, 4.200000000000003730 ) ;
#19131=CIRCLE ( 'NONE', #11949, 8.199999999999995737 ) ;
#19133=CARTESIAN_POINT ( 'NONE',  ( 6.448515921954562913, 38.49488593426744387, 77.41134261343162848 ) ) ;
#19135=EDGE_CURVE ( 'NONE', #14974, #9657, #14482, .T. ) ;
#19138=VERTEX_POINT ( 'NONE', #19473 ) ;
#19139=DIRECTION ( 'NONE',  ( 1.540237394707284220E-16, 1.793354297423764243E-16, -1.000000000000000000 ) ) ;
#19140=CARTESIAN_POINT ( 'NONE',  ( 9.353817388681445522, 42.82770861117572281, 77.06316232894263862 ) ) ;
#19141=CARTESIAN_POINT ( 'NONE',  ( 5.561379608955574483, 51.38032281970146897, 76.39036821129558064 ) ) ;
#19146=CARTESIAN_POINT ( 'NONE',  ( -4.537099264183359182, 37.70896829297682729, 78.53742703482498655 ) ) ;
#19149=CARTESIAN_POINT ( 'NONE',  ( 5.647726803872021861, 51.31654162509386907, 77.98642840401727483 ) ) ;
#19150=CARTESIAN_POINT ( 'NONE',  ( 6.519924314245371555, 49.74745151145329203, 76.63889762306028786 ) ) ;
#19152=CARTESIAN_POINT ( 'NONE',  ( 6.946924939155297629, 50.35687629745329019, 76.28194508213313441 ) ) ;
#19153=VECTOR ( 'NONE', #12767, 1000.000000000000114 ) ;
#19155=CARTESIAN_POINT ( 'NONE',  ( -5.747619332630494959, 37.85299557360038136, 79.28390783734228364 ) ) ;
#19156=CARTESIAN_POINT ( 'NONE',  ( -5.484081776600456593, 50.68611759094706315, 79.26884812577799266 ) ) ;
#19157=CARTESIAN_POINT ( 'NONE',  ( 5.290600780953200299, 50.83315677396375776, 78.89498996766396033 ) ) ;
#19161=LINE ( 'NONE', #288, #15755 ) ;
#19162=CARTESIAN_POINT ( 'NONE',  ( -0.8928399825707434845, 52.97829838868407393, 76.13122899883298089 ) ) ;
#19163=LINE ( 'NONE', #2679, #2348 ) ;
#19167=CARTESIAN_POINT ( 'NONE',  ( 8.882424425600639495, 41.41491399621057923, 75.97389479739716478 ) ) ;
#19168=EDGE_LOOP ( 'NONE', ( #4798, #7635, #12756, #3423 ) ) ;
#19171=CARTESIAN_POINT ( 'NONE',  ( 0.4001462726638131961, 52.36130254314756627, 76.02501926799072862 ) ) ;
#19172=CARTESIAN_POINT ( 'NONE',  ( 5.840776426723270021, 37.14690219845653019, 76.14207271482608519 ) ) ;
#19173=LINE ( 'NONE', #6084, #5512 ) ;
#19175=CARTESIAN_POINT ( 'NONE',  ( 8.299662904660788598, 41.56403757284476796, 75.97198585835440099 ) ) ;
#19177=CARTESIAN_POINT ( 'NONE',  ( -3.396200966244447450, 52.17804077583208766, 76.13050287850805375 ) ) ;
#19179=CARTESIAN_POINT ( 'NONE',  ( 4.611425380024144260, 52.08201574212262130, 75.94315254166910734 ) ) ;
#19180=ORIENTED_EDGE ( 'NONE', *, *, #12314, .T. ) ;
#19182=CARTESIAN_POINT ( 'NONE',  ( -5.819820656548302829, 50.44621087952127425, 78.57924047249254329 ) ) ;
#19185=CARTESIAN_POINT ( 'NONE',  ( 6.870794506624137377, 37.88291540698485704, 77.55645576794258034 ) ) ;
#19186=CARTESIAN_POINT ( 'NONE',  ( -4.052506615097486886, 50.96215335582491690, 78.79092181577959764 ) ) ;
#19188=ORIENTED_EDGE ( 'NONE', *, *, #7748, .T. ) ;
#19189=DIRECTION ( 'NONE',  ( -0.5813877811927011807, 0.8136266022444372803, 5.636455622144619183E-17 ) ) ;
#19191=VERTEX_POINT ( 'NONE', #19264 ) ;
#19192=CARTESIAN_POINT ( 'NONE',  ( 4.453501277845357542, 51.28465290960308920, 77.76130678786321937 ) ) ;
#19193=FACE_OUTER_BOUND ( 'NONE', #17673, .T. ) ;
#19196=CARTESIAN_POINT ( 'NONE',  ( 8.789147962602239517, 47.20595287382010241, 75.43669174070734584 ) ) ;
#19197=LINE ( 'NONE', #4612, #5080 ) ;
#19198=CARTESIAN_POINT ( 'NONE',  ( -3.579922675594004122, 36.25180537319517526, 77.38751485876633751 ) ) ;
#19200=CARTESIAN_POINT ( 'NONE',  ( 2.115822401559540378, 52.95418708249595596, 78.45122513788126639 ) ) ;
#19201=CARTESIAN_POINT ( 'NONE',  ( -3.899559394394521483, 36.48790814162069296, 77.72081520951157074 ) ) ;
#19205=CARTESIAN_POINT ( 'NONE',  ( 8.530649028577993676, 48.02340768410154936, 78.56977997600147035 ) ) ;
#19206=CARTESIAN_POINT ( 'NONE',  ( -2.955076890380592847, 51.58841534450542099, 76.19553520931087576 ) ) ;
#19209=EDGE_LOOP ( 'NONE', ( #1741, #18889, #3307, #12400 ) ) ;
#19210=EDGE_CURVE ( 'NONE', #3254, #11401, #1615, .T. ) ;
#19211=CARTESIAN_POINT ( 'NONE',  ( -3.492483110108918876, 37.11205023543848114, 75.53057231289058393 ) ) ;
#19212=DIRECTION ( 'NONE',  ( 1.540237394707283727E-16, 1.793354297423763257E-16, -1.000000000000000000 ) ) ;
#19214=VERTEX_POINT ( 'NONE', #9710 ) ;
#19215=CARTESIAN_POINT ( 'NONE',  ( -4.175129846843772974, 37.46622205296527142, 77.09144163344554102 ) ) ;
#19219=CARTESIAN_POINT ( 'NONE',  ( -7.775370309202131125, 41.23112419541227069, 78.65672026662821281 ) ) ;
#19220=CARTESIAN_POINT ( 'NONE',  ( -7.872343237160707830, 41.50297897882735043, 79.54775079867083321 ) ) ;
#19221=CARTESIAN_POINT ( 'NONE',  ( 5.475233562466685022, 37.62638353493751708, 75.36365925760465245 ) ) ;
#19223=EDGE_CURVE ( 'NONE', #20830, #11304, #10980, .T. ) ;
#19225=ADVANCED_FACE ( 'NONE', ( #11411 ), #8206, .T. ) ;
#19226=CARTESIAN_POINT ( 'NONE',  ( 0.8503282811412335995, 52.95606000782370870, 76.48963291717792856 ) ) ;
#19228=CARTESIAN_POINT ( 'NONE',  ( -0.8886661993129779669, 52.97949073723408731, 78.78847851419276083 ) ) ;
#19230=CARTESIAN_POINT ( 'NONE',  ( 0.5221537403065005245, 44.16218137147968292, 82.45433879953087342 ) ) ;
#19233=CARTESIAN_POINT ( 'NONE',  ( 5.581171587375775900, 51.36570328251199413, 76.09992453055346573 ) ) ;
#19234=CARTESIAN_POINT ( 'NONE',  ( 6.341737852742077131, 49.88988861453574941, 77.88538524077617353 ) ) ;
#19236=EDGE_CURVE ( 'NONE', #13342, #12496, #2028, .T. ) ;
#19237=VERTEX_POINT ( 'NONE', #11726 ) ;
#19238=EDGE_CURVE ( 'NONE', #4532, #13937, #11692, .T. ) ;
#19239=VERTEX_POINT ( 'NONE', #317 ) ;
#19240=CARTESIAN_POINT ( 'NONE',  ( 8.530649028577993676, 48.02340768410154936, 78.56977997600147035 ) ) ;
#19241=CARTESIAN_POINT ( 'NONE',  ( -4.032470478286651172, 50.98093479776591863, 76.41531757229334687 ) ) ;
#19243=CARTESIAN_POINT ( 'NONE',  ( 5.250115436669491764, 37.46233028808841681, 77.75922307965579705 ) ) ;
#19245=FACE_OUTER_BOUND ( 'NONE', #7383, .T. ) ;
#19246=CARTESIAN_POINT ( 'NONE',  ( 6.960009239587057195, 50.34721145179211987, 76.80946857459053945 ) ) ;
#19250=CARTESIAN_POINT ( 'NONE',  ( -5.324466712459397399, 37.54042977870726361, 79.49842882144521639 ) ) ;
#19252=CARTESIAN_POINT ( 'NONE',  ( -3.258387175647450729, 36.88553430894260998, 77.52493936945022313 ) ) ;
#19254=CARTESIAN_POINT ( 'NONE',  ( 5.076572431691916520, 37.34329067111212197, 76.96022115247204454 ) ) ;
#19255=EDGE_CURVE ( 'NONE', #9748, #13579, #637, .T. ) ;
#19256=LINE ( 'NONE', #13311, #1333 ) ;
#19258=CARTESIAN_POINT ( 'NONE',  ( 6.442019222303663639, 38.49630386955294625, 76.41040896618429201 ) ) ;
#19260=CARTESIAN_POINT ( 'NONE',  ( 8.911238338503892464, 41.50127112110217809, 78.09303657357962436 ) ) ;
#19261=CARTESIAN_POINT ( 'NONE',  ( 5.679435644259863913, 37.95138956464963087, 78.36972961004526894 ) ) ;
#19263=EDGE_CURVE ( 'NONE', #6443, #8901, #10128, .T. ) ;
#19264=CARTESIAN_POINT ( 'NONE',  ( 8.124283007755586539, 44.40224511508533567, 72.45433879953087342 ) ) ;
#19265=ORIENTED_EDGE ( 'NONE', *, *, #20113, .F. ) ;
#19267=ORIENTED_EDGE ( 'NONE', *, *, #19907, .F. ) ;
#19269=CARTESIAN_POINT ( 'NONE',  ( -6.907938484555407044, 47.63351044088310005, 78.83514460925654532 ) ) ;
#19271=CARTESIAN_POINT ( 'NONE',  ( -7.631668735006648774, 47.47423462861603127, 78.95249617671795761 ) ) ;
#19272=CARTESIAN_POINT ( 'NONE',  ( -5.486992102393413617, 39.49954625374182626, 72.45433879953085921 ) ) ;
#19273=DIRECTION ( 'NONE',  ( -0.5941461771851692664, -0.8043570849667761591, -2.357623395011396791E-16 ) ) ;
#19274=EDGE_CURVE ( 'NONE', #13986, #2342, #16608, .T. ) ;
#19277=CARTESIAN_POINT ( 'NONE',  ( 8.230676153864024513, 41.36595300535771713, 76.07212865946658553 ) ) ;
#19278=ORIENTED_EDGE ( 'NONE', *, *, #11326, .T. ) ;
#19279=CARTESIAN_POINT ( 'NONE',  ( -3.653968934160817916, 51.07407364116832582, 75.42336258079946276 ) ) ;
#19281=CARTESIAN_POINT ( 'NONE',  ( 4.100190290135135029, 51.54036911970691648, 75.45433879953088763 ) ) ;
#19283=CARTESIAN_POINT ( 'NONE',  ( 2.064441844012933736, 52.21584861674933364, 77.34591136093878561 ) ) ;
#19286=CARTESIAN_POINT ( 'NONE',  ( -4.559776018715442802, 36.97558356685869541, 78.86760481232144571 ) ) ;
#19287=CARTESIAN_POINT ( 'NONE',  ( -4.541431855014749885, 51.35970071229581180, 78.93463757479271692 ) ) ;
#19288=CARTESIAN_POINT ( 'NONE',  ( 5.074465183246152478, 37.34623967253333632, 77.43080938776617472 ) ) ;
#19289=ORIENTED_EDGE ( 'NONE', *, *, #19409, .T. ) ;
#19291=CARTESIAN_POINT ( 'NONE',  ( 0.3478318340824160249, 52.36035231526901157, 77.07067603543953282 ) ) ;
#19292=VERTEX_POINT ( 'NONE', #19889 ) ;
#19293=CARTESIAN_POINT ( 'NONE',  ( 4.401043237957516396, 51.32340155052948916, 77.79664654212120922 ) ) ;
#19295=CARTESIAN_POINT ( 'NONE',  ( -5.835808111729286374, 50.43478682938704338, 76.54939005541714891 ) ) ;
#19299=AXIS2_PLACEMENT_3D ( 'NONE', #10178, #11464, #11360 ) ;
#19300=CARTESIAN_POINT ( 'NONE',  ( -3.673304938980983092, 36.32078308949211021, 77.52205638859560111 ) ) ;
#19301=VERTEX_POINT ( 'NONE', #15121 ) ;
#19302=CARTESIAN_POINT ( 'NONE',  ( -7.150937614292242728, 47.05418374649208602, 77.98057391402217320 ) ) ;
#19303=ORIENTED_EDGE ( 'NONE', *, *, #5316, .T. ) ;
#19306=CARTESIAN_POINT ( 'NONE',  ( 8.239900386529042109, 41.85364674066097024, 75.36311794487049553 ) ) ;
#19307=CARTESIAN_POINT ( 'NONE',  ( -3.382060968773085374, 51.37355338276771022, 75.56522039652081446 ) ) ;
#19309=CARTESIAN_POINT ( 'NONE',  ( 0.5753667321910650445, 52.96202048236657589, 75.97198585835440099 ) ) ;
#19311=CARTESIAN_POINT ( 'NONE',  ( -3.430514640876221044, 37.06627662345849217, 75.57130654555172100 ) ) ;
#19312=DIRECTION ( 'NONE',  ( -0.5813877811926999595, 0.8136266022444382795, 5.636455622144657394E-17 ) ) ;
#19314=ORIENTED_EDGE ( 'NONE', *, *, #14942, .T. ) ;
#19315=CARTESIAN_POINT ( 'NONE',  ( -4.648332322150092288, 37.81575765971563641, 77.33253961758860839 ) ) ;
#19316=CARTESIAN_POINT ( 'NONE',  ( 8.797519961583052606, 41.16044993131110630, 77.39661844205990349 ) ) ;
#19318=AXIS2_PLACEMENT_3D ( 'NONE', #15576, #18866, #2691 ) ;
#19319=ORIENTED_EDGE ( 'NONE', *, *, #3759, .F. ) ;
#19321=DIRECTION ( 'NONE',  ( -0.3165065846431826535, -0.9485903129789529098, -2.188653791613874008E-16 ) ) ;
#19322=CARTESIAN_POINT ( 'NONE',  ( -5.927888611570137911, 47.57933715648534445, 78.32492703482499508 ) ) ;
#19324=EDGE_CURVE ( 'NONE', #13636, #20991, #19803, .T. ) ;
#19326=CARTESIAN_POINT ( 'NONE',  ( 0.3837416960959899037, 52.96765485758538006, 77.02254451525793399 ) ) ;
#19327=PLANE ( 'NONE',  #3703 ) ;
#19328=VECTOR ( 'NONE', #15802, 1000.000000000000000 ) ;
#19330=ORIENTED_EDGE ( 'NONE', *, *, #3983, .F. ) ;
#19333=CARTESIAN_POINT ( 'NONE',  ( 8.496565932950701949, 40.25847161533236829, 79.21682452846883393 ) ) ;
#19334=CARTESIAN_POINT ( 'NONE',  ( 1.424503621124223907, 52.91627723061543520, 79.43677396536959634 ) ) ;
#19335=ORIENTED_EDGE ( 'NONE', *, *, #18102, .T. ) ;
#19336=VECTOR ( 'NONE', #4519, 1000.000000000000000 ) ;
#19338=EDGE_LOOP ( 'NONE', ( #2909, #5802, #13118, #12178 ) ) ;
#19340=CARTESIAN_POINT ( 'NONE',  ( -3.508281668750850013, 47.93162672320032414, 78.65179900065425045 ) ) ;
#19342=CARTESIAN_POINT ( 'NONE',  ( 5.217094560277743653, 37.43916672944678936, 77.75463208902168333 ) ) ;
#19343=CARTESIAN_POINT ( 'NONE',  ( 4.178949506638397260, 51.50167206575788015, 78.81223402306018500 ) ) ;
#19348=PLANE ( 'NONE',  #4981 ) ;
#19349=CARTESIAN_POINT ( 'NONE',  ( 6.344124029066668058, 49.87730810044735108, 77.50555814853646552 ) ) ;
#19350=CARTESIAN_POINT ( 'NONE',  ( 4.175402538145164044, 51.50343628508133520, 78.12271961989166869 ) ) ;
#19353=VECTOR ( 'NONE', #11025, 1000.000000000000000 ) ;
#19354=ORIENTED_EDGE ( 'NONE', *, *, #9776, .T. ) ;
#19356=CARTESIAN_POINT ( 'NONE',  ( 5.497743849324332466, 37.64424434608246628, 76.58742703482498371 ) ) ;
#19358=CARTESIAN_POINT ( 'NONE',  ( 5.262496838921983056, 50.85316300622503860, 78.84209982136016492 ) ) ;
#19359=VECTOR ( 'NONE', #16510, 1000.000000000000114 ) ;
#19361=DIRECTION ( 'NONE',  ( -0.9534635866061452747, -0.3015081906286225522, -2.009271279954815797E-16 ) ) ;
#19362=CARTESIAN_POINT ( 'NONE',  ( 8.390845173051939554, 39.94161979111582639, 76.38443001783366526 ) ) ;
#19363=ORIENTED_EDGE ( 'NONE', *, *, #9256, .T. ) ;
#19364=CARTESIAN_POINT ( 'NONE',  ( 6.582016959483238949, 37.67656554461878926, 75.62429547252081363 ) ) ;
#19366=CARTESIAN_POINT ( 'NONE',  ( 5.561379608955574483, 51.38032281970146897, 76.90580938776616904 ) ) ;
#19367=LINE ( 'NONE', #11307, #15865 ) ;
#19368=FACE_OUTER_BOUND ( 'NONE', #1127, .T. ) ;
#19371=CARTESIAN_POINT ( 'NONE',  ( 8.936058775400656629, 41.57565954506093675, 76.08336210994360727 ) ) ;
#19377=CARTESIAN_POINT ( 'NONE',  ( 0.3802186396914607469, 52.36096666664144550, 76.04253254076220969 ) ) ;
#19378=CARTESIAN_POINT ( 'NONE',  ( 0.8377421044266871730, 51.35991668224300355, 76.48963291717792856 ) ) ;
#19379=EDGE_CURVE ( 'NONE', #14271, #5223, #4051, .T. ) ;
#19380=CARTESIAN_POINT ( 'NONE',  ( -7.889981766995627588, 41.56529470657834935, 78.93438826577718714 ) ) ;
#19384=DIRECTION ( 'NONE',  ( -0.3165065846431827645, -0.9485903129789529098, 0.000000000000000000 ) ) ;
#19385=EDGE_CURVE ( 'NONE', #2251, #12080, #7557, .T. ) ;
#19389=CARTESIAN_POINT ( 'NONE',  ( -3.944959226007136888, 38.51060946023304865, 77.05433879953086773 ) ) ;
#19391=CARTESIAN_POINT ( 'NONE',  ( 1.765050448036873831, 52.26768315785694341, 76.95678149889430131 ) ) ;
#19392=CARTESIAN_POINT ( 'NONE',  ( -5.522333806888468644, 37.68658623078928116, 79.43312132436682305 ) ) ;
#19394=CARTESIAN_POINT ( 'NONE',  ( 5.292744349709337826, 50.82411692241547740, 75.98863418974025308 ) ) ;
#19395=CARTESIAN_POINT ( 'NONE',  ( 5.430298293217690642, 36.85358955281711246, 77.55899030588862786 ) ) ;
#19398=CARTESIAN_POINT ( 'NONE',  ( 9.273778039597953438, 45.67340037358405169, 78.74919174070734584 ) ) ;
#19400=FACE_OUTER_BOUND ( 'NONE', #17570, .T. ) ;
#19402=CARTESIAN_POINT ( 'NONE',  ( -5.374794079232331434, 49.84443499592996574, 76.21531548689122815 ) ) ;
#19406=CARTESIAN_POINT ( 'NONE',  ( 6.545534159973747990, 50.65336749702785113, 77.68963291717794561 ) ) ;
#19407=CARTESIAN_POINT ( 'NONE',  ( 5.573315379359557120, 50.61687040490333089, 76.21496574784163158 ) ) ;
#19408=ORIENTED_EDGE ( 'NONE', *, *, #6387, .F. ) ;
#19409=EDGE_CURVE ( 'NONE', #2631, #6196, #7232, .T. ) ;
#19410=CARTESIAN_POINT ( 'NONE',  ( 1.934299931914925441, 52.20294349804878919, 79.09265199143256098 ) ) ;
#19411=CARTESIAN_POINT ( 'NONE',  ( -3.499411194686691040, 37.10634979067736339, 77.70026928173652436 ) ) ;
#19416=CARTESIAN_POINT ( 'NONE',  ( 7.975192330168971111, 41.06029990298387844, 79.49103220525971381 ) ) ;
#19419=FACE_OUTER_BOUND ( 'NONE', #15265, .T. ) ;
#19421=VECTOR ( 'NONE', #17229, 1000.000000000000000 ) ;
#19422=CARTESIAN_POINT ( 'NONE',  ( -1.117719678584871090, 36.12782917792895176, 76.86610350541323555 ) ) ;
#19423=PLANE ( 'NONE',  #4717 ) ;
#19425=AXIS2_PLACEMENT_3D ( 'NONE', #20920, #6669, #14659 ) ;
#19426=ORIENTED_EDGE ( 'NONE', *, *, #9501, .T. ) ;
#19427=CARTESIAN_POINT ( 'NONE',  ( -4.900087432442492563, 37.22695789959892920, 77.32461911834714385 ) ) ;
#19428=CARTESIAN_POINT ( 'NONE',  ( 8.211361072458180033, 41.32375023436543415, 77.14698585835439815 ) ) ;
#19430=ORIENTED_EDGE ( 'NONE', *, *, #13438, .T. ) ;
#19431=CARTESIAN_POINT ( 'NONE',  ( -4.804644443005473775, 51.17161863374556674, 76.44036821129557779 ) ) ;
#19432=CARTESIAN_POINT ( 'NONE',  ( -1.483269432489140005, 51.49895708687498086, 72.45432679953087529 ) ) ;
#19434=CARTESIAN_POINT ( 'NONE',  ( -5.387797286270752828, 50.75491896253648605, 75.54244301425877950 ) ) ;
#19435=CARTESIAN_POINT ( 'NONE',  ( -4.514796398449106185, 37.69153629922272586, 76.06698014943201258 ) ) ;
#19436=AXIS2_PLACEMENT_3D ( 'NONE', #19845, #3888, #15288 ) ;
#19437=CARTESIAN_POINT ( 'NONE',  ( -7.367656984315425817, 48.05973018190410073, 78.78375056423675460 ) ) ;
#19438=LINE ( 'NONE', #1369, #15283 ) ;
#19440=CARTESIAN_POINT ( 'NONE',  ( 8.385768451058924100, 39.92640453324153071, 77.75090705316073070 ) ) ;
#19442=CARTESIAN_POINT ( 'NONE',  ( 5.561379608955574483, 51.38032281970146897, 76.90580938776616904 ) ) ;
#19443=CARTESIAN_POINT ( 'NONE',  ( 8.561605920521204283, 42.81781863465402438, 75.72637824826109920 ) ) ;
#19444=CARTESIAN_POINT ( 'NONE',  ( 0.8431461159794668703, 52.35589634692465211, 76.25677998097611976 ) ) ;
#19445=ORIENTED_EDGE ( 'NONE', *, *, #18627, .T. ) ;
#19447=EDGE_CURVE ( 'NONE', #16624, #4579, #15438, .T. ) ;
#19449=AXIS2_PLACEMENT_3D ( 'NONE', #10418, #16786, #8918 ) ;
#19450=CARTESIAN_POINT ( 'NONE',  ( 7.705497127814430414, 40.20743238930150198, 76.12097142257781002 ) ) ;
#19452=CARTESIAN_POINT ( 'NONE',  ( 0.5221537403065013017, 44.16218137147968292, 76.86610350541323555 ) ) ;
#19455=CARTESIAN_POINT ( 'NONE',  ( 5.848951923618479931, 37.15274410921379911, 76.58742703482498371 ) ) ;
#19456=PLANE ( 'NONE',  #9764 ) ;
#19458=LINE ( 'NONE', #10010, #275 ) ;
#19459=EDGE_CURVE ( 'NONE', #19585, #11503, #8844, .T. ) ;
#19462=DIRECTION ( 'NONE',  ( 1.540237394707284220E-16, 1.793354297423764243E-16, -1.000000000000000000 ) ) ;
#19463=VECTOR ( 'NONE', #14813, 1000.000000000000114 ) ;
#19464=CARTESIAN_POINT ( 'NONE',  ( 8.924621998940734713, 41.54138280047497744, 78.88894238123772595 ) ) ;
#19465=CARTESIAN_POINT ( 'NONE',  ( 5.241745939415380917, 50.86780957443158258, 78.63052193300478621 ) ) ;
#19466=CARTESIAN_POINT ( 'NONE',  ( 8.941883057029242465, 41.59311528658734147, 77.39218765127517941 ) ) ;
#19467=CARTESIAN_POINT ( 'NONE',  ( 9.242846470233811118, 42.49512172872434945, 77.95057265855270145 ) ) ;
#19469=CARTESIAN_POINT ( 'NONE',  ( -0.3247337541324620269, 52.97381866229035552, 75.52908203832478762 ) ) ;
#19470=CARTESIAN_POINT ( 'NONE',  ( 0.5221481216947261306, 52.96836594783012941, 79.54816788430672148 ) ) ;
#19471=CARTESIAN_POINT ( 'NONE',  ( 6.716472115211415961, 37.77264227618470471, 78.07897440853361104 ) ) ;
#19473=CARTESIAN_POINT ( 'NONE',  ( 7.753636062665578699, 48.02814353133176439, 72.45433879953087342 ) ) ;
#19474=EDGE_LOOP ( 'NONE', ( #20897, #18788, #12968, #7799 ) ) ;
#19481=CARTESIAN_POINT ( 'NONE',  ( 5.008975552073978932, 51.78836144432716537, 77.68963291717794561 ) ) ;
#19483=CARTESIAN_POINT ( 'NONE',  ( -7.293281983365068832, 41.70860050496550997, 78.93589458924091673 ) ) ;
#19484=CARTESIAN_POINT ( 'NONE',  ( 8.124283007755586539, 44.40224511508533567, 75.45433879953087342 ) ) ;
#19485=ORIENTED_EDGE ( 'NONE', *, *, #13749, .F. ) ;
#19487=VERTEX_POINT ( 'NONE', #14140 ) ;
#19489=CARTESIAN_POINT ( 'NONE',  ( -3.055882809522131094, 36.78399362325244937, 72.45433879953085921 ) ) ;
#19492=VERTEX_POINT ( 'NONE', #9162 ) ;
#19494=CARTESIAN_POINT ( 'NONE',  ( 2.115041367457929589, 52.20598078514408513, 77.84551527011910821 ) ) ;
#19495=LINE ( 'NONE', #11643, #4832 ) ;
#19497=FACE_OUTER_BOUND ( 'NONE', #2598, .T. ) ;
#19499=PLANE ( 'NONE',  #2805 ) ;
#19501=CARTESIAN_POINT ( 'NONE',  ( -4.383473025373058718, 51.47257230871590394, 76.47051527011910821 ) ) ;
#19505=CARTESIAN_POINT ( 'NONE',  ( -7.807343701989813312, 41.29925972579167137, 76.45513158819304067 ) ) ;
#19507=EDGE_CURVE ( 'NONE', #9577, #597, #15763, .T. ) ;
#19513=CARTESIAN_POINT ( 'NONE',  ( 5.631785411401764918, 36.99756487055721976, 77.76022115247205591 ) ) ;
#19514=CARTESIAN_POINT ( 'NONE',  ( -7.154059339130676598, 47.04588606493869918, 75.45433879953087342 ) ) ;
#19515=ORIENTED_EDGE ( 'NONE', *, *, #13239, .T. ) ;
#19516=CARTESIAN_POINT ( 'NONE',  ( 1.515499286945060975, 52.95892085087707102, 79.40139704896512285 ) ) ;
#19517=DIRECTION ( 'NONE',  ( -1.540237394707284220E-16, -1.793354297423764243E-16, 1.000000000000000000 ) ) ;
#19518=EDGE_LOOP ( 'NONE', ( #11842, #9123, #13512, #16531 ) ) ;
#19519=DIRECTION ( 'NONE',  ( 1.540237394707284220E-16, 1.793354297423764243E-16, -1.000000000000000000 ) ) ;
#19521=CARTESIAN_POINT ( 'NONE',  ( 9.026706097321888222, 41.84733531941775198, 79.51559944055343010 ) ) ;
#19525=EDGE_LOOP ( 'NONE', ( #16247, #16322, #19515, #18745 ) ) ;
#19527=CARTESIAN_POINT ( 'NONE',  ( 1.015734901122072875, 52.94862456227837555, 76.77344627088704954 ) ) ;
#19529=ORIENTED_EDGE ( 'NONE', *, *, #14802, .T. ) ;
#19530=CARTESIAN_POINT ( 'NONE',  ( -4.956093006374739041, 37.26832696102055564, 77.32892190166411694 ) ) ;
#19534=CARTESIAN_POINT ( 'NONE',  ( -7.841408665719470150, 41.42496028907581973, 78.93240061090689608 ) ) ;
#19539=CARTESIAN_POINT ( 'NONE',  ( 6.467647404187965243, 50.71089930605690910, 75.49932683761802821 ) ) ;
#19540=DIRECTION ( 'NONE',  ( 1.540237394707284220E-16, 1.793354297423764243E-16, -1.000000000000000000 ) ) ;
#19541=CARTESIAN_POINT ( 'NONE',  ( -1.123656915330052408, 35.37488560990637865, 76.86610350541323555 ) ) ;
#19542=CARTESIAN_POINT ( 'NONE',  ( 0.5221537403065019678, 44.16218137147968292, 72.45433879953087342 ) ) ;
#19543=CARTESIAN_POINT ( 'NONE',  ( 7.676123242391161838, 40.16397087432461177, 78.01856368782078732 ) ) ;
#19548=CARTESIAN_POINT ( 'NONE',  ( 2.108066629828172722, 52.81809899402443875, 78.56377684848334297 ) ) ;
#19558=CARTESIAN_POINT ( 'NONE',  ( 6.828109521384686076, 50.44464046038347504, 77.45110917081549928 ) ) ;
#19559=CARTESIAN_POINT ( 'NONE',  ( -3.495392342740027303, 36.18936622140545012, 76.59109406773794149 ) ) ;
#19560=CARTESIAN_POINT ( 'NONE',  ( -4.511001915486199110, 37.69419204354686315, 76.06675994099744287 ) ) ;
#19563=CARTESIAN_POINT ( 'NONE',  ( -5.803682309770403336, 37.89440703645915676, 79.21211992218960063 ) ) ;
#19564=CARTESIAN_POINT ( 'NONE',  ( -5.838428831739583380, 50.43291415881836315, 78.10580938776615767 ) ) ;
#19565=CARTESIAN_POINT ( 'NONE',  ( 8.457937123238437493, 42.09516238501478824, 75.39874760587915148 ) ) ;
#19566=LINE ( 'NONE', #8306, #18024 ) ;
#19567=CARTESIAN_POINT ( 'NONE',  ( 8.509969478268430976, 40.29864289095467456, 75.64968528315669971 ) ) ;
#19568=ORIENTED_EDGE ( 'NONE', *, *, #13724, .F. ) ;
#19570=CARTESIAN_POINT ( 'NONE',  ( 0.5981972045264781768, 52.96654101249860247, 75.36022115247205022 ) ) ;
#19571=CARTESIAN_POINT ( 'NONE',  ( 0.5161363701343861798, 52.20597262174597120, 79.54816788430672148 ) ) ;
#19572=CARTESIAN_POINT ( 'NONE',  ( 6.169334044264807915, 38.30145302496794812, 78.19824744938543404 ) ) ;
#19573=CARTESIAN_POINT ( 'NONE',  ( 4.844805589496135489, 51.13093757591915534, 75.42224697063917915 ) ) ;
#19574=DIRECTION ( 'NONE',  ( -1.540237394707284467E-16, -1.793354297423764243E-16, 1.000000000000000000 ) ) ;
#19575=VERTEX_POINT ( 'NONE', #17450 ) ;
#19576=CARTESIAN_POINT ( 'NONE',  ( 8.909863635552733641, 41.49715104914803021, 76.00786757613292366 ) ) ;
#19577=VECTOR ( 'NONE', #1469, 1000.000000000000000 ) ;
#19581=FACE_OUTER_BOUND ( 'NONE', #18342, .T. ) ;
#19582=CARTESIAN_POINT ( 'NONE',  ( 8.327750958825182792, 41.64958601982033315, 75.98936102326365472 ) ) ;
#19583=EDGE_CURVE ( 'NONE', #8823, #15970, #4457, .T. ) ;
#19584=LINE ( 'NONE', #5006, #6825 ) ;
#19585=VERTEX_POINT ( 'NONE', #9475 ) ;
#19587=AXIS2_PLACEMENT_3D ( 'NONE', #11651, #18129, #671 ) ;
#19589=DIRECTION ( 'NONE',  ( -1.540237394707284467E-16, -1.793354297423764243E-16, 1.000000000000000000 ) ) ;
#19591=( BOUNDED_CURVE ( )  B_SPLINE_CURVE ( 3, ( #5346, #356, #16854, #10164 ),
 .UNSPECIFIED., .F., .T. ) 
 B_SPLINE_CURVE_WITH_KNOTS ( ( 4, 4 ),
 ( 4.662421992893787781, 4.819209660608428258 ),
 .UNSPECIFIED. ) 
 CURVE ( )  GEOMETRIC_REPRESENTATION_ITEM ( )  RATIONAL_B_SPLINE_CURVE ( ( 1.000000000000000000, 0.9979525178427032239, 0.9979525178427032239, 1.000000000000000000 ) ) 
 REPRESENTATION_ITEM ( '' )  );
#19593=CARTESIAN_POINT ( 'NONE',  ( 8.228459776970742823, 41.35979042148017015, 77.86767600988038396 ) ) ;
#19595=LINE ( 'NONE', #9945, #9136 ) ;
#19598=FACE_OUTER_BOUND ( 'NONE', #3407, .T. ) ;
#19601=CARTESIAN_POINT ( 'NONE',  ( 2.035123479059381957, 36.10296785094195826, 76.86610350541323555 ) ) ;
#19603=CARTESIAN_POINT ( 'NONE',  ( 4.160801005917750039, 51.50085880978985386, 78.17666347917207759 ) ) ;
#19604=CARTESIAN_POINT ( 'NONE',  ( -7.423027804938098662, 40.08393216593763952, 78.33343394419354411 ) ) ;
#19605=CARTESIAN_POINT ( 'NONE',  ( 4.539372959821318609, 52.13523796247791608, 76.58963291717793709 ) ) ;
#19610=EDGE_CURVE ( 'NONE', #10073, #9723, #1545, .T. ) ;
#19612=CARTESIAN_POINT ( 'NONE',  ( 5.921589662822362321, 51.11425016305613411, 76.13071926429850578 ) ) ;
#19614=CARTESIAN_POINT ( 'NONE',  ( 1.368073678578153762, 52.96008335597884553, 79.45495304649941204 ) ) ;
#19615=LINE ( 'NONE', #16338, #18053 ) ;
#19617=ORIENTED_EDGE ( 'NONE', *, *, #7380, .T. ) ;
#19619=EDGE_CURVE ( 'NONE', #9302, #19082, #13978, .T. ) ;
#19621=CARTESIAN_POINT ( 'NONE',  ( 8.990918003704509331, 41.74007613249212767, 79.53018343098241871 ) ) ;
#19624=CARTESIAN_POINT ( 'NONE',  ( -5.251100579623900977, 37.48623717174978509, 75.42164981362142839 ) ) ;
#19627=LINE ( 'NONE', #17828, #7417 ) ;
#19628=CARTESIAN_POINT ( 'NONE',  ( 0.8006569122482152245, 52.95806462237449352, 76.79591147939019891 ) ) ;
#19634=ORIENTED_EDGE ( 'NONE', *, *, #5900, .F. ) ;
#19637=B_SPLINE_CURVE_WITH_KNOTS ( 'NONE', 3,
 ( #856, #8739, #15227, #20310, #20425, #12667, #21033, #12453, #10873, #16172 ),
 .UNSPECIFIED., .F., .F.,
 ( 4, 2, 2, 2, 4 ),
 ( 0.000000000000000000, 0.0001454262934834706935, 0.0002181394402252059860, 0.0002908525869669412785, 0.0005817051739339218052 ),
 .UNSPECIFIED. ) ;
#19638=AXIS2_PLACEMENT_3D ( 'NONE', #2880, #4247, #7875 ) ;
#19639=CARTESIAN_POINT ( 'NONE',  ( -4.537099264183358294, 37.70896829297682729, 76.38448585835440952 ) ) ;
#19640=LINE ( 'NONE', #12956, #11985 ) ;
#19642=CARTESIAN_POINT ( 'NONE',  ( 4.490969506678155199, 36.18237959297783135, 75.97723610431854979 ) ) ;
#19643=ORIENTED_EDGE ( 'NONE', *, *, #4772, .T. ) ;
#19644=CARTESIAN_POINT ( 'NONE',  ( -5.362109749382325319, 38.45089291097274753, 75.75643513208801494 ) ) ;
#19645=CARTESIAN_POINT ( 'NONE',  ( 9.296966826988569466, 42.65732387124978686, 75.81656704941096336 ) ) ;
#19646=EDGE_CURVE ( 'NONE', #16959, #18997, #5327, .T. ) ;
#19648=CARTESIAN_POINT ( 'NONE',  ( 1.606955356318995554, 52.89554470253639096, 79.36023959048891641 ) ) ;
#19651=EDGE_CURVE ( 'NONE', #13622, #15829, #1454, .T. ) ;
#19652=ORIENTED_EDGE ( 'NONE', *, *, #16663, .F. ) ;
#19653=FACE_OUTER_BOUND ( 'NONE', #19871, .T. ) ;
#19656=CARTESIAN_POINT ( 'NONE',  ( 4.903891431458001549, 51.86598285117960216, 77.64500276804245971 ) ) ;
#19657=CARTESIAN_POINT ( 'NONE',  ( 0.5981602388297567741, 52.96185312741366857, 75.36022115247205022 ) ) ;
#19658=CARTESIAN_POINT ( 'NONE',  ( 4.149022253754741207, 51.51650688196784955, 78.63864101191019529 ) ) ;
#19661=CARTESIAN_POINT ( 'NONE',  ( 4.561823949912076515, 52.11865432047892455, 76.17419329630023128 ) ) ;
#19662=CARTESIAN_POINT ( 'NONE',  ( -3.501354354950024117, 36.19377011966047775, 76.40804902690982203 ) ) ;
#19663=CARTESIAN_POINT ( 'NONE',  ( -4.891140504938443989, 37.22034916465592147, 76.21310604893328389 ) ) ;
#19664=VECTOR ( 'NONE', #11640, 1000.000000000000000 ) ;
#19667=CARTESIAN_POINT ( 'NONE',  ( 6.282717385696039436, 38.32643750394947801, 78.79551527011911105 ) ) ;
#19668=EDGE_LOOP ( 'NONE', ( #238, #16200, #525, #11297 ) ) ;
#19669=CARTESIAN_POINT ( 'NONE',  ( 5.327803506469481754, 40.48109702276099853, 72.45433879953087342 ) ) ;
#19670=EDGE_CURVE ( 'NONE', #5223, #16948, #15197, .T. ) ;
#19671=CARTESIAN_POINT ( 'NONE',  ( -4.831226022076286597, 37.17609274966823563, 78.89646723195187406 ) ) ;
#19672=FACE_OUTER_BOUND ( 'NONE', #14744, .T. ) ;
#19673=CARTESIAN_POINT ( 'NONE',  ( 8.385738467910485383, 39.92631467184355643, 77.08252479744105301 ) ) ;
#19674=ORIENTED_EDGE ( 'NONE', *, *, #19769, .T. ) ;
#19675=EDGE_LOOP ( 'NONE', ( #16551, #10277, #13756, #1881, #14450, #7992, #13264, #15069, #4960, #2779, #13160, #4677 ) ) ;
#19676=CIRCLE ( 'NONE', #4048, 8.199999999999995737 ) ;
#19677=CARTESIAN_POINT ( 'NONE',  ( -0.1449331424556546677, 52.21320744800303260, 75.45826338387253429 ) ) ;
#19679=CARTESIAN_POINT ( 'NONE',  ( 7.751568289410731616, 40.29157170179672676, 78.99587745390167015 ) ) ;
#19681=CARTESIAN_POINT ( 'NONE',  ( -4.159258199808826717, 37.42984277834096929, 78.62191134682883842 ) ) ;
#19682=ORIENTED_EDGE ( 'NONE', *, *, #15640, .T. ) ;
#19683=CARTESIAN_POINT ( 'NONE',  ( 8.371529501950854879, 41.80378517845067421, 76.20405737193274831 ) ) ;
#19684=VECTOR ( 'NONE', #2427, 1000.000000000000000 ) ;
#19685=VECTOR ( 'NONE', #12024, 1000.000000000000227 ) ;
#19686=VERTEX_POINT ( 'NONE', #3386 ) ;
#19688=CARTESIAN_POINT ( 'NONE',  ( -7.199730269989208509, 41.41414085053946081, 78.68823452940202401 ) ) ;
#19689=CARTESIAN_POINT ( 'NONE',  ( -3.538351547904189154, 36.22109845575787546, 78.30834307773316993 ) ) ;
#19695=ORIENTED_EDGE ( 'NONE', *, *, #10403, .T. ) ;
#19697=ORIENTED_EDGE ( 'NONE', *, *, #17178, .T. ) ;
#19698=VECTOR ( 'NONE', #18647, 1000.000000000000000 ) ;
#19699=CARTESIAN_POINT ( 'NONE',  ( -7.607426330816210225, 47.53160628749161987, 78.30606788437694377 ) ) ;
#19701=DIRECTION ( 'NONE',  ( -0.3165065846431827090, -0.9485903129789527988, 0.000000000000000000 ) ) ;
#19702=ORIENTED_EDGE ( 'NONE', *, *, #10036, .F. ) ;
#19704=CARTESIAN_POINT ( 'NONE',  ( 8.810541937945364666, 41.19947762056773399, 75.36738766396204880 ) ) ;
#19705=CARTESIAN_POINT ( 'NONE',  ( 0.5221537403065015237, 44.16218137147968292, 75.45433879953088763 ) ) ;
#19706=DIRECTION ( 'NONE',  ( 1.540237394707284220E-16, 1.793354297423764243E-16, -1.000000000000000000 ) ) ;
#19707=CARTESIAN_POINT ( 'NONE',  ( -1.598719209087998694, 36.85794301744668644, 72.45433879953085921 ) ) ;
#19708=ORIENTED_EDGE ( 'NONE', *, *, #15944, .F. ) ;
#19709=CARTESIAN_POINT ( 'NONE',  ( -4.397525688316068937, 51.46253079027765409, 76.14127734336351239 ) ) ;
#19710=EDGE_CURVE ( 'NONE', #16492, #2288, #16692, .T. ) ;
#19711=B_SPLINE_CURVE_WITH_KNOTS ( 'NONE', 3,
 ( #8525, #527, #2455, #8734, #20201, #8842, #16715, #17027, #635, #11932, #5633, #13829, #13728, #3929 ),
 .UNSPECIFIED., .F., .F.,
 ( 4, 2, 2, 2, 2, 2, 4 ),
 ( 0.000000000000000000, 0.0003188956011945200857, 0.0004783434017918008368, 0.0006377912023890815879, 0.0007972390029863621764, 0.0009566868035836429817, 0.001275582404778193100 ),
 .UNSPECIFIED. ) ;
#19712=ORIENTED_EDGE ( 'NONE', *, *, #5756, .F. ) ;
#19714=CARTESIAN_POINT ( 'NONE',  ( -6.782498427932185159, 40.54244403944807829, 77.72888818034803649 ) ) ;
#19715=LINE ( 'NONE', #3749, #20699 ) ;
#19721=CARTESIAN_POINT ( 'NONE',  ( -7.001788291781583240, 47.28530462899436770, 78.29855163726114142 ) ) ;
#19724=FACE_OUTER_BOUND ( 'NONE', #4492, .T. ) ;
#19725=FACE_OUTER_BOUND ( 'NONE', #6695, .T. ) ;
#19726=ORIENTED_EDGE ( 'NONE', *, *, #1731, .T. ) ;
#19732=CARTESIAN_POINT ( 'NONE',  ( -4.387445420882217562, 37.78429639223235625, 75.36094808373545106 ) ) ;
#19734=CARTESIAN_POINT ( 'NONE',  ( 0.3525650168280970997, 52.96056955190729099, 77.07067564994990505 ) ) ;
#19737=CARTESIAN_POINT ( 'NONE',  ( 8.887668352622405621, 41.43063037816333605, 75.36022115247205022 ) ) ;
#19742=CARTESIAN_POINT ( 'NONE',  ( 6.323093812904748923, 50.81767522096397727, 75.43719735689487038 ) ) ;
#19743=CARTESIAN_POINT ( 'NONE',  ( 0.5789266213364873126, 51.36195753744342340, 77.38375056423674891 ) ) ;
#19744=ADVANCED_FACE ( 'NONE', ( #10325 ), #193, .T. ) ;
#19745=ORIENTED_EDGE ( 'NONE', *, *, #4787, .T. ) ;
#19746=CARTESIAN_POINT ( 'NONE',  ( 3.990048841361577114, 36.74421560769709316, 76.25036098622081226 ) ) ;
#19747=CARTESIAN_POINT ( 'NONE',  ( 8.387651578222229176, 39.93204838481331365, 78.28891658965622469 ) ) ;
#19750=CARTESIAN_POINT ( 'NONE',  ( -0.9436870690626146807, 52.23009998296728895, 77.77566232894263010 ) ) ;
#19752=DIRECTION ( 'NONE',  ( -0.2848220354341971516, 0.9585804129707224952, 1.280380753214897429E-16 ) ) ;
#19753=CARTESIAN_POINT ( 'NONE',  ( -7.294472080575377326, 41.68420623513899415, 78.93669174070734584 ) ) ;
#19755=ORIENTED_EDGE ( 'NONE', *, *, #9540, .T. ) ;
#19757=VERTEX_POINT ( 'NONE', #10103 ) ;
#19760=CARTESIAN_POINT ( 'NONE',  ( 6.457023732898393931, 39.40536329938229443, 72.45433879953087342 ) ) ;
#19765=LINE ( 'NONE', #14669, #20840 ) ;
#19766=CARTESIAN_POINT ( 'NONE',  ( -5.160557796315993428, 37.41935686500602287, 77.90139762306027649 ) ) ;
#19768=CARTESIAN_POINT ( 'NONE',  ( 4.252148395930121616, 51.42256623072658073, 75.77039595153209461 ) ) ;
#19769=EDGE_CURVE ( 'NONE', #12581, #6991, #2116, .T. ) ;
#19772=EDGE_CURVE ( 'NONE', #16377, #18140, #2215, .T. ) ;
#19774=VERTEX_POINT ( 'NONE', #9902 ) ;
#19775=CARTESIAN_POINT ( 'NONE',  ( 3.972684840124949268, 36.72331404565372281, 76.33233413694243552 ) ) ;
#19776=DIRECTION ( 'NONE',  ( -0.6080936526121348829, -0.7938652969193402686, -2.360290325043241787E-16 ) ) ;
#19777=CARTESIAN_POINT ( 'NONE',  ( 8.607847902093633152, 42.79549789786761949, 75.71644552919879345 ) ) ;
#19779=PLANE ( 'NONE',  #14623 ) ;
#19780=DIRECTION ( 'NONE',  ( -0.3165065846431824870, -0.9485903129789529098, 0.000000000000000000 ) ) ;
#19782=DIRECTION ( 'NONE',  ( 0.007885122365275663500, 0.9999689119394085113, 1.805443505845543142E-16 ) ) ;
#19785=ORIENTED_EDGE ( 'NONE', *, *, #2841, .F. ) ;
#19786=LINE ( 'NONE', #13, #11779 ) ;
#19787=CARTESIAN_POINT ( 'NONE',  ( 0.5221537403065010796, 44.16218137147968292, 78.13669174070733447 ) ) ;
#19788=CARTESIAN_POINT ( 'NONE',  ( 0.8495798803348756367, 52.95608793177016338, 76.37320741481380537 ) ) ;
#19789=ORIENTED_EDGE ( 'NONE', *, *, #5484, .F. ) ;
#19790=CARTESIAN_POINT ( 'NONE',  ( -4.393892947181490705, 51.46512661408927869, 78.70491066849456274 ) ) ;
#19791=CARTESIAN_POINT ( 'NONE',  ( -4.518589064258794252, 36.94516042271330036, 78.67445481091525039 ) ) ;
#19794=EDGE_CURVE ( 'NONE', #6337, #11401, #19029, .T. ) ;
#19795=CARTESIAN_POINT ( 'NONE',  ( -7.794531540891230570, 41.26351018813655713, 78.81104446281315745 ) ) ;
#19798=CARTESIAN_POINT ( 'NONE',  ( 8.359199713419561917, 41.74790691855383784, 79.54611504273570688 ) ) ;
#19802=CARTESIAN_POINT ( 'NONE',  ( -7.715124386663294587, 47.25851271173962687, 78.12178705274547497 ) ) ;
#19803=B_SPLINE_CURVE_WITH_KNOTS ( 'NONE', 3,
 ( #214, #8527, #19988, #16822, #5415, #13205, #11934, #5535, #19681, #6915 ),
 .UNSPECIFIED., .F., .F.,
 ( 4, 2, 2, 2, 4 ),
 ( 0.000000000000000000, 0.0001226732940611538817, 0.0002453465881223077633, 0.0003680198821834616179, 0.0004906931762446155266 ),
 .UNSPECIFIED. ) ;
#19805=ORIENTED_EDGE ( 'NONE', *, *, #6628, .F. ) ;
#19806=DIRECTION ( 'NONE',  ( 0.9585804129707226062, 0.2848220354341972071, 1.987228219138359305E-16 ) ) ;
#19807=FACE_OUTER_BOUND ( 'NONE', #3827, .T. ) ;
#19810=DIRECTION ( 'NONE',  ( 0.007885122365275663500, 0.9999689119394085113, 1.805443505845543142E-16 ) ) ;
#19812=ORIENTED_EDGE ( 'NONE', *, *, #9778, .T. ) ;
#19813=CARTESIAN_POINT ( 'NONE',  ( -4.537099264183358294, 37.70896829297682729, 72.45433879953085921 ) ) ;
#19814=VERTEX_POINT ( 'NONE', #16586 ) ;
#19815=CARTESIAN_POINT ( 'NONE',  ( -3.567022099613818664, 37.05453471803580356, 77.68963291717793140 ) ) ;
#19816=CARTESIAN_POINT ( 'NONE',  ( -6.705728293473678825, 40.29967276483549199, 78.42124021397933120 ) ) ;
#19817=LINE ( 'NONE', #14726, #13244 ) ;
#19820=CARTESIAN_POINT ( 'NONE',  ( 5.844285037446443454, 37.14940932322087264, 76.26708001093082601 ) ) ;
#19822=ORIENTED_EDGE ( 'NONE', *, *, #985, .T. ) ;
#19823=CARTESIAN_POINT ( 'NONE',  ( 0.7119631482320658566, 52.96525702863522156, 79.54746358246200089 ) ) ;
#19825=EDGE_CURVE ( 'NONE', #17827, #6925, #405, .T. ) ;
#19830=ORIENTED_EDGE ( 'NONE', *, *, #4239, .T. ) ;
#19831=CARTESIAN_POINT ( 'NONE',  ( 8.911238338503892464, 41.50127112110217809, 78.09303657357962436 ) ) ;
#19832=CARTESIAN_POINT ( 'NONE',  ( -5.508129029085064410, 38.61210022972240097, 76.73301527011911105 ) ) ;
#19833=ORIENTED_EDGE ( 'NONE', *, *, #4035, .T. ) ;
#19838=CARTESIAN_POINT ( 'NONE',  ( -4.383468690544193969, 37.62011356440623899, 77.91594000873737969 ) ) ;
#19840=DIRECTION ( 'NONE',  ( 1.540237394707283727E-16, 1.793354297423763257E-16, -1.000000000000000000 ) ) ;
#19842=CARTESIAN_POINT ( 'NONE',  ( 5.521710135516018525, 50.48479211476082185, 75.36814786694185386 ) ) ;
#19844=CARTESIAN_POINT ( 'NONE',  ( 5.526420620081125001, 50.65814065400521571, 77.23783507897452694 ) ) ;
#19845=CARTESIAN_POINT ( 'NONE',  ( 0.5221537403065019678, 44.16218137147968292, 72.45433879953087342 ) ) ;
#19846=VERTEX_POINT ( 'NONE', #1810 ) ;
#19848=EDGE_CURVE ( 'NONE', #4681, #5056, #9387, .T. ) ;
#19849=CARTESIAN_POINT ( 'NONE',  ( 4.643940233704298315, 36.29168687389493897, 75.71841013695411959 ) ) ;
#19850=CARTESIAN_POINT ( 'NONE',  ( 7.676056969765417293, 40.16377225106099758, 77.86095545630369941 ) ) ;
#19856=ORIENTED_EDGE ( 'NONE', *, *, #15209, .T. ) ;
#19858=DIRECTION ( 'NONE',  ( -1.540237394707284220E-16, -1.793354297423764243E-16, 1.000000000000000000 ) ) ;
#19862=CARTESIAN_POINT ( 'NONE',  ( 8.949781629519392823, 41.61678780941641520, 75.36311794487049553 ) ) ;
#19863=CARTESIAN_POINT ( 'NONE',  ( -7.376208160937971492, 41.95857449956633900, 78.60633356588459719 ) ) ;
#19864=DIRECTION ( 'NONE',  ( -0.5941461771851691553, -0.8043570849667760481, -2.357623395011396791E-16 ) ) ;
#19865=CARTESIAN_POINT ( 'NONE',  ( 8.385679600361122255, 39.92613824206362949, 77.69330938776616335 ) ) ;
#19866=CARTESIAN_POINT ( 'NONE',  ( 8.215888888258310985, 41.33732038555770316, 76.18655208513948196 ) ) ;
#19869=CARTESIAN_POINT ( 'NONE',  ( 4.552447320970152589, 52.12558045856467004, 76.26690125110441443 ) ) ;
#19871=EDGE_LOOP ( 'NONE', ( #20963, #10744, #8665, #1154 ) ) ;
#19873=CARTESIAN_POINT ( 'NONE',  ( 0.3347249908012886466, 52.35620383029826286, 76.14768332476499779 ) ) ;
#19879=CARTESIAN_POINT ( 'NONE',  ( -4.721994780338715003, 37.09540803149950960, 78.93613021445058564 ) ) ;
#19882=CARTESIAN_POINT ( 'NONE',  ( 8.947628219434415442, 41.61033390278195299, 77.32525259820312158 ) ) ;
#19883=CYLINDRICAL_SURFACE ( 'NONE', #10304, 6.000000000000002665 ) ;
#19886=VERTEX_POINT ( 'NONE', #13593 ) ;
#19887=CARTESIAN_POINT ( 'NONE',  ( 9.342575031381675998, 42.79401455314646086, 78.75800315165874110 ) ) ;
#19889=CARTESIAN_POINT ( 'NONE',  ( -0.02399531697664270338, 35.98038931794833672, 79.45433879953087342 ) ) ;
#19892=CARTESIAN_POINT ( 'NONE',  ( -4.661432690376159371, 37.05067325523395283, 78.93441095796421791 ) ) ;
#19894=CARTESIAN_POINT ( 'NONE',  ( 1.411666439545806506, 52.20714772099431400, 76.80858772049349170 ) ) ;
#19899=EDGE_CURVE ( 'NONE', #20176, #12108, #11163, .T. ) ;
#19901=ORIENTED_EDGE ( 'NONE', *, *, #16540, .F. ) ;
#19902=DIRECTION ( 'NONE',  ( 0.007885122365275663500, 0.9999689119394085113, 1.805443505845543142E-16 ) ) ;
#19903=EDGE_CURVE ( 'NONE', #12245, #8103, #17761, .T. ) ;
#19906=CARTESIAN_POINT ( 'NONE',  ( 6.924055141134583202, 50.37376929599953712, 78.48669174070734300 ) ) ;
#19907=EDGE_CURVE ( 'NONE', #2983, #4618, #15627, .T. ) ;
#19910=DIRECTION ( 'NONE',  ( -1.540237394707284220E-16, -1.793354297423764243E-16, 1.000000000000000000 ) ) ;
#19912=ORIENTED_EDGE ( 'NONE', *, *, #7854, .F. ) ;
#19913=DIRECTION ( 'NONE',  ( -1.540237394707284220E-16, -1.793354297423764243E-16, 1.000000000000000000 ) ) ;
#19914=VERTEX_POINT ( 'NONE', #17214 ) ;
#19915=CARTESIAN_POINT ( 'NONE',  ( -3.130400440463537048, 36.82058224111691658, 78.12965606777083849 ) ) ;
#19916=CARTESIAN_POINT ( 'NONE',  ( -6.960534101141536922, 41.10544874976162788, 76.96732277425439861 ) ) ;
#19917=DIRECTION ( 'NONE',  ( 0.8236492988270800453, 0.5670994908670431434, 2.285625759191143542E-16 ) ) ;
#19918=CARTESIAN_POINT ( 'NONE',  ( -7.507604988220667686, 45.82440120099734315, 75.45433879953087342 ) ) ;
#19923=CARTESIAN_POINT ( 'NONE',  ( 2.447781712115294273, 38.42313889284341144, 72.45433879953087342 ) ) ;
#19924=VERTEX_POINT ( 'NONE', #15519 ) ;
#19928=CARTESIAN_POINT ( 'NONE',  ( -7.176159402432388923, 41.75141254259964541, 77.91116350996777840 ) ) ;
#19929=ORIENTED_EDGE ( 'NONE', *, *, #2624, .T. ) ;
#19930=DIRECTION ( 'NONE',  ( -0.5800177190770223756, -0.8146038580541392626, -2.354238310054622287E-16 ) ) ;
#19931=CARTESIAN_POINT ( 'NONE',  ( -5.954976305145402549, 38.00616181634879354, 76.59693911441793546 ) ) ;
#19932=ORIENTED_EDGE ( 'NONE', *, *, #1286, .F. ) ;
#19933=LINE ( 'NONE', #13461, #11844 ) ;
#19934=CARTESIAN_POINT ( 'NONE',  ( 0.3849501894475816366, 52.96112454960368865, 76.04253343019715317 ) ) ;
#19939=CARTESIAN_POINT ( 'NONE',  ( -4.296394040159018601, 50.78788033116449441, 75.97399450257033493 ) ) ;
#19941=LINE ( 'NONE', #2195, #4409 ) ;
#19942=VECTOR ( 'NONE', #18101, 1000.000000000000000 ) ;
#19943=LINE ( 'NONE', #19743, #2467 ) ;
#19945=EDGE_LOOP ( 'NONE', ( #19180, #7972, #18771, #15319 ) ) ;
#19946=CARTESIAN_POINT ( 'NONE',  ( 3.959708321255010599, 36.72253538286627617, 76.60595702694484999 ) ) ;
#19948=EDGE_LOOP ( 'NONE', ( #2504, #10573, #5966, #13857 ) ) ;
#19949=LINE ( 'NONE', #2201, #1348 ) ;
#19950=LINE ( 'NONE', #1894, #16745 ) ;
#19955=CARTESIAN_POINT ( 'NONE',  ( -3.936408902674054300, 36.51512738899805299, 77.68304435440727218 ) ) ;
#19956=CARTESIAN_POINT ( 'NONE',  ( 7.906618077272564271, 40.87154522579304938, 75.47105533938442079 ) ) ;
#19960=CARTESIAN_POINT ( 'NONE',  ( -5.510796958474739604, 38.60848837797752964, 72.45433879953085921 ) ) ;
#19963=CARTESIAN_POINT ( 'NONE',  ( 8.212437538920868363, 41.32697647264386376, 76.28640183395299346 ) ) ;
#19964=CARTESIAN_POINT ( 'NONE',  ( 6.919062940419317798, 50.37745683356979498, 76.08942471621537607 ) ) ;
#19965=B_SPLINE_CURVE_WITH_KNOTS ( 'NONE', 3,
 ( #2480, #11571, #20007, #7036, #20220, #8871, #3851, #7471, #15458, #10372, #12162, #5558, #18756, #5655 ),
 .UNSPECIFIED., .F., .F.,
 ( 4, 2, 2, 2, 2, 2, 4 ),
 ( 4.336808689942017736E-19, 6.529564833732798800E-05, 0.0001305912966746555423, 0.0001958869450119831237, 0.0002611825933493106509, 0.0003917738900239288967, 0.0005223651866985471424 ),
 .UNSPECIFIED. ) ;
#19966=CARTESIAN_POINT ( 'NONE',  ( 5.902048492000326441, 51.12868443877599134, 78.59183879953087626 ) ) ;
#19970=ORIENTED_EDGE ( 'NONE', *, *, #863, .T. ) ;
#19971=CARTESIAN_POINT ( 'NONE',  ( 0.3395453217024830272, 52.96750455883004349, 76.14768332476499779 ) ) ;
#19975=EDGE_CURVE ( 'NONE', #271, #9577, #7615, .T. ) ;
#19977=CARTESIAN_POINT ( 'NONE',  ( 5.385333739904544004, 50.76442899832089495, 78.93605272602964362 ) ) ;
#19979=CARTESIAN_POINT ( 'NONE',  ( 6.691294758883309157, 37.75465145915448062, 78.79551527011911105 ) ) ;
#19985=ORIENTED_EDGE ( 'NONE', *, *, #12362, .T. ) ;
#19986=CARTESIAN_POINT ( 'NONE',  ( 9.026706097321888222, 41.84733531941775198, 79.51559944055343010 ) ) ;
#19988=CARTESIAN_POINT ( 'NONE',  ( -4.281535647588993854, 37.51643706874827444, 78.93136397943298732 ) ) ;
#19993=CARTESIAN_POINT ( 'NONE',  ( 1.764424261053175957, 52.20436609593109267, 76.95808337915808295 ) ) ;
#19995=CARTESIAN_POINT ( 'NONE',  ( 5.497743849324330689, 37.64424434608246628, 72.45433879953087342 ) ) ;
#19996=ORIENTED_EDGE ( 'NONE', *, *, #12369, .T. ) ;
#19997=DIRECTION ( 'NONE',  ( -0.3165065846431827645, -0.9485903129789529098, 0.000000000000000000 ) ) ;
#19999=ORIENTED_EDGE ( 'NONE', *, *, #15762, .F. ) ;
#20003=CARTESIAN_POINT ( 'NONE',  ( 8.364834758477957877, 41.76689748495397936, 78.11247371284943597 ) ) ;
#20004=CARTESIAN_POINT ( 'NONE',  ( 0.5221537403065009686, 44.16218137147968292, 79.40903933791013003 ) ) ;
#20006=CARTESIAN_POINT ( 'NONE',  ( -4.036263108762779162, 50.80090022068082334, 79.54642512701808243 ) ) ;
#20007=CARTESIAN_POINT ( 'NONE',  ( 0.6354033039974273933, 52.96147787572222398, 77.38615267430542133 ) ) ;
#20008=CARTESIAN_POINT ( 'NONE',  ( 5.379053567747686060, 50.76036377979792746, 77.28905211432859801 ) ) ;
#20012=CARTESIAN_POINT ( 'NONE',  ( 5.391786323697940198, 50.75965653268888644, 77.94845644658968808 ) ) ;
#20013=VECTOR ( 'NONE', #8132, 1000.000000000000000 ) ;
#20014=ORIENTED_EDGE ( 'NONE', *, *, #9120, .F. ) ;
#20015=DIRECTION ( 'NONE',  ( 1.540237394707284220E-16, 1.793354297423764243E-16, -1.000000000000000000 ) ) ;
#20016=EDGE_CURVE ( 'NONE', #4192, #1854, #7642, .T. ) ;
#20018=CIRCLE ( 'NONE', #20690, 8.199999999999995737 ) ;
#20019=CARTESIAN_POINT ( 'NONE',  ( -7.880212061628153464, 41.54679441531448703, 76.16022115247204738 ) ) ;
#20020=DIRECTION ( 'NONE',  ( -0.5941461771851692664, -0.8043570849667761591, -2.357623395011396791E-16 ) ) ;
#20022=B_SPLINE_CURVE_WITH_KNOTS ( 'NONE', 3,
 ( #9355, #20703, #20814, #15840, #7744, #6143, #11267, #14226, #12645, #19127, #16152, #6242, #21011, #12745, #6445, #19221, #5059, #3575 ),
 .UNSPECIFIED., .F., .F.,
 ( 4, 2, 2, 2, 2, 2, 2, 2, 4 ),
 ( 0.000000000000000000, 0.0002949345114877292926, 0.0005898690229754585852, 0.0008848035344631878778, 0.001179738045950917170, 0.001474672557438646463, 0.001769607068926375756, 0.002064541580414105265, 0.002359476091901834341 ),
 .UNSPECIFIED. ) ;
#20023=CARTESIAN_POINT ( 'NONE',  ( 5.493332137868558007, 37.64554666260850979, 76.40678776405631822 ) ) ;
#20025=EDGE_CURVE ( 'NONE', #3298, #9436, #15737, .T. ) ;
#20027=VECTOR ( 'NONE', #1334, 1000.000000000000227 ) ;
#20029=CARTESIAN_POINT ( 'NONE',  ( 8.814092166714758037, 41.21011788141189669, 78.88950904781501094 ) ) ;
#20034=CIRCLE ( 'NONE', #16323, 8.199999999999995737 ) ;
#20035=CARTESIAN_POINT ( 'NONE',  ( -7.913096914557509187, 41.63124252803902436, 77.76017221056694950 ) ) ;
#20036=VERTEX_POINT ( 'NONE', #6033 ) ;
#20038=CARTESIAN_POINT ( 'NONE',  ( 9.012782495821852535, 41.80560540242532852, 78.13577067582016866 ) ) ;
#20039=CYLINDRICAL_SURFACE ( 'NONE', #6537, 8.199999999999995737 ) ;
#20042=DIRECTION ( 'NONE',  ( -1.540237394707284467E-16, -1.793354297423764243E-16, 1.000000000000000000 ) ) ;
#20048=CARTESIAN_POINT ( 'NONE',  ( 0.8455950101471348956, 52.35579997042385259, 77.76169174070734869 ) ) ;
#20049=CARTESIAN_POINT ( 'NONE',  ( 5.327803506469481754, 40.48109702276099853, 72.45432679953087529 ) ) ;
#20052=DIRECTION ( 'NONE',  ( -0.9485903129789527988, 0.3165065846431829311, -8.934458285744989980E-17 ) ) ;
#20054=VECTOR ( 'NONE', #3392, 1000.000000000000227 ) ;
#20056=CARTESIAN_POINT ( 'NONE',  ( -3.411370229937075393, 36.96692943841399881, 79.28278856980307410 ) ) ;
#20059=CARTESIAN_POINT ( 'NONE',  ( 1.708921718063434181, 52.95755783200097966, 75.60954117182248524 ) ) ;
#20060=ORIENTED_EDGE ( 'NONE', *, *, #13883, .T. ) ;
#20061=CARTESIAN_POINT ( 'NONE',  ( -0.9098995361875932275, 52.23616864758587042, 78.71676077850084141 ) ) ;
#20062=CARTESIAN_POINT ( 'NONE',  ( 0.3451640418029088275, 52.96747521092283506, 77.57937361552639288 ) ) ;
#20063=CARTESIAN_POINT ( 'NONE',  ( -7.232783645916265769, 41.49729498405194761, 78.88165857690459859 ) ) ;
#20064=CARTESIAN_POINT ( 'NONE',  ( -3.349688636638950889, 52.21127678364309332, 76.69845644658968808 ) ) ;
#20065=EDGE_LOOP ( 'NONE', ( #6882, #13069, #10224, #18085 ) ) ;
#20066=VERTEX_POINT ( 'NONE', #4441 ) ;
#20067=DIRECTION ( 'NONE',  ( 0.007885122365275663500, 0.9999689119394085113, 1.805443505845543142E-16 ) ) ;
#20068=EDGE_LOOP ( 'NONE', ( #14687, #13321, #2099, #13497 ) ) ;
#20069=CARTESIAN_POINT ( 'NONE',  ( -3.537323694296532040, 36.22033922170236764, 77.24173421363296654 ) ) ;
#20071=FACE_OUTER_BOUND ( 'NONE', #19338, .T. ) ;
#20072=FACE_OUTER_BOUND ( 'NONE', #8353, .T. ) ;
#20073=CARTESIAN_POINT ( 'NONE',  ( -7.568569179903653854, 42.82598212476965216, 79.20830338942023729 ) ) ;
#20075=PRODUCT_DEFINITION_SHAPE ( 'NONE', 'NONE',  #11075 ) ;
#20076=CARTESIAN_POINT ( 'NONE',  ( 8.787829143201870252, 41.13140593384865440, 76.40801527011910821 ) ) ;
#20078=CARTESIAN_POINT ( 'NONE',  ( -4.211488180634966660, 48.16625856408043660, 78.25433879953088478 ) ) ;
#20080=LINE ( 'NONE', #9819, #5851 ) ;
#20081=CARTESIAN_POINT ( 'NONE',  ( 0.3318037965577209092, 52.35622686498843592, 76.19791476666895846 ) ) ;
#20084=CARTESIAN_POINT ( 'NONE',  ( -3.567022099613818664, 37.05453471803580356, 77.68963291717793140 ) ) ;
#20086=CARTESIAN_POINT ( 'NONE',  ( -3.553498346352079285, 52.06564182703182553, 79.13154374754441278 ) ) ;
#20092=CARTESIAN_POINT ( 'NONE',  ( 5.900862589321786977, 51.12956041731354873, 78.19629421043239859 ) ) ;
#20095=CARTESIAN_POINT ( 'NONE',  ( 8.203713612165559610, 41.74519268224744906, 79.54698768757486960 ) ) ;
#20096=CARTESIAN_POINT ( 'NONE',  ( -1.483269432489140449, 51.49895708687498086, 75.45433879953087342 ) ) ;
#20097=CARTESIAN_POINT ( 'NONE',  ( 0.8478793724089639383, 52.95615112447037376, 76.25678054482114021 ) ) ;
#20101=ADVANCED_FACE ( 'NONE', ( #4738 ), #2852, .F. ) ;
#20102=CARTESIAN_POINT ( 'NONE',  ( -4.621383371311750921, 37.02109043652605180, 78.92211507803222048 ) ) ;
#20104=CARTESIAN_POINT ( 'NONE',  ( -7.279083289042354465, 41.66508001738827005, 78.93576421268289778 ) ) ;
#20105=CARTESIAN_POINT ( 'NONE',  ( -7.722494531574873200, 47.25182341447533929, 78.06303731277932911 ) ) ;
#20108=CARTESIAN_POINT ( 'NONE',  ( 6.859321636172213132, 37.87471731380851026, 76.18799845131768222 ) ) ;
#20111=CARTESIAN_POINT ( 'NONE',  ( 5.563695719829709674, 50.62397605989450255, 77.13671500005938242 ) ) ;
#20113=EDGE_CURVE ( 'NONE', #14094, #16863, #20022, .T. ) ;
#20114=CARTESIAN_POINT ( 'NONE',  ( -4.451010579348070095, 50.67739701313279710, 78.52518475144754007 ) ) ;
#20116=ORIENTED_EDGE ( 'NONE', *, *, #5746, .T. ) ;
#20119=CARTESIAN_POINT ( 'NONE',  ( -3.935607453025473657, 50.87282506703193974, 79.53937015691786883 ) ) ;
#20121=CARTESIAN_POINT ( 'NONE',  ( 5.760694563098077481, 51.23309689197249384, 79.54845644658969661 ) ) ;
#20123=ORIENTED_EDGE ( 'NONE', *, *, #11071, .T. ) ;
#20124=DIRECTION ( 'NONE',  ( -1.540237394707284220E-16, -1.793354297423764243E-16, 1.000000000000000000 ) ) ;
#20126=ADVANCED_FACE ( 'NONE', ( #10080 ), #1676, .T. ) ;
#20127=EDGE_LOOP ( 'NONE', ( #5930, #11749, #13060, #6903 ) ) ;
#20129=CARTESIAN_POINT ( 'NONE',  ( 6.961907239250668233, 50.34580947589670075, 76.63889762306028786 ) ) ;
#20130=CARTESIAN_POINT ( 'NONE',  ( 5.491862665586171310, 37.63975666314849633, 76.14240822758154081 ) ) ;
#20131=EDGE_CURVE ( 'NONE', #2164, #8338, #11578, .T. ) ;
#20132=CARTESIAN_POINT ( 'NONE',  ( -5.529385682154831727, 44.31555110708731604, 72.45432679953087529 ) ) ;
#20134=CARTESIAN_POINT ( 'NONE',  ( -5.868264228364990842, 37.94211109820661676, 75.91870325888974946 ) ) ;
#20135=EDGE_LOOP ( 'NONE', ( #10310, #2593, #11723, #5680, #17809, #14564 ) ) ;
#20136=CARTESIAN_POINT ( 'NONE',  ( 8.789256573544019346, 41.13568403313856692, 78.71078388337100762 ) ) ;
#20139=VECTOR ( 'NONE', #12635, 1000.000000000000000 ) ;
#20140=CARTESIAN_POINT ( 'NONE',  ( -4.230491984614289436, 51.58188695944873103, 75.39163409230444302 ) ) ;
#20141=EDGE_CURVE ( 'NONE', #6705, #1396, #8160, .T. ) ;
#20144=ORIENTED_EDGE ( 'NONE', *, *, #9105, .F. ) ;
#20146=CARTESIAN_POINT ( 'NONE',  ( 0.3529277580979759410, 52.96057327895140077, 77.54150982395135827 ) ) ;
#20152=ORIENTED_EDGE ( 'NONE', *, *, #2865, .T. ) ;
#20153=CARTESIAN_POINT ( 'NONE',  ( 2.058799720203610129, 52.21693617655245134, 78.85847600527985435 ) ) ;
#20155=EDGE_LOOP ( 'NONE', ( #20681, #16734, #11542, #155 ) ) ;
#20156=CARTESIAN_POINT ( 'NONE',  ( -4.259582575189197584, 50.81418445627816993, 75.97269380145769446 ) ) ;
#20157=CARTESIAN_POINT ( 'NONE',  ( 5.078534106480070420, 37.34458401757132862, 76.40549045149212759 ) ) ;
#20162=CARTESIAN_POINT ( 'NONE',  ( -3.538351547904186045, 36.22109845575787546, 78.30834307773316993 ) ) ;
#20164=DIRECTION ( 'NONE',  ( -1.540237394707284220E-16, -1.793354297423764243E-16, 1.000000000000000000 ) ) ;
#20166=ORIENTED_EDGE ( 'NONE', *, *, #10319, .F. ) ;
#20167=CARTESIAN_POINT ( 'NONE',  ( 2.119951781669509927, 52.95431670889340836, 76.39978148915828626 ) ) ;
#20169=CARTESIAN_POINT ( 'NONE',  ( 6.919062940419317798, 50.37745683356979498, 76.08942471621537607 ) ) ;
#20170=ADVANCED_FACE ( 'NONE', ( #16253 ), #14648, .T. ) ;
#20171=DIRECTION ( 'NONE',  ( -1.540237394707284467E-16, -1.793354297423764243E-16, 1.000000000000000000 ) ) ;
#20172=CARTESIAN_POINT ( 'NONE',  ( -7.244356193800459032, 41.53104495169013433, 78.90520642705492094 ) ) ;
#20173=VERTEX_POINT ( 'NONE', #16463 ) ;
#20175=CARTESIAN_POINT ( 'NONE',  ( 6.324981017461724697, 49.90226621375084193, 79.13556070921569585 ) ) ;
#20176=VERTEX_POINT ( 'NONE', #13269 ) ;
#20177=CARTESIAN_POINT ( 'NONE',  ( -2.055347584452832166, 51.31805217249780782, 72.45432679953087529 ) ) ;
#20178=CARTESIAN_POINT ( 'NONE',  ( -6.753843712027886248, 40.38066566033639759, 76.16022115247204738 ) ) ;
#20179=CARTESIAN_POINT ( 'NONE',  ( 8.529329397667178014, 40.35666579756309602, 75.60774188071792423 ) ) ;
#20184=CARTESIAN_POINT ( 'NONE',  ( 8.831661421392389855, 41.26277405225351202, 75.98994273744924044 ) ) ;
#20186=CARTESIAN_POINT ( 'NONE',  ( 5.308657174530699407, 50.64216575474390680, 75.36022115247205022 ) ) ;
#20188=LINE ( 'NONE', #5618, #2119 ) ;
#20189=CARTESIAN_POINT ( 'NONE',  ( 8.374367785101570760, 41.81231160194442964, 78.68229860608910542 ) ) ;
#20191=CARTESIAN_POINT ( 'NONE',  ( 5.202885763635528349, 50.89499265101085967, 76.90580938776616904 ) ) ;
#20192=LINE ( 'NONE', #10444, #3781 ) ;
#20193=CARTESIAN_POINT ( 'NONE',  ( -4.434148273901388215, 50.69479882682543348, 78.79940573867644105 ) ) ;
#20197=LINE ( 'NONE', #10765, #19421 ) ;
#20198=CARTESIAN_POINT ( 'NONE',  ( 5.487513352913315323, 50.68176937092437839, 77.98758453411963387 ) ) ;
#20199=ORIENTED_EDGE ( 'NONE', *, *, #1405, .T. ) ;
#20201=CARTESIAN_POINT ( 'NONE',  ( 6.502546507733397263, 49.77243851915681461, 77.06293235403589392 ) ) ;
#20202=FACE_OUTER_BOUND ( 'NONE', #8790, .T. ) ;
#20205=CARTESIAN_POINT ( 'NONE',  ( 5.561792858816290597, 51.38001756867608094, 76.94115191089467487 ) ) ;
#20206=CARTESIAN_POINT ( 'NONE',  ( 2.091368541865487707, 52.21063245889819626, 72.45433879953087342 ) ) ;
#20208=CARTESIAN_POINT ( 'NONE',  ( -7.718146047797494802, 47.26485609621882844, 78.14247693707426379 ) ) ;
#20210=LINE ( 'NONE', #2151, #11951 ) ;
#20211=ORIENTED_EDGE ( 'NONE', *, *, #3883, .T. ) ;
#20212=CARTESIAN_POINT ( 'NONE',  ( 1.043496195706703267, 52.34607428218648550, 75.38691198841223695 ) ) ;
#20213=ORIENTED_EDGE ( 'NONE', *, *, #18211, .T. ) ;
#20218=DIRECTION ( 'NONE',  ( 0.8043570849667761591, -0.5941461771851692664, 1.733862608106489734E-17 ) ) ;
#20219=CARTESIAN_POINT ( 'NONE',  ( -3.600277166070542378, 52.03221539514291294, 79.18928797456808866 ) ) ;
#20220=CARTESIAN_POINT ( 'NONE',  ( 0.6982372515930639345, 52.96044147935328539, 77.40588267440399761 ) ) ;
#20222=CARTESIAN_POINT ( 'NONE',  ( -4.315046395865206108, 37.70882665799790345, 79.54765774203875139 ) ) ;
#20224=PLANE ( 'NONE',  #1371 ) ;
#20225=B_SPLINE_CURVE_WITH_KNOTS ( 'NONE', 3,
 ( #18900, #14108, #13792, #20590, #18800, #15721, #4213, #17201, #819, #10838, #2623, #9233, #13897, #1139, #7627, #12518, #19001, #17409, #8802, #7193, #20169, #20268, #16987, #8917, #5699, #4104, #17102 ),
 .UNSPECIFIED., .F., .F.,
 ( 4, 1, 1, 1, 1, 1, 1, 1, 1, 1, 1, 1, 1, 1, 1, 1, 1, 1, 1, 1, 1, 1, 1, 1, 4 ),
 ( 0.000000000000000000, 0.05959187408140657199, 0.1157444014141101180, 0.1691701821137891193, 0.2193251454534784761, 0.2669475916912845692, 0.3117751794269221777, 0.3541065092364359956, 0.3940487965473342680, 0.4318372767115636890, 0.4680493653760790518, 0.5025338411669280081, 0.5356117844586580912, 0.5674765898557931898, 0.5983444621881826020, 0.6284125990791417093, 0.6580179645932986432, 0.6886630208720043722, 0.7222707808379922323, 0.7592609375352028511, 0.7993858191113136780, 0.8438632570080943918, 0.8918964550480946718, 0.9439126001412549982, 1.000000000000000000 ),
 .UNSPECIFIED. ) ;
#20228=CARTESIAN_POINT ( 'NONE',  ( 4.809763630234642484, 51.93551126624419112, 77.58315289018165117 ) ) ;
#20229=CARTESIAN_POINT ( 'NONE',  ( 6.680635945739894055, 50.55357325011429026, 77.60602934391619101 ) ) ;
#20231=CARTESIAN_POINT ( 'NONE',  ( 7.753636062665578699, 48.02814353133176439, 75.45433879953087342 ) ) ;
#20235=B_SPLINE_CURVE_WITH_KNOTS ( 'NONE', 3,
 ( #4184, #17170, #17271, #5893, #15578, #10907, #13977, #13763, #2693, #9202 ),
 .UNSPECIFIED., .F., .F.,
 ( 4, 2, 2, 2, 4 ),
 ( 8.673617379884035472E-18, 0.0002090038972966693713, 0.0004180077945933300689, 0.0006270116918899907394, 0.0008360155891866514642 ),
 .UNSPECIFIED. ) ;
#20236=CARTESIAN_POINT ( 'NONE',  ( -4.834768248550900260, 37.17870924967544255, 75.36094808373545106 ) ) ;
#20238=CARTESIAN_POINT ( 'NONE',  ( 5.037341483232628647, 37.31725042616477594, 78.79551527011911105 ) ) ;
#20239=ORIENTED_EDGE ( 'NONE', *, *, #11073, .F. ) ;
#20240=CARTESIAN_POINT ( 'NONE',  ( -4.186692411740909670, 50.69340894834095934, 75.36056307228784590 ) ) ;
#20243=B_SPLINE_SURFACE_WITH_KNOTS ( 'NONE', 3, 1, ( 
 ( #666, #15036 ),
 ( #18125, #5233 ),
 ( #13230, #18223 ),
 ( #13650, #13538 ),
 ( #15251, #3956 ),
 ( #10154, #18542 ),
 ( #10265, #11646 ),
 ( #12062, #2055 ),
 ( #11748, #13338 ),
 ( #10479, #16634 ),
 ( #14919, #343 ),
 ( #5560, #5127 ),
 ( #3544, #16945 ),
 ( #5445, #2371 ),
 ( #16527, #15144 ) ),
 .UNSPECIFIED., .F., .F., .F.,
 ( 4, 1, 1, 1, 1, 1, 1, 1, 1, 1, 1, 1, 4 ),
 ( 2, 2 ),
 ( 0.000000000000000000, 0.1108870962763238432, 0.2118129606631371786, 0.3028473642999697790, 0.3830332280304867831, 0.4564275106387662428, 0.5194274750822647224, 0.5737099057017611692, 0.6206015202827788180, 0.7061516677909073225, 0.7943156106821882556, 0.8900258068991424576, 1.000000000000000000 ),
 ( 0.000000000000000000, 1.000000000000000000 ),
 .UNSPECIFIED. ) ;
#20244=ORIENTED_EDGE ( 'NONE', *, *, #11861, .T. ) ;
#20246=CARTESIAN_POINT ( 'NONE',  ( -4.736700016514431510, 50.30022223374984947, 79.44348587025405095 ) ) ;
#20250=EDGE_CURVE ( 'NONE', #5501, #4681, #16244, .T. ) ;
#20252=FACE_OUTER_BOUND ( 'NONE', #10252, .T. ) ;
#20253=ORIENTED_EDGE ( 'NONE', *, *, #3499, .F. ) ;
#20254=CARTESIAN_POINT ( 'NONE',  ( 0.7518033122594925954, 52.35898226866432026, 77.43632519350985888 ) ) ;
#20255=CARTESIAN_POINT ( 'NONE',  ( -1.123656915330052408, 35.37488560990637865, 76.16022115247204738 ) ) ;
#20259=AXIS2_PLACEMENT_3D ( 'NONE', #7616, #5686, #4404 ) ;
#20261=DIRECTION ( 'NONE',  ( 1.540237394707284220E-16, 1.793354297423764243E-16, -1.000000000000000000 ) ) ;
#20262=FACE_OUTER_BOUND ( 'NONE', #12505, .T. ) ;
#20263=DIRECTION ( 'NONE',  ( 1.540237394707284220E-16, 1.793354297423764243E-16, -1.000000000000000000 ) ) ;
#20266=CARTESIAN_POINT ( 'NONE',  ( 2.120942209650837018, 52.95430889900478633, 76.48963291717792856 ) ) ;
#20268=CARTESIAN_POINT ( 'NONE',  ( 6.934807254081542638, 50.36582714328714871, 76.18099276316716839 ) ) ;
#20269=CARTESIAN_POINT ( 'NONE',  ( 0.3642233646226559762, 52.96732492115798152, 77.51213090161979835 ) ) ;
#20271=CARTESIAN_POINT ( 'NONE',  ( -3.448085832972781262, 52.14096574969422448, 75.97742918362793318 ) ) ;
#20274=CARTESIAN_POINT ( 'NONE',  ( 6.195785479992719225, 49.99769775296549312, 79.28554042632779897 ) ) ;
#20276=LINE ( 'NONE', #6027, #18618 ) ;
#20280=CARTESIAN_POINT ( 'NONE',  ( 5.487860080568270682, 37.63670891835880639, 77.55534468517188884 ) ) ;
#20281=CARTESIAN_POINT ( 'NONE',  ( 4.142539520959306110, 51.50352989135271997, 77.22170381446332499 ) ) ;
#20284=CARTESIAN_POINT ( 'NONE',  ( 1.652727357819364640, 35.35299279957455809, 75.45433879953087342 ) ) ;
#20286=CARTESIAN_POINT ( 'NONE',  ( 0.8383918983349099019, 52.95649870062635500, 78.71055905107655803 ) ) ;
#20287=CARTESIAN_POINT ( 'NONE',  ( 4.384086297460604520, 51.32510901764887734, 75.62563104034643402 ) ) ;
#20291=EDGE_CURVE ( 'NONE', #14218, #11138, #2192, .T. ) ;
#20292=CARTESIAN_POINT ( 'NONE',  ( 8.322267033824909177, 41.65616234515825056, 78.92561463894257656 ) ) ;
#20294=EDGE_CURVE ( 'NONE', #12584, #13048, #15171, .T. ) ;
#20295=ORIENTED_EDGE ( 'NONE', *, *, #17932, .T. ) ;
#20297=CARTESIAN_POINT ( 'NONE',  ( 8.124283007755586539, 44.40224511508533567, 72.45432679953087529 ) ) ;
#20301=CARTESIAN_POINT ( 'NONE',  ( -4.891140504938443989, 37.22034916465592858, 76.21310604893328389 ) ) ;
#20302=CARTESIAN_POINT ( 'NONE',  ( -7.527012383044476174, 42.86795482616098951, 79.17794681948264213 ) ) ;
#20303=CARTESIAN_POINT ( 'NONE',  ( 8.621331711279447418, 42.87908309907099635, 77.81705000150257945 ) ) ;
#20304=CARTESIAN_POINT ( 'NONE',  ( 0.5221537403065005245, 44.16218137147968292, 82.45433879953087342 ) ) ;
#20305=EDGE_LOOP ( 'NONE', ( #5734, #6234, #5449, #6532, #6671, #10992, #18126 ) ) ;
#20307=CARTESIAN_POINT ( 'NONE',  ( 8.597226904264964276, 42.92457698268714239, 79.03485483908291087 ) ) ;
#20308=DIRECTION ( 'NONE',  ( 0.3165065846431829311, 0.9485903129789527988, 2.188653791613874255E-16 ) ) ;
#20310=CARTESIAN_POINT ( 'NONE',  ( 0.4222355217934689042, 52.36159922174551440, 78.89164400207971539 ) ) ;
#20312=CARTESIAN_POINT ( 'NONE',  ( 8.468902854075459175, 42.53998166354323018, 78.05372954401303787 ) ) ;
#20314=VECTOR ( 'NONE', #6857, 1000.000000000000227 ) ;
#20315=CARTESIAN_POINT ( 'NONE',  ( -4.486751758304120763, 51.39877310743911210, 75.98707017319573254 ) ) ;
#20316=CARTESIAN_POINT ( 'NONE',  ( -6.857750647227540242, 47.71699458730062560, 78.32480289656686523 ) ) ;
#20317=ADVANCED_FACE ( 'NONE', ( #20482 ), #8792, .T. ) ;
#20318=CARTESIAN_POINT ( 'NONE',  ( -5.506217236748579325, 38.61068806573513257, 78.67637590524894620 ) ) ;
#20320=CARTESIAN_POINT ( 'NONE',  ( 6.882377701754223587, 37.89119233413698140, 76.59354538285809610 ) ) ;
#20322=CARTESIAN_POINT ( 'NONE',  ( 0.6841097403222727857, 52.36108336152096854, 75.36125153625724238 ) ) ;
#20323=ORIENTED_EDGE ( 'NONE', *, *, #6604, .T. ) ;
#20324=CARTESIAN_POINT ( 'NONE',  ( -4.244931195431495219, 50.82465379583177167, 78.93669174070734584 ) ) ;
#20330=CARTESIAN_POINT ( 'NONE',  ( -3.013797660541937873, 51.53151659513010685, 78.93778436892569061 ) ) ;
#20332=CARTESIAN_POINT ( 'NONE',  ( 5.739698376139652503, 51.24860592950068394, 77.28905211432859801 ) ) ;
#20333=CARTESIAN_POINT ( 'NONE',  ( -3.160478584913959388, 36.85599392487655734, 78.92082147625116306 ) ) ;
#20334=ORIENTED_EDGE ( 'NONE', *, *, #13550, .F. ) ;
#20335=CARTESIAN_POINT ( 'NONE',  ( 8.215275734490949944, 41.32388948499509240, 77.23539183544390596 ) ) ;
#20337=ADVANCED_FACE ( 'NONE', ( #18467 ), #10406, .F. ) ;
#20339=CARTESIAN_POINT ( 'NONE',  ( -6.782631326057145138, 43.38225751353197523, 75.45433879953087342 ) ) ;
#20340=FACE_OUTER_BOUND ( 'NONE', #7700, .T. ) ;
#20342=CARTESIAN_POINT ( 'NONE',  ( -7.616632640849319458, 40.81216055894036288, 77.06254053058707143 ) ) ;
#20348=CARTESIAN_POINT ( 'NONE',  ( 4.100026115879673583, 51.54044873340893673, 76.58963291717793709 ) ) ;
#20350=AXIS2_PLACEMENT_3D ( 'NONE', #11164, #20821, #7858 ) ;
#20361=DIRECTION ( 'NONE',  ( -0.9999689119394086223, 0.007885122365278607326, -1.526048693634347968E-16 ) ) ;
#20362=ORIENTED_EDGE ( 'NONE', *, *, #2220, .T. ) ;
#20363=CYLINDRICAL_SURFACE ( 'NONE', #16994, 8.199999999999995737 ) ;
#20365=CARTESIAN_POINT ( 'NONE',  ( 0.8247868767332566797, 52.35233939957169014, 78.75172105370583608 ) ) ;
#20366=EDGE_LOOP ( 'NONE', ( #5459, #21008, #20639, #2685 ) ) ;
#20368=CARTESIAN_POINT ( 'NONE',  ( 5.076572431691917409, 37.34329067111212197, 76.70433879953087342 ) ) ;
#20372=CARTESIAN_POINT ( 'NONE',  ( 5.427951760950261217, 36.85191280677083370, 76.67247627436783830 ) ) ;
#20374=ADVANCED_FACE ( 'NONE', ( #12195 ), #10622, .T. ) ;
#20375=CARTESIAN_POINT ( 'NONE',  ( 5.464930624430781592, 36.87833654873140432, 76.10043865634602867 ) ) ;
#20376=CARTESIAN_POINT ( 'NONE',  ( 1.652727357819363974, 35.35299279957455099, 79.45433879953087342 ) ) ;
#20378=CARTESIAN_POINT ( 'NONE',  ( 1.879340735999647682, 52.20337590418190388, 75.75738117569228791 ) ) ;
#20379=CIRCLE ( 'NONE', #12567, 8.199999999999995737 ) ;
#20380=ORIENTED_EDGE ( 'NONE', *, *, #13907, .T. ) ;
#20381=CARTESIAN_POINT ( 'NONE',  ( 1.851481395807866859, 48.14626068599128672, 82.45433879953087342 ) ) ;
#20384=B_SPLINE_SURFACE_WITH_KNOTS ( 'NONE', 3, 1, ( 
 ( #6654, #1783 ),
 ( #14331, #6235 ),
 ( #2943, #3051 ),
 ( #11261, #8153 ),
 ( #19215, #12738 ),
 ( #6438, #3262 ),
 ( #4630, #3359 ),
 ( #6550, #20902 ),
 ( #13056, #11151 ),
 ( #6333, #13156 ),
 ( #9560, #16043 ),
 ( #1464, #14749 ),
 ( #9449, #7949 ),
 ( #15935, #19427 ),
 ( #12835, #19530 ),
 ( #19315, #4731 ),
 ( #9665, #17732 ),
 ( #4946, #1566 ),
 ( #8051, #9869 ) ),
 .UNSPECIFIED., .F., .F., .F.,
 ( 4, 1, 1, 1, 1, 1, 1, 1, 1, 1, 1, 1, 1, 1, 1, 1, 4 ),
 ( 2, 2 ),
 ( 0.000000000000000000, 0.09593561818428578136, 0.1790132514218915338, 0.2495659677033479074, 0.3103928923273128748, 0.3657232523743771391, 0.4198889549570182789, 0.4761292045875803458, 0.5349114402766786958, 0.5687027968553886037, 0.6100175737345402416, 0.6575813992106814831, 0.7121752348458817439, 0.7738275843818921418, 0.8419112148355063496, 0.9177342363179752383, 1.000000000000000000 ),
 ( 0.000000000000000000, 1.000000000000000000 ),
 .UNSPECIFIED. ) ;
#20385=CARTESIAN_POINT ( 'NONE',  ( -3.349945445540459588, 52.21109327740445138, 76.66413924479479647 ) ) ;
#20388=VECTOR ( 'NONE', #18669, 1000.000000000000114 ) ;
#20393=CARTESIAN_POINT ( 'NONE',  ( 1.658154530501164237, 36.04125148601230677, 72.45433879953085921 ) ) ;
#20394=CARTESIAN_POINT ( 'NONE',  ( 7.760798028454924946, 40.43451328883516993, 75.74322883085581282 ) ) ;
#20395=CARTESIAN_POINT ( 'NONE',  ( 5.357400835671676020, 37.53933297990715801, 77.75509786706420812 ) ) ;
#20396=CARTESIAN_POINT ( 'NONE',  ( -6.972818533526913498, 41.14430689552183651, 79.47750830342025097 ) ) ;
#20399=DIRECTION ( 'NONE',  ( -0.3165065846431826535, -0.9485903129789529098, -2.188653791613874008E-16 ) ) ;
#20400=CARTESIAN_POINT ( 'NONE',  ( -5.825614074793430852, 50.44207111495388318, 76.36675183022860836 ) ) ;
#20401=CARTESIAN_POINT ( 'NONE',  ( 4.334149498405073686, 51.36199531953422337, 75.67068799376596644 ) ) ;
#20402=EDGE_CURVE ( 'NONE', #14686, #17246, #20034, .T. ) ;
#20405=CARTESIAN_POINT ( 'NONE',  ( -7.291056197748040368, 40.11326154233370289, 78.55231559615423009 ) ) ;
#20406=ORIENTED_EDGE ( 'NONE', *, *, #20675, .T. ) ;
#20407=CARTESIAN_POINT ( 'NONE',  ( 8.289318114139261340, 41.55741234261986250, 78.93669174070734584 ) ) ;
#20408=ORIENTED_EDGE ( 'NONE', *, *, #10844, .T. ) ;
#20409=CARTESIAN_POINT ( 'NONE',  ( 0.5221537403065009686, 44.16218137147968292, 79.45433879953087342 ) ) ;
#20413=VECTOR ( 'NONE', #9682, 1000.000000000000114 ) ;
#20415=PLANE ( 'NONE',  #10908 ) ;
#20416=CARTESIAN_POINT ( 'NONE',  ( -7.388159386333283507, 42.42885804414905238, 79.45715840112796968 ) ) ;
#20418=EDGE_CURVE ( 'NONE', #11503, #9686, #11916, .T. ) ;
#20419=EDGE_LOOP ( 'NONE', ( #9618, #11783, #8035, #19996 ) ) ;
#20420=ORIENTED_EDGE ( 'NONE', *, *, #17369, .T. ) ;
#20421=CARTESIAN_POINT ( 'NONE',  ( 9.353525637756030520, 42.82683421514393274, 78.50890480505780999 ) ) ;
#20425=CARTESIAN_POINT ( 'NONE',  ( 0.4034091969759198149, 52.36133432042633729, 78.87521808986805638 ) ) ;
#20426=EDGE_CURVE ( 'NONE', #19924, #12487, #20379, .T. ) ;
#20428=CARTESIAN_POINT ( 'NONE',  ( 9.222679282817953350, 42.43467938865651945, 77.98843304575544266 ) ) ;
#20431=EDGE_CURVE ( 'NONE', #14686, #10889, #1129, .T. ) ;
#20432=CARTESIAN_POINT ( 'NONE',  ( -4.383473025373058718, 51.47257230871590394, 76.47051527011910821 ) ) ;
#20435=CARTESIAN_POINT ( 'NONE',  ( -7.986269739301712356, 41.91386901559200595, 79.52730241447633830 ) ) ;
#20436=ORIENTED_EDGE ( 'NONE', *, *, #487, .F. ) ;
#20437=CARTESIAN_POINT ( 'NONE',  ( 5.579204724385461667, 50.61252018296998045, 76.96076274685535168 ) ) ;
#20438=ORIENTED_EDGE ( 'NONE', *, *, #13550, .T. ) ;
#20439=VECTOR ( 'NONE', #13358, 1000.000000000000000 ) ;
#20440=CARTESIAN_POINT ( 'NONE',  ( -4.451329120265561379, 50.67716939545568522, 78.45066232894264147 ) ) ;
#20443=EDGE_LOOP ( 'NONE', ( #3968, #7985, #19363, #6760 ) ) ;
#20444=CARTESIAN_POINT ( 'NONE',  ( -0.9402972064945576136, 52.21947918594909765, 76.74746709665741662 ) ) ;
#20446=CARTESIAN_POINT ( 'NONE',  ( 6.114519447167765520, 37.34250893849451813, 78.36972961004526894 ) ) ;
#20449=CARTESIAN_POINT ( 'NONE',  ( -3.635499589166290679, 36.29285780047638355, 79.01720576857120193 ) ) ;
#20451=CARTESIAN_POINT ( 'NONE',  ( 5.683893922249901642, 37.03479970459495263, 77.75763958275959453 ) ) ;
#20454=FACE_OUTER_BOUND ( 'NONE', #17459, .T. ) ;
#20456=CARTESIAN_POINT ( 'NONE',  ( -7.061235947027594051, 47.28415677317426713, 78.95240186183670517 ) ) ;
#20457=PLANE ( 'NONE',  #15937 ) ;
#20460=CARTESIAN_POINT ( 'NONE',  ( 6.461625768302495132, 49.81576021970867885, 78.82409288115771062 ) ) ;
#20462=ORIENTED_EDGE ( 'NONE', *, *, #7930, .T. ) ;
#20463=CARTESIAN_POINT ( 'NONE',  ( 8.237563311767338803, 41.40248246318230230, 78.88950904781501094 ) ) ;
#20465=CARTESIAN_POINT ( 'NONE',  ( -5.955451856753747109, 38.00651308716548726, 77.05433879953086773 ) ) ;
#20467=CARTESIAN_POINT ( 'NONE',  ( 4.540684532156292086, 52.13426915682742901, 76.47586842453881673 ) ) ;
#20473=B_SPLINE_CURVE_WITH_KNOTS ( 'NONE', 3,
 ( #2003, #3800, #12016, #11796, #18490, #5182, #18271, #11905, #8500, #15091 ),
 .UNSPECIFIED., .F., .F.,
 ( 4, 2, 2, 2, 4 ),
 ( 0.000000000000000000, 0.0002779176703289528566, 0.0003473970879111939439, 0.0004168765054934349770, 0.0005558353406579482139 ),
 .UNSPECIFIED. ) ;
#20474=CARTESIAN_POINT ( 'NONE',  ( 6.467096401101858127, 37.59444752110963606, 78.28436300994860630 ) ) ;
#20476=AXIS2_PLACEMENT_3D ( 'NONE', #15308, #723, #7204 ) ;
#20478=CARTESIAN_POINT ( 'NONE',  ( 1.324134094588556687, 52.32343890518788498, 79.46661588923706177 ) ) ;
#20481=CARTESIAN_POINT ( 'NONE',  ( -4.392964107369902393, 50.72663347050586680, 79.54348553280554768 ) ) ;
#20482=FACE_OUTER_BOUND ( 'NONE', #17253, .T. ) ;
#20484=CARTESIAN_POINT ( 'NONE',  ( 5.658108625003792191, 37.01637447524286273, 75.97198585835440099 ) ) ;
#20485=CARTESIAN_POINT ( 'NONE',  ( 5.239968004300939342, 50.86462114820943725, 78.68193220087633222 ) ) ;
#20486=ADVANCED_FACE ( 'NONE', ( #19193 ), #9224, .T. ) ;
#20489=VERTEX_POINT ( 'NONE', #2717 ) ;
#20490=CARTESIAN_POINT ( 'NONE',  ( 0.9729319684334255536, 52.96336138165750640, 75.37848164766056414 ) ) ;
#20493=CARTESIAN_POINT ( 'NONE',  ( -0.9424755721682813725, 52.23032563868695632, 76.73465573240828519 ) ) ;
#20499=CARTESIAN_POINT ( 'NONE',  ( 4.759830266884094385, 51.05838002508453144, 79.48101422306089603 ) ) ;
#20500=DIRECTION ( 'NONE',  ( -0.9585804129707224952, -0.2848220354341971516, -1.987228219138359058E-16 ) ) ;
#20501=CARTESIAN_POINT ( 'NONE',  ( 8.491906929791015912, 40.24450828730113727, 75.69429397690826988 ) ) ;
#20503=ORIENTED_EDGE ( 'NONE', *, *, #12363, .F. ) ;
#20504=CARTESIAN_POINT ( 'NONE',  ( -5.160557796315993428, 37.41935686500602287, 77.90139762306027649 ) ) ;
#20505=FACE_OUTER_BOUND ( 'NONE', #19033, .T. ) ;
#20508=CARTESIAN_POINT ( 'NONE',  ( 3.117507734380600137, 51.94062193790708903, 80.45433879953087342 ) ) ;
#20512=ADVANCED_FACE ( 'NONE', ( #9424 ), #15913, .F. ) ;
#20513=CARTESIAN_POINT ( 'NONE',  ( -7.833772919943922552, 41.39643022996011723, 79.54647314732444841 ) ) ;
#20514=CARTESIAN_POINT ( 'NONE',  ( 8.950841833175557483, 41.61996530703199682, 78.68229860608910542 ) ) ;
#20517=CARTESIAN_POINT ( 'NONE',  ( -7.609845089999874190, 43.10833364818387992, 76.06610350541322418 ) ) ;
#20518=CARTESIAN_POINT ( 'NONE',  ( -4.792503378000012582, 37.91763016944491227, 77.90139762306027649 ) ) ;
#20519=CARTESIAN_POINT ( 'NONE',  ( -4.453436368711328974, 50.68011839687689957, 78.45066232894264147 ) ) ;
#20520=SURFACE_SIDE_STYLE ('',( #19038 ) ) ;
#20521=CARTESIAN_POINT ( 'NONE',  ( -8.048135109371418849, 42.06361933714661916, 79.49764826322659417 ) ) ;
#20524=ORIENTED_EDGE ( 'NONE', *, *, #16497, .F. ) ;
#20525=CARTESIAN_POINT ( 'NONE',  ( -4.483923651454749582, 37.66761685267757542, 78.88462034471059781 ) ) ;
#20526=CARTESIAN_POINT ( 'NONE',  ( -3.681032862722696031, 36.32649139546035855, 79.10742496273583413 ) ) ;
#20528=CARTESIAN_POINT ( 'NONE',  ( 5.873343927958857513, 51.14988734394304970, 77.25083512729199242 ) ) ;
#20529=CARTESIAN_POINT ( 'NONE',  ( 5.613949991644618720, 51.34149119567325670, 78.06835901908682729 ) ) ;
#20530=CARTESIAN_POINT ( 'NONE',  ( -4.084259173939017273, 50.94606869312387687, 78.87053299850630594 ) ) ;
#20534=EDGE_CURVE ( 'NONE', #17982, #10889, #7561, .T. ) ;
#20535=CARTESIAN_POINT ( 'NONE',  ( -4.423683986466107498, 51.44383902813605403, 76.03815620566271605 ) ) ;
#20538=CARTESIAN_POINT ( 'NONE',  ( 0.7364379940111278611, 52.35940638163580019, 78.88801353106350689 ) ) ;
#20539=ORIENTED_EDGE ( 'NONE', *, *, #19651, .F. ) ;
#20541=CARTESIAN_POINT ( 'NONE',  ( 2.075723384514267966, 52.21368374790338152, 76.12915149413191784 ) ) ;
#20545=ORIENTED_EDGE ( 'NONE', *, *, #17955, .F. ) ;
#20548=CARTESIAN_POINT ( 'NONE',  ( 8.206376600211122252, 41.34361096682673065, 77.83369646723784285 ) ) ;
#20553=DIRECTION ( 'NONE',  ( -1.540237394707284220E-16, -1.793354297423764243E-16, 1.000000000000000000 ) ) ;
#20555=CARTESIAN_POINT ( 'NONE',  ( 6.181291377576516588, 50.09645632270179050, 77.70598184265482189 ) ) ;
#20556=CARTESIAN_POINT ( 'NONE',  ( 4.605781907348109883, 52.08618434805546116, 77.30394856433355244 ) ) ;
#20561=EDGE_CURVE ( 'NONE', #5416, #10073, #5109, .T. ) ;
#20562=CARTESIAN_POINT ( 'NONE',  ( -5.493714318389447904, 37.66544616749837360, 75.52011153330033721 ) ) ;
#20564=EDGE_CURVE ( 'NONE', #15118, #10540, #437, .T. ) ;
#20567=ORIENTED_EDGE ( 'NONE', *, *, #19010, .F. ) ;
#20571=ORIENTED_EDGE ( 'NONE', *, *, #1848, .T. ) ;
#20574=CARTESIAN_POINT ( 'NONE',  ( 6.882043956598291601, 37.89095385206773869, 77.31245045813156480 ) ) ;
#20575=CARTESIAN_POINT ( 'NONE',  ( -5.955451856753747997, 38.00651308716548726, 78.18375056423674607 ) ) ;
#20579=CARTESIAN_POINT ( 'NONE',  ( 0.5838098620965819219, 52.35423959189261467, 78.93669174070734584 ) ) ;
#20584=CARTESIAN_POINT ( 'NONE',  ( 5.111615301690868307, 37.37278578702127874, 76.10043865634602867 ) ) ;
#20585=CARTESIAN_POINT ( 'NONE',  ( 8.817118105929894867, 41.21918681320168787, 76.01674029036281866 ) ) ;
#20586=CARTESIAN_POINT ( 'NONE',  ( -7.259306123653141540, 41.57521370724165877, 78.12833282845913629 ) ) ;
#20587=ORIENTED_EDGE ( 'NONE', *, *, #523, .F. ) ;
#20588=CARTESIAN_POINT ( 'NONE',  ( 1.769954653961227198, 52.87349229310958521, 76.95685929568175254 ) ) ;
#20590=CARTESIAN_POINT ( 'NONE',  ( 5.963693060521315203, 51.08315007920423056, 75.36814786694185386 ) ) ;
#20602=VERTEX_POINT ( 'NONE', #11627 ) ;
#20603=CARTESIAN_POINT ( 'NONE',  ( -4.555118767358830922, 36.97214344288710208, 78.05402056118774112 ) ) ;
#20604=CARTESIAN_POINT ( 'NONE',  ( -6.734383500022516067, 40.39030043969829364, 78.92129748799239053 ) ) ;
#20605=CARTESIAN_POINT ( 'NONE',  ( -4.719372061707844956, 37.85391995346009963, 79.54051286045766744 ) ) ;
#20609=EDGE_CURVE ( 'NONE', #188, #16089, #18104, .T. ) ;
#20610=CARTESIAN_POINT ( 'NONE',  ( -5.835808111729286374, 50.43478682938704338, 76.54939005541714891 ) ) ;
#20612=CARTESIAN_POINT ( 'NONE',  ( -0.1986334453709044101, 52.21160884442346628, 79.43762534667510522 ) ) ;
#20616=CARTESIAN_POINT ( 'NONE',  ( 5.619974078175711263, 51.33704144561774996, 76.01203914421944319 ) ) ;
#20618=CARTESIAN_POINT ( 'NONE',  ( -7.428991370734761901, 42.55798160200171765, 79.40422342893963048 ) ) ;
#20622=CARTESIAN_POINT ( 'NONE',  ( 2.029186242314200861, 35.35002428291939225, 76.86610350541323555 ) ) ;
#20626=VECTOR ( 'NONE', #4972, 1000.000000000000227 ) ;
#20629=EDGE_CURVE ( 'NONE', #1372, #2631, #8420, .T. ) ;
#20631=LINE ( 'NONE', #18841, #4091 ) ;
#20634=CARTESIAN_POINT ( 'NONE',  ( -3.075450579529443118, 36.79350905225846446, 77.07727084323215649 ) ) ;
#20637=CARTESIAN_POINT ( 'NONE',  ( -7.611372734017126440, 43.12018948500615778, 78.13669174070733447 ) ) ;
#20639=ORIENTED_EDGE ( 'NONE', *, *, #1692, .T. ) ;
#20642=CARTESIAN_POINT ( 'NONE',  ( -4.452887004952780892, 50.68053776405899669, 76.33594214506553044 ) ) ;
#20644=CARTESIAN_POINT ( 'NONE',  ( 0.8457014337750217159, 52.96360462446077833, 76.19252767286178596 ) ) ;
#20645=CARTESIAN_POINT ( 'NONE',  ( -4.637383097126855702, 37.03290878947739628, 79.54612747205591461 ) ) ;
#20646=ORIENTED_EDGE ( 'NONE', *, *, #13153, .F. ) ;
#20647=DIRECTION ( 'NONE',  ( 0.8136266022444372803, 0.5813877811927012917, 2.295812393977109100E-16 ) ) ;
#20648=VECTOR ( 'NONE', #2776, 1000.000000000000000 ) ;
#20653=CARTESIAN_POINT ( 'NONE',  ( -4.159821392692165887, 37.43023233986658482, 78.25884081218126198 ) ) ;
#20654=DIRECTION ( 'NONE',  ( 0.8043570849667761591, -0.5941461771851692664, 1.733862608106489734E-17 ) ) ;
#20655=ORIENTED_EDGE ( 'NONE', *, *, #9776, .F. ) ;
#20657=AXIS2_PLACEMENT_3D ( 'NONE', #20132, #2382, #8882 ) ;
#20659=CARTESIAN_POINT ( 'NONE',  ( 7.680032241523796266, 40.16158449578585277, 77.13595644658970230 ) ) ;
#20661=CARTESIAN_POINT ( 'NONE',  ( 4.591779561242093521, 52.09652731707507201, 76.01224951307210631 ) ) ;
#20662=EDGE_LOOP ( 'NONE', ( #3274, #7308, #13200, #6814 ) ) ;
#20664=CARTESIAN_POINT ( 'NONE',  ( -5.052695833059940078, 50.99437019215367428, 79.48628414162533318 ) ) ;
#20665=DIRECTION ( 'NONE',  ( 0.3165065846431827645, 0.9485903129789529098, 0.000000000000000000 ) ) ;
#20666=DIRECTION ( 'NONE',  ( 0.3165065846431827645, 0.9485903129789529098, 0.000000000000000000 ) ) ;
#20667=CARTESIAN_POINT ( 'NONE',  ( -4.224906967831221216, 50.83896237574116839, 78.93596775356181183 ) ) ;
#20669=VERTEX_POINT ( 'NONE', #18523 ) ;
#20670=CARTESIAN_POINT ( 'NONE',  ( -5.478128554961354091, 38.57320898139802523, 75.45433879953087342 ) ) ;
#20671=CARTESIAN_POINT ( 'NONE',  ( 0.8340537790549603647, 52.35226632664123514, 78.70464370717459701 ) ) ;
#20672=ORIENTED_EDGE ( 'NONE', *, *, #12077, .T. ) ;
#20675=EDGE_CURVE ( 'NONE', #7197, #16959, #16468, .T. ) ;
#20678=CARTESIAN_POINT ( 'NONE',  ( 5.291217816850873668, 37.50112316868685269, 75.97264893529829521 ) ) ;
#20679=CARTESIAN_POINT ( 'NONE',  ( 5.353448830008491477, 50.78079743354576436, 78.93442753446957738 ) ) ;
#20681=ORIENTED_EDGE ( 'NONE', *, *, #3758, .F. ) ;
#20682=CARTESIAN_POINT ( 'NONE',  ( 2.110044317469556674, 52.95423264481248538, 78.53328619179760040 ) ) ;
#20683=CARTESIAN_POINT ( 'NONE',  ( 4.393996117251955269, 36.11308595931626542, 76.73963291717792856 ) ) ;
#20685=DIRECTION ( 'NONE',  ( -0.9534635866061452747, -0.3015081906286225522, -2.009271279954815797E-16 ) ) ;
#20686=CARTESIAN_POINT ( 'NONE',  ( 5.838531714063069700, 37.14529820897372758, 77.55803991379978868 ) ) ;
#20688=DIRECTION ( 'NONE',  ( 0.007885122365275663500, 0.9999689119394085113, 1.805443505845543142E-16 ) ) ;
#20689=ORIENTED_EDGE ( 'NONE', *, *, #9247, .F. ) ;
#20690=AXIS2_PLACEMENT_3D ( 'NONE', #20409, #13927, #12130 ) ;
#20691=ORIENTED_EDGE ( 'NONE', *, *, #11100, .T. ) ;
#20692=CARTESIAN_POINT ( 'NONE',  ( -7.948187775445866521, 41.77580313715249360, 78.70894411705462801 ) ) ;
#20693=CARTESIAN_POINT ( 'NONE',  ( 8.315010726769150651, 41.60978595976011718, 78.93540621459339945 ) ) ;
#20694=CARTESIAN_POINT ( 'NONE',  ( 6.030184373421643151, 51.03403562479821431, 79.53335372712579954 ) ) ;
#20695=VERTEX_POINT ( 'NONE', #18201 ) ;
#20696=CARTESIAN_POINT ( 'NONE',  ( -4.383473025373059606, 51.47257230871590394, 78.45066232894264147 ) ) ;
#20697=CARTESIAN_POINT ( 'NONE',  ( -7.081827087393651965, 41.08818931601138047, 79.47791035122072856 ) ) ;
#20699=VECTOR ( 'NONE', #3336, 1000.000000000000114 ) ;
#20700=ORIENTED_EDGE ( 'NONE', *, *, #1405, .F. ) ;
#20703=CARTESIAN_POINT ( 'NONE',  ( 6.449941217757646506, 38.49637729627415439, 76.59474846278332905 ) ) ;
#20707=CARTESIAN_POINT ( 'NONE',  ( 6.443052452048888767, 38.48908422573293109, 77.56325133431154484 ) ) ;
#20709=B_SPLINE_CURVE_WITH_KNOTS ( 'NONE', 3,
 ( #14893, #9709, #4889, #11410, #11623, #16407, #9810, #10127, #14587, #17880, #19573, #4995, #8526, #18097 ),
 .UNSPECIFIED., .F., .F.,
 ( 4, 2, 2, 2, 2, 2, 4 ),
 ( 0.000000000000000000, 0.0005600013223350140072, 0.0008400019835025011698, 0.001120002644669988333, 0.001400003305837475495, 0.001680003967004962441, 0.002240005289339946307 ),
 .UNSPECIFIED. ) ;
#20710=CARTESIAN_POINT ( 'NONE',  ( -4.158578283022523081, 37.42937009194851328, 72.45433879953085921 ) ) ;
#20711=DIRECTION ( 'NONE',  ( -0.3165065846431827645, -0.9485903129789529098, 0.000000000000000000 ) ) ;
#20713=VECTOR ( 'NONE', #11993, 1000.000000000000114 ) ;
#20714=ORIENTED_EDGE ( 'NONE', *, *, #6835, .F. ) ;
#20716=CARTESIAN_POINT ( 'NONE',  ( 8.850491666625398324, 41.31920949178531544, 79.54734031390459847 ) ) ;
#20719=CARTESIAN_POINT ( 'NONE',  ( -8.231989325576739347, 42.64502410771121532, 79.17794681948264213 ) ) ;
#20721=VECTOR ( 'NONE', #7576, 1000.000000000000000 ) ;
#20722=CARTESIAN_POINT ( 'NONE',  ( 8.233139685699564225, 41.37244270010830149, 78.86985518176157939 ) ) ;
#20723=LINE ( 'NONE', #6159, #17915 ) ;
#20725=DIRECTION ( 'NONE',  ( 1.540237394707284220E-16, 1.793354297423764243E-16, -1.000000000000000000 ) ) ;
#20726=B_SPLINE_SURFACE_WITH_KNOTS ( 'NONE', 3, 1, ( 
 ( #5769, #5656 ),
 ( #18644, #876 ),
 ( #8661, #4171 ),
 ( #7361, #5882 ),
 ( #5559, #11958 ),
 ( #7037, #13537 ),
 ( #8872, #10696 ),
 ( #7256, #4060 ),
 ( #13851, #15143 ),
 ( #20332, #20008 ),
 ( #2578, #17158 ) ),
 .UNSPECIFIED., .F., .F., .F.,
 ( 4, 1, 1, 1, 1, 1, 1, 1, 4 ),
 ( 2, 2 ),
 ( 0.000000000000000000, 0.2026380577750736822, 0.3699241180509920679, 0.5036394156482512097, 0.6074627879459471025, 0.6969630674522783176, 0.7888943515530689732, 0.8885774882565341537, 1.000000000000000000 ),
 ( 0.000000000000000000, 1.000000000000000000 ),
 .UNSPECIFIED. ) ;
#20727=CARTESIAN_POINT ( 'NONE',  ( -4.652687709939232086, 51.28020135170361016, 75.36022115247205022 ) ) ;
#20728=CIRCLE ( 'NONE', #353, 8.199999999999995737 ) ;
#20729=CARTESIAN_POINT ( 'NONE',  ( 8.594846595468295547, 42.91744304621954598, 77.77798975163413786 ) ) ;
#20731=CARTESIAN_POINT ( 'NONE',  ( 6.961592395446249526, 50.34604203833234237, 76.59575135851817151 ) ) ;
#20733=CARTESIAN_POINT ( 'NONE',  ( 8.787893756631273590, 41.13159958439556618, 78.49453464888588883 ) ) ;
#20735=EDGE_CURVE ( 'NONE', #13402, #16327, #5312, .T. ) ;
#20736=CARTESIAN_POINT ( 'NONE',  ( -5.381123819449237899, 50.75968757759591909, 79.33884456587460932 ) ) ;
#20737=CARTESIAN_POINT ( 'NONE',  ( 5.241460166982748525, 50.86801069014953924, 78.59183879953087626 ) ) ;
#20742=CARTESIAN_POINT ( 'NONE',  ( 5.535687768410739729, 50.64618487078023890, 78.75475733230618403 ) ) ;
#20745=CARTESIAN_POINT ( 'NONE',  ( 9.026838159693451047, 41.84773111872319618, 78.13669174070733447 ) ) ;
#20747=CARTESIAN_POINT ( 'NONE',  ( 0.8175694909215609485, 52.96382645516884224, 76.07424718102974737 ) ) ;
#20748=CARTESIAN_POINT ( 'NONE',  ( -3.349688636638950889, 52.21127678364309332, 78.10580938776615767 ) ) ;
#20751=FACE_OUTER_BOUND ( 'NONE', #13562, .T. ) ;
#20754=CARTESIAN_POINT ( 'NONE',  ( -7.190018231056568787, 46.95048906439452452, 79.12198650143768930 ) ) ;
#20755=CARTESIAN_POINT ( 'NONE',  ( 0.3303954077475434459, 52.35993896991258367, 76.24030295937397739 ) ) ;
#20756=CARTESIAN_POINT ( 'NONE',  ( 5.786794573647632944, 37.10832874265046399, 76.01697444493925104 ) ) ;
#20757=CARTESIAN_POINT ( 'NONE',  ( -7.870029994478678681, 41.50220093607910599, 78.93669174070734584 ) ) ;
#20761=CARTESIAN_POINT ( 'NONE',  ( 4.685757199431944464, 52.02710982139440432, 77.94290914044947272 ) ) ;
#20763=ORIENTED_EDGE ( 'NONE', *, *, #18545, .T. ) ;
#20764=CARTESIAN_POINT ( 'NONE',  ( -2.914861642632559313, 51.60221265124933865, 76.66413924479479647 ) ) ;
#20767=ORIENTED_EDGE ( 'NONE', *, *, #12150, .T. ) ;
#20768=CARTESIAN_POINT ( 'NONE',  ( -5.832343694407396306, 50.43726237516484900, 78.41225960292398156 ) ) ;
#20771=CARTESIAN_POINT ( 'NONE',  ( 6.830172062167755520, 37.85388809545894873, 77.80469260682309596 ) ) ;
#20772=EDGE_CURVE ( 'NONE', #19214, #1174, #17139, .T. ) ;
#20773=CARTESIAN_POINT ( 'NONE',  ( -4.414789981656704221, 51.45019435834255717, 78.82303764823565473 ) ) ;
#20778=VECTOR ( 'NONE', #15473, 1000.000000000000227 ) ;
#20780=CARTESIAN_POINT ( 'NONE',  ( 4.609531566588798590, 52.08341462581984871, 78.11943565213420015 ) ) ;
#20781=DIRECTION ( 'NONE',  ( 0.9534635866061451637, 0.3015081906286225522, 2.009271279954815797E-16 ) ) ;
#20782=CARTESIAN_POINT ( 'NONE',  ( -5.319578332459784065, 49.88389014699610868, 75.98690818113186651 ) ) ;
#20784=CARTESIAN_POINT ( 'NONE',  ( 5.078529275337140270, 37.34914372394564452, 76.44059830477070250 ) ) ;
#20785=EDGE_CURVE ( 'NONE', #5209, #10061, #4502, .T. ) ;
#20787=EDGE_CURVE ( 'NONE', #19686, #15280, #2663, .T. ) ;
#20789=CARTESIAN_POINT ( 'NONE',  ( 5.528499006811445682, 50.64997445399101395, 76.04053158567903381 ) ) ;
#20791=ORIENTED_EDGE ( 'NONE', *, *, #2874, .F. ) ;
#20792=CARTESIAN_POINT ( 'NONE',  ( 1.580015341223601766, 52.89863773268244529, 76.85864713079314470 ) ) ;
#20793=DIRECTION ( 'NONE',  ( -0.5813877811927011807, 0.8136266022444372803, 5.636455622144619183E-17 ) ) ;
#20795=AXIS2_PLACEMENT_3D ( 'NONE', #2223, #617, #2324 ) ;
#20797=ADVANCED_FACE ( 'NONE', ( #5858 ), #14801, .T. ) ;
#20798=CARTESIAN_POINT ( 'NONE',  ( 5.847824973458005005, 37.15193883188941015, 77.47236191065434241 ) ) ;
#20801=LINE ( 'NONE', #8043, #10523 ) ;
#20802=VERTEX_POINT ( 'NONE', #7982 ) ;
#20804=CARTESIAN_POINT ( 'NONE',  ( -3.373121299339454815, 37.02388247401010091, 75.61442449207443417 ) ) ;
#20806=CARTESIAN_POINT ( 'NONE',  ( -5.334571511159140300, 49.90167720919038175, 75.98434391831075629 ) ) ;
#20809=CARTESIAN_POINT ( 'NONE',  ( -5.130197398460217606, 37.39693086210134254, 77.90166954077812989 ) ) ;
#20811=VERTEX_POINT ( 'NONE', #14363 ) ;
#20813=CARTESIAN_POINT ( 'NONE',  ( -6.824509517481986087, 40.67530721073914179, 79.25635544885822981 ) ) ;
#20814=CARTESIAN_POINT ( 'NONE',  ( 6.449077564475651059, 38.49547022419763920, 76.49624899266501643 ) ) ;
#20818=CARTESIAN_POINT ( 'NONE',  ( -4.790713360849209401, 51.18157327500495768, 75.36324311589748959 ) ) ;
#20819=CARTESIAN_POINT ( 'NONE',  ( 5.396517835962451493, 50.75616155517602834, 78.93669174070734584 ) ) ;
#20820=EDGE_CURVE ( 'NONE', #271, #20036, #12979, .T. ) ;
#20821=DIRECTION ( 'NONE',  ( 1.540237394707284220E-16, 1.793354297423764243E-16, -1.000000000000000000 ) ) ;
#20822=CARTESIAN_POINT ( 'NONE',  ( -0.8946779508733179176, 52.21709741114992909, 78.78847851419276083 ) ) ;
#20826=CARTESIAN_POINT ( 'NONE',  ( 8.744145067270602922, 41.00048198701652780, 79.52393066155629242 ) ) ;
#20827=CARTESIAN_POINT ( 'NONE',  ( 5.389492195292208798, 36.82443100924615464, 78.09625056423675460 ) ) ;
#20830=VERTEX_POINT ( 'NONE', #12669 ) ;
#20831=CARTESIAN_POINT ( 'NONE',  ( 8.263416355632948296, 41.45783420393981089, 78.92242849838478946 ) ) ;
#20832=CARTESIAN_POINT ( 'NONE',  ( -4.323846805489818479, 36.80131216085734991, 79.51042285023450518 ) ) ;
#20834=ADVANCED_FACE ( 'NONE', ( #11289 ), #5287, .T. ) ;
#20836=CARTESIAN_POINT ( 'NONE',  ( 5.287808634542578545, 50.82928320178807269, 77.98642840401727483 ) ) ;
#20837=CARTESIAN_POINT ( 'NONE',  ( 6.616107328214575034, 50.60123794050897317, 77.65065976741861675 ) ) ;
#20840=VECTOR ( 'NONE', #5187, 1000.000000000000114 ) ;
#20841=ORIENTED_EDGE ( 'NONE', *, *, #1848, .F. ) ;
#20842=CARTESIAN_POINT ( 'NONE',  ( -4.412207535196425390, 37.80258716859745505, 79.54807357191100436 ) ) ;
#20843=DIRECTION ( 'NONE',  ( -1.540237394707284467E-16, -1.793354297423764243E-16, 1.000000000000000000 ) ) ;
#20844=LINE ( 'NONE', #9487, #6163 ) ;
#20845=VERTEX_POINT ( 'NONE', #2219 ) ;
#20846=PLANE ( 'NONE',  #15996 ) ;
#20848=ORIENTED_EDGE ( 'NONE', *, *, #4294, .T. ) ;
#20849=CARTESIAN_POINT ( 'NONE',  ( -0.9296126965184758895, 52.21939493466130955, 76.40919915166844589 ) ) ;
#20850=CARTESIAN_POINT ( 'NONE',  ( 4.905034931190686009, 51.86513819399005598, 79.33697856897433098 ) ) ;
#20851=CARTESIAN_POINT ( 'NONE',  ( 5.577191696014057953, 37.87832978262304096, 78.37198585835440667 ) ) ;
#20854=EDGE_LOOP ( 'NONE', ( #2154, #17081, #6719, #12900 ) ) ;
#20857=DIRECTION ( 'NONE',  ( 0.5813877811926937422, -0.8136266022444427204, -5.636455622144829957E-17 ) ) ;
#20859=CARTESIAN_POINT ( 'NONE',  ( -7.583764859133458991, 47.59007672682779599, 78.90843038313050783 ) ) ;
#20860=CARTESIAN_POINT ( 'NONE',  ( 5.848563030374239524, 37.15246622033975399, 76.55482881315118959 ) ) ;
#20863=CARTESIAN_POINT ( 'NONE',  ( 8.220041259636596820, 41.33680711362989513, 76.16501461267081652 ) ) ;
#20865=CARTESIAN_POINT ( 'NONE',  ( -4.004103039135145536, 51.74365621125981107, 75.44813358671753178 ) ) ;
#20867=CARTESIAN_POINT ( 'NONE',  ( -7.854651159657231041, 41.44641869631179532, 78.04033446252860529 ) ) ;
#20868=VERTEX_POINT ( 'NONE', #8508 ) ;
#20869=CARTESIAN_POINT ( 'NONE',  ( 2.113288515708719117, 52.20632789671663687, 77.70145201013903602 ) ) ;
#20871=CARTESIAN_POINT ( 'NONE',  ( 6.604417847172709521, 37.69257239881283539, 78.19824744938543404 ) ) ;
#20874=CARTESIAN_POINT ( 'NONE',  ( 5.113845713194847598, 37.37437955742144879, 77.68578589458712713 ) ) ;
#20876=CARTESIAN_POINT ( 'NONE',  ( 6.433553176315260913, 38.47928099333162777, 72.45433879953087342 ) ) ;
#20878=ORIENTED_EDGE ( 'NONE', *, *, #3001, .T. ) ;
#20879=CARTESIAN_POINT ( 'NONE',  ( 5.008975552073979820, 51.78836144432717248, 77.68963291717793140 ) ) ;
#20885=ADVANCED_FACE ( 'NONE', ( #5514 ), #11915, .F. ) ;
#20886=VERTEX_POINT ( 'NONE', #20078 ) ;
#20887=CARTESIAN_POINT ( 'NONE',  ( 2.114902586664012318, 52.20151937974352307, 78.20017459567505114 ) ) ;
#20889=CARTESIAN_POINT ( 'NONE',  ( -5.661408436751226070, 39.74363423441516829, 75.45433879953087342 ) ) ;
#20890=CARTESIAN_POINT ( 'NONE',  ( -0.8635238853855432550, 52.24432082531686916, 76.01832139834691304 ) ) ;
#20891=CARTESIAN_POINT ( 'NONE',  ( 9.122633311574107395, 42.13483526604063201, 79.44701590970058191 ) ) ;
#20893=B_SPLINE_SURFACE_WITH_KNOTS ( 'NONE', 3, 1, ( 
 ( #4397, #10921 ),
 ( #11023, #20667 ),
 ( #19287, #4700 ),
 ( #8017, #17391 ),
 ( #15808, #17494 ),
 ( #2918, #17699 ),
 ( #20773, #6208 ),
 ( #12707, #19186 ),
 ( #13337, #14817 ),
 ( #18123, #3328 ),
 ( #18222, #1638 ),
 ( #236, #3543 ),
 ( #10047, #5019 ),
 ( #14718, #4912 ),
 ( #18013, #8120 ) ),
 .UNSPECIFIED., .F., .F., .F.,
 ( 4, 1, 1, 1, 1, 1, 1, 1, 1, 1, 1, 1, 4 ),
 ( 2, 2 ),
 ( 0.000000000000000000, 0.1142047618744220089, 0.2098279651953024738, 0.2930641324527410441, 0.3714084400245239448, 0.4142179382887971051, 0.4671782061414135323, 0.5290873093409070860, 0.6015893617863945497, 0.6852532414128420513, 0.7789222961280750646, 0.8837899115430479791, 1.000000000000000000 ),
 ( 0.000000000000000000, 1.000000000000000000 ),
 .UNSPECIFIED. ) ;
#20894=FACE_OUTER_BOUND ( 'NONE', #4429, .T. ) ;
#20897=ORIENTED_EDGE ( 'NONE', *, *, #1191, .F. ) ;
#20898=CARTESIAN_POINT ( 'NONE',  ( -4.509672285278094606, 36.93857395727002313, 75.36838243422435824 ) ) ;
#20899=FACE_OUTER_BOUND ( 'NONE', #14073, .T. ) ;
#20902=CARTESIAN_POINT ( 'NONE',  ( -4.641234702847274463, 37.03575381547093315, 77.24798498253255730 ) ) ;
#20904=FACE_OUTER_BOUND ( 'NONE', #169, .T. ) ;
#20906=ORIENTED_EDGE ( 'NONE', *, *, #5472, .F. ) ;
#20907=CARTESIAN_POINT ( 'NONE',  ( -4.804273704418943858, 51.17188354996588373, 76.37148643835737971 ) ) ;
#20909=DIRECTION ( 'NONE',  ( -0.5941461771851693774, -0.8043570849667760481, -2.357623395011396791E-16 ) ) ;
#20911=EDGE_CURVE ( 'NONE', #9681, #3376, #16486, .T. ) ;
#20913=CARTESIAN_POINT ( 'NONE',  ( 8.806278593017598411, 41.18670010535765869, 77.44807837618913027 ) ) ;
#20915=CARTESIAN_POINT ( 'NONE',  ( -0.9364695654124475244, 52.21742695338924278, 78.32762347114741885 ) ) ;
#20916=ORIENTED_EDGE ( 'NONE', *, *, #20131, .T. ) ;
#20917=CARTESIAN_POINT ( 'NONE',  ( 6.635267586053947397, 39.64667042487232607, 75.45433879953087342 ) ) ;
#20919=CARTESIAN_POINT ( 'NONE',  ( 0.8269786168830152162, 52.35651847692464855, 76.08306728897994731 ) ) ;
#20920=CARTESIAN_POINT ( 'NONE',  ( 5.902048492000326441, 51.12868443877599134, 78.59183879953087626 ) ) ;
#20922=AXIS2_PLACEMENT_3D ( 'NONE', #17757, #6573, #9690 ) ;
#20924=CARTESIAN_POINT ( 'NONE',  ( 9.350741246242593618, 42.81848921713964984, 76.37534566197098229 ) ) ;
#20927=CARTESIAN_POINT ( 'NONE',  ( -4.893796645199858020, 37.22231114847116373, 78.64904841171450300 ) ) ;
#20928=CARTESIAN_POINT ( 'NONE',  ( -4.453436368711327198, 50.68011839687689957, 72.45433879953087342 ) ) ;
#20930=CARTESIAN_POINT ( 'NONE',  ( -3.287686668943208268, 36.90074446973970623, 75.72657343730216439 ) ) ;
#20931=CARTESIAN_POINT ( 'NONE',  ( 6.961907239250668233, 50.34580947589670075, 76.63889762306028786 ) ) ;
#20933=CARTESIAN_POINT ( 'NONE',  ( 5.202885763635528349, 50.89499265101085967, 76.39036821129558064 ) ) ;
#20937=CARTESIAN_POINT ( 'NONE',  ( -5.606854386412799762, 37.74901817818727778, 79.39214668191834789 ) ) ;
#20938=ADVANCED_FACE ( 'NONE', ( #16697 ), #17041, .T. ) ;
#20939=CARTESIAN_POINT ( 'NONE',  ( -5.616859571223690395, 50.59123944021462904, 79.13778479689705136 ) ) ;
#20940=CARTESIAN_POINT ( 'NONE',  ( 5.246091170965059725, 50.86474954119325531, 78.73919069833695517 ) ) ;
#20942=CARTESIAN_POINT ( 'NONE',  ( 9.106328434870372135, 42.08596851619746104, 78.11626675975762168 ) ) ;
#20943=EDGE_LOOP ( 'NONE', ( #13768, #16178, #1711, #18377 ) ) ;
#20944=CARTESIAN_POINT ( 'NONE',  ( 6.721999984869559519, 37.77659228945417880, 75.79056106475293575 ) ) ;
#20945=AXIS2_PLACEMENT_3D ( 'NONE', #2557, #10560, #9053 ) ;
#20946=DIRECTION ( 'NONE',  ( -0.5941461771851693774, -0.8043570849667760481, -2.357623395011396791E-16 ) ) ;
#20947=CARTESIAN_POINT ( 'NONE',  ( 7.688394307443750186, 40.17658030797320379, 78.53633816310291138 ) ) ;
#20950=ORIENTED_EDGE ( 'NONE', *, *, #15594, .F. ) ;
#20952=CARTESIAN_POINT ( 'NONE',  ( 8.364438980634542276, 41.78253443625140306, 76.11674899411023887 ) ) ;
#20955=EDGE_CURVE ( 'NONE', #2109, #13986, #7537, .T. ) ;
#20957=CARTESIAN_POINT ( 'NONE',  ( -7.830524803375885412, 46.93262048933035402, 79.27433398498862971 ) ) ;
#20962=CARTESIAN_POINT ( 'NONE',  ( 0.5221537403065019678, 44.16218137147968292, 72.45433879953087342 ) ) ;
#20963=ORIENTED_EDGE ( 'NONE', *, *, #16366, .F. ) ;
#20968=CARTESIAN_POINT ( 'NONE',  ( 1.825099168086168122, 52.25818555367717266, 76.99764931820573111 ) ) ;
#20969=CARTESIAN_POINT ( 'NONE',  ( -5.940171601930140710, 37.99522617845349970, 78.80728580974474085 ) ) ;
#20970=AXIS2_PLACEMENT_3D ( 'NONE', #2491, #561, #4179 ) ;
#20973=DIRECTION ( 'NONE',  ( 0.3165065846431826535, 0.9485903129789529098, 2.188653791613874008E-16 ) ) ;
#20979=DIRECTION ( 'NONE',  ( -0.3165065846431828200, -0.9485903129789529098, 0.000000000000000000 ) ) ;
#20980=CARTESIAN_POINT ( 'NONE',  ( -5.818890812078571173, 50.44687531233557110, 76.28720437108826502 ) ) ;
#20985=CIRCLE ( 'NONE', #6739, 4.200000000000003730 ) ;
#20986=CARTESIAN_POINT ( 'NONE',  ( -3.495943983152256518, 36.18977369595653215, 76.77671532909576513 ) ) ;
#20988=CARTESIAN_POINT ( 'NONE',  ( 2.120940930817759362, 52.95414672101166076, 78.16610350541323271 ) ) ;
#20990=CARTESIAN_POINT ( 'NONE',  ( -3.623336461783060791, 52.01573806668144329, 75.70044805065693083 ) ) ;
#20991=VERTEX_POINT ( 'NONE', #12120 ) ;
#20993=LINE ( 'NONE', #16549, #20439 ) ;
#20994=CARTESIAN_POINT ( 'NONE',  ( 9.223886884231923489, 42.43829864670298946, 79.29919401074631935 ) ) ;
#20997=DIRECTION ( 'NONE',  ( 1.540237394707284220E-16, 1.793354297423764243E-16, -1.000000000000000000 ) ) ;
#21000=CARTESIAN_POINT ( 'NONE',  ( -0.9199438314403610706, 52.23437776363726215, 72.45433879953087342 ) ) ;
#21002=ORIENTED_EDGE ( 'NONE', *, *, #14059, .F. ) ;
#21003=DIRECTION ( 'NONE',  ( -0.3165065846431827645, -0.9485903129789529098, 0.000000000000000000 ) ) ;
#21004=CARTESIAN_POINT ( 'NONE',  ( 8.229810522273906415, 41.37904440587443844, 77.44807837618913027 ) ) ;
#21008=ORIENTED_EDGE ( 'NONE', *, *, #5900, .T. ) ;
#21009=CARTESIAN_POINT ( 'NONE',  ( 0.8377421044266867289, 51.35991668224300355, 78.52566232894263010 ) ) ;
#21010=DIRECTION ( 'NONE',  ( 0.009567942452863074584, -0.9999542261909885044, -1.778535306010356147E-16 ) ) ;
#21011=CARTESIAN_POINT ( 'NONE',  ( 5.853714975924201980, 37.93131711438793729, 75.43046809281631226 ) ) ;
#21014=CARTESIAN_POINT ( 'NONE',  ( -5.283659240720997019, 50.82933219714914230, 75.48294376282896678 ) ) ;
#21015=CARTESIAN_POINT ( 'NONE',  ( 6.691294758883309157, 37.75465145915448062, 78.79551527011911105 ) ) ;
#21016=CARTESIAN_POINT ( 'NONE',  ( 1.087883311600626124, 52.96210244217081708, 76.77198585835439815 ) ) ;
#21017=DIRECTION ( 'NONE',  ( 0.3165065846431826535, 0.9485903129789529098, 2.188653791613874008E-16 ) ) ;
#21018=AXIS2_PLACEMENT_3D ( 'NONE', #5333, #15035, #13122 ) ;
#21019=CARTESIAN_POINT ( 'NONE',  ( -0.8508103573721612634, 52.21675149905355795, 78.90127229107831397 ) ) ;
#21021=CARTESIAN_POINT ( 'NONE',  ( -3.566438244846302119, 38.23101125920473464, 78.34992703482498655 ) ) ;
#21022=CARTESIAN_POINT ( 'NONE',  ( 9.350741246242593618, 42.81848921713964984, 76.37534566197098229 ) ) ;
#21026=AXIS2_PLACEMENT_3D ( 'NONE', #18699, #10528, #15732 ) ;
#21029=ADVANCED_FACE ( 'NONE', ( #9254 ), #2436, .T. ) ;
#21030=CARTESIAN_POINT ( 'NONE',  ( 7.787730317602713725, 40.36046389751859209, 75.80943290476855623 ) ) ;
#21031=CARTESIAN_POINT ( 'NONE',  ( 6.545534159973747990, 50.65336749702785113, 77.68963291717794561 ) ) ;
#21033=CARTESIAN_POINT ( 'NONE',  ( 0.3653115025297660190, 52.36068438868553443, 78.81268202337827233 ) ) ;
ENDSEC;
END-ISO-10303-21;
